ISO-10303-21;
HEADER;
FILE_DESCRIPTION (('STEP AP214'),
    '1' );
FILE_NAME ('Front Cover.step',
    '2026-10-24T11:32:06',
    ( '' ),
    ( '' ),
    'SwSTEP 2.0',
    'SolidWorks 2025',
    '' );
FILE_SCHEMA (( 'AUTOMOTIVE_DESIGN' ));
ENDSEC;

DATA;
#3=DIRECTION ( 'NONE',  ( 0.5508969814521065267, -1.160734090543304660E-16, -0.8345732537212999791 ) ) ;
#4=ORIENTED_EDGE ( 'NONE', *, *, #46916, .F. ) ;
#5=FACE_OUTER_BOUND ( 'NONE', #37922, .T. ) ;
#6=EDGE_CURVE ( 'NONE', #44322, #24123, #48534, .T. ) ;
#15=LINE ( 'NONE', #8019, #14262 ) ;
#18=CARTESIAN_POINT ( 'NONE',  ( -1.221295136473707243, 0.000000000000000000, 1.323086612934683215 ) ) ;
#32=DIRECTION ( 'NONE',  ( -0.9998717552508122886, -0.01601477604151185785, 0.000000000000000000 ) ) ;
#33=DIRECTION ( 'NONE',  ( -0.2660368455666687892, 1.119010597708915320E-16, -0.9639628606958549062 ) ) ;
#35=EDGE_CURVE ( 'NONE', #20944, #31120, #9767, .T. ) ;
#36=EDGE_LOOP ( 'NONE', ( #12424, #14869, #12144, #2059, #5425, #21039 ) ) ;
#40=DIRECTION ( 'NONE',  ( 0.8090169943749422332, -6.825848574540668760E-17, 0.5877852522924802425 ) ) ;
#41=ORIENTED_EDGE ( 'NONE', *, *, #32145, .F. ) ;
#42=VERTEX_POINT ( 'NONE', #46835 ) ;
#45=FACE_OUTER_BOUND ( 'NONE', #8156, .T. ) ;
#47=VECTOR ( 'NONE', #45929, 39.37007874015748143 ) ;
#48=CARTESIAN_POINT ( 'NONE',  ( 0.08139965876239094178, 1.610780518492231694, 0.000000000000000000 ) ) ;
#56=DIRECTION ( 'NONE',  ( -6.104789737168205836E-17, 1.000000000000000000, 1.134460028949762747E-16 ) ) ;
#62=AXIS2_PLACEMENT_3D ( 'NONE', #50431, #10999, #38625 ) ;
#63=DIRECTION ( 'NONE',  ( -0.01601477604151182663, 0.9998717552508123996, -0.000000000000000000 ) ) ;
#66=DIRECTION ( 'NONE',  ( -0.01601477604151182663, 0.9998717552508123996, -0.000000000000000000 ) ) ;
#70=CARTESIAN_POINT ( 'NONE',  ( -1.775400203342670347, 1.691590761327236958, -2.359903268218729089 ) ) ;
#71=CARTESIAN_POINT ( 'NONE',  ( -1.684292108503798069, 6.692913385826772199, 1.406123411605399331 ) ) ;
#80=CARTESIAN_POINT ( 'NONE',  ( -1.723687301221637380, 0.000000000000000000, -1.311649477509825745 ) ) ;
#82=EDGE_CURVE ( 'NONE', #36271, #42094, #44767, .T. ) ;
#83=CARTESIAN_POINT ( 'NONE',  ( -2.952069331832154919, 2.755905511811027164, 1.181102362204724088 ) ) ;
#88=DIRECTION ( 'NONE',  ( -0.9362348706397368714, 0.000000000000000000, -0.3513748240813434620 ) ) ;
#90=AXIS2_PLACEMENT_3D ( 'NONE', #4084, #31446, #43558 ) ;
#92=DIRECTION ( 'NONE',  ( 0.000000000000000000, 0.000000000000000000, 1.000000000000000000 ) ) ;
#93=LINE ( 'NONE', #12233, #1484 ) ;
#94=ORIENTED_EDGE ( 'NONE', *, *, #13556, .F. ) ;
#95=DIRECTION ( 'NONE',  ( 0.000000000000000000, 0.000000000000000000, -1.000000000000000000 ) ) ;
#100=AXIS2_PLACEMENT_3D ( 'NONE', #33022, #17513, #29384 ) ;
#103=PLANE ( 'NONE',  #37876 ) ;
#108=CARTESIAN_POINT ( 'NONE',  ( 2.576863348864710801, 1.456480680773285741, 1.442554885838449596 ) ) ;
#109=ORIENTED_EDGE ( 'NONE', *, *, #48882, .F. ) ;
#111=ORIENTED_EDGE ( 'NONE', *, *, #20916, .T. ) ;
#112=CARTESIAN_POINT ( 'NONE',  ( -1.312623452344869657, 1.205361022782829114E-17, 1.722945714930904648 ) ) ;
#115=B_SPLINE_CURVE_WITH_KNOTS ( 'NONE', 3,
 ( #45279, #2696, #10703, #6825 ),
 .UNSPECIFIED., .F., .F.,
 ( 4, 4 ),
 ( 0.0008439222489648032970, 0.003344231527576960444 ),
 .UNSPECIFIED. ) ;
#116=DIRECTION ( 'NONE',  ( -0.9959742939952384022, 1.288287287306305283E-16, -0.08963930890344089242 ) ) ;
#125=CARTESIAN_POINT ( 'NONE',  ( 0.000000000000000000, 1.574803149606302854, 0.000000000000000000 ) ) ;
#127=FACE_OUTER_BOUND ( 'NONE', #15551, .T. ) ;
#137=ORIENTED_EDGE ( 'NONE', *, *, #4680, .F. ) ;
#138=ORIENTED_EDGE ( 'NONE', *, *, #50267, .T. ) ;
#141=CIRCLE ( 'NONE', #36418, 2.164630168518208109 ) ;
#145=CARTESIAN_POINT ( 'NONE',  ( 1.773598097765477277, 1.637884173412089250, 1.477342561509449759 ) ) ;
#146=EDGE_CURVE ( 'NONE', #16314, #49284, #20780, .T. ) ;
#149=CARTESIAN_POINT ( 'NONE',  ( 0.4139892466755871747, 1.013814418196932632, 2.556881760885583610 ) ) ;
#150=CARTESIAN_POINT ( 'NONE',  ( -1.613247378701003099, 1.616446044927785097, -1.474335889616294581 ) ) ;
#157=CARTESIAN_POINT ( 'NONE',  ( 0.04921259842519689481, 0.01913872127211492871, 1.877530537165238655 ) ) ;
#161=CARTESIAN_POINT ( 'NONE',  ( -2.006180841960468086, 1.679905088511975952, -1.383235759546366461 ) ) ;
#162=VERTEX_POINT ( 'NONE', #12522 ) ;
#166=B_SPLINE_CURVE_WITH_KNOTS ( 'NONE', 3,
 ( #38483, #29261, #29524, #7238 ),
 .UNSPECIFIED., .F., .F.,
 ( 4, 4 ),
 ( 0.01106655392343035803, 0.03073596134458069645 ),
 .UNSPECIFIED. ) ;
#170=DIRECTION ( 'NONE',  ( -0.9998717552508121775, -0.01601477604151182663, 0.000000000000000000 ) ) ;
#174=DIRECTION ( 'NONE',  ( -0.000000000000000000, -1.000000000000000000, -0.000000000000000000 ) ) ;
#184=EDGE_CURVE ( 'NONE', #12327, #2318, #1159, .T. ) ;
#185=DIRECTION ( 'NONE',  ( -3.986037398843765983E-20, -1.000000000000000000, -1.160734090543304660E-16 ) ) ;
#188=EDGE_CURVE ( 'NONE', #9810, #3944, #698, .T. ) ;
#189=DIRECTION ( 'NONE',  ( 0.9749279121818259508, 0.000000000000000000, -0.2225209339563041788 ) ) ;
#190=ORIENTED_EDGE ( 'NONE', *, *, #20504, .F. ) ;
#196=VERTEX_POINT ( 'NONE', #24912 ) ;
#200=B_SPLINE_CURVE_WITH_KNOTS ( 'NONE', 3,
 ( #50656, #15354, #2476, #30092 ),
 .UNSPECIFIED., .F., .F.,
 ( 4, 4 ),
 ( 0.001007621139641426671, 0.003507930418253497190 ),
 .UNSPECIFIED. ) ;
#204=DIRECTION ( 'NONE',  ( -0.000000000000000000, -1.000000000000000000, -0.000000000000000000 ) ) ;
#205=CARTESIAN_POINT ( 'NONE',  ( -0.04921259842519695726, 0.5249316497054296038, 1.883403453826241192 ) ) ;
#206=ORIENTED_EDGE ( 'NONE', *, *, #20888, .T. ) ;
#209=VERTEX_POINT ( 'NONE', #2440 ) ;
#211=VECTOR ( 'NONE', #28730, 39.37007874015748143 ) ;
#214=LINE ( 'NONE', #28342, #18968 ) ;
#215=ORIENTED_EDGE ( 'NONE', *, *, #9595, .F. ) ;
#219=DIRECTION ( 'NONE',  ( -0.9998717552508121775, -0.01601477604151182663, 0.000000000000000000 ) ) ;
#221=CARTESIAN_POINT ( 'NONE',  ( -2.612298101585049714, 1.674454801174855234, -0.6467181869387608195 ) ) ;
#222=CARTESIAN_POINT ( 'NONE',  ( -1.172858943013145749, 6.692913385826772199, 1.867085387823100850 ) ) ;
#224=EDGE_CURVE ( 'NONE', #15315, #8682, #2410, .T. ) ;
#225=CARTESIAN_POINT ( 'NONE',  ( -0.7381027496704858359, 0.000000000000000000, -2.859439394060923512 ) ) ;
#226=ORIENTED_EDGE ( 'NONE', *, *, #21083, .T. ) ;
#227=CARTESIAN_POINT ( 'NONE',  ( 0.8067290215917978236, 6.692913385826772199, 2.009464521518182334 ) ) ;
#228=ORIENTED_EDGE ( 'NONE', *, *, #16699, .T. ) ;
#229=DIRECTION ( 'NONE',  ( -0.01601477604151182663, 0.9998717552508123996, -0.000000000000000000 ) ) ;
#230=CARTESIAN_POINT ( 'NONE',  ( -1.330011864698828816, 1.686599376747761614, -1.746878811320646152 ) ) ;
#231=EDGE_CURVE ( 'NONE', #1621, #46197, #37830, .T. ) ;
#235=EDGE_CURVE ( 'NONE', #22970, #35146, #10690, .T. ) ;
#238=EDGE_LOOP ( 'NONE', ( #10056, #19126, #49833, #39898 ) ) ;
#239=CARTESIAN_POINT ( 'NONE',  ( 2.623503965249849301, 1.455362298632098428, 1.355882097269874187 ) ) ;
#240=ORIENTED_EDGE ( 'NONE', *, *, #12188, .T. ) ;
#244=DIRECTION ( 'NONE',  ( -0.9998717552508122886, -0.01601477604151185785, 0.000000000000000000 ) ) ;
#254=ORIENTED_EDGE ( 'NONE', *, *, #23636, .F. ) ;
#257=DIRECTION ( 'NONE',  ( 0.000000000000000000, 0.000000000000000000, 1.000000000000000000 ) ) ;
#258=ORIENTED_EDGE ( 'NONE', *, *, #35570, .T. ) ;
#260=B_SPLINE_CURVE_WITH_KNOTS ( 'NONE', 3,
 ( #27101, #11365, #15998, #46699 ),
 .UNSPECIFIED., .F., .F.,
 ( 4, 4 ),
 ( 0.1211775127643062860, 0.1625894504277921315 ),
 .UNSPECIFIED. ) ;
#269=CARTESIAN_POINT ( 'NONE',  ( 1.325491792074624309, 5.905511811023623991, -2.638988599164732385 ) ) ;
#274=AXIS2_PLACEMENT_3D ( 'NONE', #47978, #16530, #257 ) ;
#277=CIRCLE ( 'NONE', #14412, 2.244934639244525076 ) ;
#280=AXIS2_PLACEMENT_3D ( 'NONE', #27743, #19741, #35252 ) ;
#288=CARTESIAN_POINT ( 'NONE',  ( 1.726519710923990480, 1.205361022782829114E-17, -1.198633063221572481 ) ) ;
#289=B_SPLINE_CURVE_WITH_KNOTS ( 'NONE', 3,
 ( #15906, #43522, #47625, #4294 ),
 .UNSPECIFIED., .F., .F.,
 ( 4, 4 ),
 ( 2.219256376020187195E-07, 0.002500750338221284681 ),
 .UNSPECIFIED. ) ;
#297=ADVANCED_FACE ( 'NONE', ( #22313 ), #38067, .T. ) ;
#299=ORIENTED_EDGE ( 'NONE', *, *, #46894, .F. ) ;
#301=ORIENTED_EDGE ( 'NONE', *, *, #1688, .T. ) ;
#304=ORIENTED_EDGE ( 'NONE', *, *, #42340, .F. ) ;
#307=CARTESIAN_POINT ( 'NONE',  ( 1.511286805986086890, 0.000000000000000000, 0.8691436966267173103 ) ) ;
#312=CARTESIAN_POINT ( 'NONE',  ( 2.064489077472676737, 1.642543324816299277, 1.055063358597729595 ) ) ;
#316=ORIENTED_EDGE ( 'NONE', *, *, #43835, .F. ) ;
#320=LINE ( 'NONE', #16074, #3866 ) ;
#321=EDGE_CURVE ( 'NONE', #39685, #37024, #31709, .T. ) ;
#324=ORIENTED_EDGE ( 'NONE', *, *, #37835, .F. ) ;
#335=DIRECTION ( 'NONE',  ( 0.08963930890344089242, 0.000000000000000000, -0.9959742939952384022 ) ) ;
#340=DIRECTION ( 'NONE',  ( -0.01601477604151182663, 0.9998717552508123996, -0.000000000000000000 ) ) ;
#344=VERTEX_POINT ( 'NONE', #8074 ) ;
#347=DIRECTION ( 'NONE',  ( 0.9998717552508121775, 0.01601477604151182663, 0.000000000000000000 ) ) ;
#350=CARTESIAN_POINT ( 'NONE',  ( 2.436294546427499430, 1.753736851973850319, 1.255140413159070212 ) ) ;
#353=LINE ( 'NONE', #16108, #2771 ) ;
#354=CONICAL_SURFACE ( 'NONE', #44060, 2.246510896728926010, 0.01601546068027819014 ) ;
#355=DIRECTION ( 'NONE',  ( 1.086719731106943413E-16, -1.000000000000000000, 4.078527368698718974E-17 ) ) ;
#356=VECTOR ( 'NONE', #29132, 39.37007874015748143 ) ;
#358=VERTEX_POINT ( 'NONE', #39314 ) ;
#360=B_SPLINE_CURVE_WITH_KNOTS ( 'NONE', 3,
 ( #10008, #49206, #49453, #37388 ),
 .UNSPECIFIED., .F., .F.,
 ( 4, 4 ),
 ( 4.362154105138019244E-07, 0.04428848116889361891 ),
 .UNSPECIFIED. ) ;
#361=CARTESIAN_POINT ( 'NONE',  ( -0.7697287008055467838, 1.707258635520111145, -2.850711186138116915 ) ) ;
#363=ORIENTED_EDGE ( 'NONE', *, *, #32288, .F. ) ;
#367=EDGE_CURVE ( 'NONE', #7137, #11612, #17764, .T. ) ;
#368=CIRCLE ( 'NONE', #15223, 2.164630168518208109 ) ;
#372=DIRECTION ( 'NONE',  ( 0.000000000000000000, 0.000000000000000000, 1.000000000000000000 ) ) ;
#375=ADVANCED_FACE ( 'NONE', ( #11193 ), #27181, .T. ) ;
#380=VERTEX_POINT ( 'NONE', #23559 ) ;
#384=CARTESIAN_POINT ( 'NONE',  ( -2.014664160120487768, 1.577208220393157223, -0.8075893616760145832 ) ) ;
#386=CARTESIAN_POINT ( 'NONE',  ( 0.2508718039770792552, 1.711920121901901348, -2.238407143905190910 ) ) ;
#389=ORIENTED_EDGE ( 'NONE', *, *, #38733, .T. ) ;
#390=EDGE_CURVE ( 'NONE', #6874, #23296, #47017, .T. ) ;
#397=ORIENTED_EDGE ( 'NONE', *, *, #11216, .T. ) ;
#398=EDGE_CURVE ( 'NONE', #40889, #2346, #29466, .T. ) ;
#399=DIRECTION ( 'NONE',  ( 0.9998717552508121775, 0.01601477604151182663, 0.000000000000000000 ) ) ;
#407=CARTESIAN_POINT ( 'NONE',  ( -1.236813753895213308, 0.000000000000000000, -2.681693691597581974 ) ) ;
#411=ADVANCED_FACE ( 'NONE', ( #39062 ), #43172, .T. ) ;
#413=CARTESIAN_POINT ( 'NONE',  ( 1.542217245295272932, 0.05262109711011796892, 1.166931937029544564 ) ) ;
#415=CARTESIAN_POINT ( 'NONE',  ( 1.398572223930554026, 1.205361022782829114E-17, 1.525996566212370231 ) ) ;
#416=CARTESIAN_POINT ( 'NONE',  ( 2.168245791271197209, 0.000000000000000000, -2.004968704497248400 ) ) ;
#419=CARTESIAN_POINT ( 'NONE',  ( -2.919426793319806368, 1.205361022782829114E-17, 0.4451252810446393315 ) ) ;
#420=CARTESIAN_POINT ( 'NONE',  ( -1.083598637574820334, 1.702374950942735499, 2.747180975113330259 ) ) ;
#423=CARTESIAN_POINT ( 'NONE',  ( 0.000000000000000000, 6.692913385826772199, 0.000000000000000000 ) ) ;
#427=B_SPLINE_CURVE_WITH_KNOTS ( 'NONE', 3,
 ( #1566, #12410, #24028, #20147 ),
 .UNSPECIFIED., .F., .F.,
 ( 4, 4 ),
 ( 5.996436511574133413E-07, 0.0002691799533657123085 ),
 .UNSPECIFIED. ) ;
#428=CARTESIAN_POINT ( 'NONE',  ( 0.08119777152254364916, 1.623385212329073957, 0.000000000000000000 ) ) ;
#432=AXIS2_PLACEMENT_3D ( 'NONE', #48202, #5126, #12360 ) ;
#433=CARTESIAN_POINT ( 'NONE',  ( -1.503492009532958695, 1.205361022782829114E-17, -0.9334790059352082725 ) ) ;
#436=AXIS2_PLACEMENT_3D ( 'NONE', #1333, #41343, #17090 ) ;
#437=EDGE_CURVE ( 'NONE', #38725, #38735, #18864, .T. ) ;
#438=CARTESIAN_POINT ( 'NONE',  ( 1.130720258286322499, 1.729608259214892918, -2.234541341810120763 ) ) ;
#440=LINE ( 'NONE', #7428, #31738 ) ;
#444=VECTOR ( 'NONE', #22863, 39.37007874015748143 ) ;
#449=CARTESIAN_POINT ( 'NONE',  ( 2.823445274216730638, 1.205361022782829114E-17, 0.8656477926280680135 ) ) ;
#450=ORIENTED_EDGE ( 'NONE', *, *, #27909, .T. ) ;
#455=CARTESIAN_POINT ( 'NONE',  ( 2.168245791271197209, 1.654581109258766558, -2.004968704497248400 ) ) ;
#458=DIRECTION ( 'NONE',  ( -0.9998717552508122886, -0.01601477604151181275, 0.000000000000000000 ) ) ;
#459=EDGE_LOOP ( 'NONE', ( #26037, #28525, #7680, #34312 ) ) ;
#461=B_SPLINE_CURVE_WITH_KNOTS ( 'NONE', 3,
 ( #45919, #19073, #50764, #19573 ),
 .UNSPECIFIED., .F., .F.,
 ( 4, 4 ),
 ( 0.1211873102087489551, 0.1625992483279400380 ),
 .UNSPECIFIED. ) ;
#463=ORIENTED_EDGE ( 'NONE', *, *, #32379, .T. ) ;
#465=CARTESIAN_POINT ( 'NONE',  ( -1.299838092272570966, 1.592662749112851772, 2.079612685669299577 ) ) ;
#473=DIRECTION ( 'NONE',  ( -0.9998717552508122886, -0.01601477604151182316, 0.000000000000000000 ) ) ;
#474=DIRECTION ( 'NONE',  ( -3.986037398843765983E-20, -1.000000000000000000, -1.160734090543304660E-16 ) ) ;
#480=CARTESIAN_POINT ( 'NONE',  ( -0.4788131938641533303, 1.613355999311305133, 2.914091152102185944 ) ) ;
#482=CARTESIAN_POINT ( 'NONE',  ( 2.576863348864710801, 1.759415398959654819, 1.442554885838449819 ) ) ;
#486=DIRECTION ( 'NONE',  ( -0.5508969814520945363, 1.288287287306305530E-16, -0.8345732537213079727 ) ) ;
#487=DIRECTION ( 'NONE',  ( -1.206139481778042838E-16, 1.000000000000000000, 4.526717189434675613E-17 ) ) ;
#492=ORIENTED_EDGE ( 'NONE', *, *, #14114, .F. ) ;
#493=B_SPLINE_CURVE_WITH_KNOTS ( 'NONE', 3,
 ( #15313, #46275, #23061, #11190 ),
 .UNSPECIFIED., .F., .F.,
 ( 4, 4 ),
 ( 0.001811265126449798602, 0.04538071868018288962 ),
 .UNSPECIFIED. ) ;
#494=EDGE_CURVE ( 'NONE', #22056, #26109, #32094, .T. ) ;
#497=CARTESIAN_POINT ( 'NONE',  ( 2.951990591674675368, 2.755905511811027164, -0.08331184815398351429 ) ) ;
#500=ADVANCED_FACE ( 'NONE', ( #586 ), #24337, .T. ) ;
#503=CARTESIAN_POINT ( 'NONE',  ( 0.000000000000000000, 1.574803149606302854, 0.000000000000000000 ) ) ;
#505=ORIENTED_EDGE ( 'NONE', *, *, #14114, .T. ) ;
#507=AXIS2_PLACEMENT_3D ( 'NONE', #24841, #32864, #13735 ) ;
#512=CIRCLE ( 'NONE', #29375, 1.743387098533651480 ) ;
#523=B_SPLINE_CURVE_WITH_KNOTS ( 'NONE', 3,
 ( #40639, #632, #12248, #8379 ),
 .UNSPECIFIED., .F., .F.,
 ( 4, 4 ),
 ( 2.008317238951771178E-07, 0.002500501625894326844 ),
 .UNSPECIFIED. ) ;
#526=ORIENTED_EDGE ( 'NONE', *, *, #1137, .T. ) ;
#529=CARTESIAN_POINT ( 'NONE',  ( 2.016369045219287948, 1.641772594434526278, 1.140940039539855677 ) ) ;
#537=EDGE_LOOP ( 'NONE', ( #46849, #11263, #38337, #299, #6692, #44475, #50981, #44812, #28640, #30920, #31824, #49047, #11727 ) ) ;
#541=VECTOR ( 'NONE', #22838, 39.37007874015748143 ) ;
#543=EDGE_LOOP ( 'NONE', ( #45689, #18327, #18038, #46018 ) ) ;
#546=DIRECTION ( 'NONE',  ( -0.000000000000000000, 1.000000000000000000, -0.000000000000000000 ) ) ;
#550=CARTESIAN_POINT ( 'NONE',  ( 1.281152772984937682, 0.000000000000000000, -2.660341145381147854 ) ) ;
#554=DIRECTION ( 'NONE',  ( 0.04486483035051863633, 1.159547425261732707E-16, -0.9989930665413144784 ) ) ;
#558=CARTESIAN_POINT ( 'NONE',  ( -1.997023710742784619, 0.5251151982619056691, -0.8000494717651052134 ) ) ;
#560=CARTESIAN_POINT ( 'NONE',  ( 2.160407304981128984, 1.574803149606302854, -0.1462862061266585745 ) ) ;
#563=EDGE_CURVE ( 'NONE', #34643, #7408, #50346, .T. ) ;
#568=DIRECTION ( 'NONE',  ( -0.01601477604151182663, 0.9998717552508123996, -0.000000000000000000 ) ) ;
#570=CARTESIAN_POINT ( 'NONE',  ( 0.6504488014449565370, 1.685511682479523099, -2.171864155587596379 ) ) ;
#571=CARTESIAN_POINT ( 'NONE',  ( -2.076656781855024114, 1.674640491952791077, 0.6230015025396302697 ) ) ;
#573=AXIS2_PLACEMENT_3D ( 'NONE', #35731, #27978, #16888 ) ;
#574=ORIENTED_EDGE ( 'NONE', *, *, #10396, .F. ) ;
#577=CARTESIAN_POINT ( 'NONE',  ( -0.8952071785065484066, 0.000000000000000000, 1.972340328593134906 ) ) ;
#580=ORIENTED_EDGE ( 'NONE', *, *, #12029, .F. ) ;
#581=DIRECTION ( 'NONE',  ( 0.7227948638273978821, 0.000000000000000000, -0.6910626489868580968 ) ) ;
#584=B_SPLINE_CURVE_WITH_KNOTS ( 'NONE', 3,
 ( #9122, #44230, #350, #4485 ),
 .UNSPECIFIED., .F., .F.,
 ( 4, 4 ),
 ( 0.01454276592102258202, 0.03074978739352322854 ),
 .UNSPECIFIED. ) ;
#585=ORIENTED_EDGE ( 'NONE', *, *, #50532, .T. ) ;
#586=FACE_OUTER_BOUND ( 'NONE', #32840, .T. ) ;
#594=CARTESIAN_POINT ( 'NONE',  ( 2.078610245214651098, 0.000000000000000000, -0.4912784290244630592 ) ) ;
#595=ORIENTED_EDGE ( 'NONE', *, *, #18040, .T. ) ;
#596=VERTEX_POINT ( 'NONE', #35698 ) ;
#602=CARTESIAN_POINT ( 'NONE',  ( 0.08139965876239094178, 1.610780518492231694, 0.000000000000000000 ) ) ;
#603=ORIENTED_EDGE ( 'NONE', *, *, #42287, .T. ) ;
#613=FACE_OUTER_BOUND ( 'NONE', #23764, .T. ) ;
#615=ORIENTED_EDGE ( 'NONE', *, *, #28454, .T. ) ;
#616=DIRECTION ( 'NONE',  ( 0.9998717552508121775, 0.01601477604151182663, 0.000000000000000000 ) ) ;
#618=CARTESIAN_POINT ( 'NONE',  ( 0.002207914879453961969, 6.692913385826772199, 0.04916304461325451958 ) ) ;
#619=VERTEX_POINT ( 'NONE', #33625 ) ;
#626=CARTESIAN_POINT ( 'NONE',  ( 1.836694934015037806, 1.638894784719147513, 1.401770057403159520 ) ) ;
#632=CARTESIAN_POINT ( 'NONE',  ( 0.2483449720100243119, 1.624673919087268770, -2.942339427351925440 ) ) ;
#633=ORIENTED_EDGE ( 'NONE', *, *, #12188, .F. ) ;
#635=CARTESIAN_POINT ( 'NONE',  ( -2.633944868634075398, 1.674114007166422002, -0.5507025360789752355 ) ) ;
#640=VERTEX_POINT ( 'NONE', #9609 ) ;
#643=VERTEX_POINT ( 'NONE', #33120 ) ;
#645=CARTESIAN_POINT ( 'NONE',  ( 0.5756566573088586214, 1.205361022782829114E-17, 2.896516654582643291 ) ) ;
#646=CARTESIAN_POINT ( 'NONE',  ( 1.833791099076603537, 6.692913385826772199, -1.151507526013693772 ) ) ;
#648=ORIENTED_EDGE ( 'NONE', *, *, #37358, .T. ) ;
#649=ORIENTED_EDGE ( 'NONE', *, *, #23937, .T. ) ;
#650=DIRECTION ( 'NONE',  ( 0.000000000000000000, 0.000000000000000000, 1.000000000000000000 ) ) ;
#651=CARTESIAN_POINT ( 'NONE',  ( 0.1067246931122726866, 0.02962905676920215767, 0.000000000000000000 ) ) ;
#652=VECTOR ( 'NONE', #39363, 39.37007874015748143 ) ;
#654=CARTESIAN_POINT ( 'NONE',  ( -0.7381027496704857249, 1.531192278308824539, -2.859439394060923068 ) ) ;
#655=CARTESIAN_POINT ( 'NONE',  ( 3.937007874015748143, 2.913385826771657250, -1.023622047244094224 ) ) ;
#658=CARTESIAN_POINT ( 'NONE',  ( -2.122484638469143814, 1.673906474958827939, -0.4339650761337435214 ) ) ;
#661=CYLINDRICAL_SURFACE ( 'NONE', #36600, 2.164630168518208109 ) ;
#663=ORIENTED_EDGE ( 'NONE', *, *, #6430, .F. ) ;
#665=AXIS2_PLACEMENT_3D ( 'NONE', #3326, #47156, #19067 ) ;
#667=ADVANCED_FACE ( 'NONE', ( #17359 ), #5675, .T. ) ;
#669=VECTOR ( 'NONE', #48578, 39.37007874015748143 ) ;
#670=CARTESIAN_POINT ( 'NONE',  ( 2.153610746787201435, 1.643970771453353130, -0.8669779829368272628 ) ) ;
#671=CARTESIAN_POINT ( 'NONE',  ( -2.164823134740036181, 1.673228346456695492, 0.000000000000000000 ) ) ;
#672=ADVANCED_FACE ( 'NONE', ( #21483 ), #10651, .T. ) ;
#678=CARTESIAN_POINT ( 'NONE',  ( 0.000000000000000000, 0.000000000000000000, 0.000000000000000000 ) ) ;
#689=PLANE ( 'NONE',  #22633 ) ;
#695=VERTEX_POINT ( 'NONE', #29482 ) ;
#698=CIRCLE ( 'NONE', #5637, 1.682967650661292502 ) ;
#703=ORIENTED_EDGE ( 'NONE', *, *, #26447, .T. ) ;
#710=ORIENTED_EDGE ( 'NONE', *, *, #41702, .F. ) ;
#711=DIRECTION ( 'NONE',  ( 0.000000000000000000, 1.000000000000000000, 0.000000000000000000 ) ) ;
#715=CARTESIAN_POINT ( 'NONE',  ( -2.823445274216742629, 5.905511811023623991, 0.8656477926280273794 ) ) ;
#716=ORIENTED_EDGE ( 'NONE', *, *, #82, .F. ) ;
#719=CARTESIAN_POINT ( 'NONE',  ( -2.823445274216743073, 1.675250974312822105, 0.8656477926280276014 ) ) ;
#730=EDGE_CURVE ( 'NONE', #2835, #49324, #10628, .T. ) ;
#731=FACE_OUTER_BOUND ( 'NONE', #28856, .T. ) ;
#741=DIRECTION ( 'NONE',  ( -0.000000000000000000, -1.000000000000000000, 0.000000000000000000 ) ) ;
#746=CARTESIAN_POINT ( 'NONE',  ( -2.356822886370966152, 1.674349844980132174, -0.5884076361977262914 ) ) ;
#748=ADVANCED_FACE ( 'NONE', ( #7753 ), #38752, .T. ) ;
#750=DIRECTION ( 'NONE',  ( 0.01601477604151182663, -0.9998717552508123996, 0.000000000000000000 ) ) ;
#754=ORIENTED_EDGE ( 'NONE', *, *, #8323, .F. ) ;
#756=DIRECTION ( 'NONE',  ( -0.8584487936018655452, 5.956818571996926923E-17, -0.5128992774059071280 ) ) ;
#759=AXIS2_PLACEMENT_3D ( 'NONE', #23299, #32085, #43422 ) ;
#762=CARTESIAN_POINT ( 'NONE',  ( 0.04921259842519603439, 6.692913385826772199, -2.165433070866142007 ) ) ;
#769=DIRECTION ( 'NONE',  ( 0.9998717552508121775, 0.01601477604151182663, 0.000000000000000000 ) ) ;
#772=DIRECTION ( 'NONE',  ( 0.5877852522924802425, 0.000000000000000000, -0.8090169943749422332 ) ) ;
#774=ORIENTED_EDGE ( 'NONE', *, *, #6256, .F. ) ;
#780=DIRECTION ( 'NONE',  ( -0.9998717552508121775, -0.01601477604151182316, 0.000000000000000000 ) ) ;
#782=VERTEX_POINT ( 'NONE', #38996 ) ;
#785=ORIENTED_EDGE ( 'NONE', *, *, #39839, .F. ) ;
#786=ORIENTED_EDGE ( 'NONE', *, *, #50838, .T. ) ;
#788=EDGE_CURVE ( 'NONE', #7202, #3538, #7003, .T. ) ;
#792=EDGE_CURVE ( 'NONE', #30522, #28465, #1468, .T. ) ;
#793=LINE ( 'NONE', #16546, #46934 ) ;
#796=CARTESIAN_POINT ( 'NONE',  ( 0.9836083787002617429, 6.692913385826772199, -1.929060376159698276 ) ) ;
#798=B_SPLINE_CURVE_WITH_KNOTS ( 'NONE', 3,
 ( #25877, #2890, #34641, #26132 ),
 .UNSPECIFIED., .F., .F.,
 ( 4, 4 ),
 ( 3.578153648618482699E-07, 0.05018484914549597997 ),
 .UNSPECIFIED. ) ;
#800=FACE_OUTER_BOUND ( 'NONE', #7712, .T. ) ;
#801=CARTESIAN_POINT ( 'NONE',  ( -3.051175669084205122, 2.755905511811027164, 0.7468891277766205317 ) ) ;
#806=ORIENTED_EDGE ( 'NONE', *, *, #35915, .F. ) ;
#807=CARTESIAN_POINT ( 'NONE',  ( -1.815926437556002915, 1.042210485784169194, -1.804289983221820437 ) ) ;
#808=VECTOR ( 'NONE', #46016, 39.37007874015748854 ) ;
#810=VERTEX_POINT ( 'NONE', #34877 ) ;
#816=ORIENTED_EDGE ( 'NONE', *, *, #43057, .F. ) ;
#817=CARTESIAN_POINT ( 'NONE',  ( -2.009930929872525418, 1.574803149606302854, -0.8055662819784117357 ) ) ;
#823=DIRECTION ( 'NONE',  ( -8.032339854997460071E-17, 1.000000000000000000, 1.007223559679395367E-16 ) ) ;
#826=EDGE_CURVE ( 'NONE', #4522, #32688, #43268, .T. ) ;
#829=ORIENTED_EDGE ( 'NONE', *, *, #43509, .T. ) ;
#834=CARTESIAN_POINT ( 'NONE',  ( -1.531154912952794378, 0.000000000000000000, 1.532020527533835441 ) ) ;
#838=B_SPLINE_CURVE_WITH_KNOTS ( 'NONE', 3,
 ( #20720, #23832, #36481, #8342 ),
 .UNSPECIFIED., .F., .F.,
 ( 4, 4 ),
 ( 0.01198117231230108604, 0.03073747865870201171 ),
 .UNSPECIFIED. ) ;
#839=AXIS2_PLACEMENT_3D ( 'NONE', #48946, #26007, #44590 ) ;
#840=ORIENTED_EDGE ( 'NONE', *, *, #5321, .F. ) ;
#841=CIRCLE ( 'NONE', #18971, 2.165354330708661568 ) ;
#845=ORIENTED_EDGE ( 'NONE', *, *, #50736, .F. ) ;
#847=DIRECTION ( 'NONE',  ( -0.000000000000000000, 1.000000000000000000, -0.000000000000000000 ) ) ;
#853=CARTESIAN_POINT ( 'NONE',  ( -1.723687301221637380, 5.905511811023623991, -1.311649477509824857 ) ) ;
#855=CARTESIAN_POINT ( 'NONE',  ( 0.000000000000000000, 5.905511811023623991, 0.000000000000000000 ) ) ;
#857=EDGE_CURVE ( 'NONE', #6398, #2006, #6752, .T. ) ;
#859=ORIENTED_EDGE ( 'NONE', *, *, #6195, .T. ) ;
#860=ORIENTED_EDGE ( 'NONE', *, *, #18754, .F. ) ;
#862=DIRECTION ( 'NONE',  ( -0.7818314824680309139, 0.000000000000000000, 0.6234898018587318180 ) ) ;
#865=LINE ( 'NONE', #28473, #45696 ) ;
#866=DIRECTION ( 'NONE',  ( 0.8345732537213079727, 0.000000000000000000, -0.5508969814520945363 ) ) ;
#867=FACE_OUTER_BOUND ( 'NONE', #35638, .T. ) ;
#868=CARTESIAN_POINT ( 'NONE',  ( 1.942732458483374280, 5.905511811023623991, 2.223636218514625451 ) ) ;
#869=VERTEX_POINT ( 'NONE', #4392 ) ;
#872=VECTOR ( 'NONE', #18718, 39.37007874015748854 ) ;
#873=ORIENTED_EDGE ( 'NONE', *, *, #33508, .T. ) ;
#876=CARTESIAN_POINT ( 'NONE',  ( -0.8329809839909436686, 1.706281419137876565, -2.833254665166566877 ) ) ;
#877=CARTESIAN_POINT ( 'NONE',  ( -0.3847164040906153049, 0.5249316497054298258, 1.844349136728716143 ) ) ;
#887=CARTESIAN_POINT ( 'NONE',  ( -2.600183657057300923, 0.000000000000000000, 1.399218491554123700 ) ) ;
#888=DIRECTION ( 'NONE',  ( 0.1342332658176667026, 0.000000000000000000, -0.9909497617679331460 ) ) ;
#890=CARTESIAN_POINT ( 'NONE',  ( 0.1067246931122726866, 0.02962905676920215767, 0.000000000000000000 ) ) ;
#893=ADVANCED_FACE ( 'NONE', ( #24785 ), #13008, .T. ) ;
#894=ORIENTED_EDGE ( 'NONE', *, *, #36897, .F. ) ;
#895=ORIENTED_EDGE ( 'NONE', *, *, #5742, .T. ) ;
#898=ORIENTED_EDGE ( 'NONE', *, *, #47103, .T. ) ;
#911=FACE_OUTER_BOUND ( 'NONE', #19718, .T. ) ;
#916=CIRCLE ( 'NONE', #7504, 2.165354330708661568 ) ;
#918=AXIS2_PLACEMENT_3D ( 'NONE', #12075, #28068, #19806 ) ;
#920=ORIENTED_EDGE ( 'NONE', *, *, #34296, .F. ) ;
#921=DIRECTION ( 'NONE',  ( -0.9998717552508122886, -0.01601477604151180928, 0.000000000000000000 ) ) ;
#923=ADVANCED_FACE ( 'NONE', ( #20390 ), #46792, .T. ) ;
#927=PLANE ( 'NONE',  #48454 ) ;
#933=ORIENTED_EDGE ( 'NONE', *, *, #40776, .F. ) ;
#937=ORIENTED_EDGE ( 'NONE', *, *, #32737, .T. ) ;
#938=CARTESIAN_POINT ( 'NONE',  ( -1.971834065208965203, 5.905511811023623991, 0.8963217522329905984 ) ) ;
#939=CARTESIAN_POINT ( 'NONE',  ( 1.325491792074624087, 1.641458297549746037, -2.638988599164732385 ) ) ;
#940=ORIENTED_EDGE ( 'NONE', *, *, #4163, .T. ) ;
#946=CARTESIAN_POINT ( 'NONE',  ( 0.01632152774899451458, 0.000000000000000000, 1.931620256131032054 ) ) ;
#951=AXIS2_PLACEMENT_3D ( 'NONE', #2689, #38071, #21551 ) ;
#955=CONICAL_SURFACE ( 'NONE', #38086, 2.246510896728926010, 0.01601546068027819014 ) ;
#963=ORIENTED_EDGE ( 'NONE', *, *, #4259, .F. ) ;
#966=VECTOR ( 'NONE', #13773, 39.37007874015748143 ) ;
#970=VERTEX_POINT ( 'NONE', #36406 ) ;
#972=VERTEX_POINT ( 'NONE', #1031 ) ;
#975=VERTEX_POINT ( 'NONE', #40536 ) ;
#978=EDGE_CURVE ( 'NONE', #35509, #32131, #8266, .T. ) ;
#982=CARTESIAN_POINT ( 'NONE',  ( 2.044241703397536192, 6.692913385826772199, -0.7159595814952630644 ) ) ;
#984=CARTESIAN_POINT ( 'NONE',  ( 2.755905511811024056, 4.960629921259846142, -1.023622047244094224 ) ) ;
#989=CARTESIAN_POINT ( 'NONE',  ( 1.293618082698028804, 0.000000000000000000, -1.168738992012442246 ) ) ;
#990=DIRECTION ( 'NONE',  ( -0.000000000000000000, -1.000000000000000000, -0.000000000000000000 ) ) ;
#1004=CARTESIAN_POINT ( 'NONE',  ( 1.331808205664952505, 0.000000000000000000, 1.125026879082043685 ) ) ;
#1014=CARTESIAN_POINT ( 'NONE',  ( 0.08119777152254364916, 1.623385212329073957, 0.000000000000000000 ) ) ;
#1015=ORIENTED_EDGE ( 'NONE', *, *, #22221, .T. ) ;
#1016=EDGE_CURVE ( 'NONE', #50754, #37363, #6363, .T. ) ;
#1025=DIRECTION ( 'NONE',  ( -0.9839295885986296675, -1.160734090543305153E-16, -0.1785568947986370669 ) ) ;
#1031=CARTESIAN_POINT ( 'NONE',  ( 1.325491792074623643, 1.485765544018708750, -2.638988599164732385 ) ) ;
#1034=ORIENTED_EDGE ( 'NONE', *, *, #27811, .F. ) ;
#1036=EDGE_CURVE ( 'NONE', #3507, #3351, #25295, .T. ) ;
#1037=ORIENTED_EDGE ( 'NONE', *, *, #26495, .F. ) ;
#1040=LINE ( 'NONE', #48246, #25143 ) ;
#1044=ORIENTED_EDGE ( 'NONE', *, *, #5472, .T. ) ;
#1046=DIRECTION ( 'NONE',  ( 0.000000000000000000, -1.000000000000000000, 0.000000000000000000 ) ) ;
#1049=ADVANCED_FACE ( 'NONE', ( #45395 ), #16313, .T. ) ;
#1055=AXIS2_PLACEMENT_3D ( 'NONE', #41927, #46527, #47018 ) ;
#1061=ORIENTED_EDGE ( 'NONE', *, *, #30500, .T. ) ;
#1064=DIRECTION ( 'NONE',  ( -1.288287287306305283E-16, 1.000000000000000000, 0.000000000000000000 ) ) ;
#1066=CONICAL_SURFACE ( 'NONE', #21685, 2.165354330708661568, 0.2617993877991570129 ) ;
#1069=ORIENTED_EDGE ( 'NONE', *, *, #43915, .F. ) ;
#1072=CARTESIAN_POINT ( 'NONE',  ( -0.9788642269881570046, 0.000000000000000000, 1.542392924267547594 ) ) ;
#1077=ORIENTED_EDGE ( 'NONE', *, *, #35917, .F. ) ;
#1079=EDGE_LOOP ( 'NONE', ( #23511, #43814, #17866, #31625, #14880, #20227, #36101, #49457, #5457, #21591, #15292 ) ) ;
#1080=CARTESIAN_POINT ( 'NONE',  ( 0.000000000000000000, 6.692913385826772199, 0.000000000000000000 ) ) ;
#1081=EDGE_LOOP ( 'NONE', ( #41232, #49198, #10708, #49790, #31537, #35455, #45146 ) ) ;
#1085=FACE_OUTER_BOUND ( 'NONE', #25070, .T. ) ;
#1088=CARTESIAN_POINT ( 'NONE',  ( -2.946551303128973842, 1.574890269766889617, -0.1815919737934194866 ) ) ;
#1091=DIRECTION ( 'NONE',  ( -0.9998717552508121775, -0.01601477604151182663, 0.000000000000000000 ) ) ;
#1093=CARTESIAN_POINT ( 'NONE',  ( -0.04921259842519708216, 1.641496925592597966, 2.242214099218965195 ) ) ;
#1099=VECTOR ( 'NONE', #21493, 39.37007874015748143 ) ;
#1100=CIRCLE ( 'NONE', #19261, 1.850107469027523432 ) ;
#1104=CARTESIAN_POINT ( 'NONE',  ( 0.4506430153629077950, 0.03513753811042658048, -1.817852439337431569 ) ) ;
#1105=ORIENTED_EDGE ( 'NONE', *, *, #22057, .T. ) ;
#1107=VECTOR ( 'NONE', #1890, 39.37007874015748854 ) ;
#1108=CARTESIAN_POINT ( 'NONE',  ( 2.593208359734349600, 1.657742242070020078, 0.8943296607142533494 ) ) ;
#1118=EDGE_CURVE ( 'NONE', #12966, #34448, #33059, .T. ) ;
#1120=EDGE_CURVE ( 'NONE', #13966, #33237, #31590, .T. ) ;
#1121=ORIENTED_EDGE ( 'NONE', *, *, #19037, .F. ) ;
#1123=CARTESIAN_POINT ( 'NONE',  ( 1.905060681038603265, 5.905511811023623991, 1.081042454612135773 ) ) ;
#1128=CARTESIAN_POINT ( 'NONE',  ( -1.494044303739022972, 0.003989811691878806209, -0.9272426299426647089 ) ) ;
#1129=AXIS2_PLACEMENT_3D ( 'NONE', #36037, #4536, #16929 ) ;
#1135=PLANE ( 'NONE',  #40235 ) ;
#1137=EDGE_CURVE ( 'NONE', #21069, #35652, #9293, .T. ) ;
#1143=B_SPLINE_CURVE_WITH_KNOTS ( 'NONE', 3,
 ( #5463, #32852, #20953, #1072 ),
 .UNSPECIFIED., .F., .F.,
 ( 4, 4 ),
 ( 0.001269765538541185778, 0.002242903636894877199 ),
 .UNSPECIFIED. ) ;
#1155=FACE_OUTER_BOUND ( 'NONE', #30697, .T. ) ;
#1159=LINE ( 'NONE', #16915, #43538 ) ;
#1161=CARTESIAN_POINT ( 'NONE',  ( -0.01640406444054503393, 1.620550207048756963, 2.952755905511811108 ) ) ;
#1166=DIRECTION ( 'NONE',  ( -0.9998717552508122886, -0.01601477604151181275, 0.000000000000000000 ) ) ;
#1169=DIRECTION ( 'NONE',  ( 0.9639628606958511314, -3.091822751912359432E-17, 0.2660368455666826115 ) ) ;
#1170=ORIENTED_EDGE ( 'NONE', *, *, #6960, .T. ) ;
#1174=B_SPLINE_CURVE_WITH_KNOTS ( 'NONE', 3,
 ( #22788, #31038, #30537, #30281 ),
 .UNSPECIFIED., .F., .F.,
 ( 4, 4 ),
 ( 0.0001044316291836491680, 0.0001857920852460473622 ),
 .UNSPECIFIED. ) ;
#1175=ORIENTED_EDGE ( 'NONE', *, *, #47514, .F. ) ;
#1176=CARTESIAN_POINT ( 'NONE',  ( 1.990939428460624105, 0.03922503611537826729, 0.3193531217849331916 ) ) ;
#1181=ADVANCED_FACE ( 'NONE', ( #22943 ), #3071, .F. ) ;
#1187=CARTESIAN_POINT ( 'NONE',  ( 1.108686381432267831, 0.03016422574328766690, -1.609701364138947932 ) ) ;
#1191=EDGE_LOOP ( 'NONE', ( #46329, #19740, #20982, #5370 ) ) ;
#1197=ORIENTED_EDGE ( 'NONE', *, *, #367, .T. ) ;
#1199=EDGE_CURVE ( 'NONE', #41298, #4851, #40189, .T. ) ;
#1212=EDGE_LOOP ( 'NONE', ( #48675, #11331, #11084, #8919 ) ) ;
#1214=AXIS2_PLACEMENT_3D ( 'NONE', #28218, #32119, #4738 ) ;
#1218=CIRCLE ( 'NONE', #30918, 2.165354330708661568 ) ;
#1221=AXIS2_PLACEMENT_3D ( 'NONE', #12573, #8192, #39683 ) ;
#1223=CARTESIAN_POINT ( 'NONE',  ( -1.647545174055839556, 0.001531214329375737114, 0.5870650656849111249 ) ) ;
#1225=DIRECTION ( 'NONE',  ( 0.000000000000000000, 0.000000000000000000, 1.000000000000000000 ) ) ;
#1226=CARTESIAN_POINT ( 'NONE',  ( -0.2646829987305902021, 0.000000000000000000, -2.940868978332400463 ) ) ;
#1228=EDGE_LOOP ( 'NONE', ( #6121, #26183, #37911, #48872, #37849, #48926, #785, #4251, #9270, #6248, #19395 ) ) ;
#1229=CARTESIAN_POINT ( 'NONE',  ( 2.721588343796087717, 1.663187266887471205, -1.145422814533112899 ) ) ;
#1230=VERTEX_POINT ( 'NONE', #19308 ) ;
#1234=CARTESIAN_POINT ( 'NONE',  ( -1.483604961240789999, 6.692913385826772199, 1.623324365321668017 ) ) ;
#1238=DIRECTION ( 'NONE',  ( -0.9510565162951544194, 0.000000000000000000, 0.3090169943749447312 ) ) ;
#1241=B_SPLINE_CURVE_WITH_KNOTS ( 'NONE', 3,
 ( #46633, #50230, #27539, #3293 ),
 .UNSPECIFIED., .F., .F.,
 ( 4, 4 ),
 ( 2.175073874924207950E-07, 0.002500264360679614953 ),
 .UNSPECIFIED. ) ;
#1242=ORIENTED_EDGE ( 'NONE', *, *, #32021, .F. ) ;
#1245=DIRECTION ( 'NONE',  ( 0.9009688679024154823, -5.039827768864211898E-17, 0.4338837391175656699 ) ) ;
#1248=LINE ( 'NONE', #13380, #46404 ) ;
#1249=AXIS2_PLACEMENT_3D ( 'NONE', #6719, #22464, #38223 ) ;
#1252=FACE_OUTER_BOUND ( 'NONE', #35938, .T. ) ;
#1256=CARTESIAN_POINT ( 'NONE',  ( 0.002207914879453961969, 6.692913385826772199, 0.04916304461325451958 ) ) ;
#1259=CARTESIAN_POINT ( 'NONE',  ( 1.472219874544873131, 1.482402307789154161, 2.560030851058970214 ) ) ;
#1262=CARTESIAN_POINT ( 'NONE',  ( -2.437180031585919782, 0.000000000000000000, -1.667735833703134274 ) ) ;
#1263=DIRECTION ( 'NONE',  ( 0.000000000000000000, 0.000000000000000000, 1.000000000000000000 ) ) ;
#1264=CARTESIAN_POINT ( 'NONE',  ( 1.775400203342704764, 0.000000000000000000, -2.359903268218703332 ) ) ;
#1265=EDGE_CURVE ( 'NONE', #2673, #22594, #46900, .T. ) ;
#1268=ORIENTED_EDGE ( 'NONE', *, *, #5447, .F. ) ;
#1272=ORIENTED_EDGE ( 'NONE', *, *, #39929, .T. ) ;
#1278=FACE_OUTER_BOUND ( 'NONE', #30664, .T. ) ;
#1279=VECTOR ( 'NONE', #44855, 39.37007874015748854 ) ;
#1280=VERTEX_POINT ( 'NONE', #14438 ) ;
#1283=CARTESIAN_POINT ( 'NONE',  ( 0.3382312733057617482, 0.000000000000000000, -2.139420919314966252 ) ) ;
#1284=LINE ( 'NONE', #36919, #33960 ) ;
#1285=LINE ( 'NONE', #31765, #43320 ) ;
#1291=CARTESIAN_POINT ( 'NONE',  ( 2.009930929872536964, 5.118110236220475784, -0.8055662819783824258 ) ) ;
#1295=ORIENTED_EDGE ( 'NONE', *, *, #4075, .F. ) ;
#1297=CARTESIAN_POINT ( 'NONE',  ( 2.043634885149959057, 2.755905511811027164, 0.7157624142946238388 ) ) ;
#1298=FACE_OUTER_BOUND ( 'NONE', #33484, .T. ) ;
#1304=DIRECTION ( 'NONE',  ( 0.8584487936018655452, 1.288287287306305283E-16, 0.5128992774059071280 ) ) ;
#1318=B_SPLINE_CURVE_WITH_KNOTS ( 'NONE', 3,
 ( #4284, #20546, #16940, #48127 ),
 .UNSPECIFIED., .F., .F.,
 ( 4, 4 ),
 ( 0.001216554165443645879, 0.007368042712400780722 ),
 .UNSPECIFIED. ) ;
#1324=EDGE_CURVE ( 'NONE', #2307, #6610, #19855, .T. ) ;
#1328=EDGE_CURVE ( 'NONE', #49786, #32363, #35580, .T. ) ;
#1331=EDGE_LOOP ( 'NONE', ( #34243, #8014 ) ) ;
#1333=CARTESIAN_POINT ( 'NONE',  ( 0.000000000000000000, 0.000000000000000000, 0.000000000000000000 ) ) ;
#1337=EDGE_LOOP ( 'NONE', ( #31562, #18762, #829, #6290 ) ) ;
#1342=DIRECTION ( 'NONE',  ( -0.000000000000000000, -1.000000000000000000, -0.000000000000000000 ) ) ;
#1343=CARTESIAN_POINT ( 'NONE',  ( 1.941690073511757264, 1.644018020651508039, 1.611391439051777397 ) ) ;
#1344=EDGE_CURVE ( 'NONE', #28139, #15315, #50012, .T. ) ;
#1349=CONICAL_SURFACE ( 'NONE', #24427, 2.165354330708661568, 0.2617993877991570129 ) ;
#1353=AXIS2_PLACEMENT_3D ( 'NONE', #21371, #9494, #21114 ) ;
#1354=AXIS2_PLACEMENT_3D ( 'NONE', #33462, #21825, #37583 ) ;
#1368=LINE ( 'NONE', #32626, #40762 ) ;
#1376=CARTESIAN_POINT ( 'NONE',  ( -0.6651440563933165295, 1.049866565067837820, 1.912327269821209486 ) ) ;
#1377=CARTESIAN_POINT ( 'NONE',  ( 2.044241703397535748, 5.905511811023623991, -0.7159595814952628423 ) ) ;
#1379=CARTESIAN_POINT ( 'NONE',  ( -1.651646936617113148, 1.205361022782829114E-17, 0.5883978091303396774 ) ) ;
#1385=CYLINDRICAL_SURFACE ( 'NONE', #23000, 2.165354330708661568 ) ;
#1388=CARTESIAN_POINT ( 'NONE',  ( 2.318778318137675321, 1.461867355335562113, 1.828196727724137549 ) ) ;
#1392=ORIENTED_EDGE ( 'NONE', *, *, #10069, .T. ) ;
#1393=CARTESIAN_POINT ( 'NONE',  ( 1.823552992613439505, 0.03751337948320442039, -0.8329433802140283616 ) ) ;
#1402=DIRECTION ( 'NONE',  ( -0.2660368455666826115, -1.118798511145731007E-16, 0.9639628606958511314 ) ) ;
#1410=CARTESIAN_POINT ( 'NONE',  ( -1.052882153225050521, 1.604404232578344303, 2.758709064509768716 ) ) ;
#1415=ORIENTED_EDGE ( 'NONE', *, *, #6430, .T. ) ;
#1420=DIRECTION ( 'NONE',  ( 0.1342332658176667304, 1.288287287306305530E-16, -0.9909497617679332571 ) ) ;
#1426=VERTEX_POINT ( 'NONE', #10449 ) ;
#1428=ADVANCED_FACE ( 'NONE', ( #10192 ), #10577, .T. ) ;
#1429=CIRCLE ( 'NONE', #12961, 1.743387098533651480 ) ;
#1432=CARTESIAN_POINT ( 'NONE',  ( 1.712499999125641770, 0.5249316475426859530, -0.7854770528406901375 ) ) ;
#1434=AXIS2_PLACEMENT_3D ( 'NONE', #19771, #47873, #28542 ) ;
#1435=CARTESIAN_POINT ( 'NONE',  ( -1.790681247139289889, 1.679220913509628543, -1.240985722462402352 ) ) ;
#1436=DIRECTION ( 'NONE',  ( -0.000000000000000000, -1.000000000000000000, -0.000000000000000000 ) ) ;
#1445=CONICAL_SURFACE ( 'NONE', #35355, 3.033577403570480779, 1.554780866114618743 ) ;
#1448=CARTESIAN_POINT ( 'NONE',  ( 3.937007874015748143, 5.118110236220475784, -1.181102362204724310 ) ) ;
#1453=LINE ( 'NONE', #5838, #41719 ) ;
#1461=AXIS2_PLACEMENT_3D ( 'NONE', #11426, #8307, #26907 ) ;
#1464=VERTEX_POINT ( 'NONE', #45529 ) ;
#1466=CARTESIAN_POINT ( 'NONE',  ( 1.312248418042880171, 5.905511811023623991, -1.722429524498088727 ) ) ;
#1467=ORIENTED_EDGE ( 'NONE', *, *, #35053, .T. ) ;
#1468=CIRCLE ( 'NONE', #2320, 2.244934639244525076 ) ;
#1471=EDGE_CURVE ( 'NONE', #50937, #42335, #30310, .T. ) ;
#1475=CARTESIAN_POINT ( 'NONE',  ( 2.254349126581632667, 1.678392680027759321, -0.5650186692295513513 ) ) ;
#1484=VECTOR ( 'NONE', #23849, 39.37007874015748143 ) ;
#1489=ORIENTED_EDGE ( 'NONE', *, *, #18040, .F. ) ;
#1492=CARTESIAN_POINT ( 'NONE',  ( -2.823445274216743073, 1.576824725690453954, 0.8656477926280276014 ) ) ;
#1493=ADVANCED_FACE ( 'NONE', ( #49888 ), #34498, .T. ) ;
#1494=VECTOR ( 'NONE', #27663, 39.37007874015748143 ) ;
#1496=FACE_OUTER_BOUND ( 'NONE', #44181, .T. ) ;
#1497=EDGE_CURVE ( 'NONE', #15782, #13966, #2354, .T. ) ;
#1500=CARTESIAN_POINT ( 'NONE',  ( -1.210465362316797577, 0.005745789993395570075, 1.310690939022672863 ) ) ;
#1510=PLANE ( 'NONE',  #100 ) ;
#1516=VERTEX_POINT ( 'NONE', #6583 ) ;
#1517=CARTESIAN_POINT ( 'NONE',  ( 0.7145799201508782339, 6.692913385826772199, 2.044048657746659448 ) ) ;
#1520=CARTESIAN_POINT ( 'NONE',  ( 1.588513588560381828, 0.05336261777518135074, -1.107536019441389019 ) ) ;
#1521=CARTESIAN_POINT ( 'NONE',  ( -2.882374421592805103, 1.674323616330495756, -0.6410571176644951352 ) ) ;
#1523=LINE ( 'NONE', #47955, #33336 ) ;
#1529=CARTESIAN_POINT ( 'NONE',  ( -0.2156685157583834722, 0.000000000000000000, -2.945280361644576850 ) ) ;
#1532=LINE ( 'NONE', #13407, #45345 ) ;
#1533=EDGE_CURVE ( 'NONE', #10313, #9920, #115, .T. ) ;
#1535=DIRECTION ( 'NONE',  ( 0.4738686624730094610, 1.288287287306305530E-16, -0.8805955318567322276 ) ) ;
#1538=B_SPLINE_CURVE_WITH_KNOTS ( 'NONE', 3,
 ( #11647, #43124, #23514, #39267 ),
 .UNSPECIFIED., .F., .F.,
 ( 4, 4 ),
 ( 0.01072160763103902591, 0.03073581401287817788 ),
 .UNSPECIFIED. ) ;
#1539=CARTESIAN_POINT ( 'NONE',  ( -2.734482843737247038, 1.676638068352269029, -1.115254632218712016 ) ) ;
#1540=ORIENTED_EDGE ( 'NONE', *, *, #13965, .T. ) ;
#1542=DIRECTION ( 'NONE',  ( -3.986037398843765983E-20, -1.000000000000000000, -1.160734090543304660E-16 ) ) ;
#1543=CARTESIAN_POINT ( 'NONE',  ( -2.339241080213612545, 1.564176246289736616, 1.802537235681883843 ) ) ;
#1546=AXIS2_PLACEMENT_3D ( 'NONE', #21283, #33427, #17156 ) ;
#1549=ORIENTED_EDGE ( 'NONE', *, *, #42560, .T. ) ;
#1553=VERTEX_POINT ( 'NONE', #7833 ) ;
#1554=ORIENTED_EDGE ( 'NONE', *, *, #36695, .T. ) ;
#1557=ORIENTED_EDGE ( 'NONE', *, *, #18332, .T. ) ;
#1559=CARTESIAN_POINT ( 'NONE',  ( 0.8329809839909850799, 1.732245219823249638, -2.833254665166554442 ) ) ;
#1560=ADVANCED_FACE ( 'NONE', ( #38827 ), #34700, .T. ) ;
#1562=FACE_OUTER_BOUND ( 'NONE', #9879, .T. ) ;
#1563=EDGE_CURVE ( 'NONE', #20663, #2264, #50884, .T. ) ;
#1565=ORIENTED_EDGE ( 'NONE', *, *, #37179, .T. ) ;
#1566=CARTESIAN_POINT ( 'NONE',  ( -1.531732224425391253, 1.205361022782829114E-17, 0.8801458454442117052 ) ) ;
#1567=CARTESIAN_POINT ( 'NONE',  ( -2.878724150143177507, 0.000000000000000000, -0.6570500018395228903 ) ) ;
#1570=DIRECTION ( 'NONE',  ( -0.5128992774058949156, 0.000000000000000000, -0.8584487936018728726 ) ) ;
#1572=CARTESIAN_POINT ( 'NONE',  ( 0.1067246931122726866, 0.02962905676920215767, 0.000000000000000000 ) ) ;
#1577=DIRECTION ( 'NONE',  ( 0.000000000000000000, 0.000000000000000000, -1.000000000000000000 ) ) ;
#1592=ORIENTED_EDGE ( 'NONE', *, *, #8241, .F. ) ;
#1597=EDGE_CURVE ( 'NONE', #26915, #40703, #29559, .T. ) ;
#1607=CONICAL_SURFACE ( 'NONE', #30470, 2.165354330708661568, 0.2617993877991570129 ) ;
#1608=CARTESIAN_POINT ( 'NONE',  ( 2.011572120637293626, 1.747067225219576247, -1.855173337549795187 ) ) ;
#1615=VECTOR ( 'NONE', #32821, 39.37007874015748143 ) ;
#1618=CARTESIAN_POINT ( 'NONE',  ( -1.133754555558240673, 0.009760511380980992774, 1.372484652545675532 ) ) ;
#1619=DIRECTION ( 'NONE',  ( -0.000000000000000000, 1.000000000000000000, -0.000000000000000000 ) ) ;
#1620=B_SPLINE_CURVE_WITH_KNOTS ( 'NONE', 3,
 ( #24104, #15413, #31156, #46864 ),
 .UNSPECIFIED., .F., .F.,
 ( 4, 4 ),
 ( 0.001733726700897485554, 0.004233787427253475795 ),
 .UNSPECIFIED. ) ;
#1621=VERTEX_POINT ( 'NONE', #15824 ) ;
#1624=DIRECTION ( 'NONE',  ( -8.021399753802198224E-17, -1.000000000000000000, 8.389726389140549123E-17 ) ) ;
#1625=AXIS2_PLACEMENT_3D ( 'NONE', #18800, #12252, #34552 ) ;
#1633=CARTESIAN_POINT ( 'NONE',  ( 1.556712866041120247, 1.645058926882370542, 2.509548638715870084 ) ) ;
#1637=FACE_OUTER_BOUND ( 'NONE', #29391, .T. ) ;
#1639=VECTOR ( 'NONE', #38324, 39.37007874015748143 ) ;
#1640=VERTEX_POINT ( 'NONE', #7082 ) ;
#1643=B_SPLINE_CURVE_WITH_KNOTS ( 'NONE', 3,
 ( #17921, #45508, #10929, #2676 ),
 .UNSPECIFIED., .F., .F.,
 ( 4, 4 ),
 ( 0.1211873102087489551, 0.1625992483279400380 ),
 .UNSPECIFIED. ) ;
#1650=CARTESIAN_POINT ( 'NONE',  ( 0.002207914879453961969, 6.692913385826772199, 0.04916304461325451958 ) ) ;
#1651=CARTESIAN_POINT ( 'NONE',  ( 2.951990591674676256, 1.447429260878886348, -0.08331184815398369470 ) ) ;
#1653=AXIS2_PLACEMENT_3D ( 'NONE', #8598, #40608, #16607 ) ;
#1656=EDGE_LOOP ( 'NONE', ( #12447, #32100, #28299, #8685, #10616, #25805, #37861, #14269, #42208, #17936, #12091, #47471, #21734 ) ) ;
#1660=ADVANCED_FACE ( 'NONE', ( #30830 ), #27871, .T. ) ;
#1662=LINE ( 'NONE', #14296, #39914 ) ;
#1665=CARTESIAN_POINT ( 'NONE',  ( 2.459496094709723302, 1.652223989028923867, -0.6118421259957096403 ) ) ;
#1667=DIRECTION ( 'NONE',  ( -0.9998717552508121775, -0.01601477604151182316, 0.000000000000000000 ) ) ;
#1668=EDGE_LOOP ( 'NONE', ( #22130, #30241, #19115, #25345 ) ) ;
#1669=ORIENTED_EDGE ( 'NONE', *, *, #12384, .T. ) ;
#1671=CARTESIAN_POINT ( 'NONE',  ( -0.2430652128771638720, 6.692913385826772199, -2.151668812760861194 ) ) ;
#1678=VERTEX_POINT ( 'NONE', #23079 ) ;
#1679=CARTESIAN_POINT ( 'NONE',  ( 2.277873973731426194, 1.754757658573260048, 1.879489153247668076 ) ) ;
#1684=ORIENTED_EDGE ( 'NONE', *, *, #36213, .T. ) ;
#1685=CARTESIAN_POINT ( 'NONE',  ( 2.100227814008711835, 1.751990118145921649, -2.076109931251913565 ) ) ;
#1688=EDGE_CURVE ( 'NONE', #40324, #7249, #40096, .T. ) ;
#1692=AXIS2_PLACEMENT_3D ( 'NONE', #10784, #6664, #49473 ) ;
#1695=B_SPLINE_CURVE_WITH_KNOTS ( 'NONE', 3,
 ( #11503, #46583, #23624, #18992 ),
 .UNSPECIFIED., .F., .F.,
 ( 4, 4 ),
 ( 0.0002252789032484298071, 0.002725386641250519913 ),
 .UNSPECIFIED. ) ;
#1696=CARTESIAN_POINT ( 'NONE',  ( -0.04921259842519695726, 0.5231837827169103505, 2.213767285547495689 ) ) ;
#1699=DIRECTION ( 'NONE',  ( 3.986037398843765983E-20, 1.000000000000000000, 1.160734090543304660E-16 ) ) ;
#1703=ORIENTED_EDGE ( 'NONE', *, *, #563, .T. ) ;
#1705=DIRECTION ( 'NONE',  ( 0.000000000000000000, 1.160734090543304660E-16, -1.000000000000000000 ) ) ;
#1706=VERTEX_POINT ( 'NONE', #12728 ) ;
#1707=DIRECTION ( 'NONE',  ( -3.986037398843765983E-20, -1.000000000000000000, -1.160734090543304660E-16 ) ) ;
#1710=EDGE_LOOP ( 'NONE', ( #22231, #19484, #9226, #49238 ) ) ;
#1720=EDGE_LOOP ( 'NONE', ( #15430, #29294, #8810, #43817 ) ) ;
#1723=EDGE_CURVE ( 'NONE', #43780, #14810, #36228, .T. ) ;
#1728=EDGE_LOOP ( 'NONE', ( #7265, #35678, #33944, #14815 ) ) ;
#1729=LINE ( 'NONE', #48922, #40615 ) ;
#1730=EDGE_CURVE ( 'NONE', #48222, #50396, #16606, .T. ) ;
#1731=CARTESIAN_POINT ( 'NONE',  ( 1.491455157018016342, 0.000000000000000000, -1.448759626580099713 ) ) ;
#1734=EDGE_LOOP ( 'NONE', ( #5848, #18849, #49497, #13190 ) ) ;
#1736=ORIENTED_EDGE ( 'NONE', *, *, #21469, .T. ) ;
#1738=ORIENTED_EDGE ( 'NONE', *, *, #37835, .T. ) ;
#1739=FACE_OUTER_BOUND ( 'NONE', #27866, .T. ) ;
#1745=CARTESIAN_POINT ( 'NONE',  ( -1.152895553066196399, 5.905511811023623991, -1.833672301139088079 ) ) ;
#1748=FACE_OUTER_BOUND ( 'NONE', #35742, .T. ) ;
#1751=CARTESIAN_POINT ( 'NONE',  ( 1.198249040959072476, 0.5229268992822183604, 1.909581253797772327 ) ) ;
#1755=CARTESIAN_POINT ( 'NONE',  ( 2.755905511811024056, 0.000000000000000000, 0.000000000000000000 ) ) ;
#1757=VECTOR ( 'NONE', #29478, 39.37007874015748143 ) ;
#1761=EDGE_CURVE ( 'NONE', #2996, #43121, #35297, .T. ) ;
#1762=DIRECTION ( 'NONE',  ( -0.000000000000000000, -1.000000000000000000, -0.000000000000000000 ) ) ;
#1766=EDGE_CURVE ( 'NONE', #38164, #33053, #17116, .T. ) ;
#1769=CARTESIAN_POINT ( 'NONE',  ( 0.1250607540065018508, 1.205361022782829114E-17, -1.938545675207280272 ) ) ;
#1771=DIRECTION ( 'NONE',  ( -0.000000000000000000, 1.000000000000000000, -0.000000000000000000 ) ) ;
#1774=CARTESIAN_POINT ( 'NONE',  ( -1.068075307999488244, 6.692913385826772199, 1.883606783264637041 ) ) ;
#1775=CARTESIAN_POINT ( 'NONE',  ( -3.051175669084205122, 5.118110236220475784, 0.7468891277766208647 ) ) ;
#1777=DIRECTION ( 'NONE',  ( -0.9998717552508122886, -0.01601477604151182316, 0.000000000000000000 ) ) ;
#1779=CARTESIAN_POINT ( 'NONE',  ( 1.172646544058803419, 1.004405902117069482, -2.321602171295483519 ) ) ;
#1780=ORIENTED_EDGE ( 'NONE', *, *, #4806, .F. ) ;
#1781=FACE_OUTER_BOUND ( 'NONE', #1081, .T. ) ;
#1782=ORIENTED_EDGE ( 'NONE', *, *, #34505, .T. ) ;
#1784=CARTESIAN_POINT ( 'NONE',  ( -2.735162923786631950, 5.118110236220475784, -0.4201650439732181885 ) ) ;
#1793=CARTESIAN_POINT ( 'NONE',  ( -1.408960544533061299, 0.005352583808700523381, 1.060663264281380025 ) ) ;
#1797=AXIS2_PLACEMENT_3D ( 'NONE', #40161, #32682, #13051 ) ;
#1804=CARTESIAN_POINT ( 'NONE',  ( -2.168245791271168343, 1.560742704294596495, -2.004968704497279486 ) ) ;
#1805=VERTEX_POINT ( 'NONE', #15232 ) ;
#1807=AXIS2_PLACEMENT_3D ( 'NONE', #36604, #16468, #32221 ) ;
#1813=ADVANCED_FACE ( 'NONE', ( #31749 ), #10608, .T. ) ;
#1814=DIRECTION ( 'NONE',  ( -0.01601477604151182663, 0.9998717552508123996, -0.000000000000000000 ) ) ;
#1817=FACE_OUTER_BOUND ( 'NONE', #50210, .T. ) ;
#1822=EDGE_CURVE ( 'NONE', #24587, #45327, #31242, .T. ) ;
#1823=CARTESIAN_POINT ( 'NONE',  ( -1.599172890215280196, 1.205361022782829114E-17, 1.460879300779170498 ) ) ;
#1824=EDGE_CURVE ( 'NONE', #35318, #22173, #36431, .T. ) ;
#1830=B_SPLINE_CURVE_WITH_KNOTS ( 'NONE', 3,
 ( #8012, #19368, #3634, #11133 ),
 .UNSPECIFIED., .F., .F.,
 ( 4, 4 ),
 ( 2.136331082783953371E-07, 0.01878046567066712566 ),
 .UNSPECIFIED. ) ;
#1832=EDGE_LOOP ( 'NONE', ( #27560, #25233, #45645, #15043 ) ) ;
#1833=CARTESIAN_POINT ( 'NONE',  ( 1.942732458483374502, 0.000000000000000000, 2.223636218514625451 ) ) ;
#1835=CARTESIAN_POINT ( 'NONE',  ( 2.391446464649568338, 1.749586706978336847, 0.8287732470519283412 ) ) ;
#1845=ADVANCED_FACE ( 'NONE', ( #11360 ), #35367, .T. ) ;
#1849=VERTEX_POINT ( 'NONE', #8250 ) ;
#1851=EDGE_CURVE ( 'NONE', #33493, #44848, #29673, .T. ) ;
#1854=CARTESIAN_POINT ( 'NONE',  ( -2.576863348864732117, 1.679095609600309347, 1.442554885838411849 ) ) ;
#1856=FACE_OUTER_BOUND ( 'NONE', #10037, .T. ) ;
#1858=DIRECTION ( 'NONE',  ( -0.000000000000000000, 1.000000000000000000, -0.000000000000000000 ) ) ;
#1862=CARTESIAN_POINT ( 'NONE',  ( -0.7855418668307149188, 0.000000000000000000, -2.846347029613745416 ) ) ;
#1865=VERTEX_POINT ( 'NONE', #39744 ) ;
#1866=ORIENTED_EDGE ( 'NONE', *, *, #6780, .F. ) ;
#1867=CARTESIAN_POINT ( 'NONE',  ( 0.4788131938641111973, 1.628272305554966159, 2.914091152102192162 ) ) ;
#1868=AXIS2_PLACEMENT_3D ( 'NONE', #9555, #48999, #26061 ) ;
#1869=CARTESIAN_POINT ( 'NONE',  ( 2.947574761915768171, 5.118110236220475784, -0.1816379373804906938 ) ) ;
#1870=CARTESIAN_POINT ( 'NONE',  ( -2.455254038405515260, 1.680983089212531700, -1.640354883748661008 ) ) ;
#1874=CARTESIAN_POINT ( 'NONE',  ( -1.979793062125317471, 1.589971192595758698, 2.191257344206539948 ) ) ;
#1878=DIRECTION ( 'NONE',  ( -2.582876339026174526E-17, -1.000000000000000000, -1.131632063491654496E-16 ) ) ;
#1882=CARTESIAN_POINT ( 'NONE',  ( -1.574237088929739459, 0.000000000000000000, 0.7912475138866331692 ) ) ;
#1886=CARTESIAN_POINT ( 'NONE',  ( -1.472219874544909768, 1.546549606962118517, 2.560030851058948898 ) ) ;
#1890=DIRECTION ( 'NONE',  ( 0.9195277725514489076, -4.565640798866420661E-17, 0.3930250316539278810 ) ) ;
#1897=CARTESIAN_POINT ( 'NONE',  ( 1.942732458483374502, 0.000000000000000000, 2.223636218514625451 ) ) ;
#1898=ORIENTED_EDGE ( 'NONE', *, *, #19244, .F. ) ;
#1900=CARTESIAN_POINT ( 'NONE',  ( 2.455248528070247627, 1.458620360574546471, -1.640363231549772260 ) ) ;
#1908=EDGE_CURVE ( 'NONE', #7137, #24825, #37006, .T. ) ;
#1911=DIRECTION ( 'NONE',  ( 1.086719731106943413E-16, -1.000000000000000000, 4.078527368698718974E-17 ) ) ;
#1912=VECTOR ( 'NONE', #43681, 39.37007874015748143 ) ;
#1914=EDGE_LOOP ( 'NONE', ( #37060, #41743, #23416, #50019 ) ) ;
#1915=CARTESIAN_POINT ( 'NONE',  ( -0.2493966119946618154, 1.605482210820551758, -2.222016418551142181 ) ) ;
#1917=EDGE_CURVE ( 'NONE', #29859, #43448, #14303, .T. ) ;
#1918=ORIENTED_EDGE ( 'NONE', *, *, #33050, .T. ) ;
#1921=CARTESIAN_POINT ( 'NONE',  ( -0.5110594979943671179, 0.000000000000000000, -1.666798357583582524 ) ) ;
#1924=AXIS2_PLACEMENT_3D ( 'NONE', #31727, #42823, #23455 ) ;
#1938=DIRECTION ( 'NONE',  ( -0.9998717552508122886, -0.01601477604151181275, 0.000000000000000000 ) ) ;
#1940=ORIENTED_EDGE ( 'NONE', *, *, #43000, .T. ) ;
#1946=CARTESIAN_POINT ( 'NONE',  ( 2.947574761915768171, 1.205361022782829114E-17, -0.1816379373804913322 ) ) ;
#1948=VECTOR ( 'NONE', #40537, 39.37007874015748854 ) ;
#1951=FACE_OUTER_BOUND ( 'NONE', #36387, .T. ) ;
#1953=EDGE_CURVE ( 'NONE', #30043, #20275, #13025, .T. ) ;
#1957=ADVANCED_FACE ( 'NONE', ( #5398 ), #24769, .T. ) ;
#1962=FACE_OUTER_BOUND ( 'NONE', #20652, .T. ) ;
#1965=EDGE_CURVE ( 'NONE', #17854, #37445, #44376, .T. ) ;
#1966=DIRECTION ( 'NONE',  ( 0.000000000000000000, 0.000000000000000000, 1.000000000000000000 ) ) ;
#1968=CONICAL_SURFACE ( 'NONE', #45601, 2.246510896728926010, 0.01601546068027819014 ) ;
#1977=VERTEX_POINT ( 'NONE', #28373 ) ;
#1980=VERTEX_POINT ( 'NONE', #8506 ) ;
#1984=DIRECTION ( 'NONE',  ( 0.9998717552508121775, 0.01601477604151182663, 0.000000000000000000 ) ) ;
#1986=FACE_OUTER_BOUND ( 'NONE', #7666, .T. ) ;
#1988=DIRECTION ( 'NONE',  ( 0.01601477604151182663, -0.9998717552508123996, 0.000000000000000000 ) ) ;
#1995=EDGE_CURVE ( 'NONE', #26915, #4915, #10227, .T. ) ;
#1996=VECTOR ( 'NONE', #25407, 39.37007874015748854 ) ;
#2006=VERTEX_POINT ( 'NONE', #46570 ) ;
#2008=DIRECTION ( 'NONE',  ( -0.01601477604151182663, 0.9998717552508123996, -0.000000000000000000 ) ) ;
#2009=VERTEX_POINT ( 'NONE', #25715 ) ;
#2014=PLANE ( 'NONE',  #9984 ) ;
#2022=CARTESIAN_POINT ( 'NONE',  ( 1.834323595590318323, 0.000000000000000000, 1.151859023884926891 ) ) ;
#2028=ORIENTED_EDGE ( 'NONE', *, *, #33301, .F. ) ;
#2029=DIRECTION ( 'NONE',  ( -6.394449067488625930E-17, -1.000000000000000000, 9.687176266499597757E-17 ) ) ;
#2030=VECTOR ( 'NONE', #47127, 39.37007874015748143 ) ;
#2035=ADVANCED_FACE ( 'NONE', ( #38859 ), #24124, .T. ) ;
#2040=VERTEX_POINT ( 'NONE', #3999 ) ;
#2042=ORIENTED_EDGE ( 'NONE', *, *, #22947, .F. ) ;
#2046=ORIENTED_EDGE ( 'NONE', *, *, #38984, .T. ) ;
#2047=FACE_OUTER_BOUND ( 'NONE', #42994, .T. ) ;
#2050=CARTESIAN_POINT ( 'NONE',  ( -1.738921996492520661, 6.764728787913346618E-05, 0.1249482579781430736 ) ) ;
#2051=ORIENTED_EDGE ( 'NONE', *, *, #28454, .F. ) ;
#2052=ORIENTED_EDGE ( 'NONE', *, *, #47966, .T. ) ;
#2058=CARTESIAN_POINT ( 'NONE',  ( 0.4536155964708684651, 0.5249316475426858419, -1.828623345083124629 ) ) ;
#2059=ORIENTED_EDGE ( 'NONE', *, *, #19455, .T. ) ;
#2061=CARTESIAN_POINT ( 'NONE',  ( 0.002207914879453961969, 6.692913385826772199, 0.04916304461325451958 ) ) ;
#2063=CARTESIAN_POINT ( 'NONE',  ( -2.339241080213612989, 5.905511811023623991, 1.802537235681883843 ) ) ;
#2064=EDGE_CURVE ( 'NONE', #18162, #11395, #40734, .T. ) ;
#2066=VECTOR ( 'NONE', #16030, 39.37007874015748143 ) ;
#2068=VECTOR ( 'NONE', #9146, 39.37007874015748143 ) ;
#2070=EDGE_CURVE ( 'NONE', #2321, #4093, #16123, .T. ) ;
#2071=CARTESIAN_POINT ( 'NONE',  ( 0.8067290215917983787, 1.574803149606302854, 2.009464521518182334 ) ) ;
#2078=DIRECTION ( 'NONE',  ( 0.000000000000000000, -1.000000000000000000, 0.000000000000000000 ) ) ;
#2079=CARTESIAN_POINT ( 'NONE',  ( 1.645338673473796254, 0.05427277550655955352, -1.027111169014480296 ) ) ;
#2080=DIRECTION ( 'NONE',  ( -0.9510565162951544194, 0.000000000000000000, 0.3090169943749447312 ) ) ;
#2095=VECTOR ( 'NONE', #27789, 39.37007874015748143 ) ;
#2099=EDGE_LOOP ( 'NONE', ( #46700, #22556, #4842, #3168 ) ) ;
#2100=DIRECTION ( 'NONE',  ( -1.156061316345072978E-16, -1.000000000000000000, -1.040474016969658122E-17 ) ) ;
#2102=EDGE_CURVE ( 'NONE', #34448, #47888, #11736, .T. ) ;
#2105=CIRCLE ( 'NONE', #43287, 1.743387098533651480 ) ;
#2106=FACE_OUTER_BOUND ( 'NONE', #7010, .T. ) ;
#2111=DIRECTION ( 'NONE',  ( 0.000000000000000000, 1.160734090543304660E-16, -1.000000000000000000 ) ) ;
#2113=VERTEX_POINT ( 'NONE', #42722 ) ;
#2115=CARTESIAN_POINT ( 'NONE',  ( 0.1155636338427008941, -0.5222242541845523167, 0.000000000000000000 ) ) ;
#2118=ADVANCED_FACE ( 'NONE', ( #19227 ), #15366, .F. ) ;
#2119=ORIENTED_EDGE ( 'NONE', *, *, #28284, .F. ) ;
#2120=CARTESIAN_POINT ( 'NONE',  ( -0.4349608091551079303, 6.692913385826772199, 2.121218629000294342 ) ) ;
#2125=LINE ( 'NONE', #6761, #1099 ) ;
#2128=DIRECTION ( 'NONE',  ( 0.000000000000000000, 0.000000000000000000, 1.000000000000000000 ) ) ;
#2131=VECTOR ( 'NONE', #554, 39.37007874015748143 ) ;
#2139=AXIS2_PLACEMENT_3D ( 'NONE', #14242, #29488, #9616 ) ;
#2142=CARTESIAN_POINT ( 'NONE',  ( -0.2906532981117672110, 1.205361022782829114E-17, 1.877244666688175245 ) ) ;
#2143=CARTESIAN_POINT ( 'NONE',  ( 2.168245791271197209, 1.753049777144058297, -2.004968704497248844 ) ) ;
#2151=ORIENTED_EDGE ( 'NONE', *, *, #34267, .F. ) ;
#2153=CARTESIAN_POINT ( 'NONE',  ( 1.722303613724171623, 1.475870595485188730, -2.398480198668616392 ) ) ;
#2158=LINE ( 'NONE', #33671, #47708 ) ;
#2159=CARTESIAN_POINT ( 'NONE',  ( 0.04921259842519669359, 1.574803149606302854, 2.164795024401847456 ) ) ;
#2161=B_SPLINE_CURVE_WITH_KNOTS ( 'NONE', 3,
 ( #2715, #6846, #46062, #38846 ),
 .UNSPECIFIED., .F., .F.,
 ( 4, 4 ),
 ( 0.1211873102087489551, 0.1625992483279400380 ),
 .UNSPECIFIED. ) ;
#2162=CARTESIAN_POINT ( 'NONE',  ( 3.937007874015748143, 2.913385826771657250, 1.023622047244094446 ) ) ;
#2164=CARTESIAN_POINT ( 'NONE',  ( -0.04921259842519689481, 0.000000000000000000, -2.165433070866142007 ) ) ;
#2167=CARTESIAN_POINT ( 'NONE',  ( 1.387241876633648729, 1.574803149606302854, 1.662624236931697475 ) ) ;
#2173=AXIS2_PLACEMENT_3D ( 'NONE', #33770, #22138, #10006 ) ;
#2174=VERTEX_POINT ( 'NONE', #16899 ) ;
#2176=CARTESIAN_POINT ( 'NONE',  ( -1.681836974315507049, 0.5249316497054297148, 0.8491494812773747736 ) ) ;
#2178=VECTOR ( 'NONE', #49310, 39.37007874015748143 ) ;
#2179=VERTEX_POINT ( 'NONE', #43985 ) ;
#2182=CARTESIAN_POINT ( 'NONE',  ( 2.152441353505198940, 1.205361022782829114E-17, -0.2419059403264799679 ) ) ;
#2183=CARTESIAN_POINT ( 'NONE',  ( -2.133310810460457674, 0.5250879747123590180, 0.2393145321957796390 ) ) ;
#2186=EDGE_CURVE ( 'NONE', #24144, #19688, #25374, .T. ) ;
#2193=CARTESIAN_POINT ( 'NONE',  ( 0.4788131938641111973, 1.628272305554966159, 2.914091152102192162 ) ) ;
#2194=ORIENTED_EDGE ( 'NONE', *, *, #14285, .F. ) ;
#2201=CARTESIAN_POINT ( 'NONE',  ( 0.1067246931122726866, 0.02962905676920215767, 0.000000000000000000 ) ) ;
#2203=ADVANCED_FACE ( 'NONE', ( #21527 ), #1135, .F. ) ;
#2215=CIRCLE ( 'NONE', #49953, 1.682967650661292502 ) ;
#2226=CARTESIAN_POINT ( 'NONE',  ( 2.110884035022549732, 1.741711621820001943, -0.9557545615714394538 ) ) ;
#2228=ORIENTED_EDGE ( 'NONE', *, *, #27851, .F. ) ;
#2244=DIRECTION ( 'NONE',  ( 3.986037398843765983E-20, 1.000000000000000000, 1.160734090543304660E-16 ) ) ;
#2246=VECTOR ( 'NONE', #25440, 39.37007874015748143 ) ;
#2249=CARTESIAN_POINT ( 'NONE',  ( 1.328631193326356597, 1.732744587876588138, 2.127804219470494473 ) ) ;
#2256=ORIENTED_EDGE ( 'NONE', *, *, #8108, .F. ) ;
#2257=VECTOR ( 'NONE', #1245, 39.37007874015748143 ) ;
#2260=ADVANCED_FACE ( 'NONE', ( #6029 ), #44342, .T. ) ;
#2264=VERTEX_POINT ( 'NONE', #49102 ) ;
#2265=EDGE_CURVE ( 'NONE', #2113, #38863, #22110, .T. ) ;
#2267=DIRECTION ( 'NONE',  ( 0.000000000000000000, 0.000000000000000000, 1.000000000000000000 ) ) ;
#2272=FACE_OUTER_BOUND ( 'NONE', #23827, .T. ) ;
#2274=VERTEX_POINT ( 'NONE', #2162 ) ;
#2279=ORIENTED_EDGE ( 'NONE', *, *, #32230, .F. ) ;
#2280=CARTESIAN_POINT ( 'NONE',  ( 0.1067246931122726866, 0.02962905676920215767, 0.000000000000000000 ) ) ;
#2281=B_SPLINE_CURVE_WITH_KNOTS ( 'NONE', 3,
 ( #8835, #24840, #8067, #40343 ),
 .UNSPECIFIED., .F., .F.,
 ( 4, 4 ),
 ( 0.1211775127643062722, 0.1625894504277921315 ),
 .UNSPECIFIED. ) ;
#2290=B_SPLINE_CURVE_WITH_KNOTS ( 'NONE', 3,
 ( #44947, #40073, #9601, #4708 ),
 .UNSPECIFIED., .F., .F.,
 ( 4, 4 ),
 ( 0.001338086368243570886, 0.004829149077268580018 ),
 .UNSPECIFIED. ) ;
#2294=ORIENTED_EDGE ( 'NONE', *, *, #36093, .T. ) ;
#2301=CARTESIAN_POINT ( 'NONE',  ( -1.599172890215279974, 5.905511811023623991, 1.460879300779171164 ) ) ;
#2303=EDGE_CURVE ( 'NONE', #20098, #21303, #12173, .T. ) ;
#2305=FACE_OUTER_BOUND ( 'NONE', #48145, .T. ) ;
#2307=VERTEX_POINT ( 'NONE', #37545 ) ;
#2308=ADVANCED_FACE ( 'NONE', ( #25652 ), #2422, .F. ) ;
#2312=AXIS2_PLACEMENT_3D ( 'NONE', #38674, #46631, #14668 ) ;
#2313=EDGE_CURVE ( 'NONE', #7509, #35465, #18672, .T. ) ;
#2316=FACE_OUTER_BOUND ( 'NONE', #33186, .T. ) ;
#2318=VERTEX_POINT ( 'NONE', #33675 ) ;
#2319=ORIENTED_EDGE ( 'NONE', *, *, #49256, .T. ) ;
#2320=AXIS2_PLACEMENT_3D ( 'NONE', #31509, #42112, #35130 ) ;
#2321=VERTEX_POINT ( 'NONE', #45499 ) ;
#2323=B_SPLINE_CURVE_WITH_KNOTS ( 'NONE', 3,
 ( #41483, #6628, #44825, #6111 ),
 .UNSPECIFIED., .F., .F.,
 ( 4, 4 ),
 ( 2.018269109134904797E-07, 0.002500207302720079423 ),
 .UNSPECIFIED. ) ;
#2337=CARTESIAN_POINT ( 'NONE',  ( -0.5284761224300573712, 6.692913385826772199, -2.099874368989736784 ) ) ;
#2338=DIRECTION ( 'NONE',  ( -0.01601477604151182663, 0.9998717552508123996, -0.000000000000000000 ) ) ;
#2341=B_SPLINE_CURVE_WITH_KNOTS ( 'NONE', 3,
 ( #3364, #49796, #14483, #14740 ),
 .UNSPECIFIED., .F., .F.,
 ( 4, 4 ),
 ( 0.001822469492255983543, 0.004322476834427013172 ),
 .UNSPECIFIED. ) ;
#2344=FACE_OUTER_BOUND ( 'NONE', #43355, .T. ) ;
#2345=CARTESIAN_POINT ( 'NONE',  ( -1.546800823997126262, 1.683127104815683728, -1.546979550173933182 ) ) ;
#2346=VERTEX_POINT ( 'NONE', #30035 ) ;
#2351=ORIENTED_EDGE ( 'NONE', *, *, #26375, .T. ) ;
#2352=EDGE_LOOP ( 'NONE', ( #16503, #7392, #21030, #7725 ) ) ;
#2354=CIRCLE ( 'NONE', #33704, 2.246510896728926010 ) ;
#2360=B_SPLINE_CURVE_WITH_KNOTS ( 'NONE', 3,
 ( #26234, #50425, #15376, #39115 ),
 .UNSPECIFIED., .F., .F.,
 ( 4, 4 ),
 ( 0.001189830169353655025, 0.002095527556305008809 ),
 .UNSPECIFIED. ) ;
#2369=DIRECTION ( 'NONE',  ( -0.3513748240813304724, 1.086859790425929286E-16, -0.9362348706397417564 ) ) ;
#2372=ORIENTED_EDGE ( 'NONE', *, *, #8147, .F. ) ;
#2375=CARTESIAN_POINT ( 'NONE',  ( 1.225600105435542764, 0.000000000000000000, -1.239880218767107412 ) ) ;
#2379=CARTESIAN_POINT ( 'NONE',  ( 0.8949303405208899331, 5.905511811023623991, -1.971765468592530102 ) ) ;
#2387=DIRECTION ( 'NONE',  ( 0.3930250316539278810, 1.067170571554331359E-16, -0.9195277725514489076 ) ) ;
#2390=DIRECTION ( 'NONE',  ( -0.000000000000000000, -1.000000000000000000, 0.000000000000000000 ) ) ;
#2396=B_SPLINE_CURVE_WITH_KNOTS ( 'NONE', 3,
 ( #29789, #33680, #10162, #2167 ),
 .UNSPECIFIED., .F., .F.,
 ( 4, 4 ),
 ( 0.1211873102087489551, 0.1625992483279400103 ),
 .UNSPECIFIED. ) ;
#2397=EDGE_CURVE ( 'NONE', #47516, #33248, #27081, .T. ) ;
#2399=CARTESIAN_POINT ( 'NONE',  ( -1.511286805986099546, 0.000000000000000000, 0.8691436966266951059 ) ) ;
#2400=DIRECTION ( 'NONE',  ( 1.241861098869888840E-16, 1.000000000000000000, -3.427318860986102267E-17 ) ) ;
#2403=CARTESIAN_POINT ( 'NONE',  ( 1.971834065208953435, 5.905511811023623991, 0.8963217522330176878 ) ) ;
#2405=AXIS2_PLACEMENT_3D ( 'NONE', #1897, #9648, #21517 ) ;
#2410=B_SPLINE_CURVE_WITH_KNOTS ( 'NONE', 3,
 ( #14053, #26428, #22558, #14304 ),
 .UNSPECIFIED., .F., .F.,
 ( 4, 4 ),
 ( 0.0006976809599606449393, 0.004868339597052293195 ),
 .UNSPECIFIED. ) ;
#2411=ADVANCED_FACE ( 'NONE', ( #43661 ), #5593, .T. ) ;
#2412=LINE ( 'NONE', #5514, #37708 ) ;
#2421=ORIENTED_EDGE ( 'NONE', *, *, #42689, .T. ) ;
#2422=PLANE ( 'NONE',  #17128 ) ;
#2423=EDGE_CURVE ( 'NONE', #14924, #14452, #50054, .T. ) ;
#2424=CARTESIAN_POINT ( 'NONE',  ( 0.5550072188453405442, 1.618366210323673338, -2.196007637835879045 ) ) ;
#2426=CARTESIAN_POINT ( 'NONE',  ( 0.1067246931122726866, 0.02962905676920215767, 0.000000000000000000 ) ) ;
#2432=ORIENTED_EDGE ( 'NONE', *, *, #9263, .T. ) ;
#2440=CARTESIAN_POINT ( 'NONE',  ( 1.900276455977023549, 1.738338356005314722, -1.313328886422038710 ) ) ;
#2443=B_SPLINE_CURVE_WITH_KNOTS ( 'NONE', 3,
 ( #32915, #44748, #17912, #2424 ),
 .UNSPECIFIED., .F., .F.,
 ( 4, 4 ),
 ( 2.075194745768200593E-07, 0.01748493206081992365 ),
 .UNSPECIFIED. ) ;
#2444=ADVANCED_FACE ( 'NONE', ( #31302 ), #38583, .T. ) ;
#2451=CARTESIAN_POINT ( 'NONE',  ( 0.5110944796929292044, 1.628766292019647954, 2.908232962426333668 ) ) ;
#2452=ORIENTED_EDGE ( 'NONE', *, *, #24335, .F. ) ;
#2453=EDGE_LOOP ( 'NONE', ( #8318, #50108, #7998, #14636 ) ) ;
#2456=CARTESIAN_POINT ( 'NONE',  ( -1.285287856678015705, 0.000000000000000000, -1.251479330189099182 ) ) ;
#2459=CARTESIAN_POINT ( 'NONE',  ( -2.623503965249869729, 1.678368413758691391, 1.355882097269835107 ) ) ;
#2466=AXIS2_PLACEMENT_3D ( 'NONE', #31757, #46453, #11118 ) ;
#2468=B_SPLINE_CURVE_WITH_KNOTS ( 'NONE', 3,
 ( #3511, #19247, #47603, #19753 ),
 .UNSPECIFIED., .F., .F.,
 ( 4, 4 ),
 ( 3.374697576515009854E-07, 0.04668773305404667201 ),
 .UNSPECIFIED. ) ;
#2476=CARTESIAN_POINT ( 'NONE',  ( -0.1516443935822172906, 1.639856293254567943, -2.233914102096871801 ) ) ;
#2482=CARTESIAN_POINT ( 'NONE',  ( 0.000000000000000000, 6.692913385826772199, 0.000000000000000000 ) ) ;
#2483=ADVANCED_FACE ( 'NONE', ( #45 ), #3675, .T. ) ;
#2490=DIRECTION ( 'NONE',  ( -0.01601477604151182663, 0.9998717552508123996, -0.000000000000000000 ) ) ;
#2492=CARTESIAN_POINT ( 'NONE',  ( 1.232995795418176055, 1.205361022782829114E-17, 1.780798594093568221 ) ) ;
#2498=ORIENTED_EDGE ( 'NONE', *, *, #37156, .T. ) ;
#2499=DIRECTION ( 'NONE',  ( -3.986037398843765983E-20, -1.000000000000000000, -1.160734090543304660E-16 ) ) ;
#2500=EDGE_CURVE ( 'NONE', #25699, #47516, #3931, .T. ) ;
#2503=EDGE_CURVE ( 'NONE', #33237, #39972, #20972, .T. ) ;
#2505=ORIENTED_EDGE ( 'NONE', *, *, #15936, .T. ) ;
#2506=ADVANCED_FACE ( 'NONE', ( #34672 ), #38794, .F. ) ;
#2508=FACE_OUTER_BOUND ( 'NONE', #29409, .T. ) ;
#2512=AXIS2_PLACEMENT_3D ( 'NONE', #30832, #26943, #42690 ) ;
#2518=CARTESIAN_POINT ( 'NONE',  ( 1.305557278495039775, 1.728812839972934334, -1.880670907523083191 ) ) ;
#2519=CARTESIAN_POINT ( 'NONE',  ( -1.936702278443778624, 1.582576099004612713, 1.481523253277833740 ) ) ;
#2521=CARTESIAN_POINT ( 'NONE',  ( 1.599172890215259546, 0.000000000000000000, 1.460879300779193590 ) ) ;
#2523=CARTESIAN_POINT ( 'NONE',  ( -2.139020239325885253, 1.673641627049041514, 0.3394120305351381872 ) ) ;
#2524=FACE_OUTER_BOUND ( 'NONE', #18218, .T. ) ;
#2525=CARTESIAN_POINT ( 'NONE',  ( 2.323794147221719175, 1.745121766917047790, -0.05509951330290247667 ) ) ;
#2528=CARTESIAN_POINT ( 'NONE',  ( -2.099568260077699033, 1.574803149606302854, -0.5296909464896101261 ) ) ;
#2529=CARTESIAN_POINT ( 'NONE',  ( 2.138597145901430352, 5.118110236220475784, 0.3393547186367261159 ) ) ;
#2532=CARTESIAN_POINT ( 'NONE',  ( -2.165177485265463719, 1.673231077555005886, -0.03196544747831084332 ) ) ;
#2534=VERTEX_POINT ( 'NONE', #18044 ) ;
#2535=EDGE_CURVE ( 'NONE', #26744, #6661, #44383, .T. ) ;
#2536=EDGE_LOOP ( 'NONE', ( #23824, #22422, #1061, #6342 ) ) ;
#2541=CARTESIAN_POINT ( 'NONE',  ( 0.002207914879453961969, 5.905511811023623991, 0.04916304461325442243 ) ) ;
#2542=VECTOR ( 'NONE', #42779, 39.37007874015748143 ) ;
#2543=CARTESIAN_POINT ( 'NONE',  ( -2.399155757346499218, 1.673679064067194133, 0.3746497807080386155 ) ) ;
#2545=EDGE_LOOP ( 'NONE', ( #20541, #44905, #9589, #35485, #7751, #29242, #48570, #9649, #7172, #17047, #27660, #5011, #13651 ) ) ;
#2546=CARTESIAN_POINT ( 'NONE',  ( 0.000000000000000000, 5.905511811023623991, 0.000000000000000000 ) ) ;
#2550=ORIENTED_EDGE ( 'NONE', *, *, #43827, .T. ) ;
#2553=CARTESIAN_POINT ( 'NONE',  ( -1.152114531865843006, 1.205361022782829114E-17, 1.393499336327983729 ) ) ;
#2557=DIRECTION ( 'NONE',  ( 9.964307797194671432E-17, -1.000000000000000000, -5.953396763000495864E-17 ) ) ;
#2560=ORIENTED_EDGE ( 'NONE', *, *, #1723, .T. ) ;
#2562=DIRECTION ( 'NONE',  ( -0.3513748240813434620, 0.000000000000000000, 0.9362348706397368714 ) ) ;
#2564=ORIENTED_EDGE ( 'NONE', *, *, #231, .F. ) ;
#2565=CARTESIAN_POINT ( 'NONE',  ( 0.9442395380435398833, 1.624600478255878055, -2.074157072296122450 ) ) ;
#2568=ORIENTED_EDGE ( 'NONE', *, *, #29344, .T. ) ;
#2569=DIRECTION ( 'NONE',  ( -0.01601477604151182663, 0.9998717552508123996, -0.000000000000000000 ) ) ;
#2570=PLANE ( 'NONE',  #14674 ) ;
#2572=ORIENTED_EDGE ( 'NONE', *, *, #13681, .T. ) ;
#2573=ORIENTED_EDGE ( 'NONE', *, *, #46894, .T. ) ;
#2574=CARTESIAN_POINT ( 'NONE',  ( 0.7572931578342089187, 1.049866565067838486, 1.877743133592741698 ) ) ;
#2577=VECTOR ( 'NONE', #28841, 39.37007874015748143 ) ;
#2581=ORIENTED_EDGE ( 'NONE', *, *, #32205, .T. ) ;
#2587=CARTESIAN_POINT ( 'NONE',  ( -0.8240339662865816539, 1.629086743072089005, 2.055573381764717489 ) ) ;
#2592=VERTEX_POINT ( 'NONE', #8823 ) ;
#2594=CARTESIAN_POINT ( 'NONE',  ( -0.3136974817027967100, 1.522126940893053337, -2.936457595020224520 ) ) ;
#2598=ORIENTED_EDGE ( 'NONE', *, *, #23941, .F. ) ;
#2600=EDGE_LOOP ( 'NONE', ( #16707, #9194, #43189, #50480 ) ) ;
#2607=DIRECTION ( 'NONE',  ( -0.01601477604151182663, 0.9998717552508123996, -0.000000000000000000 ) ) ;
#2609=EDGE_CURVE ( 'NONE', #23622, #3117, #25270, .T. ) ;
#2611=ORIENTED_EDGE ( 'NONE', *, *, #41833, .T. ) ;
#2613=CARTESIAN_POINT ( 'NONE',  ( 2.951990591674675368, 0.000000000000000000, -0.08331184815398383348 ) ) ;
#2616=EDGE_CURVE ( 'NONE', #972, #5208, #21617, .T. ) ;
#2617=CARTESIAN_POINT ( 'NONE',  ( -2.216704495933535579, 1.676569812073664512, -1.000984397190004094 ) ) ;
#2624=DIRECTION ( 'NONE',  ( 0.9998717552508121775, 0.01601477604151182663, 0.000000000000000000 ) ) ;
#2626=CARTESIAN_POINT ( 'NONE',  ( -1.743268982565497449, 0.0004610889948519912205, -0.02902809809614041725 ) ) ;
#2628=CARTESIAN_POINT ( 'NONE',  ( 0.07982360342473591996, 1.709180471932028711, 0.000000000000000000 ) ) ;
#2634=ADVANCED_FACE ( 'NONE', ( #20172 ), #36139, .F. ) ;
#2637=DIRECTION ( 'NONE',  ( 3.986037398843765983E-20, 1.000000000000000000, 1.160734090543304660E-16 ) ) ;
#2638=ORIENTED_EDGE ( 'NONE', *, *, #48244, .T. ) ;
#2639=ORIENTED_EDGE ( 'NONE', *, *, #41074, .T. ) ;
#2641=CARTESIAN_POINT ( 'NONE',  ( -0.7329371533687082385, 1.663354224513332591, 2.092961330735970904 ) ) ;
#2643=CARTESIAN_POINT ( 'NONE',  ( 2.074656761899007495, 1.205361022782829114E-17, -0.6223516566630619140 ) ) ;
#2646=CARTESIAN_POINT ( 'NONE',  ( 0.002207914879453961535, -5.712274067634378313E-18, 0.04916304461325374242 ) ) ;
#2651=CARTESIAN_POINT ( 'NONE',  ( 2.259006893506616986, 1.652495484661263836, -1.550124774990060628 ) ) ;
#2652=LINE ( 'NONE', #22525, #15322 ) ;
#2655=EDGE_CURVE ( 'NONE', #21677, #13391, #15391, .T. ) ;
#2667=ORIENTED_EDGE ( 'NONE', *, *, #8525, .F. ) ;
#2670=CARTESIAN_POINT ( 'NONE',  ( 0.000000000000000000, 6.692913385826772199, 0.000000000000000000 ) ) ;
#2671=CARTESIAN_POINT ( 'NONE',  ( 1.716372756112214626, 1.049866565877818347, -1.074000356430005798 ) ) ;
#2673=VERTEX_POINT ( 'NONE', #25783 ) ;
#2676=CARTESIAN_POINT ( 'NONE',  ( 1.661821349926414726, 1.574803149606302854, 1.388203579611976268 ) ) ;
#2682=CIRCLE ( 'NONE', #25749, 2.164630168518208109 ) ;
#2684=DIRECTION ( 'NONE',  ( 5.779879058770898378E-18, 1.000000000000000000, 1.286990067732318227E-16 ) ) ;
#2685=CARTESIAN_POINT ( 'NONE',  ( -2.043634885149970160, 6.692913385826772199, 0.7157624142945935297 ) ) ;
#2688=EDGE_LOOP ( 'NONE', ( #6169, #6988, #41784, #45022, #137, #30100, #45760, #17085, #36619, #17847, #20834 ) ) ;
#2689=CARTESIAN_POINT ( 'NONE',  ( -2.308557526972533136, 0.000000000000000000, 1.841013194464759639 ) ) ;
#2690=CIRCLE ( 'NONE', #37345, 2.165354330708661568 ) ;
#2696=CARTESIAN_POINT ( 'NONE',  ( 0.2509224957585530213, 1.679112537684454676, -2.238970375727059370 ) ) ;
#2697=CARTESIAN_POINT ( 'NONE',  ( -1.326676825859837816, 1.205361022782829114E-17, -1.200346386814097999 ) ) ;
#2699=CONICAL_SURFACE ( 'NONE', #44721, 1.850107469027523210, 0.6386652850508578450 ) ;
#2701=CARTESIAN_POINT ( 'NONE',  ( 0.07982360342473591996, 1.709180471932028711, 0.000000000000000000 ) ) ;
#2707=LINE ( 'NONE', #11470, #20330 ) ;
#2709=EDGE_CURVE ( 'NONE', #33470, #13670, #38428, .T. ) ;
#2712=CARTESIAN_POINT ( 'NONE',  ( -1.930387128362887283, 1.555218655107503789, 2.234422008625466471 ) ) ;
#2715=CARTESIAN_POINT ( 'NONE',  ( 1.743145509346915256, 0.000000000000000000, -0.02902255290747513330 ) ) ;
#2719=CARTESIAN_POINT ( 'NONE',  ( 0.000000000000000000, 1.574803149606302854, 0.000000000000000000 ) ) ;
#2720=VERTEX_POINT ( 'NONE', #30675 ) ;
#2721=CYLINDRICAL_SURFACE ( 'NONE', #3171, 2.164630168518208109 ) ;
#2727=B_SPLINE_CURVE_WITH_KNOTS ( 'NONE', 3,
 ( #37920, #18037, #34301, #10287 ),
 .UNSPECIFIED., .F., .F.,
 ( 4, 4 ),
 ( 0.1211775127643062860, 0.1625894504277921315 ),
 .UNSPECIFIED. ) ;
#2738=CARTESIAN_POINT ( 'NONE',  ( 2.153610746787201435, 1.643970771453353130, -0.8669779829368272628 ) ) ;
#2748=B_SPLINE_CURVE_WITH_KNOTS ( 'NONE', 3,
 ( #23805, #23293, #4437, #39552 ),
 .UNSPECIFIED., .F., .F.,
 ( 4, 4 ),
 ( 0.01320882309506746059, 0.03074212603091753399 ),
 .UNSPECIFIED. ) ;
#2755=EDGE_CURVE ( 'NONE', #26908, #33352, #36962, .T. ) ;
#2756=ADVANCED_FACE ( 'NONE', ( #6425 ), #42542, .T. ) ;
#2757=ORIENTED_EDGE ( 'NONE', *, *, #13860, .F. ) ;
#2764=LINE ( 'NONE', #12294, #7112 ) ;
#2766=CIRCLE ( 'NONE', #37425, 2.165354330708661568 ) ;
#2767=B_SPLINE_CURVE_WITH_KNOTS ( 'NONE', 3,
 ( #17208, #28558, #24702, #5072 ),
 .UNSPECIFIED., .F., .F.,
 ( 4, 4 ),
 ( 0.01476714571944508919, 0.03075156743765733100 ),
 .UNSPECIFIED. ) ;
#2768=CARTESIAN_POINT ( 'NONE',  ( 0.000000000000000000, 0.000000000000000000, 2.952755905511811108 ) ) ;
#2771=VECTOR ( 'NONE', #40117, 39.37007874015748143 ) ;
#2772=ORIENTED_EDGE ( 'NONE', *, *, #37237, .F. ) ;
#2773=CARTESIAN_POINT ( 'NONE',  ( 1.129352609985932121, 1.660373803670742721, 1.986167711467785368 ) ) ;
#2774=DIRECTION ( 'NONE',  ( 0.000000000000000000, 0.000000000000000000, 1.000000000000000000 ) ) ;
#2781=ORIENTED_EDGE ( 'NONE', *, *, #12812, .T. ) ;
#2783=B_SPLINE_CURVE_WITH_KNOTS ( 'NONE', 3,
 ( #48143, #12820, #19525, #47113 ),
 .UNSPECIFIED., .F., .F.,
 ( 4, 4 ),
 ( 0.1211873102087489551, 0.1625992483279400103 ),
 .UNSPECIFIED. ) ;
#2784=EDGE_CURVE ( 'NONE', #15952, #45538, #14853, .T. ) ;
#2787=EDGE_LOOP ( 'NONE', ( #23679, #21720, #40074, #26383 ) ) ;
#2792=CARTESIAN_POINT ( 'NONE',  ( -1.567214440306964107, 0.002817858044914879883, 0.7874684655159520652 ) ) ;
#2794=CARTESIAN_POINT ( 'NONE',  ( -2.009930929872525418, 6.692913385826772199, -0.8055662819784122908 ) ) ;
#2798=VECTOR ( 'NONE', #32690, 39.37007874015748143 ) ;
#2807=B_SPLINE_CURVE_WITH_KNOTS ( 'NONE', 3,
 ( #28351, #17009, #44101, #9766 ),
 .UNSPECIFIED., .F., .F.,
 ( 4, 4 ),
 ( 3.600755517447333241E-07, 0.04362148976465617112 ),
 .UNSPECIFIED. ) ;
#2808=ORIENTED_EDGE ( 'NONE', *, *, #34482, .F. ) ;
#2809=CIRCLE ( 'NONE', #18471, 2.165354330708661568 ) ;
#2827=B_SPLINE_CURVE_WITH_KNOTS ( 'NONE', 3,
 ( #29053, #5313, #1696, #5571 ),
 .UNSPECIFIED., .F., .F.,
 ( 4, 4 ),
 ( 0.07024079619148275444, 0.1174078461799845929 ),
 .UNSPECIFIED. ) ;
#2828=EDGE_LOOP ( 'NONE', ( #11380, #18244, #20241, #10926 ) ) ;
#2829=B_SPLINE_CURVE_WITH_KNOTS ( 'NONE', 3,
 ( #26609, #15691, #26360, #39956 ),
 .UNSPECIFIED., .F., .F.,
 ( 4, 4 ),
 ( 0.001847190087347970510, 0.04527886744616707593 ),
 .UNSPECIFIED. ) ;
#2831=LINE ( 'NONE', #46165, #28508 ) ;
#2834=VERTEX_POINT ( 'NONE', #19544 ) ;
#2835=VERTEX_POINT ( 'NONE', #35561 ) ;
#2841=CARTESIAN_POINT ( 'NONE',  ( 0.2928062650698783909, 1.621632777088613198, -2.704337167149358567 ) ) ;
#2843=PLANE ( 'NONE',  #48668 ) ;
#2844=AXIS2_PLACEMENT_3D ( 'NONE', #37146, #20875, #8745 ) ;
#2846=DIRECTION ( 'NONE',  ( 2.866708903754326305E-17, 1.000000000000000000, 1.255987235303924321E-16 ) ) ;
#2847=EDGE_CURVE ( 'NONE', #18948, #5697, #47901, .T. ) ;
#2852=EDGE_CURVE ( 'NONE', #46840, #24596, #28805, .T. ) ;
#2858=ORIENTED_EDGE ( 'NONE', *, *, #857, .F. ) ;
#2866=CARTESIAN_POINT ( 'NONE',  ( 2.437165669488590147, 1.655293914011273682, 1.255609184467661565 ) ) ;
#2870=VECTOR ( 'NONE', #30210, 39.37007874015748143 ) ;
#2872=CARTESIAN_POINT ( 'NONE',  ( -0.5110942158649443012, 1.612844421080423585, 2.908233010304054122 ) ) ;
#2873=FACE_OUTER_BOUND ( 'NONE', #31931, .T. ) ;
#2874=DIRECTION ( 'NONE',  ( -3.986037398843765983E-20, -1.000000000000000000, -1.160734090543304660E-16 ) ) ;
#2880=ORIENTED_EDGE ( 'NONE', *, *, #41807, .T. ) ;
#2881=DIRECTION ( 'NONE',  ( -0.9998717552508121775, -0.01601477604151182316, 0.000000000000000000 ) ) ;
#2890=CARTESIAN_POINT ( 'NONE',  ( -2.327682539360300229, 1.048322422875415105, -1.048418689369857715 ) ) ;
#2893=ORIENTED_EDGE ( 'NONE', *, *, #41242, .F. ) ;
#2894=CARTESIAN_POINT ( 'NONE',  ( -0.9959141369039302694, 1.049866565067838264, 1.762829326557763254 ) ) ;
#2895=DIRECTION ( 'NONE',  ( 3.986037398843765983E-20, 1.000000000000000000, 1.160734090543304660E-16 ) ) ;
#2897=FACE_OUTER_BOUND ( 'NONE', #36066, .T. ) ;
#2900=CARTESIAN_POINT ( 'NONE',  ( -2.338262049203568171, 5.118110236220475784, -0.7080022065394827591 ) ) ;
#2903=ORIENTED_EDGE ( 'NONE', *, *, #41295, .F. ) ;
#2904=CIRCLE ( 'NONE', #36703, 1.743387098533651480 ) ;
#2906=CARTESIAN_POINT ( 'NONE',  ( 0.1155636338427008941, -0.5222242541845523167, 0.000000000000000000 ) ) ;
#2907=CIRCLE ( 'NONE', #28468, 2.165354330708661568 ) ;
#2910=CARTESIAN_POINT ( 'NONE',  ( -2.277873973731453727, 1.562946399538843290, 1.879489153247635214 ) ) ;
#2912=ORIENTED_EDGE ( 'NONE', *, *, #38774, .T. ) ;
#2916=ORIENTED_EDGE ( 'NONE', *, *, #28214, .T. ) ;
#2917=CARTESIAN_POINT ( 'NONE',  ( -2.491402175429631605, 1.581999109372839385, -1.585592796919542025 ) ) ;
#2921=B_SPLINE_CURVE_WITH_KNOTS ( 'NONE', 3,
 ( #18113, #41106, #2617, #33873 ),
 .UNSPECIFIED., .F., .F.,
 ( 4, 4 ),
 ( 2.175031271859537185E-07, 0.01985119632386593558 ),
 .UNSPECIFIED. ) ;
#2924=EDGE_CURVE ( 'NONE', #38926, #9751, #30057, .T. ) ;
#2925=CARTESIAN_POINT ( 'NONE',  ( -0.2707497483110039016, 1.707396405527592087, -2.459269194452897267 ) ) ;
#2933=ORIENTED_EDGE ( 'NONE', *, *, #23168, .F. ) ;
#2938=EDGE_LOOP ( 'NONE', ( #17566, #39632, #24346, #26723 ) ) ;
#2942=ORIENTED_EDGE ( 'NONE', *, *, #32110, .T. ) ;
#2943=CARTESIAN_POINT ( 'NONE',  ( -0.1515599155143076138, 1.705474441417569320, -2.232975473887063966 ) ) ;
#2945=VECTOR ( 'NONE', #30142, 39.37007874015748143 ) ;
#2946=ORIENTED_EDGE ( 'NONE', *, *, #41862, .F. ) ;
#2951=ORIENTED_EDGE ( 'NONE', *, *, #41510, .F. ) ;
#2953=CARTESIAN_POINT ( 'NONE',  ( 2.996777194923521126, 2.755905511811027164, 0.9139393566314084616 ) ) ;
#2957=EDGE_CURVE ( 'NONE', #5918, #22349, #11403, .T. ) ;
#2963=VECTOR ( 'NONE', #21923, 39.37007874015748143 ) ;
#2981=AXIS2_PLACEMENT_3D ( 'NONE', #44162, #20419, #4166 ) ;
#2986=ORIENTED_EDGE ( 'NONE', *, *, #3772, .T. ) ;
#2987=LINE ( 'NONE', #18735, #15620 ) ;
#2992=CARTESIAN_POINT ( 'NONE',  ( -1.400213059116977909, 1.591076668371641745, -2.010953412639263416 ) ) ;
#2996=VERTEX_POINT ( 'NONE', #1466 ) ;
#2997=VERTEX_POINT ( 'NONE', #37615 ) ;
#3001=CARTESIAN_POINT ( 'NONE',  ( 1.225600105435542764, 0.000000000000000000, -1.239880218767107412 ) ) ;
#3002=CARTESIAN_POINT ( 'NONE',  ( 0.07982360342473591996, 1.709180471932028711, 0.000000000000000000 ) ) ;
#3003=EDGE_CURVE ( 'NONE', #26865, #9331, #40519, .T. ) ;
#3004=CARTESIAN_POINT ( 'NONE',  ( 0.000000000000000000, 5.905511811023623991, 0.000000000000000000 ) ) ;
#3009=ORIENTED_EDGE ( 'NONE', *, *, #8241, .T. ) ;
#3011=ORIENTED_EDGE ( 'NONE', *, *, #41706, .F. ) ;
#3020=B_SPLINE_CURVE_WITH_KNOTS ( 'NONE', 3,
 ( #36411, #43623, #31772, #36155 ),
 .UNSPECIFIED., .F., .F.,
 ( 4, 4 ),
 ( 2.271256559101463624E-07, 0.002500295287316845264 ),
 .UNSPECIFIED. ) ;
#3023=VECTOR ( 'NONE', #46540, 39.37007874015748143 ) ;
#3026=FACE_OUTER_BOUND ( 'NONE', #29811, .T. ) ;
#3027=CARTESIAN_POINT ( 'NONE',  ( 0.002207914879453961969, 5.905511811023623991, 0.04916304461325442243 ) ) ;
#3028=ORIENTED_EDGE ( 'NONE', *, *, #15970, .T. ) ;
#3031=CARTESIAN_POINT ( 'NONE',  ( -0.7030424734358586836, 1.700546966416025096, -2.362433046144440052 ) ) ;
#3034=CARTESIAN_POINT ( 'NONE',  ( 1.472219874544872020, 5.905511811023623991, 2.560030851058969770 ) ) ;
#3037=CARTESIAN_POINT ( 'NONE',  ( -1.001904449526793695, 1.691854617476330036, -1.967052558704270426 ) ) ;
#3042=CARTESIAN_POINT ( 'NONE',  ( -1.977278193622379332, 1.577807025067274882, -0.8986486843887250275 ) ) ;
#3044=FACE_OUTER_BOUND ( 'NONE', #47672, .T. ) ;
#3045=CARTESIAN_POINT ( 'NONE',  ( -1.088485032206041980, 1.592042674141829650, 1.917766907668551069 ) ) ;
#3047=CARTESIAN_POINT ( 'NONE',  ( -2.084291548511494785, -9.441392994058988408E-17, 0.6254821886024599653 ) ) ;
#3051=CARTESIAN_POINT ( 'NONE',  ( -2.077098083605152024, 1.682859781437124225, 1.719375723742733175 ) ) ;
#3054=ORIENTED_EDGE ( 'NONE', *, *, #37642, .F. ) ;
#3056=ORIENTED_EDGE ( 'NONE', *, *, #3876, .T. ) ;
#3058=LINE ( 'NONE', #26296, #38659 ) ;
#3062=CONICAL_SURFACE ( 'NONE', #12944, 2.244934639244524632, 1.554780866114618743 ) ;
#3063=DIRECTION ( 'NONE',  ( -0.9998717552508122886, -0.01601477604151185785, 0.000000000000000000 ) ) ;
#3064=CARTESIAN_POINT ( 'NONE',  ( -0.7697287008956239518, 1.608815407510722606, -2.850711186113256801 ) ) ;
#3066=ORIENTED_EDGE ( 'NONE', *, *, #35114, .F. ) ;
#3069=ORIENTED_EDGE ( 'NONE', *, *, #42157, .T. ) ;
#3071=PLANE ( 'NONE',  #34462 ) ;
#3076=EDGE_CURVE ( 'NONE', #23904, #47505, #46599, .T. ) ;
#3077=LINE ( 'NONE', #6448, #4797 ) ;
#3078=VERTEX_POINT ( 'NONE', #17728 ) ;
#3088=CIRCLE ( 'NONE', #1434, 2.246510896728926010 ) ;
#3089=CARTESIAN_POINT ( 'NONE',  ( 2.576863348864709913, 5.905511811023623991, 1.442554885838450041 ) ) ;
#3090=DIRECTION ( 'NONE',  ( -0.01601477604151182663, 0.9998717552508123996, -0.000000000000000000 ) ) ;
#3091=LINE ( 'NONE', #46674, #25801 ) ;
#3092=PLANE ( 'NONE',  #28424 ) ;
#3093=DIRECTION ( 'NONE',  ( 0.000000000000000000, 1.160734090543304660E-16, -1.000000000000000000 ) ) ;
#3094=CARTESIAN_POINT ( 'NONE',  ( 0.8851946049640924130, 0.02786979497863227920, -1.724702069279120620 ) ) ;
#3096=ORIENTED_EDGE ( 'NONE', *, *, #21228, .F. ) ;
#3097=DIRECTION ( 'NONE',  ( -0.000000000000000000, 1.000000000000000000, 0.000000000000000000 ) ) ;
#3101=CARTESIAN_POINT ( 'NONE',  ( 0.6423411368267323285, 0.5233491696640697466, -2.142486692618893684 ) ) ;
#3104=EDGE_LOOP ( 'NONE', ( #29069, #28174, #40713, #4819 ) ) ;
#3106=EDGE_CURVE ( 'NONE', #30941, #13400, #3499, .T. ) ;
#3113=CIRCLE ( 'NONE', #38953, 2.165354330708661568 ) ;
#3115=CARTESIAN_POINT ( 'NONE',  ( 2.623503965249849301, 1.661669217907264740, 1.355882097269874187 ) ) ;
#3117=VERTEX_POINT ( 'NONE', #11250 ) ;
#3127=CARTESIAN_POINT ( 'NONE',  ( 0.2646829987306325571, 0.000000000000000000, -2.940868978332396910 ) ) ;
#3130=EDGE_CURVE ( 'NONE', #13030, #11129, #46580, .T. ) ;
#3131=CIRCLE ( 'NONE', #28695, 1.743387098533651480 ) ;
#3132=CARTESIAN_POINT ( 'NONE',  ( 0.000000000000000000, 6.692913385826772199, 0.000000000000000000 ) ) ;
#3135=ORIENTED_EDGE ( 'NONE', *, *, #19551, .T. ) ;
#3142=EDGE_LOOP ( 'NONE', ( #24679, #26358, #50088, #35426 ) ) ;
#3143=VERTEX_POINT ( 'NONE', #18491 ) ;
#3146=ORIENTED_EDGE ( 'NONE', *, *, #38843, .T. ) ;
#3148=CARTESIAN_POINT ( 'NONE',  ( 2.020961963619422264, 0.000000000000000000, 0.6739302580930450759 ) ) ;
#3150=CARTESIAN_POINT ( 'NONE',  ( -1.735196932040237394, 1.680109596358665636, 1.320828101803479315 ) ) ;
#3151=CARTESIAN_POINT ( 'NONE',  ( 1.556712866041120247, 1.645058926882370542, 2.509548638715870084 ) ) ;
#3153=ORIENTED_EDGE ( 'NONE', *, *, #29643, .T. ) ;
#3155=CARTESIAN_POINT ( 'NONE',  ( -1.088485032206041980, 1.592042674141829650, 1.917766907668551069 ) ) ;
#3158=ORIENTED_EDGE ( 'NONE', *, *, #3617, .F. ) ;
#3159=VECTOR ( 'NONE', #11112, 39.37007874015748143 ) ;
#3160=CARTESIAN_POINT ( 'NONE',  ( -1.971834065208965203, 0.000000000000000000, 0.8963217522329899323 ) ) ;
#3164=AXIS2_PLACEMENT_3D ( 'NONE', #16738, #39971, #12348 ) ;
#3165=CARTESIAN_POINT ( 'NONE',  ( 1.905060681038603487, -1.256585629014249294E-16, 1.081042454612135106 ) ) ;
#3168=ORIENTED_EDGE ( 'NONE', *, *, #10013, .T. ) ;
#3170=ORIENTED_EDGE ( 'NONE', *, *, #32471, .F. ) ;
#3171=AXIS2_PLACEMENT_3D ( 'NONE', #21586, #1707, #41214 ) ;
#3172=CARTESIAN_POINT ( 'NONE',  ( -1.236813753895212642, 1.541669022091038732, -2.681693691597581974 ) ) ;
#3173=EDGE_CURVE ( 'NONE', #14116, #12624, #35575, .T. ) ;
#3174=ORIENTED_EDGE ( 'NONE', *, *, #38464, .F. ) ;
#3175=CARTESIAN_POINT ( 'NONE',  ( 1.312623452344844566, 0.000000000000000000, 1.722945714930923744 ) ) ;
#3176=LINE ( 'NONE', #34178, #808 ) ;
#3178=EDGE_LOOP ( 'NONE', ( #19252, #27222, #23843, #48316 ) ) ;
#3186=CARTESIAN_POINT ( 'NONE',  ( -2.548348758378718326, 1.050013800432074706, -0.06518427251839807590 ) ) ;
#3193=DIRECTION ( 'NONE',  ( -0.8584487936018655452, 0.000000000000000000, -0.5128992774059071280 ) ) ;
#3198=EDGE_CURVE ( 'NONE', #45979, #19989, #23215, .T. ) ;
#3199=FACE_OUTER_BOUND ( 'NONE', #6239, .T. ) ;
#3200=VERTEX_POINT ( 'NONE', #23116 ) ;
#3203=CARTESIAN_POINT ( 'NONE',  ( 0.5272349255864849926, 0.000000000000000000, 2.905303903342417726 ) ) ;
#3204=AXIS2_PLACEMENT_3D ( 'NONE', #38568, #10938, #31068 ) ;
#3207=CARTESIAN_POINT ( 'NONE',  ( -0.1824162227212925702, 1.021972889971727971, -2.575817126301924720 ) ) ;
#3210=CONICAL_SURFACE ( 'NONE', #46087, 1.850107469027523210, 0.6386652850508578450 ) ;
#3211=ORIENTED_EDGE ( 'NONE', *, *, #15642, .F. ) ;
#3213=LINE ( 'NONE', #15092, #6963 ) ;
#3214=CARTESIAN_POINT ( 'NONE',  ( 0.07982360342473591996, 1.709180471932028711, 0.000000000000000000 ) ) ;
#3216=EDGE_LOOP ( 'NONE', ( #43220, #10851, #17471, #40232, #47933, #5909, #8649, #32382, #28969, #29769, #45034 ) ) ;
#3223=AXIS2_PLACEMENT_3D ( 'NONE', #15563, #39306, #35439 ) ;
#3224=B_SPLINE_CURVE_WITH_KNOTS ( 'NONE', 3,
 ( #34791, #19030, #27279, #26526 ),
 .UNSPECIFIED., .F., .F.,
 ( 4, 4 ),
 ( 0.001786984533467655609, 0.004287017325207927165 ),
 .UNSPECIFIED. ) ;
#3228=EDGE_CURVE ( 'NONE', #47957, #869, #10741, .T. ) ;
#3230=ORIENTED_EDGE ( 'NONE', *, *, #47814, .F. ) ;
#3240=AXIS2_PLACEMENT_3D ( 'NONE', #39108, #6611, #14862 ) ;
#3241=EDGE_LOOP ( 'NONE', ( #4466, #3607, #39192, #8451, #33437, #10241, #41815, #15004, #38481, #19779, #50318 ) ) ;
#3243=CYLINDRICAL_SURFACE ( 'NONE', #9213, 2.164630168518208109 ) ;
#3250=DIRECTION ( 'NONE',  ( -0.000000000000000000, 1.000000000000000000, -0.000000000000000000 ) ) ;
#3251=ORIENTED_EDGE ( 'NONE', *, *, #1563, .F. ) ;
#3266=B_SPLINE_CURVE_WITH_KNOTS ( 'NONE', 3,
 ( #41625, #14762, #18639, #1867 ),
 .UNSPECIFIED., .F., .F.,
 ( 4, 4 ),
 ( 0.01307398419200031005, 0.03074127892600248685 ),
 .UNSPECIFIED. ) ;
#3267=B_SPLINE_CURVE_WITH_KNOTS ( 'NONE', 3,
 ( #4982, #44968, #9626, #25366 ),
 .UNSPECIFIED., .F., .F.,
 ( 4, 4 ),
 ( 2.656727046556617721E-07, 0.01658836988290275996 ),
 .UNSPECIFIED. ) ;
#3271=CIRCLE ( 'NONE', #51004, 2.246510896728926010 ) ;
#3273=DIRECTION ( 'NONE',  ( 0.000000000000000000, 1.000000000000000000, 0.000000000000000000 ) ) ;
#3274=CARTESIAN_POINT ( 'NONE',  ( 0.3941266864751867272, 0.01134630888347559936, 1.896204066697775970 ) ) ;
#3276=DIRECTION ( 'NONE',  ( 0.000000000000000000, 1.160734090543304660E-16, -1.000000000000000000 ) ) ;
#3282=CARTESIAN_POINT ( 'NONE',  ( -3.073077335812187894, 2.755905511811027164, 0.6509316561051810002 ) ) ;
#3284=ORIENTED_EDGE ( 'NONE', *, *, #4359, .F. ) ;
#3285=DIRECTION ( 'NONE',  ( -9.390536051998861478E-17, -1.000000000000000000, 6.822623802544654332E-17 ) ) ;
#3288=ORIENTED_EDGE ( 'NONE', *, *, #20336, .F. ) ;
#3290=EDGE_CURVE ( 'NONE', #24851, #9179, #30639, .T. ) ;
#3291=CARTESIAN_POINT ( 'NONE',  ( 1.629109206296508017, 1.701186718475893533, -1.625674421363809907 ) ) ;
#3293=CARTESIAN_POINT ( 'NONE',  ( 2.695799277629594037, 1.761268146152256575, -1.205759334241453651 ) ) ;
#3297=ORIENTED_EDGE ( 'NONE', *, *, #4382, .F. ) ;
#3298=EDGE_CURVE ( 'NONE', #40227, #35873, #39370, .T. ) ;
#3300=VERTEX_POINT ( 'NONE', #47069 ) ;
#3302=CARTESIAN_POINT ( 'NONE',  ( -1.648912428261716023, 0.001020809608550144430, 0.5875093135061575378 ) ) ;
#3304=CARTESIAN_POINT ( 'NONE',  ( 2.009930929872536964, 1.574803149606302854, -0.8055662819783826478 ) ) ;
#3308=CARTESIAN_POINT ( 'NONE',  ( 2.685986181519757210, 2.755905511811027164, -1.228718213908074119 ) ) ;
#3309=AXIS2_PLACEMENT_3D ( 'NONE', #31850, #340, #11460 ) ;
#3310=LINE ( 'NONE', #19052, #24950 ) ;
#3311=CARTESIAN_POINT ( 'NONE',  ( 0.4349608091550764555, 1.574803149606302854, 2.121218629000301004 ) ) ;
#3314=DIRECTION ( 'NONE',  ( -0.9909497617679332571, 0.000000000000000000, -0.1342332658176667304 ) ) ;
#3319=B_SPLINE_CURVE_WITH_KNOTS ( 'NONE', 3,
 ( #43400, #558, #3664, #34910 ),
 .UNSPECIFIED., .F., .F.,
 ( 4, 4 ),
 ( 5.924731125040265931E-05, 0.05030560113089571628 ),
 .UNSPECIFIED. ) ;
#3320=ADVANCED_FACE ( 'NONE', ( #19739 ), #27901, .T. ) ;
#3321=ORIENTED_EDGE ( 'NONE', *, *, #45459, .F. ) ;
#3323=CARTESIAN_POINT ( 'NONE',  ( -0.5859249214279436124, 1.049866565067837820, -1.938067127089992070 ) ) ;
#3324=DIRECTION ( 'NONE',  ( 8.881784197001252323E-16, 0.000000000000000000, 1.000000000000000000 ) ) ;
#3326=CARTESIAN_POINT ( 'NONE',  ( 0.000000000000000000, 1.574803149606302854, 0.000000000000000000 ) ) ;
#3327=EDGE_CURVE ( 'NONE', #44522, #9751, #7231, .T. ) ;
#3329=CARTESIAN_POINT ( 'NONE',  ( 2.947574761915768171, 1.205361022782829114E-17, -0.1816379373804913322 ) ) ;
#3335=CARTESIAN_POINT ( 'NONE',  ( -2.139229417893219853, 1.205361022782829114E-17, -0.3394403656973710159 ) ) ;
#3336=DIRECTION ( 'NONE',  ( 0.000000000000000000, 1.000000000000000000, 0.000000000000000000 ) ) ;
#3337=CARTESIAN_POINT ( 'NONE',  ( -2.543969358050849117, 1.049938081865076756, -0.1635119977925399981 ) ) ;
#3338=ADVANCED_FACE ( 'NONE', ( #50928 ), #8388, .T. ) ;
#3342=VECTOR ( 'NONE', #4674, 39.37007874015748143 ) ;
#3343=AXIS2_PLACEMENT_3D ( 'NONE', #15060, #38561, #23059 ) ;
#3344=CARTESIAN_POINT ( 'NONE',  ( 1.398572223930554026, 1.205361022782829114E-17, 1.525996566212370231 ) ) ;
#3346=ORIENTED_EDGE ( 'NONE', *, *, #30233, .F. ) ;
#3348=CARTESIAN_POINT ( 'NONE',  ( -0.2156685157583833057, 1.520013147563287648, -2.945280361644576850 ) ) ;
#3351=VERTEX_POINT ( 'NONE', #12512 ) ;
#3354=CARTESIAN_POINT ( 'NONE',  ( 0.9914495361338625523, 1.734714548371065312, 2.781765111341823360 ) ) ;
#3355=( BOUNDED_CURVE ( )  B_SPLINE_CURVE ( 3, ( #14492, #22745, #4329, #35829 ),
 .UNSPECIFIED., .F., .F. ) 
 B_SPLINE_CURVE_WITH_KNOTS ( ( 4, 4 ),
 ( 1.825764642043493646, 1.876704608224056381 ),
 .UNSPECIFIED. ) 
 CURVE ( )  GEOMETRIC_REPRESENTATION_ITEM ( )  RATIONAL_B_SPLINE_CURVE ( ( 1.000000000000000000, 0.9997837716768099847, 0.9997837716768099847, 1.000000000000000000 ) ) 
 REPRESENTATION_ITEM ( '' )  );
#3356=ORIENTED_EDGE ( 'NONE', *, *, #3900, .T. ) ;
#3357=EDGE_CURVE ( 'NONE', #17408, #38652, #22684, .T. ) ;
#3363=ORIENTED_EDGE ( 'NONE', *, *, #13778, .F. ) ;
#3364=CARTESIAN_POINT ( 'NONE',  ( 2.312113436335841321, 1.646509482104762334, 0.2635349935491774209 ) ) ;
#3367=DIRECTION ( 'NONE',  ( -0.9998717552508121775, -0.01601477604151185438, 0.000000000000000000 ) ) ;
#3372=DIRECTION ( 'NONE',  ( -0.000000000000000000, -1.000000000000000000, -0.000000000000000000 ) ) ;
#3374=ORIENTED_EDGE ( 'NONE', *, *, #7664, .F. ) ;
#3377=DIRECTION ( 'NONE',  ( -3.986037398843765983E-20, -1.000000000000000000, -1.160734090543304660E-16 ) ) ;
#3383=CIRCLE ( 'NONE', #32223, 2.165354330708661568 ) ;
#3389=FACE_OUTER_BOUND ( 'NONE', #42721, .T. ) ;
#3392=CARTESIAN_POINT ( 'NONE',  ( -2.047329853004924427, 1.609493418792719233, 0.7169629821276162218 ) ) ;
#3393=LINE ( 'NONE', #11644, #48565 ) ;
#3394=ORIENTED_EDGE ( 'NONE', *, *, #38672, .T. ) ;
#3395=VERTEX_POINT ( 'NONE', #29280 ) ;
#3397=CARTESIAN_POINT ( 'NONE',  ( -0.2156685157583831947, 1.617455082123532062, -2.945280361644576850 ) ) ;
#3400=DIRECTION ( 'NONE',  ( -3.981026654148454344E-17, 1.000000000000000000, -1.225234019452869602E-16 ) ) ;
#3401=CARTESIAN_POINT ( 'NONE',  ( 2.867773316779195447, 2.755905511811027164, -0.7050287376752003565 ) ) ;
#3402=EDGE_CURVE ( 'NONE', #22349, #41895, #25662, .T. ) ;
#3404=CARTESIAN_POINT ( 'NONE',  ( -0.5443978225238782498, 1.600757226547528500, -2.157565353623420723 ) ) ;
#3408=( NAMED_UNIT ( * ) PLANE_ANGLE_UNIT ( ) SI_UNIT ( $, .RADIAN. ) );
#3414=AXIS2_PLACEMENT_3D ( 'NONE', #46093, #10748, #26488 ) ;
#3416=FACE_OUTER_BOUND ( 'NONE', #36091, .T. ) ;
#3417=EDGE_LOOP ( 'NONE', ( #1170, #50567, #20684, #22013 ) ) ;
#3419=FACE_OUTER_BOUND ( 'NONE', #50236, .T. ) ;
#3423=DIRECTION ( 'NONE',  ( -0.01601477604151182663, 0.9998717552508123996, -0.000000000000000000 ) ) ;
#3429=CARTESIAN_POINT ( 'NONE',  ( -1.293618082698012151, 0.000000000000000000, -1.168738992012460898 ) ) ;
#3431=CARTESIAN_POINT ( 'NONE',  ( -2.947574761915765063, 0.000000000000000000, -0.1816379373805331598 ) ) ;
#3436=CARTESIAN_POINT ( 'NONE',  ( 1.312248418042879727, 1.574803149606302854, -1.722429524498089393 ) ) ;
#3438=ORIENTED_EDGE ( 'NONE', *, *, #44602, .T. ) ;
#3442=ORIENTED_EDGE ( 'NONE', *, *, #8413, .T. ) ;
#3445=CARTESIAN_POINT ( 'NONE',  ( 2.222091332265985208, 1.743492810207595500, 0.6702560524809636489 ) ) ;
#3446=LINE ( 'NONE', #26182, #46136 ) ;
#3447=ORIENTED_EDGE ( 'NONE', *, *, #24272, .F. ) ;
#3448=DIRECTION ( 'NONE',  ( -0.9998717552508122886, -0.01601477604151180928, 0.000000000000000000 ) ) ;
#3457=AXIS2_PLACEMENT_3D ( 'NONE', #2628, #18123, #33630 ) ;
#3459=CARTESIAN_POINT ( 'NONE',  ( -0.1158910538491989134, 0.02606345816900213982, -1.836661962001401305 ) ) ;
#3460=CARTESIAN_POINT ( 'NONE',  ( -2.951990591674674480, 1.673246673531018525, -0.08331184815402598032 ) ) ;
#3463=VECTOR ( 'NONE', #27048, 39.37007874015748143 ) ;
#3464=B_SPLINE_CURVE_WITH_KNOTS ( 'NONE', 3,
 ( #560, #47757, #24562, #31547 ),
 .UNSPECIFIED., .F., .F.,
 ( 4, 4 ),
 ( 0.1211775127643062860, 0.1625894504277921315 ),
 .UNSPECIFIED. ) ;
#3467=B_SPLINE_CURVE_WITH_KNOTS ( 'NONE', 3,
 ( #5095, #45083, #36856, #32480 ),
 .UNSPECIFIED., .F., .F.,
 ( 4, 4 ),
 ( 0.004647244867734754738, 0.007368060854785507194 ),
 .UNSPECIFIED. ) ;
#3470=FACE_OUTER_BOUND ( 'NONE', #6524, .T. ) ;
#3472=DIRECTION ( 'NONE',  ( -0.01601477604151182663, 0.9998717552508123996, -0.000000000000000000 ) ) ;
#3474=B_SPLINE_CURVE_WITH_KNOTS ( 'NONE', 3,
 ( #12705, #21222, #4957, #20699 ),
 .UNSPECIFIED., .F., .F.,
 ( 4, 4 ),
 ( 0.01081890587439299049, 0.03073583352486373987 ),
 .UNSPECIFIED. ) ;
#3475=ORIENTED_EDGE ( 'NONE', *, *, #26253, .T. ) ;
#3476=CARTESIAN_POINT ( 'NONE',  ( -2.422796457295655959, 1.673308113726643898, -0.1580701165447715717 ) ) ;
#3479=ORIENTED_EDGE ( 'NONE', *, *, #36883, .T. ) ;
#3490=ORIENTED_EDGE ( 'NONE', *, *, #23462, .T. ) ;
#3491=CARTESIAN_POINT ( 'NONE',  ( 1.461782879395301160, 6.692913385826772199, -1.598346982901808655 ) ) ;
#3494=LINE ( 'NONE', #7119, #26823 ) ;
#3499=LINE ( 'NONE', #18989, #46030 ) ;
#3502=CARTESIAN_POINT ( 'NONE',  ( 0.7145799201508789000, 1.574803149606302854, 2.044048657746659448 ) ) ;
#3504=FACE_OUTER_BOUND ( 'NONE', #11513, .T. ) ;
#3505=AXIS2_PLACEMENT_3D ( 'NONE', #9310, #32047, #33076 ) ;
#3506=ORIENTED_EDGE ( 'NONE', *, *, #26603, .T. ) ;
#3507=VERTEX_POINT ( 'NONE', #26173 ) ;
#3510=VERTEX_POINT ( 'NONE', #18931 ) ;
#3511=CARTESIAN_POINT ( 'NONE',  ( 0.3136974817028395091, 1.508467219206862664, -2.936457595020219635 ) ) ;
#3512=ORIENTED_EDGE ( 'NONE', *, *, #17558, .F. ) ;
#3514=VERTEX_POINT ( 'NONE', #34683 ) ;
#3528=DIRECTION ( 'NONE',  ( 0.000000000000000000, 0.000000000000000000, 1.000000000000000000 ) ) ;
#3530=ORIENTED_EDGE ( 'NONE', *, *, #49862, .F. ) ;
#3536=CONICAL_SURFACE ( 'NONE', #29894, 3.033577403570480779, 1.554780866114618743 ) ;
#3538=VERTEX_POINT ( 'NONE', #38315 ) ;
#3542=CARTESIAN_POINT ( 'NONE',  ( -2.221680436774566392, 1.680589266716277397, -1.525485796625656087 ) ) ;
#3545=CARTESIAN_POINT ( 'NONE',  ( 2.437180031585944207, 1.757239404341893518, -1.667735833703099191 ) ) ;
#3548=CARTESIAN_POINT ( 'NONE',  ( 2.706338173250262269, 5.118110236220475784, -1.181102362204724310 ) ) ;
#3551=DIRECTION ( 'NONE',  ( -0.01601477604151182663, 0.9998717552508123996, -0.000000000000000000 ) ) ;
#3552=FACE_OUTER_BOUND ( 'NONE', #11455, .T. ) ;
#3558=ORIENTED_EDGE ( 'NONE', *, *, #22776, .F. ) ;
#3559=LINE ( 'NONE', #15933, #33742 ) ;
#3560=CARTESIAN_POINT ( 'NONE',  ( -1.647545174055839556, 0.001531214329375737114, 0.5870650656849111249 ) ) ;
#3569=AXIS2_PLACEMENT_3D ( 'NONE', #31877, #13015, #27983 ) ;
#3570=ORIENTED_EDGE ( 'NONE', *, *, #42491, .F. ) ;
#3574=B_SPLINE_CURVE_WITH_KNOTS ( 'NONE', 3,
 ( #48348, #15680, #27040, #27549 ),
 .UNSPECIFIED., .F., .F.,
 ( 4, 4 ),
 ( 0.06640258829275558217, 0.1134071559262696122 ),
 .UNSPECIFIED. ) ;
#3577=DIRECTION ( 'NONE',  ( 0.9510565162951544194, 3.583074652439903135E-17, -0.3090169943749447312 ) ) ;
#3578=CIRCLE ( 'NONE', #15119, 1.850107469027523432 ) ;
#3579=EDGE_CURVE ( 'NONE', #31373, #16654, #1643, .T. ) ;
#3580=CARTESIAN_POINT ( 'NONE',  ( 2.793030215715258446, 1.664308485742666877, 0.9592557174602684977 ) ) ;
#3581=ORIENTED_EDGE ( 'NONE', *, *, #4699, .T. ) ;
#3582=CARTESIAN_POINT ( 'NONE',  ( 1.236813753895252832, 5.905511811023623991, -2.681693691597563767 ) ) ;
#3586=LINE ( 'NONE', #7710, #7729 ) ;
#3587=EDGE_CURVE ( 'NONE', #11648, #28908, #23015, .T. ) ;
#3591=ORIENTED_EDGE ( 'NONE', *, *, #22148, .T. ) ;
#3595=PLANE ( 'NONE',  #47412 ) ;
#3596=DIRECTION ( 'NONE',  ( -3.986037398843765983E-20, -1.000000000000000000, -1.160734090543304660E-16 ) ) ;
#3598=EDGE_CURVE ( 'NONE', #9322, #23592, #38688, .T. ) ;
#3600=VECTOR ( 'NONE', #19696, 39.37007874015748143 ) ;
#3604=AXIS2_PLACEMENT_3D ( 'NONE', #47384, #50475, #15426 ) ;
#3606=AXIS2_PLACEMENT_3D ( 'NONE', #28510, #21035, #40913 ) ;
#3607=ORIENTED_EDGE ( 'NONE', *, *, #23937, .F. ) ;
#3611=ORIENTED_EDGE ( 'NONE', *, *, #39705, .T. ) ;
#3615=ORIENTED_EDGE ( 'NONE', *, *, #6256, .T. ) ;
#3617=EDGE_CURVE ( 'NONE', #45769, #23504, #16428, .T. ) ;
#3622=DIRECTION ( 'NONE',  ( 1.086719731106949452E-16, -1.000000000000000000, -4.078527368698568598E-17 ) ) ;
#3632=CARTESIAN_POINT ( 'NONE',  ( 2.099568260077707027, 5.118110236220475784, -0.5296909464895783737 ) ) ;
#3633=ORIENTED_EDGE ( 'NONE', *, *, #35346, .T. ) ;
#3634=CARTESIAN_POINT ( 'NONE',  ( -0.9104082785719770365, 1.697261530667331764, 2.285716913819229923 ) ) ;
#3639=ORIENTED_EDGE ( 'NONE', *, *, #36140, .F. ) ;
#3642=FACE_OUTER_BOUND ( 'NONE', #11191, .T. ) ;
#3647=EDGE_CURVE ( 'NONE', #22357, #12775, #13959, .T. ) ;
#3653=DIRECTION ( 'NONE',  ( -0.9998717552508122886, -0.01601477604151180928, 0.000000000000000000 ) ) ;
#3658=DIRECTION ( 'NONE',  ( 0.000000000000000000, -1.000000000000000000, -0.000000000000000000 ) ) ;
#3663=ORIENTED_EDGE ( 'NONE', *, *, #34769, .T. ) ;
#3664=CARTESIAN_POINT ( 'NONE',  ( -2.365769827427975258, 1.048560651377708153, -0.9576591258817255259 ) ) ;
#3667=B_SPLINE_CURVE_WITH_KNOTS ( 'NONE', 3,
 ( #48983, #21158, #29407, #21660 ),
 .UNSPECIFIED., .F., .F.,
 ( 4, 4 ),
 ( 0.1211775127643062444, 0.1625894504277921315 ),
 .UNSPECIFIED. ) ;
#3670=VECTOR ( 'NONE', #30014, 39.37007874015748854 ) ;
#3675=PLANE ( 'NONE',  #12219 ) ;
#3684=ORIENTED_EDGE ( 'NONE', *, *, #12782, .F. ) ;
#3687=CARTESIAN_POINT ( 'NONE',  ( -1.675725316865139813, 1.615445346360514733, 1.399291623245470184 ) ) ;
#3694=CARTESIAN_POINT ( 'NONE',  ( 0.07982360342473591996, 1.709180471932028711, 0.000000000000000000 ) ) ;
#3698=CARTESIAN_POINT ( 'NONE',  ( -0.4788131938641533303, 1.525670379232220375, 2.914091152102185944 ) ) ;
#3700=ADVANCED_FACE ( 'NONE', ( #35689 ), #39485, .F. ) ;
#3705=CARTESIAN_POINT ( 'NONE',  ( 0.000000000000000000, 6.692913385826772199, 0.000000000000000000 ) ) ;
#3706=EDGE_LOOP ( 'NONE', ( #21359, #40431, #26582, #33419 ) ) ;
#3708=CARTESIAN_POINT ( 'NONE',  ( -1.068402561569948617, 1.205361022782829114E-17, -1.884154513482188431 ) ) ;
#3709=FACE_OUTER_BOUND ( 'NONE', #33870, .T. ) ;
#3720=VERTEX_POINT ( 'NONE', #3436 ) ;
#3722=CARTESIAN_POINT ( 'NONE',  ( -2.919165122154194769, 1.575328909575085090, 0.4450898352768660748 ) ) ;
#3724=CARTESIAN_POINT ( 'NONE',  ( 0.1155636338427008941, -0.5222242541845523167, 0.000000000000000000 ) ) ;
#3727=ORIENTED_EDGE ( 'NONE', *, *, #16699, .F. ) ;
#3729=CARTESIAN_POINT ( 'NONE',  ( 1.887300604142603921, 1.205361022782829114E-17, 0.9597141752041703500 ) ) ;
#3730=ORIENTED_EDGE ( 'NONE', *, *, #49685, .F. ) ;
#3733=CARTESIAN_POINT ( 'NONE',  ( 2.164823134740036625, 2.755905511811027164, -0.04796011690015051371 ) ) ;
#3736=CARTESIAN_POINT ( 'NONE',  ( 0.000000000000000000, 1.574803149606302854, 0.000000000000000000 ) ) ;
#3738=ORIENTED_EDGE ( 'NONE', *, *, #19711, .F. ) ;
#3740=ORIENTED_EDGE ( 'NONE', *, *, #27137, .F. ) ;
#3744=ADVANCED_FACE ( 'NONE', ( #34931 ), #22220, .F. ) ;
#3751=CARTESIAN_POINT ( 'NONE',  ( 2.168245791271197209, 1.654581109258766558, -2.004968704497248400 ) ) ;
#3756=DIRECTION ( 'NONE',  ( -0.000000000000000000, 1.000000000000000000, -0.000000000000000000 ) ) ;
#3757=CIRCLE ( 'NONE', #11972, 2.164630168518208109 ) ;
#3762=CARTESIAN_POINT ( 'NONE',  ( -1.330011864698828816, 1.686599376747761614, -1.746878811320646152 ) ) ;
#3767=DIRECTION ( 'NONE',  ( 0.2660368455666826115, 1.118798511145731007E-16, -0.9639628606958511314 ) ) ;
#3772=EDGE_CURVE ( 'NONE', #19191, #34229, #11523, .T. ) ;
#3773=ORIENTED_EDGE ( 'NONE', *, *, #50240, .F. ) ;
#3782=CARTESIAN_POINT ( 'NONE',  ( -0.8221900955658363319, -2.487559435141135932E-16, 2.050660405798877317 ) ) ;
#3784=CARTESIAN_POINT ( 'NONE',  ( 0.000000000000000000, 6.692913385826772199, 0.000000000000000000 ) ) ;
#3785=CARTESIAN_POINT ( 'NONE',  ( 2.121469926805689354, 1.574803149606302854, -0.4337334748181394528 ) ) ;
#3786=CIRCLE ( 'NONE', #45811, 2.165354330708661568 ) ;
#3790=CARTESIAN_POINT ( 'NONE',  ( 0.9914495361338622192, 1.493354361723550294, 2.781765111341823360 ) ) ;
#3791=CONICAL_SURFACE ( 'NONE', #30185, 2.165354330708661568, 0.2617993877991570129 ) ;
#3794=CARTESIAN_POINT ( 'NONE',  ( 2.437180031585944207, 1.459818316683583639, -1.667735833703099191 ) ) ;
#3795=CARTESIAN_POINT ( 'NONE',  ( 2.099568260077706583, 1.574803149606302854, -0.5296909464895790398 ) ) ;
#3796=ORIENTED_EDGE ( 'NONE', *, *, #28196, .T. ) ;
#3798=VECTOR ( 'NONE', #39322, 39.37007874015748143 ) ;
#3799=CARTESIAN_POINT ( 'NONE',  ( 0.9319704666822036243, 0.04284687812831378811, 1.655805649632502430 ) ) ;
#3800=CIRCLE ( 'NONE', #5459, 2.246510896728926010 ) ;
#3804=DIRECTION ( 'NONE',  ( 0.01601477604151182663, -0.9998717552508123996, 0.000000000000000000 ) ) ;
#3809=ORIENTED_EDGE ( 'NONE', *, *, #45756, .T. ) ;
#3812=B_SPLINE_CURVE_WITH_KNOTS ( 'NONE', 3,
 ( #47102, #45659, #15650, #29693 ),
 .UNSPECIFIED., .F., .F.,
 ( 4, 4 ),
 ( 6.235017842663103921E-07, 0.001940962322214974823 ),
 .UNSPECIFIED. ) ;
#3813=VERTEX_POINT ( 'NONE', #16841 ) ;
#3822=CIRCLE ( 'NONE', #1353, 2.246510896728926010 ) ;
#3827=ORIENTED_EDGE ( 'NONE', *, *, #17562, .T. ) ;
#3830=ADVANCED_FACE ( 'NONE', ( #8574 ), #40587, .T. ) ;
#3835=B_SPLINE_CURVE_WITH_KNOTS ( 'NONE', 3,
 ( #13251, #37259, #49075, #1874 ),
 .UNSPECIFIED., .F., .F.,
 ( 4, 4 ),
 ( 0.01136448766669267627, 0.03073633765498568968 ),
 .UNSPECIFIED. ) ;
#3836=VECTOR ( 'NONE', #16591, 39.37007874015748143 ) ;
#3838=CARTESIAN_POINT ( 'NONE',  ( -2.151809081513409438, 6.692913385826772199, 0.2418202932658334581 ) ) ;
#3839=EDGE_CURVE ( 'NONE', #36975, #47775, #2290, .T. ) ;
#3840=ORIENTED_EDGE ( 'NONE', *, *, #2709, .T. ) ;
#3843=CARTESIAN_POINT ( 'NONE',  ( 1.698224779224786429, 1.735102128624146811, -1.555582603516539875 ) ) ;
#3844=CARTESIAN_POINT ( 'NONE',  ( -1.672606463373382590, 0.000000000000000000, 0.4917175957957677923 ) ) ;
#3846=ORIENTED_EDGE ( 'NONE', *, *, #8624, .F. ) ;
#3853=CARTESIAN_POINT ( 'NONE',  ( -2.875073865529052419, 1.576011620654163226, -0.6730429436919832531 ) ) ;
#3854=CARTESIAN_POINT ( 'NONE',  ( -0.2483447015969799665, 1.715384992028094358, -2.942339451689540031 ) ) ;
#3855=ORIENTED_EDGE ( 'NONE', *, *, #38524, .T. ) ;
#3856=AXIS2_PLACEMENT_3D ( 'NONE', #9770, #10022, #16813 ) ;
#3863=FACE_OUTER_BOUND ( 'NONE', #36099, .T. ) ;
#3866=VECTOR ( 'NONE', #2369, 39.37007874015748854 ) ;
#3869=EDGE_CURVE ( 'NONE', #28527, #6610, #3474, .T. ) ;
#3872=ORIENTED_EDGE ( 'NONE', *, *, #32213, .T. ) ;
#3876=EDGE_CURVE ( 'NONE', #9331, #2040, #17853, .T. ) ;
#3878=VERTEX_POINT ( 'NONE', #26356 ) ;
#3879=CARTESIAN_POINT ( 'NONE',  ( 2.919426793319799707, 1.448220119383965443, 0.4451252810446820196 ) ) ;
#3880=ORIENTED_EDGE ( 'NONE', *, *, #12937, .T. ) ;
#3884=DIRECTION ( 'NONE',  ( -0.000000000000000000, -1.000000000000000000, -0.000000000000000000 ) ) ;
#3889=VECTOR ( 'NONE', #2029, 39.37007874015748143 ) ;
#3891=ORIENTED_EDGE ( 'NONE', *, *, #26620, .T. ) ;
#3895=ORIENTED_EDGE ( 'NONE', *, *, #33238, .T. ) ;
#3897=ORIENTED_EDGE ( 'NONE', *, *, #32265, .T. ) ;
#3899=LINE ( 'NONE', #39518, #24988 ) ;
#3900=EDGE_CURVE ( 'NONE', #10170, #19859, #37992, .T. ) ;
#3902=CARTESIAN_POINT ( 'NONE',  ( -2.889674983507169337, 1.575792602931942232, -0.6090712660038034576 ) ) ;
#3903=ORIENTED_EDGE ( 'NONE', *, *, #19551, .F. ) ;
#3904=ORIENTED_EDGE ( 'NONE', *, *, #29954, .T. ) ;
#3905=DIRECTION ( 'NONE',  ( -0.9749279121818259508, -2.578990239907041302E-17, 0.2225209339563041788 ) ) ;
#3911=DIRECTION ( 'NONE',  ( 0.01601477604151182663, -0.9998717552508123996, 0.000000000000000000 ) ) ;
#3914=LINE ( 'NONE', #16559, #42549 ) ;
#3915=CARTESIAN_POINT ( 'NONE',  ( 0.9587803188866059756, 1.007227695720354754, 2.414603754317795392 ) ) ;
#3917=CARTESIAN_POINT ( 'NONE',  ( 1.412396057062171861, 6.692913385826772199, 1.691415513056039988 ) ) ;
#3919=ORIENTED_EDGE ( 'NONE', *, *, #49429, .T. ) ;
#3923=DIRECTION ( 'NONE',  ( -0.000000000000000000, -1.000000000000000000, 0.000000000000000000 ) ) ;
#3925=ORIENTED_EDGE ( 'NONE', *, *, #42786, .T. ) ;
#3926=VECTOR ( 'NONE', #46440, 39.37007874015748143 ) ;
#3929=VECTOR ( 'NONE', #18063, 39.37007874015748143 ) ;
#3930=ORIENTED_EDGE ( 'NONE', *, *, #46196, .F. ) ;
#3931=LINE ( 'NONE', #19406, #1494 ) ;
#3933=EDGE_CURVE ( 'NONE', #10525, #37287, #17016, .T. ) ;
#3936=DIRECTION ( 'NONE',  ( -5.207613805428889878E-18, -1.000000000000000000, 1.159565308550899675E-16 ) ) ;
#3938=VECTOR ( 'NONE', #37700, 39.37007874015748143 ) ;
#3940=EDGE_LOOP ( 'NONE', ( #40661, #48022, #4146, #35435 ) ) ;
#3944=VERTEX_POINT ( 'NONE', #34371 ) ;
#3949=CONICAL_SURFACE ( 'NONE', #29494, 1.850107469027523210, 0.6386652850508578450 ) ;
#3953=CARTESIAN_POINT ( 'NONE',  ( -0.7572931579105153244, 1.049866565877818125, 1.877743133795977792 ) ) ;
#3955=EDGE_LOOP ( 'NONE', ( #2573, #39036, #34564, #5801 ) ) ;
#3956=PLANE ( 'NONE',  #23233 ) ;
#3963=DIRECTION ( 'NONE',  ( 0.04486483035050446017, 0.000000000000000000, 0.9989930665413151445 ) ) ;
#3971=ORIENTED_EDGE ( 'NONE', *, *, #25858, .F. ) ;
#3972=AXIS2_PLACEMENT_3D ( 'NONE', #19439, #27193, #35205 ) ;
#3975=ADVANCED_FACE ( 'NONE', ( #2106 ), #8166, .T. ) ;
#3976=DIRECTION ( 'NONE',  ( 8.741157232058247392E-17, -1.000000000000000000, -7.636919086868415696E-17 ) ) ;
#3978=EDGE_CURVE ( 'NONE', #45979, #45433, #23822, .T. ) ;
#3983=FACE_OUTER_BOUND ( 'NONE', #48661, .T. ) ;
#3986=FACE_OUTER_BOUND ( 'NONE', #10959, .T. ) ;
#3991=DIRECTION ( 'NONE',  ( -0.01601477604151182663, 0.9998717552508123996, -0.000000000000000000 ) ) ;
#3996=ORIENTED_EDGE ( 'NONE', *, *, #10396, .T. ) ;
#3999=CARTESIAN_POINT ( 'NONE',  ( 0.9914495361338622192, 1.493354361723550294, 2.781765111341823360 ) ) ;
#4004=EDGE_CURVE ( 'NONE', #17434, #48626, #9054, .T. ) ;
#4008=ADVANCED_FACE ( 'NONE', ( #45695 ), #41602, .T. ) ;
#4009=DIRECTION ( 'NONE',  ( -0.9909497617679352555, 0.000000000000000000, 0.1342332658176522697 ) ) ;
#4013=DIRECTION ( 'NONE',  ( -0.9998717552508122886, -0.01601477604151180928, 0.000000000000000000 ) ) ;
#4014=CARTESIAN_POINT ( 'NONE',  ( -1.405431157298717260, 1.652583001446659816, 1.683443543830524414 ) ) ;
#4015=CARTESIAN_POINT ( 'NONE',  ( 1.472697644137372697, 1.731489898814932316, 1.760436233057293354 ) ) ;
#4021=ADVANCED_FACE ( 'NONE', ( #46947 ), #44055, .T. ) ;
#4031=EDGE_CURVE ( 'NONE', #41056, #26744, #26853, .T. ) ;
#4034=B_SPLINE_CURVE_WITH_KNOTS ( 'NONE', 3,
 ( #6490, #50297, #33612, #38244 ),
 .UNSPECIFIED., .F., .F.,
 ( 4, 4 ),
 ( 6.486800511562401857E-07, 0.004335704572669431961 ),
 .UNSPECIFIED. ) ;
#4035=ORIENTED_EDGE ( 'NONE', *, *, #8635, .T. ) ;
#4038=DIRECTION ( 'NONE',  ( 0.9989930665413144784, 0.000000000000000000, 0.04486483035051863633 ) ) ;
#4040=VECTOR ( 'NONE', #50426, 39.37007874015748854 ) ;
#4042=DIRECTION ( 'NONE',  ( 0.000000000000000000, 0.000000000000000000, -1.000000000000000000 ) ) ;
#4045=CARTESIAN_POINT ( 'NONE',  ( 1.386843392441768241, 1.730114785850798587, -1.825100698618727257 ) ) ;
#4046=ORIENTED_EDGE ( 'NONE', *, *, #20099, .F. ) ;
#4047=DIRECTION ( 'NONE',  ( -0.01601477604151182663, 0.9998717552508123996, -0.000000000000000000 ) ) ;
#4050=B_SPLINE_CURVE_WITH_KNOTS ( 'NONE', 3,
 ( #22443, #34068, #39393, #35518 ),
 .UNSPECIFIED., .F., .F.,
 ( 4, 4 ),
 ( 6.183086360362561446E-07, 0.001526023582687786959 ),
 .UNSPECIFIED. ) ;
#4053=ORIENTED_EDGE ( 'NONE', *, *, #15996, .T. ) ;
#4055=FACE_OUTER_BOUND ( 'NONE', #23077, .T. ) ;
#4060=CARTESIAN_POINT ( 'NONE',  ( -1.775400203342670347, 1.593155925640307835, -2.359903268218729089 ) ) ;
#4064=ORIENTED_EDGE ( 'NONE', *, *, #26659, .T. ) ;
#4067=EDGE_CURVE ( 'NONE', #11914, #44591, #23484, .T. ) ;
#4071=EDGE_CURVE ( 'NONE', #6252, #14452, #48961, .T. ) ;
#4075=EDGE_CURVE ( 'NONE', #43798, #10470, #13901, .T. ) ;
#4076=ORIENTED_EDGE ( 'NONE', *, *, #41516, .T. ) ;
#4077=CARTESIAN_POINT ( 'NONE',  ( -1.574237088929739459, 0.000000000000000000, 0.7912475138866331692 ) ) ;
#4078=CARTESIAN_POINT ( 'NONE',  ( -2.029373727807297634, 0.5254167564079418318, 0.7111286833828837084 ) ) ;
#4079=ORIENTED_EDGE ( 'NONE', *, *, #14437, .T. ) ;
#4084=CARTESIAN_POINT ( 'NONE',  ( 0.000000000000000000, 5.118110236220475784, 0.000000000000000000 ) ) ;
#4088=ORIENTED_EDGE ( 'NONE', *, *, #28864, .F. ) ;
#4089=B_SPLINE_CURVE_WITH_KNOTS ( 'NONE', 3,
 ( #20871, #16752, #12359, #23977 ),
 .UNSPECIFIED., .F., .F.,
 ( 4, 4 ),
 ( 0.1211873102087489551, 0.1625992483279400103 ),
 .UNSPECIFIED. ) ;
#4090=VECTOR ( 'NONE', #2387, 39.37007874015748854 ) ;
#4093=VERTEX_POINT ( 'NONE', #27607 ) ;
#4096=ORIENTED_EDGE ( 'NONE', *, *, #26659, .F. ) ;
#4103=EDGE_LOOP ( 'NONE', ( #50125, #2228, #13862, #12884, #9667, #2772, #15477, #18382, #19379, #46321, #49552 ) ) ;
#4104=EDGE_LOOP ( 'NONE', ( #8643, #44794, #35310, #17285 ) ) ;
#4105=EDGE_CURVE ( 'NONE', #28109, #42832, #14994, .T. ) ;
#4108=EDGE_CURVE ( 'NONE', #12775, #7408, #41601, .T. ) ;
#4110=DIRECTION ( 'NONE',  ( 0.04486483035051863633, -1.160734090543304660E-16, -0.9989930665413144784 ) ) ;
#4116=FACE_OUTER_BOUND ( 'NONE', #49295, .T. ) ;
#4120=DIRECTION ( 'NONE',  ( 1.241861098869888840E-16, 1.000000000000000000, -3.427318860986102267E-17 ) ) ;
#4121=CONICAL_SURFACE ( 'NONE', #31318, 3.483074324928249421, 1.244861948955335196 ) ;
#4122=DIRECTION ( 'NONE',  ( 0.9998717552508121775, 0.01601477604151182663, 0.000000000000000000 ) ) ;
#4123=EDGE_CURVE ( 'NONE', #1865, #36153, #35434, .T. ) ;
#4126=EDGE_CURVE ( 'NONE', #19249, #42663, #14804, .T. ) ;
#4127=ORIENTED_EDGE ( 'NONE', *, *, #7056, .F. ) ;
#4128=CARTESIAN_POINT ( 'NONE',  ( 0.6150616064519864867, 0.03777100275179151589, 1.778883059170359493 ) ) ;
#4140=ORIENTED_EDGE ( 'NONE', *, *, #15173, .F. ) ;
#4146=ORIENTED_EDGE ( 'NONE', *, *, #38884, .T. ) ;
#4150=CARTESIAN_POINT ( 'NONE',  ( -2.576863348864732117, 5.905511811023623991, 1.442554885838411849 ) ) ;
#4155=ORIENTED_EDGE ( 'NONE', *, *, #48945, .F. ) ;
#4160=AXIS2_PLACEMENT_3D ( 'NONE', #19854, #7493, #244 ) ;
#4163=EDGE_CURVE ( 'NONE', #29523, #13784, #4898, .T. ) ;
#4164=DIRECTION ( 'NONE',  ( 0.01601477604151182663, -0.9998717552508123996, 0.000000000000000000 ) ) ;
#4166=DIRECTION ( 'NONE',  ( 0.000000000000000000, 0.000000000000000000, 1.000000000000000000 ) ) ;
#4167=CARTESIAN_POINT ( 'NONE',  ( 0.000000000000000000, 2.755905511811027164, 0.000000000000000000 ) ) ;
#4174=EDGE_CURVE ( 'NONE', #37363, #31047, #50767, .T. ) ;
#4175=CARTESIAN_POINT ( 'NONE',  ( 0.000000000000000000, 5.905511811023623991, 0.000000000000000000 ) ) ;
#4177=EDGE_CURVE ( 'NONE', #50925, #37890, #46500, .T. ) ;
#4179=CARTESIAN_POINT ( 'NONE',  ( 0.5665031287202806354, 0.01222701028677279297, -1.867693841696119517 ) ) ;
#4182=ORIENTED_EDGE ( 'NONE', *, *, #43505, .F. ) ;
#4187=CONICAL_SURFACE ( 'NONE', #3343, 1.850107469027523210, 0.6386652850508578450 ) ;
#4188=ORIENTED_EDGE ( 'NONE', *, *, #13638, .T. ) ;
#4191=CARTESIAN_POINT ( 'NONE',  ( 0.000000000000000000, 1.574803149606302854, 0.000000000000000000 ) ) ;
#4194=VERTEX_POINT ( 'NONE', #16258 ) ;
#4196=DIRECTION ( 'NONE',  ( -0.01601477604151182663, 0.9998717552508123996, -0.000000000000000000 ) ) ;
#4199=B_SPLINE_CURVE_WITH_KNOTS ( 'NONE', 3,
 ( #22328, #14830, #13117, #26441 ),
 .UNSPECIFIED., .F., .F.,
 ( 4, 4 ),
 ( 2.471583195156979454E-07, 0.002500589363332148332 ),
 .UNSPECIFIED. ) ;
#4200=ADVANCED_FACE ( 'NONE', ( #1278 ), #13185, .T. ) ;
#4209=CARTESIAN_POINT ( 'NONE',  ( -0.8244711865321519006, 0.01471425056033665718, -1.598608591632243892 ) ) ;
#4213=CARTESIAN_POINT ( 'NONE',  ( 2.138597145901430352, 1.574803149606302854, 0.3393547186367255608 ) ) ;
#4214=CARTESIAN_POINT ( 'NONE',  ( -0.04921259842519758176, 5.905511811023623103, 2.952755905511810663 ) ) ;
#4217=ORIENTED_EDGE ( 'NONE', *, *, #51006, .T. ) ;
#4218=AXIS2_PLACEMENT_3D ( 'NONE', #36097, #28078, #40481 ) ;
#4219=ORIENTED_EDGE ( 'NONE', *, *, #17462, .F. ) ;
#4222=ADVANCED_FACE ( 'NONE', ( #36656 ), #9865, .T. ) ;
#4225=EDGE_CURVE ( 'NONE', #31499, #42563, #9048, .T. ) ;
#4226=EDGE_CURVE ( 'NONE', #4194, #42469, #43864, .T. ) ;
#4232=EDGE_LOOP ( 'NONE', ( #22749, #21481, #45871, #26634 ) ) ;
#4235=CARTESIAN_POINT ( 'NONE',  ( -1.146850602398337360, 0.5249316475426863970, -1.494778961359568337 ) ) ;
#4238=ORIENTED_EDGE ( 'NONE', *, *, #21310, .F. ) ;
#4240=CARTESIAN_POINT ( 'NONE',  ( 2.059921668671832240, -8.380087113460787161E-17, 0.7210543110491615115 ) ) ;
#4241=FACE_OUTER_BOUND ( 'NONE', #6102, .T. ) ;
#4251=ORIENTED_EDGE ( 'NONE', *, *, #22247, .F. ) ;
#4254=CARTESIAN_POINT ( 'NONE',  ( 2.139229417893225182, 6.692913385826772199, -0.3394403656973405958 ) ) ;
#4255=ORIENTED_EDGE ( 'NONE', *, *, #7491, .T. ) ;
#4257=DIRECTION ( 'NONE',  ( -0.9749279121818227312, 2.586762438145473843E-17, -0.2225209339563184452 ) ) ;
#4259=EDGE_CURVE ( 'NONE', #18093, #40146, #25593, .T. ) ;
#4261=CARTESIAN_POINT ( 'NONE',  ( -1.775400203342670347, 1.691590761327236958, -2.359903268218729089 ) ) ;
#4263=AXIS2_PLACEMENT_3D ( 'NONE', #33698, #22563, #33942 ) ;
#4274=ORIENTED_EDGE ( 'NONE', *, *, #51035, .T. ) ;
#4277=PLANE ( 'NONE',  #18462 ) ;
#4278=EDGE_CURVE ( 'NONE', #21187, #13750, #49402, .T. ) ;
#4279=CIRCLE ( 'NONE', #39729, 2.165354330708661568 ) ;
#4282=CARTESIAN_POINT ( 'NONE',  ( -2.165354330708661568, 1.673228346456695492, -4.271103535670736336E-20 ) ) ;
#4284=CARTESIAN_POINT ( 'NONE',  ( -2.165354330708661568, 1.673228346456695492, -4.271103535670736336E-20 ) ) ;
#4286=CARTESIAN_POINT ( 'NONE',  ( -2.951990591674674480, 5.905511811023623991, -0.08331184815402592481 ) ) ;
#4289=ADVANCED_FACE ( 'NONE', ( #47709 ), #12385, .F. ) ;
#4291=CARTESIAN_POINT ( 'NONE',  ( -0.5455270741695672498, 1.205361022782829114E-17, -1.791688814994948808 ) ) ;
#4293=VERTEX_POINT ( 'NONE', #17793 ) ;
#4294=CARTESIAN_POINT ( 'NONE',  ( 1.236813753895252166, 1.487789312410982445, -2.681693691597563767 ) ) ;
#4304=FACE_OUTER_BOUND ( 'NONE', #8787, .T. ) ;
#4306=AXIS2_PLACEMENT_3D ( 'NONE', #10504, #14882, #42495 ) ;
#4314=ORIENTED_EDGE ( 'NONE', *, *, #26071, .F. ) ;
#4315=B_SPLINE_CURVE_WITH_KNOTS ( 'NONE', 3,
 ( #32011, #31244, #4637, #23228 ),
 .UNSPECIFIED., .F., .F.,
 ( 4, 4 ),
 ( 0.001317995325350678881, 0.003818249576796051148 ),
 .UNSPECIFIED. ) ;
#4316=EDGE_CURVE ( 'NONE', #23504, #9482, #14171, .T. ) ;
#4318=ORIENTED_EDGE ( 'NONE', *, *, #44772, .F. ) ;
#4327=CARTESIAN_POINT ( 'NONE',  ( -1.798122294034776969, 1.683198194172631279, -1.651094407303121070 ) ) ;
#4329=CARTESIAN_POINT ( 'NONE',  ( -0.3542690518128642219, 0.000000000000000000, 1.859817525206697075 ) ) ;
#4331=FACE_OUTER_BOUND ( 'NONE', #8715, .T. ) ;
#4337=EDGE_CURVE ( 'NONE', #47004, #2534, #9600, .T. ) ;
#4339=AXIS2_PLACEMENT_3D ( 'NONE', #24969, #32739, #47911 ) ;
#4341=ORIENTED_EDGE ( 'NONE', *, *, #32965, .F. ) ;
#4343=CARTESIAN_POINT ( 'NONE',  ( 2.889674983507178219, 1.764288196056212454, -0.6090712660037608250 ) ) ;
#4352=B_SPLINE_CURVE_WITH_KNOTS ( 'NONE', 3,
 ( #2917, #46499, #15989, #25898 ),
 .UNSPECIFIED., .F., .F.,
 ( 4, 4 ),
 ( 2.396517271797282383E-07, 0.002500331769455057130 ),
 .UNSPECIFIED. ) ;
#4357=CARTESIAN_POINT ( 'NONE',  ( 2.339241080213585899, 5.905511811023623991, 1.802537235681918037 ) ) ;
#4359=EDGE_CURVE ( 'NONE', #358, #46032, #22182, .T. ) ;
#4368=ORIENTED_EDGE ( 'NONE', *, *, #1328, .F. ) ;
#4372=VERTEX_POINT ( 'NONE', #14686 ) ;
#4381=DIRECTION ( 'NONE',  ( 0.000000000000000000, 1.160734090543304660E-16, -1.000000000000000000 ) ) ;
#4382=EDGE_CURVE ( 'NONE', #33806, #43121, #37689, .T. ) ;
#4390=LINE ( 'NONE', #28899, #14485 ) ;
#4392=CARTESIAN_POINT ( 'NONE',  ( -2.867773316779185677, 1.574658946938755522, -0.7050287376752426560 ) ) ;
#4395=CARTESIAN_POINT ( 'NONE',  ( 0.000000000000000000, 5.118110236220475784, 0.000000000000000000 ) ) ;
#4404=CARTESIAN_POINT ( 'NONE',  ( 0.2304536187852652684, 1.049866565877818347, -2.011542525805705139 ) ) ;
#4406=EDGE_CURVE ( 'NONE', #26900, #23170, #48960, .T. ) ;
#4409=CARTESIAN_POINT ( 'NONE',  ( -2.138597145901436125, 1.574803149606302854, 0.3393547186366939750 ) ) ;
#4412=CARTESIAN_POINT ( 'NONE',  ( 2.295325967725798222, 1.744665796922353351, 0.3605850800666594580 ) ) ;
#4413=AXIS2_PLACEMENT_3D ( 'NONE', #10729, #5583, #1966 ) ;
#4414=ORIENTED_EDGE ( 'NONE', *, *, #4259, .T. ) ;
#4419=DIRECTION ( 'NONE',  ( 0.000000000000000000, 0.000000000000000000, -1.000000000000000000 ) ) ;
#4430=EDGE_LOOP ( 'NONE', ( #50784, #19816, #19898, #41367 ) ) ;
#4431=ORIENTED_EDGE ( 'NONE', *, *, #8411, .T. ) ;
#4434=CARTESIAN_POINT ( 'NONE',  ( 1.019791434298717325, 0.5230628772194416687, -2.004195265303256868 ) ) ;
#4436=CARTESIAN_POINT ( 'NONE',  ( 0.9914495361338625523, 1.636256239573039117, 2.781765111341823360 ) ) ;
#4437=CARTESIAN_POINT ( 'NONE',  ( 0.6769013455170100890, 1.726104531401197351, -2.637681086482273063 ) ) ;
#4439=ORIENTED_EDGE ( 'NONE', *, *, #9993, .F. ) ;
#4442=EDGE_LOOP ( 'NONE', ( #12704, #50473, #29299, #46664 ) ) ;
#4443=VERTEX_POINT ( 'NONE', #20531 ) ;
#4444=FACE_OUTER_BOUND ( 'NONE', #11122, .T. ) ;
#4448=B_SPLINE_CURVE_WITH_KNOTS ( 'NONE', 3,
 ( #22263, #38268, #19130, #41626 ),
 .UNSPECIFIED., .F., .F.,
 ( 4, 4 ),
 ( 0.1211873102087489551, 0.1625992483279400380 ),
 .UNSPECIFIED. ) ;
#4461=LINE ( 'NONE', #39822, #37737 ) ;
#4462=ORIENTED_EDGE ( 'NONE', *, *, #8893, .T. ) ;
#4463=CARTESIAN_POINT ( 'NONE',  ( 0.8949303405208896001, 1.574803149606302854, -1.971765468592530102 ) ) ;
#4466=ORIENTED_EDGE ( 'NONE', *, *, #1730, .F. ) ;
#4467=CARTESIAN_POINT ( 'NONE',  ( 2.069752515245542046, 1.205361022782829114E-17, -0.5228856972975560735 ) ) ;
#4474=CARTESIAN_POINT ( 'NONE',  ( -0.4120130461783780840, 1.024878400823626245, 2.545991998580761084 ) ) ;
#4475=CARTESIAN_POINT ( 'NONE',  ( -1.775400203342670347, 1.552775173289138166, -2.359903268218729089 ) ) ;
#4477=EDGE_LOOP ( 'NONE', ( #27767, #31917, #9478, #40036 ) ) ;
#4478=EDGE_CURVE ( 'NONE', #15500, #596, #47339, .T. ) ;
#4481=CARTESIAN_POINT ( 'NONE',  ( 0.1067246931122726866, 0.02962905676920215767, 0.000000000000000000 ) ) ;
#4483=( GEOMETRIC_REPRESENTATION_CONTEXT ( 3 ) GLOBAL_UNCERTAINTY_ASSIGNED_CONTEXT ( ( #21565 ) ) GLOBAL_UNIT_ASSIGNED_CONTEXT ( ( #25362, #33386, #6515 ) ) REPRESENTATION_CONTEXT ( 'NONE', 'WORKASPACE' ) );
#4484=DIRECTION ( 'NONE',  ( 1.558091277195270436E-17, -1.000000000000000000, -1.150229170499806500E-16 ) ) ;
#4485=CARTESIAN_POINT ( 'NONE',  ( 2.623503965249849301, 1.760141956857387724, 1.355882097269874187 ) ) ;
#4487=VECTOR ( 'NONE', #37585, 39.37007874015748143 ) ;
#4489=AXIS2_PLACEMENT_3D ( 'NONE', #45316, #2490, #34239 ) ;
#4490=EDGE_CURVE ( 'NONE', #16195, #8210, #17843, .T. ) ;
#4496=FACE_OUTER_BOUND ( 'NONE', #49725, .T. ) ;
#4497=CARTESIAN_POINT ( 'NONE',  ( 1.929629134066521701, 2.755905511811027164, 0.9824921284572420976 ) ) ;
#4498=VERTEX_POINT ( 'NONE', #44008 ) ;
#4499=CARTESIAN_POINT ( 'NONE',  ( -1.775400203342670347, 1.552775173289138166, -2.359903268218729089 ) ) ;
#4501=CARTESIAN_POINT ( 'NONE',  ( -0.1516866087075746383, 1.607047215343822222, -2.234383150555500297 ) ) ;
#4506=CARTESIAN_POINT ( 'NONE',  ( 0.7148041136150538044, 5.905511811023623991, -2.044646019095610168 ) ) ;
#4509=DIRECTION ( 'NONE',  ( -0.01601477604151182663, 0.9998717552508123996, -0.000000000000000000 ) ) ;
#4513=DIRECTION ( 'NONE',  ( 0.000000000000000000, 0.000000000000000000, -1.000000000000000000 ) ) ;
#4514=ADVANCED_FACE ( 'NONE', ( #38691 ), #1607, .T. ) ;
#4517=LINE ( 'NONE', #645, #39232 ) ;
#4522=VERTEX_POINT ( 'NONE', #3311 ) ;
#4523=EDGE_CURVE ( 'NONE', #40819, #42, #48622, .T. ) ;
#4530=CIRCLE ( 'NONE', #8655, 1.850107469027523432 ) ;
#4534=VERTEX_POINT ( 'NONE', #12788 ) ;
#4536=DIRECTION ( 'NONE',  ( -0.000000000000000000, -1.000000000000000000, -0.000000000000000000 ) ) ;
#4537=AXIS2_PLACEMENT_3D ( 'NONE', #10986, #31371, #47064 ) ;
#4539=EDGE_LOOP ( 'NONE', ( #649, #30828, #44912, #45581 ) ) ;
#4545=FACE_OUTER_BOUND ( 'NONE', #36474, .T. ) ;
#4546=DIRECTION ( 'NONE',  ( 0.000000000000000000, 0.000000000000000000, 1.000000000000000000 ) ) ;
#4558=CARTESIAN_POINT ( 'NONE',  ( 1.219594629708742994, 0.01552060224298149917, -1.594902525371822533 ) ) ;
#4559=CARTESIAN_POINT ( 'NONE',  ( -1.733853452330418987, 0.0001488292986583184614, 0.1852043564780690432 ) ) ;
#4566=ADVANCED_FACE ( 'NONE', ( #35511 ), #48618, .T. ) ;
#4567=AXIS2_PLACEMENT_3D ( 'NONE', #49464, #29644, #44857 ) ;
#4569=CARTESIAN_POINT ( 'NONE',  ( 2.164658444855302122, 5.905511811023623991, -0.04795272066889885720 ) ) ;
#4572=AXIS2_PLACEMENT_3D ( 'NONE', #34111, #42602, #37986 ) ;
#4577=ORIENTED_EDGE ( 'NONE', *, *, #20236, .T. ) ;
#4581=CARTESIAN_POINT ( 'NONE',  ( 2.926032761125787029, 5.905511811023623991, 0.3963580683592528575 ) ) ;
#4584=CARTESIAN_POINT ( 'NONE',  ( 2.141071258218635531, 0.000000000000000000, -0.04689341889560144638 ) ) ;
#4586=CARTESIAN_POINT ( 'NONE',  ( 2.255357468390372322, 1.645600431408117847, -0.5652488166673508285 ) ) ;
#4589=ORIENTED_EDGE ( 'NONE', *, *, #11000, .T. ) ;
#4590=FACE_OUTER_BOUND ( 'NONE', #18175, .T. ) ;
#4591=ORIENTED_EDGE ( 'NONE', *, *, #30071, .F. ) ;
#4597=AXIS2_PLACEMENT_3D ( 'NONE', #29691, #26321, #5692 ) ;
#4600=VECTOR ( 'NONE', #49680, 39.37007874015748143 ) ;
#4606=CARTESIAN_POINT ( 'NONE',  ( -0.2431224069213033800, 1.205361022782829114E-17, 2.152304290637669926 ) ) ;
#4607=ORIENTED_EDGE ( 'NONE', *, *, #50282, .F. ) ;
#4609=CONICAL_SURFACE ( 'NONE', #47425, 2.246510896728926010, 0.01601546068027819014 ) ;
#4610=DIRECTION ( 'NONE',  ( 0.000000000000000000, -1.000000000000000000, 0.000000000000000000 ) ) ;
#4615=CARTESIAN_POINT ( 'NONE',  ( 0.4518890234970225350, 1.682331384353711101, 2.214500778602899178 ) ) ;
#4622=CARTESIAN_POINT ( 'NONE',  ( 0.7521025634872258170, 1.621523052975431867, 2.144027383376515328 ) ) ;
#4628=DIRECTION ( 'NONE',  ( 5.779879058770898378E-18, 1.000000000000000000, 1.286990067732318227E-16 ) ) ;
#4629=CARTESIAN_POINT ( 'NONE',  ( -1.779568955232874394, 6.692913385826772199, -1.233650562797313999 ) ) ;
#4632=DIRECTION ( 'NONE',  ( -3.986037398843765983E-20, -1.000000000000000000, -1.160734090543304660E-16 ) ) ;
#4635=CIRCLE ( 'NONE', #32708, 2.164630168518208109 ) ;
#4636=ORIENTED_EDGE ( 'NONE', *, *, #30917, .F. ) ;
#4637=CARTESIAN_POINT ( 'NONE',  ( -0.9148539695939212901, 1.627632094643381988, -2.013137310660124690 ) ) ;
#4645=AXIS2_PLACEMENT_3D ( 'NONE', #9981, #38372, #21863 ) ;
#4648=ORIENTED_EDGE ( 'NONE', *, *, #11157, .T. ) ;
#4663=CONICAL_SURFACE ( 'NONE', #31052, 2.165354330708661568, 0.2617993877991570129 ) ;
#4664=CARTESIAN_POINT ( 'NONE',  ( 1.769879628650530723, 0.05626752682809384870, -0.8100022834900426627 ) ) ;
#4665=CARTESIAN_POINT ( 'NONE',  ( 0.000000000000000000, 6.692913385826772199, 0.000000000000000000 ) ) ;
#4668=CARTESIAN_POINT ( 'NONE',  ( 1.473258485933809592, 1.698690484189727901, 1.761078168145147727 ) ) ;
#4669=VECTOR ( 'NONE', #35092, 39.37007874015748854 ) ;
#4674=DIRECTION ( 'NONE',  ( 3.986037398843765983E-20, 1.000000000000000000, 1.160734090543304660E-16 ) ) ;
#4675=EDGE_CURVE ( 'NONE', #14034, #20924, #25252, .T. ) ;
#4677=VECTOR ( 'NONE', #16158, 39.37007874015748143 ) ;
#4679=CARTESIAN_POINT ( 'NONE',  ( 0.000000000000000000, 5.905511811023623991, 0.000000000000000000 ) ) ;
#4680=EDGE_CURVE ( 'NONE', #12101, #48279, #35122, .T. ) ;
#4681=DIRECTION ( 'NONE',  ( -0.000000000000000000, 1.000000000000000000, -0.000000000000000000 ) ) ;
#4687=ORIENTED_EDGE ( 'NONE', *, *, #20066, .T. ) ;
#4689=DIRECTION ( 'NONE',  ( 0.6910626489868684219, 8.386971787576741778E-17, -0.7227948638273878901 ) ) ;
#4690=CARTESIAN_POINT ( 'NONE',  ( 0.000000000000000000, 6.692913385826772199, 0.000000000000000000 ) ) ;
#4693=DIRECTION ( 'NONE',  ( 0.000000000000000000, -1.000000000000000000, 0.000000000000000000 ) ) ;
#4699=EDGE_CURVE ( 'NONE', #33287, #23952, #39360, .T. ) ;
#4700=CARTESIAN_POINT ( 'NONE',  ( -2.325586279745288643, 1.674843395074420149, 0.7038835993775438560 ) ) ;
#4704=ORIENTED_EDGE ( 'NONE', *, *, #3327, .F. ) ;
#4708=CARTESIAN_POINT ( 'NONE',  ( 0.9989521216866641407, 0.000000000000000000, 1.767914056614194651 ) ) ;
#4717=( BOUNDED_CURVE ( )  B_SPLINE_CURVE ( 3, ( #7106, #18730, #10974, #30855 ),
 .UNSPECIFIED., .F., .F. ) 
 B_SPLINE_CURVE_WITH_KNOTS ( ( 4, 4 ),
 ( 3.480195768903311837, 3.530968440970385203 ),
 .UNSPECIFIED. ) 
 CURVE ( )  GEOMETRIC_REPRESENTATION_ITEM ( )  RATIONAL_B_SPLINE_CURVE ( ( 1.000000000000000000, 0.9997851895178078152, 0.9997851895178078152, 1.000000000000000000 ) ) 
 REPRESENTATION_ITEM ( '' )  );
#4718=CARTESIAN_POINT ( 'NONE',  ( -2.684503303748676739, 1.574886512437883246, -0.1698233845712802670 ) ) ;
#4723=ORIENTED_EDGE ( 'NONE', *, *, #17860, .T. ) ;
#4726=ORIENTED_EDGE ( 'NONE', *, *, #34442, .F. ) ;
#4728=CONICAL_SURFACE ( 'NONE', #15557, 3.483074324928249421, 1.244861948955335196 ) ;
#4729=DIRECTION ( 'NONE',  ( 0.000000000000000000, 0.000000000000000000, -1.000000000000000000 ) ) ;
#4731=CARTESIAN_POINT ( 'NONE',  ( 2.803168581536171100, 1.664457329461095592, 0.9280530358793855905 ) ) ;
#4732=B_SPLINE_CURVE_WITH_KNOTS ( 'NONE', 3,
 ( #26076, #14199, #41827, #37962 ),
 .UNSPECIFIED., .F., .F.,
 ( 4, 4 ),
 ( 2.136331377199711613E-07, 0.01867141251301646793 ),
 .UNSPECIFIED. ) ;
#4734=ORIENTED_EDGE ( 'NONE', *, *, #4806, .T. ) ;
#4737=DIRECTION ( 'NONE',  ( -0.6234898018587431423, -9.072499293938425721E-17, 0.7818314824680221431 ) ) ;
#4738=DIRECTION ( 'NONE',  ( 0.000000000000000000, 0.000000000000000000, -1.000000000000000000 ) ) ;
#4741=CARTESIAN_POINT ( 'NONE',  ( 1.293618082698028804, 0.000000000000000000, -1.168738992012442246 ) ) ;
#4743=CARTESIAN_POINT ( 'NONE',  ( 2.932638728931774352, 1.764957438482779528, 0.3475908556738225297 ) ) ;
#4749=EDGE_CURVE ( 'NONE', #51046, #26290, #3446, .T. ) ;
#4750=VERTEX_POINT ( 'NONE', #18184 ) ;
#4755=CARTESIAN_POINT ( 'NONE',  ( -1.316980176754435350, 0.5242972887528047909, -1.728942231640760330 ) ) ;
#4756=CARTESIAN_POINT ( 'NONE',  ( 2.339241080213585899, 1.462148010760873307, 1.802537235681917815 ) ) ;
#4757=CARTESIAN_POINT ( 'NONE',  ( -2.164823134740035737, 1.574811347331577016, -0.04796011690018289753 ) ) ;
#4760=CARTESIAN_POINT ( 'NONE',  ( -1.511286805986099546, 0.000000000000000000, 0.8691436966266951059 ) ) ;
#4761=EDGE_LOOP ( 'NONE', ( #26551, #13226, #22270, #34587 ) ) ;
#4762=CONICAL_SURFACE ( 'NONE', #26212, 2.246510896728926010, 0.01601546068027819014 ) ;
#4766=CARTESIAN_POINT ( 'NONE',  ( -0.2431224069213033800, 1.205361022782829114E-17, 2.152304290637669926 ) ) ;
#4768=ORIENTED_EDGE ( 'NONE', *, *, #28064, .T. ) ;
#4769=ORIENTED_EDGE ( 'NONE', *, *, #494, .T. ) ;
#4772=ADVANCED_FACE ( 'NONE', ( #30817 ), #41929, .F. ) ;
#4773=ORIENTED_EDGE ( 'NONE', *, *, #42061, .T. ) ;
#4776=DIRECTION ( 'NONE',  ( 1.086719731106949452E-16, -1.000000000000000000, -4.078527368698568598E-17 ) ) ;
#4779=ORIENTED_EDGE ( 'NONE', *, *, #48601, .F. ) ;
#4785=DIRECTION ( 'NONE',  ( -0.9998717552508122886, -0.01601477604151181275, 0.000000000000000000 ) ) ;
#4793=CIRCLE ( 'NONE', #22957, 2.165354330708661568 ) ;
#4795=EDGE_LOOP ( 'NONE', ( #9962, #24972, #5751, #19182 ) ) ;
#4797=VECTOR ( 'NONE', #23190, 39.37007874015748143 ) ;
#4801=B_SPLINE_CURVE_WITH_KNOTS ( 'NONE', 3,
 ( #21541, #25666, #6044, #41418 ),
 .UNSPECIFIED., .F., .F.,
 ( 4, 4 ),
 ( 2.558223320794676908E-07, 0.002500373615005052706 ),
 .UNSPECIFIED. ) ;
#4804=CARTESIAN_POINT ( 'NONE',  ( 0.4787700707360283414, 1.205361022782829114E-17, -1.919768535593459724 ) ) ;
#4805=B_SPLINE_CURVE_WITH_KNOTS ( 'NONE', 3,
 ( #27926, #12698, #48023, #4436 ),
 .UNSPECIFIED., .F., .F.,
 ( 4, 4 ),
 ( 0.01343717635322695669, 0.03074301205234334158 ),
 .UNSPECIFIED. ) ;
#4806=EDGE_CURVE ( 'NONE', #29472, #6874, #45773, .T. ) ;
#4808=LINE ( 'NONE', #416, #22891 ) ;
#4809=ORIENTED_EDGE ( 'NONE', *, *, #45684, .T. ) ;
#4810=ADVANCED_FACE ( 'NONE', ( #14819 ), #26681, .T. ) ;
#4819=ORIENTED_EDGE ( 'NONE', *, *, #6838, .F. ) ;
#4828=ORIENTED_EDGE ( 'NONE', *, *, #13224, .F. ) ;
#4831=VECTOR ( 'NONE', #41423, 39.37007874015747433 ) ;
#4841=CARTESIAN_POINT ( 'NONE',  ( 0.04921259842519689481, -2.508534783339706724E-16, 2.213282802432568808 ) ) ;
#4842=ORIENTED_EDGE ( 'NONE', *, *, #25364, .F. ) ;
#4843=CARTESIAN_POINT ( 'NONE',  ( 1.083317450960588735, 1.005119572744525236, -2.362955334258993290 ) ) ;
#4844=VECTOR ( 'NONE', #741, 39.37007874015748143 ) ;
#4848=CARTESIAN_POINT ( 'NONE',  ( -1.598949219967723101, 0.5249316475426858419, -0.9964897588581769217 ) ) ;
#4851=VERTEX_POINT ( 'NONE', #41678 ) ;
#4855=ORIENTED_EDGE ( 'NONE', *, *, #14244, .T. ) ;
#4857=CARTESIAN_POINT ( 'NONE',  ( -1.632855683316659867, 1.205361022782829114E-17, -0.6443965869051290207 ) ) ;
#4868=FACE_OUTER_BOUND ( 'NONE', #6174, .T. ) ;
#4870=CARTESIAN_POINT ( 'NONE',  ( 0.5284761224300892346, 6.692913385826772199, -2.099874368989729234 ) ) ;
#4875=CARTESIAN_POINT ( 'NONE',  ( 2.099568260077707027, 6.692913385826772199, -0.5296909464895783737 ) ) ;
#4882=ORIENTED_EDGE ( 'NONE', *, *, #9929, .F. ) ;
#4883=DIRECTION ( 'NONE',  ( 0.000000000000000000, 0.000000000000000000, 1.000000000000000000 ) ) ;
#4891=CARTESIAN_POINT ( 'NONE',  ( 1.276224672101352153, 0.5249316475426865081, 1.385958525304569200 ) ) ;
#4898=LINE ( 'NONE', #12909, #27163 ) ;
#4904=CIRCLE ( 'NONE', #14827, 2.165354330708661568 ) ;
#4907=CARTESIAN_POINT ( 'NONE',  ( 0.07982360342473591996, 1.709180471932028711, 0.000000000000000000 ) ) ;
#4909=VERTEX_POINT ( 'NONE', #31836 ) ;
#4911=B_SPLINE_CURVE_WITH_KNOTS ( 'NONE', 3,
 ( #9794, #20178, #24063, #16835 ),
 .UNSPECIFIED., .F., .F.,
 ( 4, 4 ),
 ( 3.862052508787299689E-07, 0.04892898802743299996 ),
 .UNSPECIFIED. ) ;
#4914=ORIENTED_EDGE ( 'NONE', *, *, #10069, .F. ) ;
#4915=VERTEX_POINT ( 'NONE', #19931 ) ;
#4916=EDGE_CURVE ( 'NONE', #15234, #8249, #1429, .T. ) ;
#4924=DIRECTION ( 'NONE',  ( 0.01601477604151182663, -0.9998717552508123996, 0.000000000000000000 ) ) ;
#4925=LINE ( 'NONE', #28668, #25465 ) ;
#4928=DIRECTION ( 'NONE',  ( -0.9749279121818259508, 0.000000000000000000, 0.2225209339563041788 ) ) ;
#4932=EDGE_CURVE ( 'NONE', #39028, #26808, #50844, .T. ) ;
#4937=FACE_OUTER_BOUND ( 'NONE', #23184, .T. ) ;
#4952=CARTESIAN_POINT ( 'NONE',  ( 1.882988517681383200, 1.574803149606302854, 1.069164917025817507 ) ) ;
#4957=CARTESIAN_POINT ( 'NONE',  ( -2.544445989810643294, 1.675520440985067916, 0.8784858062910045895 ) ) ;
#4965=ORIENTED_EDGE ( 'NONE', *, *, #2303, .F. ) ;
#4971=EDGE_CURVE ( 'NONE', #17488, #5041, #4461, .T. ) ;
#4976=ORIENTED_EDGE ( 'NONE', *, *, #47779, .F. ) ;
#4981=CARTESIAN_POINT ( 'NONE',  ( -1.149923682057703456, 1.049866565877818125, -1.666459639168880402 ) ) ;
#4982=CARTESIAN_POINT ( 'NONE',  ( 1.979793062125284608, 1.651646828087945051, 2.191257344206569257 ) ) ;
#4985=ORIENTED_EDGE ( 'NONE', *, *, #7603, .F. ) ;
#4986=VERTEX_POINT ( 'NONE', #23309 ) ;
#4998=LINE ( 'NONE', #20742, #39027 ) ;
#5003=LINE ( 'NONE', #9129, #966 ) ;
#5004=VECTOR ( 'NONE', #46131, 39.37007874015748143 ) ;
#5005=DIRECTION ( 'NONE',  ( -8.021399753802077430E-17, -1.000000000000000000, -8.389726389140663754E-17 ) ) ;
#5010=CARTESIAN_POINT ( 'NONE',  ( -0.04921259842519689481, 0.000000000000000000, 2.952755905511811108 ) ) ;
#5011=ORIENTED_EDGE ( 'NONE', *, *, #10243, .T. ) ;
#5015=ORIENTED_EDGE ( 'NONE', *, *, #32273, .T. ) ;
#5017=CARTESIAN_POINT ( 'NONE',  ( 2.715732320886252271, 2.755905511811027164, 1.948858261851765361 ) ) ;
#5019=LINE ( 'NONE', #13283, #28438 ) ;
#5021=DIRECTION ( 'NONE',  ( 0.000000000000000000, 0.000000000000000000, -1.000000000000000000 ) ) ;
#5022=ORIENTED_EDGE ( 'NONE', *, *, #48676, .T. ) ;
#5029=CARTESIAN_POINT ( 'NONE',  ( 2.663634708613022539, 1.658847949249850462, -0.6584354324901854350 ) ) ;
#5031=ORIENTED_EDGE ( 'NONE', *, *, #38373, .T. ) ;
#5036=CARTESIAN_POINT ( 'NONE',  ( -0.04921259842519688094, 0.02713143566191717967, 1.843522435433914142 ) ) ;
#5038=DIRECTION ( 'NONE',  ( 0.000000000000000000, 0.000000000000000000, 1.000000000000000000 ) ) ;
#5041=VERTEX_POINT ( 'NONE', #5985 ) ;
#5044=VERTEX_POINT ( 'NONE', #32609 ) ;
#5045=DIRECTION ( 'NONE',  ( 0.9009688679024218105, 0.000000000000000000, -0.4338837391175526803 ) ) ;
#5056=CARTESIAN_POINT ( 'NONE',  ( 0.4788131938641111973, 1.504819983455083277, 2.914091152102192162 ) ) ;
#5066=CARTESIAN_POINT ( 'NONE',  ( -2.121469926805683137, 6.692913385826772199, -0.4337334748181714827 ) ) ;
#5067=ORIENTED_EDGE ( 'NONE', *, *, #46689, .T. ) ;
#5070=ORIENTED_EDGE ( 'NONE', *, *, #32379, .F. ) ;
#5071=CARTESIAN_POINT ( 'NONE',  ( 2.923830433158672637, 1.447338937300884254, 0.4126163062934453118 ) ) ;
#5072=CARTESIAN_POINT ( 'NONE',  ( 2.947574761915768171, 1.765190094501404072, -0.1816379373804911379 ) ) ;
#5074=ORIENTED_EDGE ( 'NONE', *, *, #11349, .F. ) ;
#5075=CARTESIAN_POINT ( 'NONE',  ( -3.001271764839907430, 5.118110236220475784, 0.08552506819282497397 ) ) ;
#5078=DIRECTION ( 'NONE',  ( 0.9998717552508121775, 0.01601477604151182663, 0.000000000000000000 ) ) ;
#5079=CONICAL_SURFACE ( 'NONE', #38079, 3.483074324928249421, 1.244861948955335196 ) ;
#5080=AXIS2_PLACEMENT_3D ( 'NONE', #5292, #16409, #4785 ) ;
#5090=ORIENTED_EDGE ( 'NONE', *, *, #21562, .T. ) ;
#5092=AXIS2_PLACEMENT_3D ( 'NONE', #37785, #30280, #45490 ) ;
#5095=CARTESIAN_POINT ( 'NONE',  ( -2.150518151785907772, 1.673457466938482296, -0.2530435858860717313 ) ) ;
#5101=EDGE_CURVE ( 'NONE', #25743, #36107, #9153, .T. ) ;
#5110=CIRCLE ( 'NONE', #21594, 2.244934639244525076 ) ;
#5111=CARTESIAN_POINT ( 'NONE',  ( 2.755905511811024056, 2.913385826771657250, -1.023622047244094224 ) ) ;
#5112=EDGE_CURVE ( 'NONE', #41298, #26467, #48801, .T. ) ;
#5115=B_SPLINE_CURVE_WITH_KNOTS ( 'NONE', 3,
 ( #47195, #32015, #47707, #12382 ),
 .UNSPECIFIED., .F., .F.,
 ( 4, 4 ),
 ( 0.001822208875684674370, 0.04534500198965564499 ),
 .UNSPECIFIED. ) ;
#5116=AXIS2_PLACEMENT_3D ( 'NONE', #4191, #24067, #28893 ) ;
#5117=CARTESIAN_POINT ( 'NONE',  ( 0.6233543567505464011, 1.574803149606302854, -2.073689640095370379 ) ) ;
#5118=CARTESIAN_POINT ( 'NONE',  ( 1.838947341486932396, 0.05737377265108637575, 0.6492553997849701553 ) ) ;
#5121=EDGE_CURVE ( 'NONE', #41095, #36016, #44700, .T. ) ;
#5124=CARTESIAN_POINT ( 'NONE',  ( 1.531154912952772396, 1.205361022782829114E-17, 1.532020527533857646 ) ) ;
#5126=DIRECTION ( 'NONE',  ( -0.01601477604151182663, 0.9998717552508123996, -0.000000000000000000 ) ) ;
#5129=CARTESIAN_POINT ( 'NONE',  ( 0.000000000000000000, 6.692913385826772199, 0.000000000000000000 ) ) ;
#5130=VERTEX_POINT ( 'NONE', #41114 ) ;
#5132=ORIENTED_EDGE ( 'NONE', *, *, #18754, .T. ) ;
#5137=CYLINDRICAL_SURFACE ( 'NONE', #40765, 2.165354330708661568 ) ;
#5140=DIRECTION ( 'NONE',  ( -0.01601477604151182663, 0.9998717552508123996, -0.000000000000000000 ) ) ;
#5142=EDGE_LOOP ( 'NONE', ( #50252, #42769, #12288, #35125 ) ) ;
#5143=DIRECTION ( 'NONE',  ( -0.01601477604151182663, 0.9998717552508123996, -0.000000000000000000 ) ) ;
#5145=DIRECTION ( 'NONE',  ( 7.097135778201662695E-17, 1.000000000000000000, -1.075170113095010447E-16 ) ) ;
#5148=DIRECTION ( 'NONE',  ( 0.000000000000000000, -1.000000000000000000, -0.000000000000000000 ) ) ;
#5150=EDGE_CURVE ( 'NONE', #31480, #46130, #22877, .T. ) ;
#5152=CARTESIAN_POINT ( 'NONE',  ( 1.312248418042879727, 1.574803149606302854, -1.722429524498089393 ) ) ;
#5153=CIRCLE ( 'NONE', #25795, 2.164630168518208109 ) ;
#5158=AXIS2_PLACEMENT_3D ( 'NONE', #28147, #4924, #36684 ) ;
#5159=DIRECTION ( 'NONE',  ( 0.000000000000000000, -1.000000000000000000, 0.000000000000000000 ) ) ;
#5164=DIRECTION ( 'NONE',  ( -3.986037398843765983E-20, -1.000000000000000000, -1.160734090543304660E-16 ) ) ;
#5167=B_SPLINE_CURVE_WITH_KNOTS ( 'NONE', 3,
 ( #3729, #19460, #31868, #31353 ),
 .UNSPECIFIED., .F., .F.,
 ( 4, 4 ),
 ( 6.518678076764506353E-07, 0.004612785042107461070 ),
 .UNSPECIFIED. ) ;
#5169=DIRECTION ( 'NONE',  ( -0.000000000000000000, -1.000000000000000000, -0.000000000000000000 ) ) ;
#5176=CARTESIAN_POINT ( 'NONE',  ( 1.152895553066221934, 1.205361022782829114E-17, -1.833672301139072092 ) ) ;
#5179=EDGE_CURVE ( 'NONE', #23170, #34848, #14732, .T. ) ;
#5182=LINE ( 'NONE', #17073, #37526 ) ;
#5185=AXIS2_PLACEMENT_3D ( 'NONE', #21996, #12978, #21484 ) ;
#5187=DIRECTION ( 'NONE',  ( -0.9998717552508121775, -0.01601477604151182663, 0.000000000000000000 ) ) ;
#5196=ORIENTED_EDGE ( 'NONE', *, *, #25031, .F. ) ;
#5200=PLANE ( 'NONE',  #34503 ) ;
#5201=VERTEX_POINT ( 'NONE', #45711 ) ;
#5205=CARTESIAN_POINT ( 'NONE',  ( -0.7582255214199161708, 0.000000000000000000, -1.687894986714875811 ) ) ;
#5208=VERTEX_POINT ( 'NONE', #18632 ) ;
#5210=ORIENTED_EDGE ( 'NONE', *, *, #43069, .T. ) ;
#5211=ORIENTED_EDGE ( 'NONE', *, *, #35567, .T. ) ;
#5213=CARTESIAN_POINT ( 'NONE',  ( 2.164823134740036625, 6.692913385826772199, -0.04796011690015051371 ) ) ;
#5214=CARTESIAN_POINT ( 'NONE',  ( -1.613060539954027872, 1.682065834201676324, -1.474157253483306507 ) ) ;
#5215=ADVANCED_FACE ( 'NONE', ( #41867 ), #6508, .T. ) ;
#5229=DIRECTION ( 'NONE',  ( 0.000000000000000000, -1.000000000000000000, 0.000000000000000000 ) ) ;
#5233=DIRECTION ( 'NONE',  ( 0.000000000000000000, 0.000000000000000000, -1.000000000000000000 ) ) ;
#5236=ORIENTED_EDGE ( 'NONE', *, *, #26883, .T. ) ;
#5241=LINE ( 'NONE', #32628, #43907 ) ;
#5246=CARTESIAN_POINT ( 'NONE',  ( -1.002259110181423551, 1.593423740086483020, -1.967789019142131002 ) ) ;
#5251=ORIENTED_EDGE ( 'NONE', *, *, #16199, .F. ) ;
#5253=EDGE_CURVE ( 'NONE', #20106, #10800, #33627, .T. ) ;
#5257=EDGE_CURVE ( 'NONE', #6252, #10014, #36998, .T. ) ;
#5258=CARTESIAN_POINT ( 'NONE',  ( -1.359688503674094884, 0.002096987401480311045, 1.147260674818413761 ) ) ;
#5260=AXIS2_PLACEMENT_3D ( 'NONE', #16155, #24414, #48116 ) ;
#5263=AXIS2_PLACEMENT_3D ( 'NONE', #21144, #13654, #5653 ) ;
#5264=CARTESIAN_POINT ( 'NONE',  ( -1.022179187220786156, 1.536459357544157411, 2.770232080386278106 ) ) ;
#5265=CARTESIAN_POINT ( 'NONE',  ( 2.190654571063535005, 1.742989292944022939, 0.7635320059819211691 ) ) ;
#5266=ORIENTED_EDGE ( 'NONE', *, *, #21122, .T. ) ;
#5268=CIRCLE ( 'NONE', #28364, 1.743387098533651480 ) ;
#5270=CARTESIAN_POINT ( 'NONE',  ( -1.891439052599157122, 1.677607092856729709, 1.073712343777111222 ) ) ;
#5276=FACE_OUTER_BOUND ( 'NONE', #27759, .T. ) ;
#5282=CARTESIAN_POINT ( 'NONE',  ( -1.252056778656947422, 1.687847970117562602, -1.807033786809818077 ) ) ;
#5283=EDGE_CURVE ( 'NONE', #22536, #17189, #5897, .T. ) ;
#5285=ORIENTED_EDGE ( 'NONE', *, *, #6185, .F. ) ;
#5288=CARTESIAN_POINT ( 'NONE',  ( 0.4788131938641112528, 1.726726173772622941, 2.914091152102192162 ) ) ;
#5290=EDGE_CURVE ( 'NONE', #24015, #11634, #33859, .T. ) ;
#5291=ORIENTED_EDGE ( 'NONE', *, *, #5283, .T. ) ;
#5292=CARTESIAN_POINT ( 'NONE',  ( 0.07982360342473591996, 1.709180471932028711, 0.000000000000000000 ) ) ;
#5294=ORIENTED_EDGE ( 'NONE', *, *, #35057, .F. ) ;
#5296=CARTESIAN_POINT ( 'NONE',  ( -1.946505901478385203, 6.692913385826772199, 0.9915739042680188353 ) ) ;
#5298=ORIENTED_EDGE ( 'NONE', *, *, #13965, .F. ) ;
#5310=B_SPLINE_CURVE_WITH_KNOTS ( 'NONE', 3,
 ( #4060, #36322, #47887, #15918 ),
 .UNSPECIFIED., .F., .F.,
 ( 4, 4 ),
 ( 2.472324174565337688E-07, 0.002500445842694518778 ),
 .UNSPECIFIED. ) ;
#5313=CARTESIAN_POINT ( 'NONE',  ( -0.04921259842519701277, 1.019748554299324761, 2.583324191532910596 ) ) ;
#5315=AXIS2_PLACEMENT_3D ( 'NONE', #31108, #35234, #13903 ) ;
#5321=EDGE_CURVE ( 'NONE', #3351, #1706, #41800, .T. ) ;
#5328=CARTESIAN_POINT ( 'NONE',  ( 2.113646359261424745, 1.643330668647667858, -0.9569352356128659753 ) ) ;
#5331=VERTEX_POINT ( 'NONE', #9780 ) ;
#5339=AXIS2_PLACEMENT_3D ( 'NONE', #4481, #35469, #31598 ) ;
#5342=VECTOR ( 'NONE', #22513, 39.37007874015747433 ) ;
#5345=ORIENTED_EDGE ( 'NONE', *, *, #7538, .T. ) ;
#5352=CARTESIAN_POINT ( 'NONE',  ( -0.6383587639822442261, 1.599252270110662399, -2.128056888689588089 ) ) ;
#5356=CARTESIAN_POINT ( 'NONE',  ( 2.734482843737263025, 1.663397001319319113, -1.115254632218672493 ) ) ;
#5365=DIRECTION ( 'NONE',  ( -0.000000000000000000, -1.000000000000000000, -0.000000000000000000 ) ) ;
#5370=ORIENTED_EDGE ( 'NONE', *, *, #42658, .T. ) ;
#5373=AXIS2_PLACEMENT_3D ( 'NONE', #6716, #34839, #34592 ) ;
#5378=CARTESIAN_POINT ( 'NONE',  ( 1.766507679922142415, 0.000000000000000000, -1.146458082145294544 ) ) ;
#5380=CARTESIAN_POINT ( 'NONE',  ( 0.9225641151090032688, 1.049866565877818347, -1.802300656674452384 ) ) ;
#5381=ORIENTED_EDGE ( 'NONE', *, *, #32867, .F. ) ;
#5383=CARTESIAN_POINT ( 'NONE',  ( -1.295932337655932853, 1.699056454769137137, -2.653223682158572405 ) ) ;
#5385=VECTOR ( 'NONE', #33990, 39.37007874015748143 ) ;
#5395=CARTESIAN_POINT ( 'NONE',  ( -2.160844847985643025, 1.574872742815768500, 0.1614166013721432535 ) ) ;
#5398=FACE_OUTER_BOUND ( 'NONE', #5721, .T. ) ;
#5400=CARTESIAN_POINT ( 'NONE',  ( 1.183645401082124904, 0.000000000000000000, 1.279993023352361980 ) ) ;
#5404=EDGE_CURVE ( 'NONE', #25030, #21072, #46214, .T. ) ;
#5406=CARTESIAN_POINT ( 'NONE',  ( -1.450036433410862635, 0.001605425820709399697, -1.016128049641541020 ) ) ;
#5419=CARTESIAN_POINT ( 'NONE',  ( -1.461782879395278512, 5.905511811023623991, -1.598346982901828639 ) ) ;
#5422=DIRECTION ( 'NONE',  ( 0.000000000000000000, -1.000000000000000000, -0.000000000000000000 ) ) ;
#5425=ORIENTED_EDGE ( 'NONE', *, *, #4126, .F. ) ;
#5426=ORIENTED_EDGE ( 'NONE', *, *, #11216, .F. ) ;
#5430=DIRECTION ( 'NONE',  ( -0.01601477604151182663, 0.9998717552508123996, -0.000000000000000000 ) ) ;
#5433=VERTEX_POINT ( 'NONE', #14917 ) ;
#5440=VECTOR ( 'NONE', #31863, 39.37007874015748143 ) ;
#5445=CARTESIAN_POINT ( 'NONE',  ( -0.3500732549360408563, 1.603869690133923331, 2.204675616574417685 ) ) ;
#5446=CARTESIAN_POINT ( 'NONE',  ( 0.1067246931122726866, 0.02962905676920215767, 0.000000000000000000 ) ) ;
#5447=EDGE_CURVE ( 'NONE', #8302, #39762, #6914, .T. ) ;
#5450=AXIS2_PLACEMENT_3D ( 'NONE', #31632, #43486, #47332 ) ;
#5454=CARTESIAN_POINT ( 'NONE',  ( 2.867773316779195447, 5.118110236220475784, -0.7050287376752000235 ) ) ;
#5457=ORIENTED_EDGE ( 'NONE', *, *, #12375, .F. ) ;
#5458=EDGE_CURVE ( 'NONE', #1865, #39550, #12261, .T. ) ;
#5459=AXIS2_PLACEMENT_3D ( 'NONE', #50993, #20321, #43552 ) ;
#5463=CARTESIAN_POINT ( 'NONE',  ( -0.9602959360900468200, 0.01253876862113688373, 1.511314840084332145 ) ) ;
#5465=EDGE_CURVE ( 'NONE', #2174, #9322, #29904, .T. ) ;
#5468=ORIENTED_EDGE ( 'NONE', *, *, #6520, .T. ) ;
#5470=EDGE_LOOP ( 'NONE', ( #3066, #26099, #48653 ) ) ;
#5472=EDGE_CURVE ( 'NONE', #162, #21208, #42433, .T. ) ;
#5474=LINE ( 'NONE', #5213, #2178 ) ;
#5475=DIRECTION ( 'NONE',  ( 7.815966141386463688E-14, 0.000000000000000000, 1.000000000000000000 ) ) ;
#5481=AXIS2_PLACEMENT_3D ( 'NONE', #48391, #39926, #27785 ) ;
#5491=ADVANCED_FACE ( 'NONE', ( #45616 ), #31394, .T. ) ;
#5496=CARTESIAN_POINT ( 'NONE',  ( 1.780101451746607610, 5.905511811023623991, 1.234002060668518919 ) ) ;
#5498=ORIENTED_EDGE ( 'NONE', *, *, #37642, .T. ) ;
#5499=CONICAL_SURFACE ( 'NONE', #21165, 3.033577403570480779, 1.554780866114618743 ) ;
#5505=APPLICATION_CONTEXT ( 'automotive_design' ) ;
#5508=ORIENTED_EDGE ( 'NONE', *, *, #826, .F. ) ;
#5514=CARTESIAN_POINT ( 'NONE',  ( -2.139229417893220297, 6.692913385826772199, -0.3394403656973701833 ) ) ;
#5517=ORIENTED_EDGE ( 'NONE', *, *, #39704, .T. ) ;
#5520=ADVANCED_FACE ( 'NONE', ( #26528 ), #46377, .F. ) ;
#5521=DIRECTION ( 'NONE',  ( 0.9998717552508121775, 0.01601477604151182663, 0.000000000000000000 ) ) ;
#5522=VECTOR ( 'NONE', #36620, 39.37007874015748854 ) ;
#5525=CARTESIAN_POINT ( 'NONE',  ( 2.168245791271197209, 1.466194936398640181, -2.004968704497248400 ) ) ;
#5533=ORIENTED_EDGE ( 'NONE', *, *, #8314, .T. ) ;
#5535=CARTESIAN_POINT ( 'NONE',  ( -1.695772546416001836, 1.692832103184166437, -2.417756147381374010 ) ) ;
#5538=CARTESIAN_POINT ( 'NONE',  ( -2.494543283151989144, 1.577876278647536434, -1.012699542302954114 ) ) ;
#5545=CARTESIAN_POINT ( 'NONE',  ( 0.5433756366782908076, 1.727723484189010561, 2.902374796132115353 ) ) ;
#5554=ORIENTED_EDGE ( 'NONE', *, *, #23913, .F. ) ;
#5560=VERTEX_POINT ( 'NONE', #19534 ) ;
#5568=LINE ( 'NONE', #1946, #4487 ) ;
#5571=CARTESIAN_POINT ( 'NONE',  ( -0.04921259842519688094, 0.02713143566191717967, 1.843522435433914142 ) ) ;
#5577=ADVANCED_FACE ( 'NONE', ( #50982 ), #23979, .T. ) ;
#5583=DIRECTION ( 'NONE',  ( -0.000000000000000000, 1.000000000000000000, -0.000000000000000000 ) ) ;
#5584=EDGE_CURVE ( 'NONE', #5934, #3813, #21499, .T. ) ;
#5587=LINE ( 'NONE', #29594, #12534 ) ;
#5588=ORIENTED_EDGE ( 'NONE', *, *, #11493, .F. ) ;
#5590=DIRECTION ( 'NONE',  ( 0.000000000000000000, 0.000000000000000000, -1.000000000000000000 ) ) ;
#5593=CONICAL_SURFACE ( 'NONE', #26193, 2.246510896728926010, 0.01601546068027819014 ) ;
#5594=VECTOR ( 'NONE', #45178, 39.37007874015748854 ) ;
#5595=EDGE_CURVE ( 'NONE', #41400, #1980, #11594, .T. ) ;
#5599=ORIENTED_EDGE ( 'NONE', *, *, #35021, .T. ) ;
#5600=VECTOR ( 'NONE', #41551, 39.37007874015748143 ) ;
#5604=VECTOR ( 'NONE', #9021, 39.37007874015748143 ) ;
#5605=VERTEX_POINT ( 'NONE', #43023 ) ;
#5610=ORIENTED_EDGE ( 'NONE', *, *, #50282, .T. ) ;
#5611=CARTESIAN_POINT ( 'NONE',  ( 0.5272349255864849926, 0.000000000000000000, 2.905303903342417726 ) ) ;
#5613=ORIENTED_EDGE ( 'NONE', *, *, #48081, .F. ) ;
#5626=CARTESIAN_POINT ( 'NONE',  ( 0.07982360342473591996, 1.709180471932028711, 0.000000000000000000 ) ) ;
#5629=CARTESIAN_POINT ( 'NONE',  ( 2.724759210110882179, 1.758266479573719510, 0.3194316615506513357 ) ) ;
#5635=LINE ( 'NONE', #41265, #1279 ) ;
#5637=AXIS2_PLACEMENT_3D ( 'NONE', #9163, #16664, #650 ) ;
#5644=EDGE_CURVE ( 'NONE', #26643, #48342, #32473, .T. ) ;
#5645=VECTOR ( 'NONE', #20343, 39.37007874015748143 ) ;
#5653=DIRECTION ( 'NONE',  ( 5.779879058772725700E-18, 1.000000000000000000, -1.286990067732317241E-16 ) ) ;
#5658=CARTESIAN_POINT ( 'NONE',  ( -2.491402175429631605, 1.680428061220146096, -1.585592796919542025 ) ) ;
#5660=CARTESIAN_POINT ( 'NONE',  ( 2.078641700530069691, 0.5219575377975975705, -0.9419735264436572830 ) ) ;
#5662=DIRECTION ( 'NONE',  ( -3.986037398843765983E-20, -1.000000000000000000, -1.160734090543304660E-16 ) ) ;
#5672=CARTESIAN_POINT ( 'NONE',  ( -2.996855935080999345, 2.755905511811027164, 0.1838511574193319453 ) ) ;
#5675=CONICAL_SURFACE ( 'NONE', #6530, 3.483074324928249421, 1.244861948955335196 ) ;
#5676=AXIS2_PLACEMENT_3D ( 'NONE', #23478, #39746, #46696 ) ;
#5677=DIRECTION ( 'NONE',  ( 0.01601477604151182663, -0.9998717552508123996, 0.000000000000000000 ) ) ;
#5682=AXIS2_PLACEMENT_3D ( 'NONE', #5699, #48762, #20929 ) ;
#5683=DIRECTION ( 'NONE',  ( -0.000000000000000000, -1.000000000000000000, -0.000000000000000000 ) ) ;
#5687=ORIENTED_EDGE ( 'NONE', *, *, #26874, .F. ) ;
#5688=ORIENTED_EDGE ( 'NONE', *, *, #26874, .T. ) ;
#5690=EDGE_CURVE ( 'NONE', #21621, #8302, #20086, .T. ) ;
#5692=DIRECTION ( 'NONE',  ( 0.000000000000000000, 0.000000000000000000, 1.000000000000000000 ) ) ;
#5695=DIRECTION ( 'NONE',  ( -0.01601477604151182663, 0.9998717552508123996, -0.000000000000000000 ) ) ;
#5697=VERTEX_POINT ( 'NONE', #34935 ) ;
#5699=CARTESIAN_POINT ( 'NONE',  ( 0.000000000000000000, 0.000000000000000000, 0.000000000000000000 ) ) ;
#5709=CARTESIAN_POINT ( 'NONE',  ( -2.734482843737247038, 1.572033689214636709, -1.115254632218712016 ) ) ;
#5711=ORIENTED_EDGE ( 'NONE', *, *, #14378, .F. ) ;
#5713=AXIS2_PLACEMENT_3D ( 'NONE', #33458, #10707, #9693 ) ;
#5718=ORIENTED_EDGE ( 'NONE', *, *, #40325, .F. ) ;
#5721=EDGE_LOOP ( 'NONE', ( #30256, #9334, #27245, #19437 ) ) ;
#5735=CARTESIAN_POINT ( 'NONE',  ( 0.1155636338427008941, -0.5222242541845523167, 0.000000000000000000 ) ) ;
#5738=ORIENTED_EDGE ( 'NONE', *, *, #17303, .T. ) ;
#5739=DIRECTION ( 'NONE',  ( 0.000000000000000000, 0.000000000000000000, -1.000000000000000000 ) ) ;
#5742=EDGE_CURVE ( 'NONE', #29455, #13127, #29747, .T. ) ;
#5745=ORIENTED_EDGE ( 'NONE', *, *, #18280, .F. ) ;
#5746=EDGE_CURVE ( 'NONE', #26109, #23437, #50866, .T. ) ;
#5749=CARTESIAN_POINT ( 'NONE',  ( -1.648387110752326468, 1.040182331015016670, 1.961529008066261071 ) ) ;
#5750=FACE_OUTER_BOUND ( 'NONE', #8062, .T. ) ;
#5751=ORIENTED_EDGE ( 'NONE', *, *, #21446, .T. ) ;
#5752=ORIENTED_EDGE ( 'NONE', *, *, #49279, .T. ) ;
#5753=CARTESIAN_POINT ( 'NONE',  ( 1.662320194739497436, 6.692913385826772199, -1.388601395075552469 ) ) ;
#5757=CARTESIAN_POINT ( 'NONE',  ( -2.100190309385016274, 0.000000000000000000, 0.5298329251847215815 ) ) ;
#5758=ADVANCED_FACE ( 'NONE', ( #26923 ), #4187, .T. ) ;
#5759=FACE_OUTER_BOUND ( 'NONE', #15559, .T. ) ;
#5760=B_SPLINE_CURVE_WITH_KNOTS ( 'NONE', 3,
 ( #33157, #9651, #3101, #46437 ),
 .UNSPECIFIED., .F., .F.,
 ( 4, 4 ),
 ( 3.500189189202590508E-07, 0.04605799665413929517 ),
 .UNSPECIFIED. ) ;
#5764=LINE ( 'NONE', #2403, #1107 ) ;
#5769=CARTESIAN_POINT ( 'NONE',  ( -0.5325339963216841888, 1.608673276636491511, 2.658891206781928584 ) ) ;
#5772=AXIS2_PLACEMENT_3D ( 'NONE', #19180, #30565, #3193 ) ;
#5773=VERTEX_POINT ( 'NONE', #19419 ) ;
#5777=CARTESIAN_POINT ( 'NONE',  ( 1.877225812761377011, 0.01875739138253415192, -0.8558842445003409516 ) ) ;
#5778=CARTESIAN_POINT ( 'NONE',  ( 0.04921259842519670746, 1.514263714023589502, 2.952755905511811108 ) ) ;
#5785=DIRECTION ( 'NONE',  ( -0.000000000000000000, -1.000000000000000000, -0.000000000000000000 ) ) ;
#5787=CARTESIAN_POINT ( 'NONE',  ( -0.6235241006192316915, 5.905511811023623991, 2.074304693190350157 ) ) ;
#5788=ORIENTED_EDGE ( 'NONE', *, *, #23109, .F. ) ;
#5792=ORIENTED_EDGE ( 'NONE', *, *, #48412, .T. ) ;
#5798=DIRECTION ( 'NONE',  ( -0.04486483035050446017, 1.288287287306305283E-16, -0.9989930665413151445 ) ) ;
#5801=ORIENTED_EDGE ( 'NONE', *, *, #45713, .T. ) ;
#5809=CARTESIAN_POINT ( 'NONE',  ( 2.013783482383322720, 1.740156378764222245, 1.139548688847630942 ) ) ;
#5810=DIRECTION ( 'NONE',  ( -3.986037398843765983E-20, -1.000000000000000000, -1.160734090543304660E-16 ) ) ;
#5812=EDGE_CURVE ( 'NONE', #28481, #42469, #42249, .T. ) ;
#5822=EDGE_CURVE ( 'NONE', #47516, #15540, #35564, .T. ) ;
#5824=CARTESIAN_POINT ( 'NONE',  ( -1.651646936617113148, 1.205361022782829114E-17, 0.5883978091303396774 ) ) ;
#5826=ORIENTED_EDGE ( 'NONE', *, *, #45810, .T. ) ;
#5827=DIRECTION ( 'NONE',  ( -0.000000000000000000, 1.000000000000000000, -0.000000000000000000 ) ) ;
#5834=ORIENTED_EDGE ( 'NONE', *, *, #21122, .F. ) ;
#5835=CARTESIAN_POINT ( 'NONE',  ( -0.6982598466389058345, 0.000000000000000000, 1.720449438420079691 ) ) ;
#5836=EDGE_CURVE ( 'NONE', #41060, #29553, #31815, .T. ) ;
#5838=CARTESIAN_POINT ( 'NONE',  ( 0.04921259842519689481, 1.205361022782829114E-17, -2.165433070866142007 ) ) ;
#5839=ORIENTED_EDGE ( 'NONE', *, *, #4031, .T. ) ;
#5840=FACE_OUTER_BOUND ( 'NONE', #34649, .T. ) ;
#5844=CARTESIAN_POINT ( 'NONE',  ( 2.878724150143186833, 0.000000000000000000, -0.6570500018394808128 ) ) ;
#5848=ORIENTED_EDGE ( 'NONE', *, *, #3869, .T. ) ;
#5851=EDGE_CURVE ( 'NONE', #29348, #8682, #32342, .T. ) ;
#5856=CARTESIAN_POINT ( 'NONE',  ( 0.07982360342473591996, 1.709180471932028711, 0.000000000000000000 ) ) ;
#5863=ORIENTED_EDGE ( 'NONE', *, *, #4225, .T. ) ;
#5864=AXIS2_PLACEMENT_3D ( 'NONE', #45833, #6626, #37367 ) ;
#5872=ORIENTED_EDGE ( 'NONE', *, *, #321, .T. ) ;
#5875=CARTESIAN_POINT ( 'NONE',  ( 0.000000000000000000, 6.692913385826772199, 0.000000000000000000 ) ) ;
#5877=CARTESIAN_POINT ( 'NONE',  ( -1.295932337743544771, 1.600617638626312678, -2.653223682116380377 ) ) ;
#5881=CARTESIAN_POINT ( 'NONE',  ( 0.000000000000000000, 1.574803149606302854, 0.000000000000000000 ) ) ;
#5885=VECTOR ( 'NONE', #29805, 39.37007874015748143 ) ;
#5888=ORIENTED_EDGE ( 'NONE', *, *, #21921, .F. ) ;
#5889=FACE_OUTER_BOUND ( 'NONE', #25561, .T. ) ;
#5890=EDGE_CURVE ( 'NONE', #21800, #640, #2281, .T. ) ;
#5895=AXIS2_PLACEMENT_3D ( 'NONE', #6748, #21293, #46457 ) ;
#5897=LINE ( 'NONE', #1262, #3889 ) ;
#5907=VERTEX_POINT ( 'NONE', #40076 ) ;
#5909=ORIENTED_EDGE ( 'NONE', *, *, #1016, .F. ) ;
#5910=FACE_OUTER_BOUND ( 'NONE', #16784, .T. ) ;
#5913=DIRECTION ( 'NONE',  ( -0.9362348706397417564, -4.074795501490096117E-17, 0.3513748240813304724 ) ) ;
#5914=CARTESIAN_POINT ( 'NONE',  ( 1.915720322920900331, 0.05860343245220329955, -0.3867724703730804348 ) ) ;
#5917=ORIENTED_EDGE ( 'NONE', *, *, #4031, .F. ) ;
#5918=VERTEX_POINT ( 'NONE', #39565 ) ;
#5921=EDGE_LOOP ( 'NONE', ( #21543, #37183, #2903, #51009 ) ) ;
#5926=ORIENTED_EDGE ( 'NONE', *, *, #47886, .T. ) ;
#5928=EDGE_CURVE ( 'NONE', #9867, #380, #34292, .T. ) ;
#5930=CARTESIAN_POINT ( 'NONE',  ( -0.7381027496704857249, 1.531192278308824539, -2.859439394060923068 ) ) ;
#5931=AXIS2_PLACEMENT_3D ( 'NONE', #50611, #15057, #49865 ) ;
#5934=VERTEX_POINT ( 'NONE', #49050 ) ;
#5935=AXIS2_PLACEMENT_3D ( 'NONE', #5611, #21365, #48174 ) ;
#5936=B_SPLINE_CURVE_WITH_KNOTS ( 'NONE', 3,
 ( #39698, #38500, #8459, #455 ),
 .UNSPECIFIED., .F., .F.,
 ( 4, 4 ),
 ( 2.767188889283819338E-07, 0.002500421436352599953 ),
 .UNSPECIFIED. ) ;
#5938=CARTESIAN_POINT ( 'NONE',  ( 0.6584127755596609344, 0.000000000000000000, 1.614277297217986851 ) ) ;
#5940=CARTESIAN_POINT ( 'NONE',  ( 0.002207914879453961969, 6.692913385826772199, 0.04916304461325451958 ) ) ;
#5946=CARTESIAN_POINT ( 'NONE',  ( 1.738775347548010775, 0.01809092828461609376, -1.088788177563327242 ) ) ;
#5953=FACE_OUTER_BOUND ( 'NONE', #42865, .T. ) ;
#5961=EDGE_CURVE ( 'NONE', #48339, #18734, #41353, .T. ) ;
#5965=AXIS2_PLACEMENT_3D ( 'NONE', #32946, #8406, #9428 ) ;
#5970=CARTESIAN_POINT ( 'NONE',  ( 0.1071992566810385378, 0.000000000000000000, -1.740088185897661788 ) ) ;
#5971=B_SPLINE_CURVE_WITH_KNOTS ( 'NONE', 3,
 ( #14393, #1751, #17506, #41011 ),
 .UNSPECIFIED., .F., .F.,
 ( 4, 4 ),
 ( 0.001391672322771502933, 0.04655779653607895058 ),
 .UNSPECIFIED. ) ;
#5974=CARTESIAN_POINT ( 'NONE',  ( -1.812426027168695164, 1.687013308263498601, 1.999690358701252224 ) ) ;
#5978=FACE_OUTER_BOUND ( 'NONE', #45627, .T. ) ;
#5981=ORIENTED_EDGE ( 'NONE', *, *, #38170, .F. ) ;
#5984=FACE_OUTER_BOUND ( 'NONE', #45319, .T. ) ;
#5985=CARTESIAN_POINT ( 'NONE',  ( 0.3136974817028399531, 5.905511811023623991, -2.936457595020219635 ) ) ;
#5988=DIRECTION ( 'NONE',  ( -0.9510565162951500895, 0.000000000000000000, -0.3090169943749582204 ) ) ;
#5990=EDGE_CURVE ( 'NONE', #22920, #47415, #18279, .T. ) ;
#5991=CARTESIAN_POINT ( 'NONE',  ( -0.8069532150559463046, 5.905511811023623991, -2.010061882867142380 ) ) ;
#5993=ORIENTED_EDGE ( 'NONE', *, *, #9951, .F. ) ;
#5998=CARTESIAN_POINT ( 'NONE',  ( -2.715141060683412100, 5.905511811023623991, -1.160506983230101596 ) ) ;
#6002=CARTESIAN_POINT ( 'NONE',  ( -0.7681069143398193688, 1.604975391610140578, -2.598188753026931419 ) ) ;
#6004=ORIENTED_EDGE ( 'NONE', *, *, #28121, .F. ) ;
#6005=CARTESIAN_POINT ( 'NONE',  ( 2.277873973731426194, 5.905511811023623991, 1.879489153247668742 ) ) ;
#6006=DIRECTION ( 'NONE',  ( 0.6579387259397027066, 0.000000000000000000, 0.7530714660036195163 ) ) ;
#6007=AXIS2_PLACEMENT_3D ( 'NONE', #29638, #29379, #33778 ) ;
#6012=VECTOR ( 'NONE', #5827, 39.37007874015748143 ) ;
#6014=DIRECTION ( 'NONE',  ( 0.000000000000000000, 1.000000000000000000, 0.000000000000000000 ) ) ;
#6016=CARTESIAN_POINT ( 'NONE',  ( 0.8227799331039057362, -2.325738524975369762E-16, 2.052232022298799752 ) ) ;
#6017=VERTEX_POINT ( 'NONE', #1854 ) ;
#6018=CARTESIAN_POINT ( 'NONE',  ( -0.4462886659516242527, 1.602328624241157851, 2.183640264916793861 ) ) ;
#6026=CARTESIAN_POINT ( 'NONE',  ( 3.937007874015748143, 2.755905511811027164, -1.181102362204724088 ) ) ;
#6027=DIRECTION ( 'NONE',  ( -0.000000000000000000, 1.000000000000000000, -0.000000000000000000 ) ) ;
#6029=FACE_OUTER_BOUND ( 'NONE', #38587, .T. ) ;
#6030=EDGE_CURVE ( 'NONE', #24792, #13472, #2921, .T. ) ;
#6033=CARTESIAN_POINT ( 'NONE',  ( -1.171400696859933532, 1.590714628027123823, 1.864644694871980590 ) ) ;
#6034=LINE ( 'NONE', #25401, #50144 ) ;
#6035=AXIS2_PLACEMENT_3D ( 'NONE', #20530, #16145, #36029 ) ;
#6040=EDGE_LOOP ( 'NONE', ( #21498, #11570, #39933, #5298 ) ) ;
#6042=CARTESIAN_POINT ( 'NONE',  ( 2.139229417893225182, 5.905511811023623991, -0.3394403656973405403 ) ) ;
#6044=CARTESIAN_POINT ( 'NONE',  ( 2.298329729270955024, 1.656597557696453116, 1.853838447124175337 ) ) ;
#6048=ORIENTED_EDGE ( 'NONE', *, *, #17080, .F. ) ;
#6052=CARTESIAN_POINT ( 'NONE',  ( -0.04921259842519708216, 1.620047916482694861, 2.952755905511811108 ) ) ;
#6061=ORIENTED_EDGE ( 'NONE', *, *, #36534, .F. ) ;
#6064=VERTEX_POINT ( 'NONE', #33114 ) ;
#6070=DIRECTION ( 'NONE',  ( 0.01601477604151182663, -0.9998717552508123996, 0.000000000000000000 ) ) ;
#6071=DIRECTION ( 'NONE',  ( 0.3090169943749582204, 0.000000000000000000, -0.9510565162951500895 ) ) ;
#6073=LINE ( 'NONE', #49653, #43456 ) ;
#6078=B_SPLINE_CURVE_WITH_KNOTS ( 'NONE', 3,
 ( #38563, #43167, #3186, #50618 ),
 .UNSPECIFIED., .F., .F.,
 ( 4, 4 ),
 ( 5.483124400437757281E-06, 0.05042175502089817074 ),
 .UNSPECIFIED. ) ;
#6085=ORIENTED_EDGE ( 'NONE', *, *, #26950, .F. ) ;
#6088=LINE ( 'NONE', #44554, #29329 ) ;
#6089=AXIS2_PLACEMENT_3D ( 'NONE', #35665, #35415, #32 ) ;
#6090=B_SPLINE_CURVE_WITH_KNOTS ( 'NONE', 3,
 ( #31933, #38899, #23398, #43775 ),
 .UNSPECIFIED., .F., .F.,
 ( 4, 4 ),
 ( 2.472340781885933090E-07, 0.002500445822774367312 ),
 .UNSPECIFIED. ) ;
#6097=PLANE ( 'NONE',  #44024 ) ;
#6101=EDGE_CURVE ( 'NONE', #8816, #34870, #10825, .T. ) ;
#6102=EDGE_LOOP ( 'NONE', ( #42682, #48907, #11238, #44775 ) ) ;
#6106=PLANE ( 'NONE',  #27705 ) ;
#6111=CARTESIAN_POINT ( 'NONE',  ( -2.919426793319806368, 1.673754417692067564, 0.4451252810446391095 ) ) ;
#6112=B_SPLINE_CURVE_WITH_KNOTS ( 'NONE', 3,
 ( #44208, #12725, #32101, #44462 ),
 .UNSPECIFIED., .F., .F.,
 ( 4, 4 ),
 ( 2.051433888766743662E-07, 0.01998722169972024648 ),
 .UNSPECIFIED. ) ;
#6115=AXIS2_PLACEMENT_3D ( 'NONE', #44654, #5430, #28401 ) ;
#6116=EDGE_LOOP ( 'NONE', ( #34655, #4965, #40977, #24570 ) ) ;
#6119=DIRECTION ( 'NONE',  ( -1.000000000000000000, -1.160734090543304660E-16, 0.000000000000000000 ) ) ;
#6120=CONICAL_SURFACE ( 'NONE', #12709, 3.033577403570480779, 1.554780866114618743 ) ;
#6121=ORIENTED_EDGE ( 'NONE', *, *, #32920, .F. ) ;
#6123=CIRCLE ( 'NONE', #36640, 1.743387098533651480 ) ;
#6124=VECTOR ( 'NONE', #41331, 39.37007874015748143 ) ;
#6125=EDGE_CURVE ( 'NONE', #29367, #18870, #30588, .T. ) ;
#6128=CARTESIAN_POINT ( 'NONE',  ( 0.5550072188453405442, 1.618366210323673338, -2.196007637835879045 ) ) ;
#6130=ORIENTED_EDGE ( 'NONE', *, *, #32991, .F. ) ;
#6137=CARTESIAN_POINT ( 'NONE',  ( 0.3381173457103291979, 1.574803149606302854, 2.138793126519850762 ) ) ;
#6140=CARTESIAN_POINT ( 'NONE',  ( -2.926032761125793247, 5.905511811023623991, 0.3963580683592101139 ) ) ;
#6145=CARTESIAN_POINT ( 'NONE',  ( 0.8615171519027529090, 0.5249316497054297148, -1.675535331380912263 ) ) ;
#6149=PLANE ( 'NONE',  #31697 ) ;
#6152=CARTESIAN_POINT ( 'NONE',  ( -1.731485473375985240, 1.585829450765412707, -1.723556154981469524 ) ) ;
#6155=ORIENTED_EDGE ( 'NONE', *, *, #22723, .F. ) ;
#6159=CARTESIAN_POINT ( 'NONE',  ( -0.5284761224300580373, 1.574803149606302854, -2.099874368989736784 ) ) ;
#6161=CARTESIAN_POINT ( 'NONE',  ( -1.344308260564831103, 1.595933994539297185, 2.345942870151215498 ) ) ;
#6162=CARTESIAN_POINT ( 'NONE',  ( -1.472219874544909768, 1.696317054561777171, 2.560030851058948898 ) ) ;
#6165=EDGE_CURVE ( 'NONE', #40104, #29343, #3355, .T. ) ;
#6166=DIRECTION ( 'NONE',  ( -3.986037398843765983E-20, -1.000000000000000000, -1.160734090543304660E-16 ) ) ;
#6169=ORIENTED_EDGE ( 'NONE', *, *, #36702, .F. ) ;
#6174=EDGE_LOOP ( 'NONE', ( #38247, #10916, #9031, #28698 ) ) ;
#6180=DIRECTION ( 'NONE',  ( 0.9909497617679352555, 0.000000000000000000, -0.1342332658176522420 ) ) ;
#6185=EDGE_CURVE ( 'NONE', #42163, #9179, #5936, .T. ) ;
#6192=EDGE_LOOP ( 'NONE', ( #32167, #40299, #13222, #4182 ) ) ;
#6195=EDGE_CURVE ( 'NONE', #31499, #36192, #10235, .T. ) ;
#6196=CONICAL_SURFACE ( 'NONE', #49005, 1.850107469027523210, 0.6386652850508578450 ) ;
#6208=CARTESIAN_POINT ( 'NONE',  ( -1.556712866041156440, 0.000000000000000000, 2.509548638715847435 ) ) ;
#6209=CARTESIAN_POINT ( 'NONE',  ( 2.009930929872536520, 5.905511811023623991, -0.8055662819783819817 ) ) ;
#6210=EDGE_CURVE ( 'NONE', #45968, #50288, #2829, .T. ) ;
#6211=LINE ( 'NONE', #42824, #16049 ) ;
#6212=EDGE_CURVE ( 'NONE', #23878, #38339, #50065, .T. ) ;
#6213=CARTESIAN_POINT ( 'NONE',  ( -0.1158910538491989134, 0.02606345816900213982, -1.836661962001401305 ) ) ;
#6214=DIRECTION ( 'NONE',  ( -0.6910626489868580968, 1.288287287306305530E-16, -0.7227948638273978821 ) ) ;
#6220=ORIENTED_EDGE ( 'NONE', *, *, #7603, .T. ) ;
#6226=AXIS2_PLACEMENT_3D ( 'NONE', #1283, #1025, #41048 ) ;
#6234=EDGE_CURVE ( 'NONE', #21432, #23486, #19451, .T. ) ;
#6235=EDGE_LOOP ( 'NONE', ( #38994, #17685, #26554, #42471 ) ) ;
#6239=EDGE_LOOP ( 'NONE', ( #24602, #3170, #6731, #40250 ) ) ;
#6240=ORIENTED_EDGE ( 'NONE', *, *, #26128, .F. ) ;
#6246=CYLINDRICAL_SURFACE ( 'NONE', #29138, 2.164630168518208109 ) ;
#6248=ORIENTED_EDGE ( 'NONE', *, *, #35882, .F. ) ;
#6252=VERTEX_POINT ( 'NONE', #44575 ) ;
#6256=EDGE_CURVE ( 'NONE', #44591, #8682, #13925, .T. ) ;
#6258=CARTESIAN_POINT ( 'NONE',  ( 0.7518624479397288951, 1.654327608218965073, 2.143387597788184440 ) ) ;
#6261=EDGE_CURVE ( 'NONE', #45433, #41060, #8714, .T. ) ;
#6265=B_SPLINE_CURVE_WITH_KNOTS ( 'NONE', 3,
 ( #50957, #42755, #23138, #43253 ),
 .UNSPECIFIED., .F., .F.,
 ( 4, 4 ),
 ( 3.515646365857402650E-07, 0.04348590293487804986 ),
 .UNSPECIFIED. ) ;
#6267=DIRECTION ( 'NONE',  ( -0.9998717552508122886, -0.01601477604151185785, 0.000000000000000000 ) ) ;
#6268=LINE ( 'NONE', #13000, #21823 ) ;
#6269=AXIS2_PLACEMENT_3D ( 'NONE', #46942, #39493, #769 ) ;
#6273=CARTESIAN_POINT ( 'NONE',  ( 0.000000000000000000, 6.692913385826772199, 0.000000000000000000 ) ) ;
#6277=DIRECTION ( 'NONE',  ( 0.000000000000000000, 1.160734090543304660E-16, -1.000000000000000000 ) ) ;
#6279=CARTESIAN_POINT ( 'NONE',  ( 2.009025172380753066, 0.000000000000000000, 0.7045170369349440520 ) ) ;
#6282=EDGE_CURVE ( 'NONE', #37890, #38377, #3467, .T. ) ;
#6284=DIRECTION ( 'NONE',  ( -0.000000000000000000, -1.000000000000000000, -0.000000000000000000 ) ) ;
#6290=ORIENTED_EDGE ( 'NONE', *, *, #29344, .F. ) ;
#6292=LINE ( 'NONE', #37543, #19195 ) ;
#6297=CARTESIAN_POINT ( 'NONE',  ( 1.598949220451570508, 0.5249316497054297148, -0.9964897591775290220 ) ) ;
#6298=VECTOR ( 'NONE', #2400, 39.37007874015748143 ) ;
#6302=AXIS2_PLACEMENT_3D ( 'NONE', #5446, #33600, #25831 ) ;
#6303=CARTESIAN_POINT ( 'NONE',  ( 0.002207914879453961969, 5.905511811023623991, 0.04916304461325442243 ) ) ;
#6305=ORIENTED_EDGE ( 'NONE', *, *, #15139, .T. ) ;
#6311=EDGE_LOOP ( 'NONE', ( #10821, #43405, #37434, #23378 ) ) ;
#6315=CARTESIAN_POINT ( 'NONE',  ( 2.437180031585944207, 1.205361022782829114E-17, -1.667735833703099413 ) ) ;
#6316=ORIENTED_EDGE ( 'NONE', *, *, #49811, .T. ) ;
#6317=B_SPLINE_CURVE_WITH_KNOTS ( 'NONE', 3,
 ( #19994, #35759, #24657, #36788 ),
 .UNSPECIFIED., .F., .F.,
 ( 4, 4 ),
 ( 5.974790683084733931E-07, 3.893004845545902756E-05 ),
 .UNSPECIFIED. ) ;
#6318=CARTESIAN_POINT ( 'NONE',  ( -2.139038182717881487, 1.575216142802386754, 0.3394144611327329364 ) ) ;
#6320=AXIS2_PLACEMENT_3D ( 'NONE', #3002, #45574, #41735 ) ;
#6324=ORIENTED_EDGE ( 'NONE', *, *, #27947, .F. ) ;
#6326=DIRECTION ( 'NONE',  ( -0.9998717552508122886, -0.01601477604151185785, 0.000000000000000000 ) ) ;
#6330=CARTESIAN_POINT ( 'NONE',  ( 2.126910391174609671, 1.205361022782829114E-17, 0.2384475364948296372 ) ) ;
#6331=ORIENTED_EDGE ( 'NONE', *, *, #46049, .T. ) ;
#6332=ADVANCED_FACE ( 'NONE', ( #32219 ), #48674, .F. ) ;
#6342=ORIENTED_EDGE ( 'NONE', *, *, #7399, .T. ) ;
#6347=CARTESIAN_POINT ( 'NONE',  ( -0.9838852166859199944, 1.205361022782829114E-17, 1.929635236160303302 ) ) ;
#6348=EDGE_CURVE ( 'NONE', #48222, #45550, #16726, .T. ) ;
#6354=CARTESIAN_POINT ( 'NONE',  ( 0.1067246931122726866, 0.02962905676920215767, 0.000000000000000000 ) ) ;
#6356=EDGE_CURVE ( 'NONE', #33511, #43816, #14532, .T. ) ;
#6361=CARTESIAN_POINT ( 'NONE',  ( 2.576863348864710801, 1.456480680773285741, 1.442554885838449596 ) ) ;
#6362=DIRECTION ( 'NONE',  ( -0.9998717552508121775, -0.01601477604151182663, 0.000000000000000000 ) ) ;
#6363=B_SPLINE_CURVE_WITH_KNOTS ( 'NONE', 3,
 ( #10059, #13937, #45647, #37435 ),
 .UNSPECIFIED., .F., .F.,
 ( 4, 4 ),
 ( 3.949417831791902674E-07, 0.04989286874765130886 ),
 .UNSPECIFIED. ) ;
#6369=VERTEX_POINT ( 'NONE', #715 ) ;
#6370=CARTESIAN_POINT ( 'NONE',  ( -1.299599272623047641, 1.691095615222215187, 2.079212968904131209 ) ) ;
#6371=ORIENTED_EDGE ( 'NONE', *, *, #18228, .F. ) ;
#6381=( BOUNDED_CURVE ( )  B_SPLINE_CURVE ( 3, ( #27943, #36217, #27683, #28447 ),
 .UNSPECIFIED., .F., .F. ) 
 B_SPLINE_CURVE_WITH_KNOTS ( ( 4, 4 ),
 ( 2.171587567367763594, 2.222479831755601598 ),
 .UNSPECIFIED. ) 
 CURVE ( )  GEOMETRIC_REPRESENTATION_ITEM ( )  RATIONAL_B_SPLINE_CURVE ( ( 1.000000000000000000, 0.9997841764314150392, 0.9997841764314150392, 1.000000000000000000 ) ) 
 REPRESENTATION_ITEM ( '' )  );
#6387=B_SPLINE_CURVE_WITH_KNOTS ( 'NONE', 3,
 ( #2459, #18452, #7586, #45790 ),
 .UNSPECIFIED., .F., .F.,
 ( 4, 4 ),
 ( 2.271194390675191284E-07, 0.01981312671808579604 ),
 .UNSPECIFIED. ) ;
#6389=CIRCLE ( 'NONE', #35240, 2.164630168518208109 ) ;
#6394=EDGE_CURVE ( 'NONE', #16625, #33493, #9986, .T. ) ;
#6397=CARTESIAN_POINT ( 'NONE',  ( 0.08119777152254364916, 1.623385212329073957, 0.000000000000000000 ) ) ;
#6398=VERTEX_POINT ( 'NONE', #37371 ) ;
#6401=CARTESIAN_POINT ( 'NONE',  ( 2.533192966889194597, 1.751833986009839306, -0.06450362513773535977 ) ) ;
#6402=DIRECTION ( 'NONE',  ( 0.8805955318567321166, 0.000000000000000000, 0.4738686624730094055 ) ) ;
#6403=ORIENTED_EDGE ( 'NONE', *, *, #42440, .T. ) ;
#6406=CARTESIAN_POINT ( 'NONE',  ( 2.004210316087306154, 1.645011016312011520, 1.535359116834265070 ) ) ;
#6407=VERTEX_POINT ( 'NONE', #21869 ) ;
#6408=CARTESIAN_POINT ( 'NONE',  ( -1.002259110181423551, 1.593423740086483020, -1.967789019142131002 ) ) ;
#6410=AXIS2_PLACEMENT_3D ( 'NONE', #27403, #39286, #40054 ) ;
#6411=CARTESIAN_POINT ( 'NONE',  ( -2.100227814008681637, 1.686526752338742385, -2.076109931251943763 ) ) ;
#6415=ORIENTED_EDGE ( 'NONE', *, *, #25695, .F. ) ;
#6416=DIRECTION ( 'NONE',  ( -0.2660368455666826670, 0.000000000000000000, 0.9639628606958512425 ) ) ;
#6425=FACE_OUTER_BOUND ( 'NONE', #6040, .T. ) ;
#6430=EDGE_CURVE ( 'NONE', #5697, #17250, #50192, .T. ) ;
#6432=DIRECTION ( 'NONE',  ( -0.000000000000000000, -1.000000000000000000, -0.000000000000000000 ) ) ;
#6433=DIRECTION ( 'NONE',  ( -0.9998717552508122886, -0.01601477604151180928, 0.000000000000000000 ) ) ;
#6439=EDGE_LOOP ( 'NONE', ( #23840, #50761, #42513, #42633 ) ) ;
#6443=B_SPLINE_CURVE_WITH_KNOTS ( 'NONE', 3,
 ( #6656, #27273, #43014, #3794 ),
 .UNSPECIFIED., .F., .F.,
 ( 4, 4 ),
 ( 0.001673364190201165683, 0.04575664440331616428 ),
 .UNSPECIFIED. ) ;
#6447=CARTESIAN_POINT ( 'NONE',  ( 0.000000000000000000, 5.118110236220475784, 0.000000000000000000 ) ) ;
#6448=CARTESIAN_POINT ( 'NONE',  ( 1.556712866041120469, 1.205361022782829114E-17, 2.509548638715870084 ) ) ;
#6450=EDGE_LOOP ( 'NONE', ( #14283, #2781, #17082, #7057 ) ) ;
#6452=ORIENTED_EDGE ( 'NONE', *, *, #19765, .T. ) ;
#6454=EDGE_CURVE ( 'NONE', #15353, #34370, #41485, .T. ) ;
#6456=AXIS2_PLACEMENT_3D ( 'NONE', #47246, #8563, #11925 ) ;
#6459=EDGE_CURVE ( 'NONE', #50666, #29472, #42854, .T. ) ;
#6465=CARTESIAN_POINT ( 'NONE',  ( 2.160407304981128984, 6.692913385826772199, -0.1462862061266579361 ) ) ;
#6466=DIRECTION ( 'NONE',  ( 0.5508969814520945363, -9.689372162470668980E-17, 0.8345732537213079727 ) ) ;
#6468=FACE_OUTER_BOUND ( 'NONE', #25943, .T. ) ;
#6469=CARTESIAN_POINT ( 'NONE',  ( -0.1227720337126170513, 0.000000000000000000, -1.913115909999223652 ) ) ;
#6472=ORIENTED_EDGE ( 'NONE', *, *, #47592, .F. ) ;
#6477=CARTESIAN_POINT ( 'NONE',  ( 2.100190309385009169, 1.205361022782829114E-17, 0.5298329251847523347 ) ) ;
#6488=VECTOR ( 'NONE', #13404, 39.37007874015748143 ) ;
#6490=CARTESIAN_POINT ( 'NONE',  ( 1.669153017917641924, 1.205361022782829114E-17, 1.268159837793114031 ) ) ;
#6492=VERTEX_POINT ( 'NONE', #22377 ) ;
#6493=ORIENTED_EDGE ( 'NONE', *, *, #11840, .F. ) ;
#6501=LINE ( 'NONE', #22246, #37575 ) ;
#6505=CIRCLE ( 'NONE', #18035, 2.165354330708661568 ) ;
#6508=PLANE ( 'NONE',  #35259 ) ;
#6510=CARTESIAN_POINT ( 'NONE',  ( 2.823445274216730638, 1.450545469922353892, 0.8656477926280681245 ) ) ;
#6515=( NAMED_UNIT ( * ) SI_UNIT ( $, .STERADIAN. ) SOLID_ANGLE_UNIT ( ) );
#6516=ADVANCED_FACE ( 'NONE', ( #7136 ), #15749, .T. ) ;
#6520=EDGE_CURVE ( 'NONE', #28976, #50937, #9884, .T. ) ;
#6523=ORIENTED_EDGE ( 'NONE', *, *, #30910, .T. ) ;
#6524=EDGE_LOOP ( 'NONE', ( #36692, #15073, #9338, #3919, #2808, #9299, #44307, #31432, #4096, #19910, #40163 ) ) ;
#6525=EDGE_CURVE ( 'NONE', #45880, #42094, #22124, .T. ) ;
#6526=CARTESIAN_POINT ( 'NONE',  ( 2.530770726936613535, 1.653353769313707478, -0.1629192465856815764 ) ) ;
#6530=AXIS2_PLACEMENT_3D ( 'NONE', #2115, #14499, #2624 ) ;
#6531=CIRCLE ( 'NONE', #23834, 1.850107469027523432 ) ;
#6533=CARTESIAN_POINT ( 'NONE',  ( 2.141071258218635531, 0.000000000000000000, -0.04689341889560144638 ) ) ;
#6535=DIRECTION ( 'NONE',  ( 0.000000000000000000, 0.000000000000000000, -1.000000000000000000 ) ) ;
#6536=ORIENTED_EDGE ( 'NONE', *, *, #4523, .T. ) ;
#6541=EDGE_LOOP ( 'NONE', ( #46529, #40930, #38382, #43744, #16650, #46339, #47442, #17754, #43480, #32406, #4687 ) ) ;
#6542=CARTESIAN_POINT ( 'NONE',  ( -0.1942989824301265822, 1.712426749178000751, -2.707845400019115001 ) ) ;
#6543=CARTESIAN_POINT ( 'NONE',  ( -2.099568260077699033, 1.574803149606302854, -0.5296909464896101261 ) ) ;
#6546=ADVANCED_FACE ( 'NONE', ( #14630 ), #13342, .T. ) ;
#6547=PLANE ( 'NONE',  #44836 ) ;
#6551=DIRECTION ( 'NONE',  ( 0.7227948638273978821, 8.018518666443169432E-17, -0.6910626489868580968 ) ) ;
#6557=AXIS2_PLACEMENT_3D ( 'NONE', #1080, #32859, #28952 ) ;
#6565=CARTESIAN_POINT ( 'NONE',  ( 2.793030215715258446, 0.000000000000000000, 0.9592557174602679426 ) ) ;
#6567=CONICAL_SURFACE ( 'NONE', #20593, 1.850107469027523210, 0.6386652850508578450 ) ;
#6576=CARTESIAN_POINT ( 'NONE',  ( 1.958513403246152640, 1.640845930445798073, -1.233835998176425308 ) ) ;
#6577=VERTEX_POINT ( 'NONE', #23631 ) ;
#6583=CARTESIAN_POINT ( 'NONE',  ( 2.867773316779195447, 1.665472095473279790, -0.7050287376752005786 ) ) ;
#6590=EDGE_CURVE ( 'NONE', #9082, #47888, #46590, .T. ) ;
#6597=CARTESIAN_POINT ( 'NONE',  ( 0.000000000000000000, 1.574803149606302854, 0.000000000000000000 ) ) ;
#6598=DIRECTION ( 'NONE',  ( -0.9998717552508122886, -0.01601477604151181275, 0.000000000000000000 ) ) ;
#6599=CARTESIAN_POINT ( 'NONE',  ( 0.1067246931122726866, 0.02962905676920215767, 0.000000000000000000 ) ) ;
#6602=CARTESIAN_POINT ( 'NONE',  ( 2.160407304981128984, 1.574803149606302854, -0.1462862061266585745 ) ) ;
#6605=FACE_OUTER_BOUND ( 'NONE', #36274, .T. ) ;
#6607=CARTESIAN_POINT ( 'NONE',  ( -2.019856298843366371, 1.049866565877817237, -0.1399740531627085005 ) ) ;
#6608=CARTESIAN_POINT ( 'NONE',  ( -1.722370577523733459, 1.205361022782829114E-17, 0.2829729990490794655 ) ) ;
#6610=VERTEX_POINT ( 'NONE', #28013 ) ;
#6611=DIRECTION ( 'NONE',  ( -0.01601477604151182663, 0.9998717552508123996, -0.000000000000000000 ) ) ;
#6626=DIRECTION ( 'NONE',  ( -0.01601477604151182663, 0.9998717552508123996, -0.000000000000000000 ) ) ;
#6628=CARTESIAN_POINT ( 'NONE',  ( -2.928234748147720445, 1.673608555435994516, 0.3801023473834607147 ) ) ;
#6639=ORIENTED_EDGE ( 'NONE', *, *, #29980, .T. ) ;
#6643=ORIENTED_EDGE ( 'NONE', *, *, #50223, .F. ) ;
#6647=FACE_OUTER_BOUND ( 'NONE', #37327, .T. ) ;
#6648=CARTESIAN_POINT ( 'NONE',  ( 1.472219874544873131, 1.643743200001983151, 2.560030851058970214 ) ) ;
#6649=FACE_OUTER_BOUND ( 'NONE', #25581, .T. ) ;
#6651=CARTESIAN_POINT ( 'NONE',  ( 0.4521076751547876138, 1.616718085813380945, 2.215705648545971407 ) ) ;
#6656=CARTESIAN_POINT ( 'NONE',  ( 1.588513588560381828, 0.05336261777518135074, -1.107536019441389019 ) ) ;
#6661=VERTEX_POINT ( 'NONE', #43748 ) ;
#6664=DIRECTION ( 'NONE',  ( 0.01601477604151182663, -0.9998717552508123996, 0.000000000000000000 ) ) ;
#6665=DIRECTION ( 'NONE',  ( -0.000000000000000000, 1.000000000000000000, -0.000000000000000000 ) ) ;
#6668=AXIS2_PLACEMENT_3D ( 'NONE', #36900, #11041, #50227 ) ;
#6676=ADVANCED_FACE ( 'NONE', ( #50436 ), #30883, .F. ) ;
#6678=ORIENTED_EDGE ( 'NONE', *, *, #44605, .T. ) ;
#6679=DIRECTION ( 'NONE',  ( 0.3513748240813304724, 0.000000000000000000, 0.9362348706397417564 ) ) ;
#6692=ORIENTED_EDGE ( 'NONE', *, *, #30725, .F. ) ;
#6699=CARTESIAN_POINT ( 'NONE',  ( 0.000000000000000000, 0.000000000000000000, 0.000000000000000000 ) ) ;
#6700=ADVANCED_FACE ( 'NONE', ( #48364 ), #31464, .T. ) ;
#6715=ADVANCED_FACE ( 'NONE', ( #29032 ), #27318, .T. ) ;
#6716=CARTESIAN_POINT ( 'NONE',  ( 1.662320194739497659, 0.000000000000000000, -1.388601395075552025 ) ) ;
#6719=CARTESIAN_POINT ( 'NONE',  ( 0.1067246931122726866, 0.02962905676920215767, 0.000000000000000000 ) ) ;
#6722=DIRECTION ( 'NONE',  ( -0.8345732537212999791, 6.397775707690033618E-17, -0.5508969814521065267 ) ) ;
#6729=B_SPLINE_CURVE_WITH_KNOTS ( 'NONE', 3,
 ( #31992, #28091, #43838, #8489 ),
 .UNSPECIFIED., .F., .F.,
 ( 4, 4 ),
 ( 6.402262811813191204E-07, 0.003597790540659576587 ),
 .UNSPECIFIED. ) ;
#6731=ORIENTED_EDGE ( 'NONE', *, *, #7911, .F. ) ;
#6735=VECTOR ( 'NONE', #41391, 39.37007874015748143 ) ;
#6736=DIRECTION ( 'NONE',  ( -0.2225209339563041788, 1.288287287306305283E-16, -0.9749279121818259508 ) ) ;
#6739=EDGE_CURVE ( 'NONE', #5130, #47474, #8402, .T. ) ;
#6741=ORIENTED_EDGE ( 'NONE', *, *, #36496, .F. ) ;
#6744=ORIENTED_EDGE ( 'NONE', *, *, #30060, .T. ) ;
#6746=DIRECTION ( 'NONE',  ( 0.9909497617679331460, 0.000000000000000000, 0.1342332658176667026 ) ) ;
#6748=CARTESIAN_POINT ( 'NONE',  ( -1.735586374879336535, 0.000000000000000000, -2.388829707800051327 ) ) ;
#6749=CARTESIAN_POINT ( 'NONE',  ( 0.8114156045248139826, 0.01345147374945592292, -1.798345332367593974 ) ) ;
#6750=AXIS2_PLACEMENT_3D ( 'NONE', #27215, #19966, #20228 ) ;
#6752=LINE ( 'NONE', #42358, #25380 ) ;
#6753=ADVANCED_FACE ( 'NONE', ( #39894 ), #20268, .T. ) ;
#6754=CARTESIAN_POINT ( 'NONE',  ( 1.905671854841463952, 1.748959039950288341, 2.256015092822681645 ) ) ;
#6757=LINE ( 'NONE', #21743, #14178 ) ;
#6759=EDGE_LOOP ( 'NONE', ( #22888, #43957, #47969, #26195, #16612, #31945, #46156, #38805, #16354, #33640, #19704, #49541, #40406 ) ) ;
#6761=CARTESIAN_POINT ( 'NONE',  ( 1.152895553066221046, 5.905511811023623991, -1.833672301139072092 ) ) ;
#6762=EDGE_CURVE ( 'NONE', #35582, #41056, #10020, .T. ) ;
#6763=CARTESIAN_POINT ( 'NONE',  ( -1.598711713507984022, 1.574803149606302854, -1.460438370699401522 ) ) ;
#6768=LINE ( 'NONE', #10890, #5342 ) ;
#6769=VERTEX_POINT ( 'NONE', #12790 ) ;
#6770=DIRECTION ( 'NONE',  ( -0.01601477604151182663, 0.9998717552508123996, -0.000000000000000000 ) ) ;
#6773=AXIS2_PLACEMENT_3D ( 'NONE', #31839, #27949, #39824 ) ;
#6774=CARTESIAN_POINT ( 'NONE',  ( 1.491164160533713590, 0.9997502734738330510, -2.136136864276135139 ) ) ;
#6776=CARTESIAN_POINT ( 'NONE',  ( -1.971247363764855320, 1.574803149606302854, -0.8960709840011922278 ) ) ;
#6780=EDGE_CURVE ( 'NONE', #32449, #16395, #44273, .T. ) ;
#6781=CONICAL_SURFACE ( 'NONE', #4306, 1.850107469027523210, 0.6386652850508578450 ) ;
#6785=VECTOR ( 'NONE', #28306, 39.37007874015748143 ) ;
#6786=CARTESIAN_POINT ( 'NONE',  ( -0.2156685157583831947, 1.715903002249486997, -2.945280361644576850 ) ) ;
#6787=CARTESIAN_POINT ( 'NONE',  ( 2.312967662867831287, 1.751800206377446267, -1.467809206421157864 ) ) ;
#6791=ORIENTED_EDGE ( 'NONE', *, *, #25745, .F. ) ;
#6794=DIRECTION ( 'NONE',  ( 0.01601477604151182663, -0.9998717552508123996, 0.000000000000000000 ) ) ;
#6805=CARTESIAN_POINT ( 'NONE',  ( 1.162932091021788183, 1.205361022782829114E-17, -1.684364178081092067 ) ) ;
#6808=B_SPLINE_CURVE_WITH_KNOTS ( 'NONE', 3,
 ( #42577, #11838, #27075, #38959 ),
 .UNSPECIFIED., .F., .F.,
 ( 4, 4 ),
 ( 2.002016750735623173E-07, 0.002500200813382404130 ),
 .UNSPECIFIED. ) ;
#6809=VERTEX_POINT ( 'NONE', #14058 ) ;
#6811=ORIENTED_EDGE ( 'NONE', *, *, #13364, .T. ) ;
#6813=CARTESIAN_POINT ( 'NONE',  ( -0.8952071785065484066, 0.000000000000000000, 1.972340328593134906 ) ) ;
#6815=EDGE_CURVE ( 'NONE', #7509, #18296, #26432, .T. ) ;
#6817=CARTESIAN_POINT ( 'NONE',  ( 3.937007874015748143, 5.118110236220475784, -1.181102362204724310 ) ) ;
#6819=DIRECTION ( 'NONE',  ( 0.9998717552508121775, 0.01601477604151182663, 0.000000000000000000 ) ) ;
#6822=ORIENTED_EDGE ( 'NONE', *, *, #2755, .F. ) ;
#6825=CARTESIAN_POINT ( 'NONE',  ( 0.2510238314733705400, 1.613497360050089036, -2.240096307734528835 ) ) ;
#6826=CARTESIAN_POINT ( 'NONE',  ( 0.1155636338427008941, -0.5222242541845523167, 0.000000000000000000 ) ) ;
#6830=ADVANCED_FACE ( 'NONE', ( #30062 ), #14308, .F. ) ;
#6831=CARTESIAN_POINT ( 'NONE',  ( -1.325491792074585451, 1.600165750963108646, -2.638988599164751481 ) ) ;
#6838=EDGE_CURVE ( 'NONE', #35113, #33474, #45272, .T. ) ;
#6840=DIRECTION ( 'NONE',  ( 0.000000000000000000, 1.000000000000000000, 0.000000000000000000 ) ) ;
#6846=CARTESIAN_POINT ( 'NONE',  ( 1.883714906751835061, 0.5249316497054297148, -0.03533553182421467903 ) ) ;
#6848=CARTESIAN_POINT ( 'NONE',  ( 0.7381027496705279134, 5.905511811023624880, -2.859439394060913298 ) ) ;
#6851=FACE_OUTER_BOUND ( 'NONE', #47791, .T. ) ;
#6857=VERTEX_POINT ( 'NONE', #2943 ) ;
#6864=EDGE_CURVE ( 'NONE', #7807, #15130, #15457, .T. ) ;
#6865=VERTEX_POINT ( 'NONE', #22063 ) ;
#6869=ADVANCED_FACE ( 'NONE', ( #18441 ), #26517, .F. ) ;
#6872=FACE_OUTER_BOUND ( 'NONE', #38956, .T. ) ;
#6873=CARTESIAN_POINT ( 'NONE',  ( -0.7242357167440469645, 0.5244080516102115341, 2.069776435762439082 ) ) ;
#6874=VERTEX_POINT ( 'NONE', #10442 ) ;
#6875=EDGE_LOOP ( 'NONE', ( #2351, #25446, #5291, #25679 ) ) ;
#6880=EDGE_LOOP ( 'NONE', ( #22112, #8729, #15832, #47326 ) ) ;
#6882=ORIENTED_EDGE ( 'NONE', *, *, #23382, .T. ) ;
#6884=FACE_OUTER_BOUND ( 'NONE', #6450, .T. ) ;
#6886=AXIS2_PLACEMENT_3D ( 'NONE', #3736, #31109, #22600 ) ;
#6887=CARTESIAN_POINT ( 'NONE',  ( -2.803168555509503168, 1.577132182987436071, 0.9280531159812355213 ) ) ;
#6889=AXIS2_PLACEMENT_3D ( 'NONE', #50513, #39460, #15206 ) ;
#6893=CARTESIAN_POINT ( 'NONE',  ( 2.426524993341469649, 0.9874350405758482996, -0.9836271300236743009 ) ) ;
#6897=CARTESIAN_POINT ( 'NONE',  ( 1.723188456408574432, 1.574803149606302854, 1.311251662046225785 ) ) ;
#6898=AXIS2_PLACEMENT_3D ( 'NONE', #37779, #6014, #13515 ) ;
#6900=DIRECTION ( 'NONE',  ( 0.000000000000000000, 0.000000000000000000, 1.000000000000000000 ) ) ;
#6902=CARTESIAN_POINT ( 'NONE',  ( 1.835231397189315938, 1.704488142544798857, 1.400602925730996651 ) ) ;
#6903=CARTESIAN_POINT ( 'NONE',  ( -1.692470051079808302, 0.0002787164204499768426, -0.4367734368499223141 ) ) ;
#6904=ORIENTED_EDGE ( 'NONE', *, *, #1497, .T. ) ;
#6905=LINE ( 'NONE', #42022, #44613 ) ;
#6910=ORIENTED_EDGE ( 'NONE', *, *, #35600, .F. ) ;
#6914=LINE ( 'NONE', #22665, #5004 ) ;
#6915=CARTESIAN_POINT ( 'NONE',  ( -1.547114303032252502, 1.584696887024839906, -1.547279266820049237 ) ) ;
#6917=EDGE_CURVE ( 'NONE', #31200, #5130, #26683, .T. ) ;
#6921=B_SPLINE_CURVE_WITH_KNOTS ( 'NONE', 3,
 ( #45510, #34186, #26175, #46023 ),
 .UNSPECIFIED., .F., .F.,
 ( 4, 4 ),
 ( 2.219923521421416046E-07, 0.01892337025898207375 ),
 .UNSPECIFIED. ) ;
#6926=VERTEX_POINT ( 'NONE', #19183 ) ;
#6935=VECTOR ( 'NONE', #18914, 39.37007874015748143 ) ;
#6938=CARTESIAN_POINT ( 'NONE',  ( -1.008242766279392466, 0.5249316497054292707, 1.591564316631172815 ) ) ;
#6939=AXIS2_PLACEMENT_3D ( 'NONE', #20941, #12948, #25071 ) ;
#6940=DIRECTION ( 'NONE',  ( -0.000000000000000000, 1.000000000000000000, -0.000000000000000000 ) ) ;
#6941=VERTEX_POINT ( 'NONE', #50379 ) ;
#6946=CARTESIAN_POINT ( 'NONE',  ( 1.149923681930125285, 1.049866565067837820, -1.666459638993234682 ) ) ;
#6947=EDGE_LOOP ( 'NONE', ( #15864, #12976, #859, #33392 ) ) ;
#6949=LINE ( 'NONE', #38944, #29881 ) ;
#6950=CARTESIAN_POINT ( 'NONE',  ( -1.572333874580302826, 1.588350329550590745, 1.874479074994480410 ) ) ;
#6951=ORIENTED_EDGE ( 'NONE', *, *, #28234, .F. ) ;
#6954=CARTESIAN_POINT ( 'NONE',  ( 2.168245791271197209, 1.466194936398640181, -2.004968704497248400 ) ) ;
#6960=EDGE_CURVE ( 'NONE', #27704, #6577, #26512, .T. ) ;
#6962=DIRECTION ( 'NONE',  ( 9.964307797194585150E-17, -1.000000000000000000, 5.953396763000637613E-17 ) ) ;
#6963=VECTOR ( 'NONE', #46548, 39.37007874015748854 ) ;
#6965=CARTESIAN_POINT ( 'NONE',  ( 2.464291103507799896, 5.905511811023623991, -1.626664315311302067 ) ) ;
#6966=CONICAL_SURFACE ( 'NONE', #30888, 2.246510896728926010, 0.01601546068027819014 ) ;
#6968=EDGE_CURVE ( 'NONE', #20663, #10224, #17498, .T. ) ;
#6975=ORIENTED_EDGE ( 'NONE', *, *, #38343, .F. ) ;
#6978=ORIENTED_EDGE ( 'NONE', *, *, #22695, .T. ) ;
#6984=B_SPLINE_CURVE_WITH_KNOTS ( 'NONE', 3,
 ( #35730, #31870, #47565, #43713 ),
 .UNSPECIFIED., .F., .F.,
 ( 4, 4 ),
 ( 2.894122142360316399E-07, 0.01944866240183671519 ),
 .UNSPECIFIED. ) ;
#6985=ADVANCED_FACE ( 'NONE', ( #42680 ), #15025, .T. ) ;
#6988=ORIENTED_EDGE ( 'NONE', *, *, #26375, .F. ) ;
#6989=CARTESIAN_POINT ( 'NONE',  ( -0.3382312733057317167, 5.905511811023623991, -2.139420919314969805 ) ) ;
#6993=VECTOR ( 'NONE', #16033, 39.37007874015748143 ) ;
#6994=ORIENTED_EDGE ( 'NONE', *, *, #28941, .F. ) ;
#6996=AXIS2_PLACEMENT_3D ( 'NONE', #1572, #17326, #37206 ) ;
#6998=CARTESIAN_POINT ( 'NONE',  ( -0.4788131938641533303, 1.613355999311305133, 2.914091152102185944 ) ) ;
#7001=AXIS2_PLACEMENT_3D ( 'NONE', #25214, #29601, #6362 ) ;
#7002=ORIENTED_EDGE ( 'NONE', *, *, #28973, .T. ) ;
#7003=LINE ( 'NONE', #19364, #9735 ) ;
#7005=CARTESIAN_POINT ( 'NONE',  ( 1.971834065208952769, 1.205361022782829114E-17, 0.8963217522330182430 ) ) ;
#7006=EDGE_LOOP ( 'NONE', ( #44844, #29079, #46691, #47581 ) ) ;
#7007=CARTESIAN_POINT ( 'NONE',  ( 0.04921259842519667277, 1.720031199985617265, 2.952755905511811108 ) ) ;
#7008=VECTOR ( 'NONE', #36936, 39.37007874015748143 ) ;
#7010=EDGE_LOOP ( 'NONE', ( #25602, #38121, #49873, #20075 ) ) ;
#7015=EDGE_LOOP ( 'NONE', ( #26654, #6155, #42628, #37805, #28586, #48930, #21818, #46234, #39240, #4140, #20643, #36964, #43074 ) ) ;
#7016=ORIENTED_EDGE ( 'NONE', *, *, #14202, .F. ) ;
#7019=ADVANCED_FACE ( 'NONE', ( #39577 ), #3956, .T. ) ;
#7020=CARTESIAN_POINT ( 'NONE',  ( -0.4478186997240815592, 0.006973536065449309831, -1.807618761453886558 ) ) ;
#7023=CARTESIAN_POINT ( 'NONE',  ( 2.009025172380753066, 0.000000000000000000, 0.7045170369349440520 ) ) ;
#7026=EDGE_CURVE ( 'NONE', #24792, #40146, #30829, .T. ) ;
#7027=DIRECTION ( 'NONE',  ( 0.01601477604151182663, -0.9998717552508123996, 0.000000000000000000 ) ) ;
#7028=FACE_OUTER_BOUND ( 'NONE', #15823, .T. ) ;
#7029=CARTESIAN_POINT ( 'NONE',  ( 0.1067246931122726866, 0.02962905676920215767, 0.000000000000000000 ) ) ;
#7033=CARTESIAN_POINT ( 'NONE',  ( -0.8329809839909440017, 1.205361022782829114E-17, -2.833254665166566877 ) ) ;
#7035=CIRCLE ( 'NONE', #432, 2.244934639244525076 ) ;
#7037=VECTOR ( 'NONE', #14286, 39.37007874015748143 ) ;
#7038=B_SPLINE_CURVE_WITH_KNOTS ( 'NONE', 3,
 ( #31978, #47673, #12350, #43823 ),
 .UNSPECIFIED., .F., .F.,
 ( 4, 4 ),
 ( 2.271256658651362855E-07, 0.002500295160485191577 ),
 .UNSPECIFIED. ) ;
#7052=VERTEX_POINT ( 'NONE', #43940 ) ;
#7054=CARTESIAN_POINT ( 'NONE',  ( 1.295932559131132811, 1.739450087534528233, -2.653223575501737486 ) ) ;
#7056=EDGE_CURVE ( 'NONE', #25849, #21432, #31495, .T. ) ;
#7057=ORIENTED_EDGE ( 'NONE', *, *, #49747, .T. ) ;
#7060=CARTESIAN_POINT ( 'NONE',  ( 0.000000000000000000, 1.574803149606302854, 0.000000000000000000 ) ) ;
#7062=ORIENTED_EDGE ( 'NONE', *, *, #28196, .F. ) ;
#7063=CARTESIAN_POINT ( 'NONE',  ( 1.247448100859587239, 0.000000000000000000, -1.633239539486209591 ) ) ;
#7064=CARTESIAN_POINT ( 'NONE',  ( -2.491402175429631605, 1.680428061220146096, -1.585592796919542025 ) ) ;
#7068=ORIENTED_EDGE ( 'NONE', *, *, #15690, .F. ) ;
#7071=PLANE ( 'NONE',  #38192 ) ;
#7072=DIRECTION ( 'NONE',  ( 0.6910626489868685329, -1.160734090543304907E-16, -0.7227948638273880011 ) ) ;
#7073=ORIENTED_EDGE ( 'NONE', *, *, #26757, .F. ) ;
#7077=ORIENTED_EDGE ( 'NONE', *, *, #2709, .F. ) ;
#7081=ORIENTED_EDGE ( 'NONE', *, *, #1497, .F. ) ;
#7082=CARTESIAN_POINT ( 'NONE',  ( 1.628466770324754176, 1.733984826446373750, -1.625060189682509870 ) ) ;
#7084=VECTOR ( 'NONE', #5145, 39.37007874015748143 ) ;
#7086=CONICAL_SURFACE ( 'NONE', #26057, 2.246510896728926010, 0.01601546068027819014 ) ;
#7092=EDGE_LOOP ( 'NONE', ( #9123, #240, #31636, #1467 ) ) ;
#7096=EDGE_CURVE ( 'NONE', #8220, #32363, #35963, .T. ) ;
#7099=DIRECTION ( 'NONE',  ( -0.000000000000000000, 1.000000000000000000, -0.000000000000000000 ) ) ;
#7103=VERTEX_POINT ( 'NONE', #16858 ) ;
#7106=CARTESIAN_POINT ( 'NONE',  ( -1.632855683316659867, 1.205361022782829114E-17, -0.6443965869051290207 ) ) ;
#7107=AXIS2_PLACEMENT_3D ( 'NONE', #43704, #16622, #16103 ) ;
#7112=VECTOR ( 'NONE', #20804, 39.37007874015748143 ) ;
#7113=ORIENTED_EDGE ( 'NONE', *, *, #21562, .F. ) ;
#7115=EDGE_LOOP ( 'NONE', ( #27472, #33878, #3773, #18100 ) ) ;
#7118=FACE_OUTER_BOUND ( 'NONE', #6880, .T. ) ;
#7119=CARTESIAN_POINT ( 'NONE',  ( 2.339241080213586343, 1.205361022782829114E-17, 1.802537235681917815 ) ) ;
#7125=CARTESIAN_POINT ( 'NONE',  ( 1.618143960770675349, 1.638891035385505290, 1.926912937609726484 ) ) ;
#7126=CARTESIAN_POINT ( 'NONE',  ( -1.429001793884109528, 1.049866565877818125, -1.434352145260018974 ) ) ;
#7130=EDGE_CURVE ( 'NONE', #22332, #7807, #40705, .T. ) ;
#7131=CARTESIAN_POINT ( 'NONE',  ( -2.793030215715272213, 5.905511811023623991, 0.9592557174602281966 ) ) ;
#7133=DIRECTION ( 'NONE',  ( -0.01601477604151182663, 0.9998717552508123996, -0.000000000000000000 ) ) ;
#7136=FACE_OUTER_BOUND ( 'NONE', #11307, .T. ) ;
#7137=VERTEX_POINT ( 'NONE', #4463 ) ;
#7143=B_SPLINE_CURVE_WITH_KNOTS ( 'NONE', 3,
 ( #3843, #30458, #35338, #50268 ),
 .UNSPECIFIED., .F., .F.,
 ( 4, 4 ),
 ( 0.0002550707838865089627, 0.002755222585228180900 ),
 .UNSPECIFIED. ) ;
#7152=EDGE_CURVE ( 'NONE', #29864, #43566, #48555, .T. ) ;
#7156=ADVANCED_FACE ( 'NONE', ( #16082 ), #47789, .T. ) ;
#7157=VECTOR ( 'NONE', #4776, 39.37007874015748143 ) ;
#7158=CARTESIAN_POINT ( 'NONE',  ( -0.5440951526915226433, 1.699187271209207983, -2.156468654116168171 ) ) ;
#7163=CARTESIAN_POINT ( 'NONE',  ( -0.2052282226254269204, 0.000000000000000000, -1.731265419273310346 ) ) ;
#7167=LINE ( 'NONE', #15914, #8790 ) ;
#7168=ORIENTED_EDGE ( 'NONE', *, *, #36072, .T. ) ;
#7172=ORIENTED_EDGE ( 'NONE', *, *, #18048, .F. ) ;
#7175=DIRECTION ( 'NONE',  ( 8.741157232058135226E-17, -1.000000000000000000, 7.636919086868543885E-17 ) ) ;
#7180=EDGE_CURVE ( 'NONE', #45138, #46569, #40307, .T. ) ;
#7182=CONICAL_SURFACE ( 'NONE', #41787, 2.244934639244524632, 1.554780866114618743 ) ;
#7184=VERTEX_POINT ( 'NONE', #9869 ) ;
#7187=CARTESIAN_POINT ( 'NONE',  ( -2.623503965249869729, 1.569838463031876685, 1.355882097269834885 ) ) ;
#7190=EDGE_CURVE ( 'NONE', #38704, #34644, #49320, .T. ) ;
#7191=CARTESIAN_POINT ( 'NONE',  ( -2.100190309385016274, 0.000000000000000000, 0.5298329251847215815 ) ) ;
#7192=EDGE_CURVE ( 'NONE', #9810, #48829, #6757, .T. ) ;
#7196=ADVANCED_FACE ( 'NONE', ( #33380 ), #37501, .F. ) ;
#7200=FACE_OUTER_BOUND ( 'NONE', #1337, .T. ) ;
#7202=VERTEX_POINT ( 'NONE', #2120 ) ;
#7203=CARTESIAN_POINT ( 'NONE',  ( 0.9845150457423212931, 0.000000000000000000, -1.438794182654551390 ) ) ;
#7206=B_SPLINE_CURVE_WITH_KNOTS ( 'NONE', 3,
 ( #34838, #43068, #19578, #35350 ),
 .UNSPECIFIED., .F., .F.,
 ( 4, 4 ),
 ( 0.0006178172717985424374, 0.04871068883268091926 ),
 .UNSPECIFIED. ) ;
#7217=AXIS2_PLACEMENT_3D ( 'NONE', #19094, #34852, #50537 ) ;
#7218=FACE_OUTER_BOUND ( 'NONE', #13221, .T. ) ;
#7222=AXIS2_PLACEMENT_3D ( 'NONE', #26454, #3472, #38346 ) ;
#7231=B_SPLINE_CURVE_WITH_KNOTS ( 'NONE', 3,
 ( #47584, #19487, #15624, #16132 ),
 .UNSPECIFIED., .F., .F.,
 ( 4, 4 ),
 ( 0.0003597596266483848982, 0.004912093308215493247 ),
 .UNSPECIFIED. ) ;
#7232=ORIENTED_EDGE ( 'NONE', *, *, #32651, .F. ) ;
#7237=ORIENTED_EDGE ( 'NONE', *, *, #20051, .T. ) ;
#7238=CARTESIAN_POINT ( 'NONE',  ( -2.437180031585919782, 1.582844051365913662, -1.667735833703134718 ) ) ;
#7241=VERTEX_POINT ( 'NONE', #6510 ) ;
#7242=LINE ( 'NONE', #49542, #11377 ) ;
#7245=CARTESIAN_POINT ( 'NONE',  ( 1.779568955232893268, 1.574803149606302854, -1.233650562797287797 ) ) ;
#7246=ADVANCED_FACE ( 'NONE', ( #17364 ), #45966, .F. ) ;
#7247=VECTOR ( 'NONE', #20242, 39.37007874015748854 ) ;
#7248=VECTOR ( 'NONE', #48717, 39.37007874015748143 ) ;
#7249=VERTEX_POINT ( 'NONE', #2379 ) ;
#7250=ADVANCED_FACE ( 'NONE', ( #34127 ), #42218, .T. ) ;
#7252=ADVANCED_FACE ( 'NONE', ( #26120 ), #29993, .T. ) ;
#7254=ORIENTED_EDGE ( 'NONE', *, *, #39554, .T. ) ;
#7255=CARTESIAN_POINT ( 'NONE',  ( 0.08139965876239094178, 1.610780518492231694, 0.000000000000000000 ) ) ;
#7256=DIRECTION ( 'NONE',  ( -3.986037398843765983E-20, -1.000000000000000000, -1.160734090543304660E-16 ) ) ;
#7265=ORIENTED_EDGE ( 'NONE', *, *, #26128, .T. ) ;
#7267=EDGE_CURVE ( 'NONE', #3143, #13018, #10633, .T. ) ;
#7270=ORIENTED_EDGE ( 'NONE', *, *, #39535, .T. ) ;
#7274=CARTESIAN_POINT ( 'NONE',  ( 2.074049943651431693, 2.755905511811027164, 0.6221544894624241318 ) ) ;
#7275=DIRECTION ( 'NONE',  ( -3.986037398843765983E-20, -1.000000000000000000, -1.160734090543304660E-16 ) ) ;
#7280=VERTEX_POINT ( 'NONE', #13487 ) ;
#7284=DIRECTION ( 'NONE',  ( -3.986037398843765983E-20, -1.000000000000000000, -1.160734090543304660E-16 ) ) ;
#7289=CARTESIAN_POINT ( 'NONE',  ( 0.08139965876239094178, 1.610780518492231694, 0.000000000000000000 ) ) ;
#7299=ORIENTED_EDGE ( 'NONE', *, *, #8153, .F. ) ;
#7304=ORIENTED_EDGE ( 'NONE', *, *, #46443, .F. ) ;
#7305=DIRECTION ( 'NONE',  ( 0.000000000000000000, 0.000000000000000000, 1.000000000000000000 ) ) ;
#7307=VECTOR ( 'NONE', #30393, 39.37007874015748143 ) ;
#7312=ORIENTED_EDGE ( 'NONE', *, *, #10696, .T. ) ;
#7313=DIRECTION ( 'NONE',  ( 0.000000000000000000, 0.000000000000000000, 1.000000000000000000 ) ) ;
#7321=ADVANCED_FACE ( 'NONE', ( #7757 ), #14991, .T. ) ;
#7334=ORIENTED_EDGE ( 'NONE', *, *, #41074, .F. ) ;
#7340=DIRECTION ( 'NONE',  ( 0.000000000000000000, 1.000000000000000000, -0.000000000000000000 ) ) ;
#7341=ADVANCED_FACE ( 'NONE', ( #5 ), #33181, .T. ) ;
#7342=LINE ( 'NONE', #23082, #21163 ) ;
#7344=CARTESIAN_POINT ( 'NONE',  ( 0.5859249214857252808, 1.049866565877817237, -1.938067127299249792 ) ) ;
#7351=DIRECTION ( 'NONE',  ( 0.9998717552508121775, 0.01601477604151182663, 0.000000000000000000 ) ) ;
#7354=CARTESIAN_POINT ( 'NONE',  ( -2.947574761915765063, 1.673315526576397261, -0.1816379373805333819 ) ) ;
#7360=FACE_OUTER_BOUND ( 'NONE', #49193, .T. ) ;
#7363=DIRECTION ( 'NONE',  ( -0.000000000000000000, 1.000000000000000000, -0.000000000000000000 ) ) ;
#7368=VECTOR ( 'NONE', #13248, 39.37007874015748143 ) ;
#7369=CARTESIAN_POINT ( 'NONE',  ( -1.547992802794810663, 1.592736631120135860, -2.214354780049298199 ) ) ;
#7378=CARTESIAN_POINT ( 'NONE',  ( 0.07982360342473591996, 1.709180471932028711, 0.000000000000000000 ) ) ;
#7380=CARTESIAN_POINT ( 'NONE',  ( 0.08119777152254364916, 1.623385212329073957, 0.000000000000000000 ) ) ;
#7381=EDGE_CURVE ( 'NONE', #39165, #31511, #1830, .T. ) ;
#7383=ORIENTED_EDGE ( 'NONE', *, *, #11346, .T. ) ;
#7385=ORIENTED_EDGE ( 'NONE', *, *, #12845, .F. ) ;
#7387=ADVANCED_FACE ( 'NONE', ( #38258 ), #30507, .T. ) ;
#7388=DIRECTION ( 'NONE',  ( 0.9639628606958511314, 0.000000000000000000, 0.2660368455666826115 ) ) ;
#7390=DIRECTION ( 'NONE',  ( 5.779879058772725700E-18, 1.000000000000000000, -1.286990067732317241E-16 ) ) ;
#7392=ORIENTED_EDGE ( 'NONE', *, *, #7530, .T. ) ;
#7393=EDGE_CURVE ( 'NONE', #48759, #48160, #28208, .T. ) ;
#7395=ORIENTED_EDGE ( 'NONE', *, *, #35, .T. ) ;
#7398=B_SPLINE_CURVE_WITH_KNOTS ( 'NONE', 3,
 ( #13012, #8112, #11984, #8370 ),
 .UNSPECIFIED., .F., .F.,
 ( 4, 4 ),
 ( 0.01416295713610008465, 0.03074759226334981832 ),
 .UNSPECIFIED. ) ;
#7399=EDGE_CURVE ( 'NONE', #36975, #3200, #43046, .T. ) ;
#7401=CARTESIAN_POINT ( 'NONE',  ( -2.151809081513409438, 1.574803149606302854, 0.2418202932658341242 ) ) ;
#7405=LINE ( 'NONE', #34018, #13231 ) ;
#7407=LINE ( 'NONE', #27009, #19560 ) ;
#7408=VERTEX_POINT ( 'NONE', #7007 ) ;
#7413=ADVANCED_FACE ( 'NONE', ( #22755 ), #38511, .T. ) ;
#7414=CARTESIAN_POINT ( 'NONE',  ( -1.691705575432908004, 0.0005574328069680100587, -0.4365989502721870363 ) ) ;
#7417=DIRECTION ( 'NONE',  ( -1.045785279492541006E-16, -1.000000000000000000, -5.036236473261559574E-17 ) ) ;
#7419=FACE_OUTER_BOUND ( 'NONE', #16415, .T. ) ;
#7420=CARTESIAN_POINT ( 'NONE',  ( 2.615580629650553046, 0.9847334299463360585, -0.1667280637083841666 ) ) ;
#7422=CARTESIAN_POINT ( 'NONE',  ( 2.164971648505046975, 6.692913385826772199, -0.04070796836118355938 ) ) ;
#7426=FACE_OUTER_BOUND ( 'NONE', #22803, .T. ) ;
#7428=CARTESIAN_POINT ( 'NONE',  ( -0.9836083787002326551, 6.692913385826772199, -1.929060376159713597 ) ) ;
#7430=B_SPLINE_CURVE_WITH_KNOTS ( 'NONE', 3,
 ( #9909, #9396, #36515, #16896 ),
 .UNSPECIFIED., .F., .F.,
 ( 4, 4 ),
 ( 6.447518927879251161E-07, 0.003992160187270875696 ),
 .UNSPECIFIED. ) ;
#7433=CARTESIAN_POINT ( 'NONE',  ( -1.651646936617113148, 1.205361022782829114E-17, 0.5883978091303396774 ) ) ;
#7435=CARTESIAN_POINT ( 'NONE',  ( 1.880560108460158419, 1.049866565877817681, -0.7502705392085819991 ) ) ;
#7437=ORIENTED_EDGE ( 'NONE', *, *, #34010, .F. ) ;
#7438=EDGE_CURVE ( 'NONE', #34884, #48573, #47723, .T. ) ;
#7440=AXIS2_PLACEMENT_3D ( 'NONE', #27958, #50636, #15586 ) ;
#7444=ORIENTED_EDGE ( 'NONE', *, *, #16165, .F. ) ;
#7448=AXIS2_PLACEMENT_3D ( 'NONE', #39235, #15736, #23999 ) ;
#7451=ORIENTED_EDGE ( 'NONE', *, *, #47807, .F. ) ;
#7454=ORIENTED_EDGE ( 'NONE', *, *, #35915, .T. ) ;
#7456=ORIENTED_EDGE ( 'NONE', *, *, #3598, .T. ) ;
#7461=B_SPLINE_CURVE_WITH_KNOTS ( 'NONE', 3,
 ( #40203, #36328, #48403, #48156 ),
 .UNSPECIFIED., .F., .F.,
 ( 4, 4 ),
 ( 0.0004689409862730576284, 0.04913255646355430689 ),
 .UNSPECIFIED. ) ;
#7462=ORIENTED_EDGE ( 'NONE', *, *, #25838, .T. ) ;
#7463=ORIENTED_EDGE ( 'NONE', *, *, #8411, .F. ) ;
#7470=CARTESIAN_POINT ( 'NONE',  ( -1.738757879605812073, 7.027592017269983715E-05, -0.1273499085982673085 ) ) ;
#7475=EDGE_CURVE ( 'NONE', #32131, #22636, #34017, .T. ) ;
#7476=CARTESIAN_POINT ( 'NONE',  ( 2.190654571063535005, 1.742989292944022939, 0.7635320059819211691 ) ) ;
#7480=ORIENTED_EDGE ( 'NONE', *, *, #47894, .T. ) ;
#7481=ORIENTED_EDGE ( 'NONE', *, *, #16363, .T. ) ;
#7483=CARTESIAN_POINT ( 'NONE',  ( 0.7513820654849657776, 1.719936709731724189, 2.142107623314860376 ) ) ;
#7486=B_SPLINE_CURVE_WITH_KNOTS ( 'NONE', 3,
 ( #43025, #46876, #438, #7927 ),
 .UNSPECIFIED., .F., .F.,
 ( 4, 4 ),
 ( 2.220418065680204351E-07, 0.01710792206032625551 ),
 .UNSPECIFIED. ) ;
#7491=EDGE_CURVE ( 'NONE', #23622, #50196, #3020, .T. ) ;
#7492=DIRECTION ( 'NONE',  ( 0.000000000000000000, 0.000000000000000000, 1.000000000000000000 ) ) ;
#7493=DIRECTION ( 'NONE',  ( -0.01601477604151182663, 0.9998717552508123996, -0.000000000000000000 ) ) ;
#7499=VERTEX_POINT ( 'NONE', #12654 ) ;
#7501=DIRECTION ( 'NONE',  ( 0.9009688679024218105, -1.160734090543304660E-16, -0.4338837391175526803 ) ) ;
#7503=CARTESIAN_POINT ( 'NONE',  ( 0.4350747367505080065, 6.692913385826772199, -2.121846421795415605 ) ) ;
#7504=AXIS2_PLACEMENT_3D ( 'NONE', #29893, #18266, #13642 ) ;
#7505=VERTEX_POINT ( 'NONE', #1291 ) ;
#7508=CARTESIAN_POINT ( 'NONE',  ( 1.979793062125284608, 1.750113821271474857, 2.191257344206569257 ) ) ;
#7509=VERTEX_POINT ( 'NONE', #8269 ) ;
#7510=CARTESIAN_POINT ( 'NONE',  ( 0.000000000000000000, 1.574803149606302854, 0.000000000000000000 ) ) ;
#7511=VERTEX_POINT ( 'NONE', #28388 ) ;
#7514=ORIENTED_EDGE ( 'NONE', *, *, #34299, .T. ) ;
#7521=ORIENTED_EDGE ( 'NONE', *, *, #9107, .F. ) ;
#7530=EDGE_CURVE ( 'NONE', #35509, #18363, #10936, .T. ) ;
#7538=EDGE_CURVE ( 'NONE', #27191, #34440, #28653, .T. ) ;
#7542=DIRECTION ( 'NONE',  ( -0.000000000000000000, -1.000000000000000000, -0.000000000000000000 ) ) ;
#7543=ORIENTED_EDGE ( 'NONE', *, *, #41962, .T. ) ;
#7544=CIRCLE ( 'NONE', #32287, 2.244934639244525076 ) ;
#7547=AXIS2_PLACEMENT_3D ( 'NONE', #10808, #22939, #46154 ) ;
#7549=EDGE_LOOP ( 'NONE', ( #43921, #41304, #25724, #32061 ) ) ;
#7550=CARTESIAN_POINT ( 'NONE',  ( -1.461782879395278290, 0.000000000000000000, -1.598346982901829527 ) ) ;
#7555=CARTESIAN_POINT ( 'NONE',  ( 1.236813753895251722, 1.205361022782829114E-17, -2.681693691597563767 ) ) ;
#7560=ORIENTED_EDGE ( 'NONE', *, *, #11458, .T. ) ;
#7561=DIRECTION ( 'NONE',  ( -0.000000000000000000, 1.000000000000000000, -0.000000000000000000 ) ) ;
#7576=DIRECTION ( 'NONE',  ( 0.9749279121818227312, -2.586762438145473843E-17, 0.2225209339563184452 ) ) ;
#7578=CARTESIAN_POINT ( 'NONE',  ( 0.1067246931122726866, 0.02962905676920215767, 0.000000000000000000 ) ) ;
#7584=DIRECTION ( 'NONE',  ( 0.7818314824680221431, 0.000000000000000000, 0.6234898018587431423 ) ) ;
#7586=CARTESIAN_POINT ( 'NONE',  ( -2.165574327476177174, 1.677377729380559845, 1.109459651199706576 ) ) ;
#7587=DIRECTION ( 'NONE',  ( 0.9998717552508121775, 0.01601477604151182663, 0.000000000000000000 ) ) ;
#7588=VERTEX_POINT ( 'NONE', #49758 ) ;
#7591=CONICAL_SURFACE ( 'NONE', #26565, 2.244934639244524632, 1.554780866114618743 ) ;
#7598=CARTESIAN_POINT ( 'NONE',  ( 1.083598637574781920, 1.736150426126270130, 2.747180975113346246 ) ) ;
#7601=CARTESIAN_POINT ( 'NONE',  ( -1.205050450470247725, 0.008618577144216254052, 1.304493073717302165 ) ) ;
#7603=EDGE_CURVE ( 'NONE', #39521, #8450, #2682, .T. ) ;
#7605=CARTESIAN_POINT ( 'NONE',  ( -1.775400203342670347, 1.593155925640307835, -2.359903268218729089 ) ) ;
#7614=CARTESIAN_POINT ( 'NONE',  ( -2.378214753669538162, 1.674009934365706220, -0.4923338061332758198 ) ) ;
#7615=AXIS2_PLACEMENT_3D ( 'NONE', #31005, #26863, #14759 ) ;
#7620=ORIENTED_EDGE ( 'NONE', *, *, #390, .T. ) ;
#7624=EDGE_CURVE ( 'NONE', #16195, #3395, #42423, .T. ) ;
#7626=ORIENTED_EDGE ( 'NONE', *, *, #50115, .F. ) ;
#7627=AXIS2_PLACEMENT_3D ( 'NONE', #9020, #48468, #8504 ) ;
#7632=CARTESIAN_POINT ( 'NONE',  ( -1.748857564090981809, 1.691995931334618453, -2.379187624440585402 ) ) ;
#7635=EDGE_LOOP ( 'NONE', ( #40109, #10309, #18116, #46703 ) ) ;
#7636=CARTESIAN_POINT ( 'NONE',  ( 0.000000000000000000, 5.905511811023623991, 0.000000000000000000 ) ) ;
#7641=ORIENTED_EDGE ( 'NONE', *, *, #11859, .T. ) ;
#7642=CARTESIAN_POINT ( 'NONE',  ( -2.044241703397525978, 1.205361022782829114E-17, -0.7159595814952911530 ) ) ;
#7645=CARTESIAN_POINT ( 'NONE',  ( -0.4433489891367851654, -2.598029575652208120E-16, 2.167441310503416041 ) ) ;
#7650=LINE ( 'NONE', #42250, #40438 ) ;
#7652=CARTESIAN_POINT ( 'NONE',  ( 2.100227814008711835, 1.751990118145921649, -2.076109931251913565 ) ) ;
#7657=CARTESIAN_POINT ( 'NONE',  ( -2.544472138398716332, 1.577093961458839511, 0.8784943024822983171 ) ) ;
#7659=ADVANCED_FACE ( 'NONE', ( #2316 ), #9812, .T. ) ;
#7662=ORIENTED_EDGE ( 'NONE', *, *, #13281, .T. ) ;
#7664=EDGE_CURVE ( 'NONE', #32363, #32877, #50450, .T. ) ;
#7666=EDGE_LOOP ( 'NONE', ( #31190, #7996, #41338, #38938 ) ) ;
#7669=CARTESIAN_POINT ( 'NONE',  ( 2.889674983507178219, 1.448941827424379936, -0.6090712660037606030 ) ) ;
#7675=DIRECTION ( 'NONE',  ( 0.9749279121818227312, 0.000000000000000000, 0.2225209339563184452 ) ) ;
#7676=EDGE_CURVE ( 'NONE', #7505, #50172, #30728, .T. ) ;
#7680=ORIENTED_EDGE ( 'NONE', *, *, #32428, .F. ) ;
#7682=ORIENTED_EDGE ( 'NONE', *, *, #20356, .T. ) ;
#7683=EDGE_CURVE ( 'NONE', #25794, #33804, #48810, .T. ) ;
#7685=DIRECTION ( 'NONE',  ( -5.207613805428889878E-18, -1.000000000000000000, 1.159565308550899675E-16 ) ) ;
#7691=AXIS2_PLACEMENT_3D ( 'NONE', #32284, #3, #40021 ) ;
#7696=ORIENTED_EDGE ( 'NONE', *, *, #6960, .F. ) ;
#7699=AXIS2_PLACEMENT_3D ( 'NONE', #34153, #7027, #14525 ) ;
#7701=ORIENTED_EDGE ( 'NONE', *, *, #51018, .F. ) ;
#7702=EDGE_LOOP ( 'NONE', ( #37085, #42448, #41875, #19793 ) ) ;
#7705=CARTESIAN_POINT ( 'NONE',  ( 0.8329809839909850799, 1.633788288308783976, -2.833254665166554442 ) ) ;
#7708=VERTEX_POINT ( 'NONE', #41306 ) ;
#7709=CARTESIAN_POINT ( 'NONE',  ( 3.937007874015748143, 5.118110236220475784, 1.181102362204724310 ) ) ;
#7710=CARTESIAN_POINT ( 'NONE',  ( 3.937007874015748143, 4.960629921259846142, 1.023622047244094446 ) ) ;
#7712=EDGE_LOOP ( 'NONE', ( #21443, #35019, #27850, #16548 ) ) ;
#7717=CARTESIAN_POINT ( 'NONE',  ( 1.779568955232893268, 5.905511811023623991, -1.233650562797287575 ) ) ;
#7718=PLANE ( 'NONE',  #14919 ) ;
#7724=AXIS2_PLACEMENT_3D ( 'NONE', #17942, #5810, #33707 ) ;
#7725=ORIENTED_EDGE ( 'NONE', *, *, #7475, .F. ) ;
#7727=AXIS2_PLACEMENT_3D ( 'NONE', #15167, #174, #35049 ) ;
#7729=VECTOR ( 'NONE', #19570, 39.37007874015748143 ) ;
#7731=DIRECTION ( 'NONE',  ( 1.000000000000000000, 0.000000000000000000, 0.000000000000000000 ) ) ;
#7735=CONICAL_SURFACE ( 'NONE', #17668, 1.850107469027523210, 0.6386652850508578450 ) ;
#7737=EDGE_LOOP ( 'NONE', ( #14910, #4636, #7383, #38881 ) ) ;
#7740=DIRECTION ( 'NONE',  ( -0.3090169943749582204, -1.160734090543304660E-16, 0.9510565162951500895 ) ) ;
#7747=CARTESIAN_POINT ( 'NONE',  ( -0.3742159057234073494, 0.02192591290182492950, 1.786486621533327712 ) ) ;
#7750=ADVANCED_FACE ( 'NONE', ( #46409 ), #10093, .T. ) ;
#7751=ORIENTED_EDGE ( 'NONE', *, *, #3076, .F. ) ;
#7753=FACE_OUTER_BOUND ( 'NONE', #44676, .T. ) ;
#7757=FACE_OUTER_BOUND ( 'NONE', #42751, .T. ) ;
#7759=EDGE_CURVE ( 'NONE', #4498, #19371, #9237, .T. ) ;
#7761=VECTOR ( 'NONE', #862, 39.37007874015748854 ) ;
#7766=DIRECTION ( 'NONE',  ( -0.01601477604151182663, 0.9998717552508123996, -0.000000000000000000 ) ) ;
#7773=CONICAL_SURFACE ( 'NONE', #5315, 3.033577403570480779, 1.554780866114618743 ) ;
#7775=CARTESIAN_POINT ( 'NONE',  ( 2.298430379965446857, 1.646290322915411997, 0.3610056012771685197 ) ) ;
#7778=FACE_OUTER_BOUND ( 'NONE', #4477, .T. ) ;
#7781=EDGE_CURVE ( 'NONE', #45728, #49614, #6949, .T. ) ;
#7782=DIRECTION ( 'NONE',  ( -0.8584487936018727616, -5.949974954004205321E-17, 0.5128992774058948045 ) ) ;
#7785=ORIENTED_EDGE ( 'NONE', *, *, #19979, .T. ) ;
#7789=ORIENTED_EDGE ( 'NONE', *, *, #32395, .F. ) ;
#7790=EDGE_LOOP ( 'NONE', ( #46824, #50217, #19341, #6048, #8898, #25320, #45794, #28968, #324, #24316, #47067, #27145, #50018 ) ) ;
#7794=ORIENTED_EDGE ( 'NONE', *, *, #40061, .T. ) ;
#7795=AXIS2_PLACEMENT_3D ( 'NONE', #5757, #21504, #1878 ) ;
#7798=CARTESIAN_POINT ( 'NONE',  ( 2.164658444855302122, 5.905511811023623991, -0.04795272066889885720 ) ) ;
#7804=CARTESIAN_POINT ( 'NONE',  ( -1.129536109867572691, 1.599305403152165184, -2.458929368400313287 ) ) ;
#7805=DIRECTION ( 'NONE',  ( -0.01601477604151182663, 0.9998717552508123996, -0.000000000000000000 ) ) ;
#7807=VERTEX_POINT ( 'NONE', #14698 ) ;
#7811=AXIS2_PLACEMENT_3D ( 'NONE', #24194, #39938, #28054 ) ;
#7815=CARTESIAN_POINT ( 'NONE',  ( 0.3673703023927838429, 0.000000000000000000, 1.932961348296883042 ) ) ;
#7819=VERTEX_POINT ( 'NONE', #19564 ) ;
#7833=CARTESIAN_POINT ( 'NONE',  ( -2.121469926805683137, 1.574803149606302854, -0.4337334748181708721 ) ) ;
#7834=DIRECTION ( 'NONE',  ( 0.9998717552508121775, 0.01601477604151182663, 0.000000000000000000 ) ) ;
#7838=ORIENTED_EDGE ( 'NONE', *, *, #11258, .F. ) ;
#7839=ORIENTED_EDGE ( 'NONE', *, *, #25427, .T. ) ;
#7845=DIRECTION ( 'NONE',  ( 0.01601477604151182663, -0.9998717552508123996, 0.000000000000000000 ) ) ;
#7849=LINE ( 'NONE', #20738, #5440 ) ;
#7850=DIRECTION ( 'NONE',  ( -0.000000000000000000, -1.000000000000000000, -0.000000000000000000 ) ) ;
#7853=ADVANCED_FACE ( 'NONE', ( #24478 ), #47151, .F. ) ;
#7854=DIRECTION ( 'NONE',  ( -1.267583980596140612E-16, 1.000000000000000000, 2.300325776299552367E-17 ) ) ;
#7855=ADVANCED_FACE ( 'NONE', ( #24221 ), #12343, .T. ) ;
#7856=CARTESIAN_POINT ( 'NONE',  ( -2.159905143290286045, 6.692913385826772199, 0.1535224723189609897 ) ) ;
#7858=LINE ( 'NONE', #36253, #40547 ) ;
#7866=VERTEX_POINT ( 'NONE', #11825 ) ;
#7870=ORIENTED_EDGE ( 'NONE', *, *, #3003, .F. ) ;
#7882=VERTEX_POINT ( 'NONE', #1234 ) ;
#7885=VECTOR ( 'NONE', #13989, 39.37007874015748143 ) ;
#7889=ORIENTED_EDGE ( 'NONE', *, *, #38149, .T. ) ;
#7891=CARTESIAN_POINT ( 'NONE',  ( 2.539930011093434192, 1.755364253847478961, -1.032098760813036531 ) ) ;
#7894=LINE ( 'NONE', #23637, #2798 ) ;
#7903=EDGE_CURVE ( 'NONE', #3510, #46048, #13444, .T. ) ;
#7906=CARTESIAN_POINT ( 'NONE',  ( 0.4001787029124908024, 1.205361022782829114E-17, 1.929553426015793605 ) ) ;
#7910=AXIS2_PLACEMENT_3D ( 'NONE', #48128, #28282, #4546 ) ;
#7911=EDGE_CURVE ( 'NONE', #4986, #13914, #12087, .T. ) ;
#7916=CARTESIAN_POINT ( 'NONE',  ( 4.821444091131312140E-17, 0.000000000000000000, 0.3937007874015748254 ) ) ;
#7921=CARTESIAN_POINT ( 'NONE',  ( 2.882373499243445103, 1.448344807863587436, -0.6410611587410768308 ) ) ;
#7923=CIRCLE ( 'NONE', #12054, 2.165354330708661568 ) ;
#7925=ORIENTED_EDGE ( 'NONE', *, *, #25100, .T. ) ;
#7927=CARTESIAN_POINT ( 'NONE',  ( 1.033334490728470723, 1.724452693827607908, -2.032317711754626277 ) ) ;
#7928=CARTESIAN_POINT ( 'NONE',  ( 2.044241703397536636, 0.000000000000000000, -0.7159595814952622872 ) ) ;
#7931=VERTEX_POINT ( 'NONE', #4857 ) ;
#7933=DIRECTION ( 'NONE',  ( 0.9909497617679352555, 1.554141314384320336E-17, -0.1342332658176522420 ) ) ;
#7938=DIRECTION ( 'NONE',  ( 0.9749279121818259508, 0.000000000000000000, -0.2225209339563041788 ) ) ;
#7954=AXIS2_PLACEMENT_3D ( 'NONE', #29043, #41694, #45284 ) ;
#7956=ORIENTED_EDGE ( 'NONE', *, *, #29980, .F. ) ;
#7958=CARTESIAN_POINT ( 'NONE',  ( 0.000000000000000000, 0.000000000000000000, 0.000000000000000000 ) ) ;
#7959=AXIS2_PLACEMENT_3D ( 'NONE', #7380, #11505, #42976 ) ;
#7967=DIRECTION ( 'NONE',  ( 0.8345732537212999791, 0.000000000000000000, 0.5508969814521065267 ) ) ;
#7975=CARTESIAN_POINT ( 'NONE',  ( 0.002207914879453961969, 6.692913385826772199, 0.04916304461325451958 ) ) ;
#7978=AXIS2_PLACEMENT_3D ( 'NONE', #44042, #24183, #12821 ) ;
#7980=DIMENSIONAL_EXPONENTS ( 1.000000000000000000, 0.000000000000000000, 0.000000000000000000, 0.000000000000000000, 0.000000000000000000, 0.000000000000000000, 0.000000000000000000 ) ;
#7985=EDGE_CURVE ( 'NONE', #11918, #7241, #10334, .T. ) ;
#7986=CARTESIAN_POINT ( 'NONE',  ( 0.1067246931122726866, 0.02962905676920215767, 0.000000000000000000 ) ) ;
#7993=ORIENTED_EDGE ( 'NONE', *, *, #48676, .F. ) ;
#7996=ORIENTED_EDGE ( 'NONE', *, *, #4278, .F. ) ;
#7997=CARTESIAN_POINT ( 'NONE',  ( 0.04921259842519667971, 1.708690180665275005, 2.244725876464058523 ) ) ;
#7998=ORIENTED_EDGE ( 'NONE', *, *, #33732, .T. ) ;
#8002=CARTESIAN_POINT ( 'NONE',  ( -2.168245791271168343, 1.587034731952809752, -2.004968704497279930 ) ) ;
#8003=EDGE_CURVE ( 'NONE', #30012, #26738, #34851, .T. ) ;
#8004=ORIENTED_EDGE ( 'NONE', *, *, #31857, .T. ) ;
#8005=CARTESIAN_POINT ( 'NONE',  ( 2.121469926805689354, 6.692913385826772199, -0.4337334748181388422 ) ) ;
#8010=EDGE_CURVE ( 'NONE', #38642, #37024, #20190, .T. ) ;
#8012=CARTESIAN_POINT ( 'NONE',  ( -1.083598637574820334, 1.702374950942735499, 2.747180975113330259 ) ) ;
#8014=ORIENTED_EDGE ( 'NONE', *, *, #188, .F. ) ;
#8018=DIRECTION ( 'NONE',  ( 0.000000000000000000, 0.000000000000000000, 1.000000000000000000 ) ) ;
#8019=CARTESIAN_POINT ( 'NONE',  ( -2.903572669614648660, 2.755905511811027164, 1.294565943894125715 ) ) ;
#8020=EDGE_CURVE ( 'NONE', #3944, #39458, #34455, .T. ) ;
#8021=CARTESIAN_POINT ( 'NONE',  ( 0.2430652128771959297, 1.574803149606302854, -2.151668812760857641 ) ) ;
#8023=ORIENTED_EDGE ( 'NONE', *, *, #25009, .T. ) ;
#8024=B_SPLINE_CURVE_WITH_KNOTS ( 'NONE', 3,
 ( #47310, #23857, #4235, #36507 ),
 .UNSPECIFIED., .F., .F.,
 ( 4, 4 ),
 ( 0.1211775127643062444, 0.1625894504277921315 ),
 .UNSPECIFIED. ) ;
#8026=CARTESIAN_POINT ( 'NONE',  ( 1.929629134066521701, 5.118110236220475784, 0.9824921284572420976 ) ) ;
#8027=CARTESIAN_POINT ( 'NONE',  ( 2.297395577996739213, 1.679082147652236845, 0.3608654278263103699 ) ) ;
#8031=CARTESIAN_POINT ( 'NONE',  ( 1.305557278495039775, 1.728812839972934334, -1.880670907523083191 ) ) ;
#8032=EDGE_CURVE ( 'NONE', #7866, #30710, #26414, .T. ) ;
#8033=CARTESIAN_POINT ( 'NONE',  ( 2.326943258702977246, 1.646747008850265370, -0.05524094006260020506 ) ) ;
#8034=PLANE ( 'NONE',  #9574 ) ;
#8035=CARTESIAN_POINT ( 'NONE',  ( 0.7090793742677682365, 0.03927686936677046714, 1.749277966691849429 ) ) ;
#8036=ORIENTED_EDGE ( 'NONE', *, *, #11862, .F. ) ;
#8037=FACE_OUTER_BOUND ( 'NONE', #16201, .T. ) ;
#8040=ADVANCED_FACE ( 'NONE', ( #42187 ), #37832, .F. ) ;
#8042=CARTESIAN_POINT ( 'NONE',  ( -0.04921259842519689481, -2.628659302178988761E-16, 2.213182383082910487 ) ) ;
#8046=VERTEX_POINT ( 'NONE', #18194 ) ;
#8048=EDGE_CURVE ( 'NONE', #50385, #36720, #4199, .T. ) ;
#8053=CARTESIAN_POINT ( 'NONE',  ( 1.236813753895252166, 1.738537790538875027, -2.681693691597563767 ) ) ;
#8058=DIRECTION ( 'NONE',  ( -1.000000000000000000, 0.000000000000000000, -0.000000000000000000 ) ) ;
#8059=AXIS2_PLACEMENT_3D ( 'NONE', #21430, #48496, #33317 ) ;
#8062=EDGE_LOOP ( 'NONE', ( #27589, #48368, #10518, #18589 ) ) ;
#8065=ORIENTED_EDGE ( 'NONE', *, *, #42297, .T. ) ;
#8067=CARTESIAN_POINT ( 'NONE',  ( -0.8615171516511902494, 0.5249316475426858419, -1.675535330858600291 ) ) ;
#8070=AXIS2_PLACEMENT_3D ( 'NONE', #15840, #24876, #47810 ) ;
#8072=ORIENTED_EDGE ( 'NONE', *, *, #35, .F. ) ;
#8074=CARTESIAN_POINT ( 'NONE',  ( -0.04921259842519706829, 1.516406576848131849, 2.952755905511811108 ) ) ;
#8079=ORIENTED_EDGE ( 'NONE', *, *, #2784, .F. ) ;
#8080=CARTESIAN_POINT ( 'NONE',  ( 0.07982360342473591996, 1.709180471932028711, 0.000000000000000000 ) ) ;
#8086=DIRECTION ( 'NONE',  ( -0.9998717552508122886, -0.01601477604151181275, 0.000000000000000000 ) ) ;
#8087=CARTESIAN_POINT ( 'NONE',  ( 0.7381027496705269142, 1.205361022782829114E-17, -2.859439394060913298 ) ) ;
#8096=CARTESIAN_POINT ( 'NONE',  ( -2.734482843737247038, 1.578211097029592169, -1.115254632218712016 ) ) ;
#8107=DIRECTION ( 'NONE',  ( -6.104789737168205836E-17, 1.000000000000000000, 1.134460028949762747E-16 ) ) ;
#8108=EDGE_CURVE ( 'NONE', #12124, #24792, #34205, .T. ) ;
#8112=CARTESIAN_POINT ( 'NONE',  ( 1.785720468602152611, 1.739985735216158291, -1.775410119839885059 ) ) ;
#8114=VERTEX_POINT ( 'NONE', #28851 ) ;
#8116=CARTESIAN_POINT ( 'NONE',  ( -1.735275627622573369, 1.647299937921974822, 1.320890859436214981 ) ) ;
#8118=DIRECTION ( 'NONE',  ( 0.000000000000000000, 0.000000000000000000, 1.000000000000000000 ) ) ;
#8119=ORIENTED_EDGE ( 'NONE', *, *, #31265, .F. ) ;
#8121=CYLINDRICAL_SURFACE ( 'NONE', #10101, 2.165354330708661568 ) ;
#8125=PLANE ( 'NONE',  #32977 ) ;
#8126=CARTESIAN_POINT ( 'NONE',  ( 2.100227814008711391, 1.205361022782829114E-17, -2.076109931251913565 ) ) ;
#8128=ORIENTED_EDGE ( 'NONE', *, *, #14437, .F. ) ;
#8132=EDGE_LOOP ( 'NONE', ( #10456, #3479, #12842, #35760, #38257, #40095, #3558, #50362, #32166, #19210, #21526 ) ) ;
#8134=AXIS2_PLACEMENT_3D ( 'NONE', #503, #19345, #36907 ) ;
#8135=DIRECTION ( 'NONE',  ( -0.1342332658176667026, 0.000000000000000000, 0.9909497617679331460 ) ) ;
#8136=CARTESIAN_POINT ( 'NONE',  ( -1.405314191946755997, 1.685393272164901646, 1.683309666213049560 ) ) ;
#8147=EDGE_CURVE ( 'NONE', #16522, #2113, #36861, .T. ) ;
#8153=EDGE_CURVE ( 'NONE', #8620, #27696, #36305, .T. ) ;
#8155=ORIENTED_EDGE ( 'NONE', *, *, #17879, .F. ) ;
#8156=EDGE_LOOP ( 'NONE', ( #49636, #14082, #38758, #11857, #37984, #33506, #14864, #27441, #41258, #2119, #24412, #4726, #43380 ) ) ;
#8164=DIRECTION ( 'NONE',  ( -1.000000000000000000, -1.908195823574487557E-16, 0.000000000000000000 ) ) ;
#8165=CARTESIAN_POINT ( 'NONE',  ( 0.08139965876239094178, 1.610780518492231694, 0.000000000000000000 ) ) ;
#8166=CONICAL_SURFACE ( 'NONE', #14764, 2.165354330708661568, 0.2617993877991570129 ) ;
#8170=ORIENTED_EDGE ( 'NONE', *, *, #3647, .T. ) ;
#8173=DIRECTION ( 'NONE',  ( 0.3930250316539147803, -1.067483894049308527E-16, 0.9195277725514544587 ) ) ;
#8175=AXIS2_PLACEMENT_3D ( 'NONE', #38831, #31592, #14833 ) ;
#8180=ORIENTED_EDGE ( 'NONE', *, *, #13908, .T. ) ;
#8184=EDGE_CURVE ( 'NONE', #36555, #26915, #27447, .T. ) ;
#8188=B_SPLINE_CURVE_WITH_KNOTS ( 'NONE', 3,
 ( #35839, #39710, #36098, #16478 ),
 .UNSPECIFIED., .F., .F.,
 ( 4, 4 ),
 ( 6.555779620287635616E-07, 0.004917953202330906451 ),
 .UNSPECIFIED. ) ;
#8190=DIRECTION ( 'NONE',  ( -0.01601477604151182663, 0.9998717552508123996, -0.000000000000000000 ) ) ;
#8191=DIRECTION ( 'NONE',  ( -0.9998717552508122886, -0.01601477604151185785, 0.000000000000000000 ) ) ;
#8192=DIRECTION ( 'NONE',  ( -0.01601477604151182663, 0.9998717552508123996, -0.000000000000000000 ) ) ;
#8194=ORIENTED_EDGE ( 'NONE', *, *, #7538, .F. ) ;
#8197=CARTESIAN_POINT ( 'NONE',  ( 2.152441353505198940, 5.905511811023623991, -0.2419059403264807173 ) ) ;
#8201=LINE ( 'NONE', #449, #32684 ) ;
#8206=ORIENTED_EDGE ( 'NONE', *, *, #31071, .F. ) ;
#8207=CARTESIAN_POINT ( 'NONE',  ( -1.613060539954027872, 1.682065834201676324, -1.474157253483306507 ) ) ;
#8210=VERTEX_POINT ( 'NONE', #19196 ) ;
#8212=DIRECTION ( 'NONE',  ( -0.9998717552508121775, -0.01601477604151182316, 0.000000000000000000 ) ) ;
#8216=VERTEX_POINT ( 'NONE', #4213 ) ;
#8220=VERTEX_POINT ( 'NONE', #46785 ) ;
#8223=ORIENTED_EDGE ( 'NONE', *, *, #2265, .F. ) ;
#8224=LINE ( 'NONE', #36360, #19474 ) ;
#8229=CARTESIAN_POINT ( 'NONE',  ( -1.477797890860239383, 1.651423915540254361, 1.616677638457519883 ) ) ;
#8232=CARTESIAN_POINT ( 'NONE',  ( 2.867773316779195447, 1.665472095473279790, -0.7050287376752005786 ) ) ;
#8233=CARTESIAN_POINT ( 'NONE',  ( 2.823445274216730638, 5.118110236220475784, 0.8656477926280686797 ) ) ;
#8237=PLANE ( 'NONE',  #34976 ) ;
#8238=ADVANCED_FACE ( 'NONE', ( #19700 ), #42934, .T. ) ;
#8241=EDGE_CURVE ( 'NONE', #31373, #18885, #35462, .T. ) ;
#8244=PLANE ( 'NONE',  #22589 ) ;
#8249=VERTEX_POINT ( 'NONE', #35207 ) ;
#8250=CARTESIAN_POINT ( 'NONE',  ( 1.236813753895252166, 1.487789312410982445, -2.681693691597563767 ) ) ;
#8252=LINE ( 'NONE', #35874, #17987 ) ;
#8253=AXIS2_PLACEMENT_3D ( 'NONE', #23543, #20442, #823 ) ;
#8258=DIRECTION ( 'NONE',  ( 1.160706738777443955E-16, 1.000000000000000000, -5.589669052740684758E-17 ) ) ;
#8260=EDGE_LOOP ( 'NONE', ( #18045, #38130, #20351, #7682 ) ) ;
#8266=LINE ( 'NONE', #8005, #38589 ) ;
#8269=CARTESIAN_POINT ( 'NONE',  ( 1.598711713508005339, 5.905511811023623991, -1.460438370699377986 ) ) ;
#8277=CARTESIAN_POINT ( 'NONE',  ( 0.000000000000000000, 6.692913385826772199, 0.000000000000000000 ) ) ;
#8280=DIRECTION ( 'NONE',  ( 1.042246309068005903E-16, 1.000000000000000000, -7.572362681945165783E-17 ) ) ;
#8283=PLANE ( 'NONE',  #14743 ) ;
#8284=DIRECTION ( 'NONE',  ( -1.118904554427325505E-16, -1.000000000000000000, 3.087980359898369198E-17 ) ) ;
#8294=ADVANCED_FACE ( 'NONE', ( #15083 ), #20627, .T. ) ;
#8296=EDGE_CURVE ( 'NONE', #29864, #34114, #41247, .T. ) ;
#8302=VERTEX_POINT ( 'NONE', #36231 ) ;
#8307=DIRECTION ( 'NONE',  ( -0.01601477604151182663, 0.9998717552508123996, -0.000000000000000000 ) ) ;
#8309=CIRCLE ( 'NONE', #40498, 2.164630168518208109 ) ;
#8314=EDGE_CURVE ( 'NONE', #25218, #26467, #841, .T. ) ;
#8315=ORIENTED_EDGE ( 'NONE', *, *, #31170, .T. ) ;
#8316=B_SPLINE_CURVE_WITH_KNOTS ( 'NONE', 3,
 ( #47511, #8568, #11429, #36201 ),
 .UNSPECIFIED., .F., .F.,
 ( 4, 4 ),
 ( 2.657285469857138443E-07, 0.002500653588094312214 ),
 .UNSPECIFIED. ) ;
#8318=ORIENTED_EDGE ( 'NONE', *, *, #49103, .T. ) ;
#8319=CARTESIAN_POINT ( 'NONE',  ( -0.9914495361339010771, 1.205361022782829114E-17, 2.781765111341808705 ) ) ;
#8321=EDGE_LOOP ( 'NONE', ( #33182, #37567 ) ) ;
#8323=EDGE_CURVE ( 'NONE', #23316, #7708, #49157, .T. ) ;
#8328=VERTEX_POINT ( 'NONE', #35973 ) ;
#8330=SHAPE_REPRESENTATION ( 'Front Cover', ( #26741 ), #4483 ) ;
#8335=CARTESIAN_POINT ( 'NONE',  ( -2.139038182717881487, 1.575216142802386754, 0.3394144611327329364 ) ) ;
#8339=ORIENTED_EDGE ( 'NONE', *, *, #1199, .T. ) ;
#8342=CARTESIAN_POINT ( 'NONE',  ( -1.083598637574820334, 1.603934357758587614, 2.747180975113330259 ) ) ;
#8343=EDGE_CURVE ( 'NONE', #14514, #36209, #17370, .T. ) ;
#8345=CARTESIAN_POINT ( 'NONE',  ( 0.3544269074453565982, 1.680770349861149038, 2.228666219274223259 ) ) ;
#8347=EDGE_LOOP ( 'NONE', ( #23306, #42798, #25496, #35056 ) ) ;
#8348=ORIENTED_EDGE ( 'NONE', *, *, #22840, .F. ) ;
#8351=VECTOR ( 'NONE', #20072, 39.37007874015748143 ) ;
#8352=ORIENTED_EDGE ( 'NONE', *, *, #15012, .F. ) ;
#8354=CARTESIAN_POINT ( 'NONE',  ( -1.037524086854360483, 0.000000000000000000, 2.764473043227569260 ) ) ;
#8359=PLANE ( 'NONE',  #12893 ) ;
#8361=CARTESIAN_POINT ( 'NONE',  ( -2.074656761898998170, 5.905511811023623991, -0.6223516566630905578 ) ) ;
#8362=ORIENTED_EDGE ( 'NONE', *, *, #18332, .F. ) ;
#8365=LINE ( 'NONE', #48072, #20775 ) ;
#8366=EDGE_CURVE ( 'NONE', #1230, #7184, #14854, .T. ) ;
#8370=CARTESIAN_POINT ( 'NONE',  ( 2.100227814008711835, 1.751990118145921649, -2.076109931251913565 ) ) ;
#8371=CARTESIAN_POINT ( 'NONE',  ( -0.4532322590609024759, 0.000000000000000000, -1.827234353172969561 ) ) ;
#8373=CARTESIAN_POINT ( 'NONE',  ( -1.613190494289090227, 1.049866565877818125, 1.223531214424602220 ) ) ;
#8374=CARTESIAN_POINT ( 'NONE',  ( 2.113646359261424745, 1.643330668647667858, -0.9569352356128659753 ) ) ;
#8379=CARTESIAN_POINT ( 'NONE',  ( 0.3136974817028393425, 1.625700591256411531, -2.936457595020219635 ) ) ;
#8382=CARTESIAN_POINT ( 'NONE',  ( -1.139874548450032332, 0.006507011016954251416, 1.379489548043156377 ) ) ;
#8385=ORIENTED_EDGE ( 'NONE', *, *, #14185, .F. ) ;
#8387=DIRECTION ( 'NONE',  ( 1.776356839400250149E-14, 0.000000000000000000, 1.000000000000000000 ) ) ;
#8388=CYLINDRICAL_SURFACE ( 'NONE', #41969, 2.165354330708661568 ) ;
#8401=CARTESIAN_POINT ( 'NONE',  ( -0.7381027496704858359, 1.609316782724114825, -2.859439394060923512 ) ) ;
#8402=LINE ( 'NONE', #655, #10858 ) ;
#8406=DIRECTION ( 'NONE',  ( 0.000000000000000000, 1.000000000000000000, 0.000000000000000000 ) ) ;
#8408=AXIS2_PLACEMENT_3D ( 'NONE', #19558, #46652, #458 ) ;
#8410=DIRECTION ( 'NONE',  ( -4.561975526775602830E-17, -1.000000000000000000, -1.067327232801823148E-16 ) ) ;
#8411=EDGE_CURVE ( 'NONE', #10925, #37629, #47782, .T. ) ;
#8412=CONICAL_SURFACE ( 'NONE', #46305, 2.165354330708661568, 0.2617993877991570129 ) ;
#8413=EDGE_CURVE ( 'NONE', #30219, #13738, #42871, .T. ) ;
#8415=ORIENTED_EDGE ( 'NONE', *, *, #30886, .T. ) ;
#8417=DIRECTION ( 'NONE',  ( 0.9998717552508121775, 0.01601477604151182663, 0.000000000000000000 ) ) ;
#8418=ORIENTED_EDGE ( 'NONE', *, *, #42498, .T. ) ;
#8420=PLANE ( 'NONE',  #41905 ) ;
#8432=DIRECTION ( 'NONE',  ( 0.9195277725514544587, 4.558310254684937226E-17, -0.3930250316539147803 ) ) ;
#8434=ORIENTED_EDGE ( 'NONE', *, *, #40195, .F. ) ;
#8436=DIRECTION ( 'NONE',  ( -0.000000000000000000, 1.000000000000000000, -0.000000000000000000 ) ) ;
#8447=DIRECTION ( 'NONE',  ( 5.063291518729136385E-17, 1.000000000000000000, -1.184615939703115601E-16 ) ) ;
#8450=VERTEX_POINT ( 'NONE', #45973 ) ;
#8451=ORIENTED_EDGE ( 'NONE', *, *, #6234, .F. ) ;
#8453=ORIENTED_EDGE ( 'NONE', *, *, #7624, .T. ) ;
#8459=CARTESIAN_POINT ( 'NONE',  ( 2.145573199460771630, 1.654219156693913284, -2.028682376382505481 ) ) ;
#8460=EDGE_LOOP ( 'NONE', ( #32086, #7701, #47016, #38522, #45587, #36125, #8119, #45578, #45850, #37069, #10508 ) ) ;
#8461=CARTESIAN_POINT ( 'NONE',  ( 0.07982360342473591996, 1.709180471932028711, 0.000000000000000000 ) ) ;
#8462=VERTEX_POINT ( 'NONE', #33637 ) ;
#8467=ORIENTED_EDGE ( 'NONE', *, *, #46770, .F. ) ;
#8471=VECTOR ( 'NONE', #47083, 39.37007874015748143 ) ;
#8472=CARTESIAN_POINT ( 'NONE',  ( -0.9914495361339010771, 1.205361022782829114E-17, 2.781765111341808705 ) ) ;
#8473=ORIENTED_EDGE ( 'NONE', *, *, #2064, .F. ) ;
#8476=ORIENTED_EDGE ( 'NONE', *, *, #27531, .T. ) ;
#8479=VECTOR ( 'NONE', #47992, 39.37007874015748854 ) ;
#8489=CARTESIAN_POINT ( 'NONE',  ( 1.018961996185594021, 0.04424020667788951949, 1.609505285524495344 ) ) ;
#8491=ADVANCED_FACE ( 'NONE', ( #45722 ), #8510, .T. ) ;
#8492=FACE_OUTER_BOUND ( 'NONE', #42747, .T. ) ;
#8494=DIRECTION ( 'NONE',  ( -0.000000000000000000, -1.000000000000000000, -0.000000000000000000 ) ) ;
#8495=EDGE_CURVE ( 'NONE', #29934, #8220, #2125, .T. ) ;
#8497=DIRECTION ( 'NONE',  ( -3.981026654148627524E-17, 1.000000000000000000, 1.225234019452863932E-16 ) ) ;
#8500=CARTESIAN_POINT ( 'NONE',  ( 0.7381027496705270252, 1.499047760149736952, -2.859439394060913298 ) ) ;
#8504=DIRECTION ( 'NONE',  ( -9.701723960855733411E-17, 1.000000000000000000, -8.476140964546406840E-17 ) ) ;
#8506=CARTESIAN_POINT ( 'NONE',  ( 2.252332422952718183, 1.743977176619643910, -0.5645583697864726691 ) ) ;
#8507=ORIENTED_EDGE ( 'NONE', *, *, #8296, .T. ) ;
#8510=CONICAL_SURFACE ( 'NONE', #10176, 2.165354330708661568, 0.2617993877991570129 ) ;
#8511=CIRCLE ( 'NONE', #10985, 2.165354330708661568 ) ;
#8513=DIRECTION ( 'NONE',  ( -0.9998717552508122886, -0.01601477604151185785, 0.000000000000000000 ) ) ;
#8514=VECTOR ( 'NONE', #7854, 39.37007874015748143 ) ;
#8525=EDGE_CURVE ( 'NONE', #1230, #37126, #3266, .T. ) ;
#8532=DIRECTION ( 'NONE',  ( -0.9998717552508122886, -0.01601477604151180928, 0.000000000000000000 ) ) ;
#8533=DIRECTION ( 'NONE',  ( -0.000000000000000000, -1.000000000000000000, -0.000000000000000000 ) ) ;
#8541=AXIS2_PLACEMENT_3D ( 'NONE', #39424, #43537, #38917 ) ;
#8551=AXIS2_PLACEMENT_3D ( 'NONE', #11101, #15225, #42328 ) ;
#8553=CARTESIAN_POINT ( 'NONE',  ( -1.531618802077458597, 0.5250564235503655253, -1.532464050950231194 ) ) ;
#8558=FACE_OUTER_BOUND ( 'NONE', #45663, .T. ) ;
#8563=DIRECTION ( 'NONE',  ( -0.5128992774058949156, 0.000000000000000000, -0.8584487936018728726 ) ) ;
#8567=DIRECTION ( 'NONE',  ( -0.000000000000000000, 1.000000000000000000, -0.000000000000000000 ) ) ;
#8568=CARTESIAN_POINT ( 'NONE',  ( 1.930368855416772611, 1.471021869409010030, 2.234437973217711093 ) ) ;
#8572=ORIENTED_EDGE ( 'NONE', *, *, #22408, .F. ) ;
#8574=FACE_OUTER_BOUND ( 'NONE', #46090, .T. ) ;
#8575=CONICAL_SURFACE ( 'NONE', #15981, 2.246510896728926010, 0.01601546068027819014 ) ;
#8576=ORIENTED_EDGE ( 'NONE', *, *, #19455, .F. ) ;
#8581=VECTOR ( 'NONE', #48608, 39.37007874015748143 ) ;
#8582=CIRCLE ( 'NONE', #37466, 2.246510896728926010 ) ;
#8591=ORIENTED_EDGE ( 'NONE', *, *, #27706, .T. ) ;
#8593=CARTESIAN_POINT ( 'NONE',  ( 0.002207914879453961969, 5.905511811023623991, 0.04916304461325442243 ) ) ;
#8595=ORIENTED_EDGE ( 'NONE', *, *, #2609, .F. ) ;
#8598=CARTESIAN_POINT ( 'NONE',  ( 0.002207914879453961969, 5.905511811023623991, 0.04916304461325442243 ) ) ;
#8601=LINE ( 'NONE', #5496, #7368 ) ;
#8605=VERTEX_POINT ( 'NONE', #269 ) ;
#8609=CARTESIAN_POINT ( 'NONE',  ( 2.715732320886252271, 5.118110236220475784, 1.948858261851765583 ) ) ;
#8610=AXIS2_PLACEMENT_3D ( 'NONE', #6826, #38828, #7834 ) ;
#8612=LINE ( 'NONE', #868, #36910 ) ;
#8613=EDGE_LOOP ( 'NONE', ( #30438, #35733, #2498, #36194 ) ) ;
#8616=EDGE_CURVE ( 'NONE', #20464, #19026, #47191, .T. ) ;
#8619=AXIS2_PLACEMENT_3D ( 'NONE', #35615, #18158, #12370 ) ;
#8620=VERTEX_POINT ( 'NONE', #46720 ) ;
#8622=CARTESIAN_POINT ( 'NONE',  ( -0.7381027496704855029, 1.707760278544290689, -2.859439394060923512 ) ) ;
#8623=CARTESIAN_POINT ( 'NONE',  ( 2.711393191283637982, 1.758056152059489063, 0.4169452149318388368 ) ) ;
#8624=EDGE_CURVE ( 'NONE', #29978, #39017, #15, .T. ) ;
#8630=ORIENTED_EDGE ( 'NONE', *, *, #48756, .T. ) ;
#8632=DIRECTION ( 'NONE',  ( 8.881784197001252323E-16, 0.000000000000000000, -1.000000000000000000 ) ) ;
#8634=DIRECTION ( 'NONE',  ( -0.9998717552508122886, -0.01601477604151180928, 0.000000000000000000 ) ) ;
#8635=EDGE_CURVE ( 'NONE', #50807, #7499, #3899, .T. ) ;
#8638=DIRECTION ( 'NONE',  ( -0.08963930890342654279, 1.156097046908844086E-16, -0.9959742939952397345 ) ) ;
#8640=ORIENTED_EDGE ( 'NONE', *, *, #28715, .T. ) ;
#8642=CARTESIAN_POINT ( 'NONE',  ( -2.671951887028160666, 1.575085747223753829, 0.3122784236066050711 ) ) ;
#8643=ORIENTED_EDGE ( 'NONE', *, *, #33338, .F. ) ;
#8646=LINE ( 'NONE', #646, #40145 ) ;
#8647=CARTESIAN_POINT ( 'NONE',  ( -2.074656761898998170, 0.000000000000000000, -0.6223516566630912239 ) ) ;
#8649=ORIENTED_EDGE ( 'NONE', *, *, #30946, .F. ) ;
#8652=CARTESIAN_POINT ( 'NONE',  ( -0.8013547813281791665, 1.608322728230706655, -2.841982942506608989 ) ) ;
#8653=DIRECTION ( 'NONE',  ( 0.000000000000000000, -1.000000000000000000, -0.000000000000000000 ) ) ;
#8655=AXIS2_PLACEMENT_3D ( 'NONE', #32051, #12416, #20414 ) ;
#8659=ORIENTED_EDGE ( 'NONE', *, *, #9951, .T. ) ;
#8665=ORIENTED_EDGE ( 'NONE', *, *, #48313, .T. ) ;
#8671=VECTOR ( 'NONE', #19038, 39.37007874015748143 ) ;
#8673=CARTESIAN_POINT ( 'NONE',  ( -1.675814739737315540, 1.582635513994296250, 1.399362935606387470 ) ) ;
#8679=DIRECTION ( 'NONE',  ( -3.986037398843765983E-20, -1.000000000000000000, -1.160734090543304660E-16 ) ) ;
#8680=DIRECTION ( 'NONE',  ( -3.986037398843765983E-20, -1.000000000000000000, -1.160734090543304660E-16 ) ) ;
#8682=VERTEX_POINT ( 'NONE', #34887 ) ;
#8685=ORIENTED_EDGE ( 'NONE', *, *, #3772, .F. ) ;
#8687=ADVANCED_FACE ( 'NONE', ( #3389 ), #26868, .T. ) ;
#8688=CARTESIAN_POINT ( 'NONE',  ( 1.215807329263347114, 1.628950133432788494, 1.938968878379255578 ) ) ;
#8690=CONICAL_SURFACE ( 'NONE', #29293, 3.483074324928249421, 1.244861948955335196 ) ;
#8691=VECTOR ( 'NONE', #43614, 39.37007874015748854 ) ;
#8695=CARTESIAN_POINT ( 'NONE',  ( 2.695799277629594037, 1.761268146152256575, -1.205759334241453651 ) ) ;
#8712=VERTEX_POINT ( 'NONE', #4150 ) ;
#8714=LINE ( 'NONE', #36601, #34714 ) ;
#8715=EDGE_LOOP ( 'NONE', ( #22586, #42494, #43460, #30061 ) ) ;
#8719=CARTESIAN_POINT ( 'NONE',  ( 1.673977678072228414, 0.5225566574842699374, -1.532400001105657106 ) ) ;
#8725=VECTOR ( 'NONE', #14953, 39.37007874015748143 ) ;
#8727=CARTESIAN_POINT ( 'NONE',  ( 2.867773316779195447, 1.763947033723992641, -0.7050287376752004675 ) ) ;
#8729=ORIENTED_EDGE ( 'NONE', *, *, #44896, .F. ) ;
#8732=AXIS2_PLACEMENT_3D ( 'NONE', #25867, #10634, #41117 ) ;
#8733=FACE_OUTER_BOUND ( 'NONE', #15885, .T. ) ;
#8738=CARTESIAN_POINT ( 'NONE',  ( 2.607957125086718175, 1.759890798980135118, 1.384772967391346921 ) ) ;
#8742=DIRECTION ( 'NONE',  ( 0.000000000000000000, 0.000000000000000000, -1.000000000000000000 ) ) ;
#8745=DIRECTION ( 'NONE',  ( -0.9998717552508122886, -0.01601477604151180928, 0.000000000000000000 ) ) ;
#8746=ORIENTED_EDGE ( 'NONE', *, *, #43855, .F. ) ;
#8753=CARTESIAN_POINT ( 'NONE',  ( 0.000000000000000000, 6.692913385826772199, 0.000000000000000000 ) ) ;
#8760=CARTESIAN_POINT ( 'NONE',  ( 0.6502734851936936566, 1.718317270777941941, -2.171228911417812046 ) ) ;
#8762=ORIENTED_EDGE ( 'NONE', *, *, #32213, .F. ) ;
#8763=DIRECTION ( 'NONE',  ( -0.01601477604151182663, 0.9998717552508123996, -0.000000000000000000 ) ) ;
#8773=ORIENTED_EDGE ( 'NONE', *, *, #39535, .F. ) ;
#8774=CARTESIAN_POINT ( 'NONE',  ( 1.951523201471517588, 0.05917688107560774985, -0.1369052102211298083 ) ) ;
#8776=LINE ( 'NONE', #24783, #44979 ) ;
#8777=EDGE_CURVE ( 'NONE', #14924, #10014, #40855, .T. ) ;
#8779=LINE ( 'NONE', #39761, #19222 ) ;
#8781=EDGE_CURVE ( 'NONE', #3510, #23904, #32447, .T. ) ;
#8783=EDGE_CURVE ( 'NONE', #30043, #46764, #50038, .T. ) ;
#8787=EDGE_LOOP ( 'NONE', ( #33163, #34853, #24233, #50293 ) ) ;
#8790=VECTOR ( 'NONE', #7417, 39.37007874015748143 ) ;
#8792=FACE_OUTER_BOUND ( 'NONE', #13756, .T. ) ;
#8794=ORIENTED_EDGE ( 'NONE', *, *, #46353, .T. ) ;
#8795=CARTESIAN_POINT ( 'NONE',  ( -1.055804188380104813, 0.000000000000000000, -1.480985967717771690 ) ) ;
#8797=PLANE ( 'NONE',  #49339 ) ;
#8802=CARTESIAN_POINT ( 'NONE',  ( -1.936750629140493007, 1.578456148182591168, 0.9863243683714766341 ) ) ;
#8803=AXIS2_PLACEMENT_3D ( 'NONE', #32109, #35975, #44217 ) ;
#8807=EDGE_LOOP ( 'NONE', ( #37740, #32720, #3581, #44901 ) ) ;
#8810=ORIENTED_EDGE ( 'NONE', *, *, #35364, .F. ) ;
#8816=VERTEX_POINT ( 'NONE', #36678 ) ;
#8817=ADVANCED_FACE ( 'NONE', ( #1298 ), #47477, .T. ) ;
#8822=B_SPLINE_CURVE_WITH_KNOTS ( 'NONE', 3,
 ( #14273, #30021, #45740, #2910 ),
 .UNSPECIFIED., .F., .F.,
 ( 4, 4 ),
 ( 2.558985349373473962E-07, 0.002500451054789445439 ),
 .UNSPECIFIED. ) ;
#8823=CARTESIAN_POINT ( 'NONE',  ( -1.721400284384397628, 0.0003482895740541699209, 0.2828415639128913361 ) ) ;
#8826=CARTESIAN_POINT ( 'NONE',  ( 0.07982360342473591996, 1.709180471932028711, 0.000000000000000000 ) ) ;
#8831=ORIENTED_EDGE ( 'NONE', *, *, #24971, .F. ) ;
#8835=CARTESIAN_POINT ( 'NONE',  ( -0.9836083787002332102, 1.574803149606302854, -1.929060376159713375 ) ) ;
#8847=ORIENTED_EDGE ( 'NONE', *, *, #10414, .T. ) ;
#8851=ORIENTED_EDGE ( 'NONE', *, *, #30946, .T. ) ;
#8853=CARTESIAN_POINT ( 'NONE',  ( 0.3467207527347879736, 6.692913385826772199, 2.186201806782071877 ) ) ;
#8867=CARTESIAN_POINT ( 'NONE',  ( 2.923830774216937822, 1.666335789833975900, 0.4126137885002218453 ) ) ;
#8871=LINE ( 'NONE', #27715, #37392 ) ;
#8875=CARTESIAN_POINT ( 'NONE',  ( 0.1450362469327826365, 1.574803149606302854, -2.160491579385212191 ) ) ;
#8877=ORIENTED_EDGE ( 'NONE', *, *, #20324, .T. ) ;
#8883=ORIENTED_EDGE ( 'NONE', *, *, #15012, .T. ) ;
#8886=ORIENTED_EDGE ( 'NONE', *, *, #37655, .F. ) ;
#8892=CARTESIAN_POINT ( 'NONE',  ( 0.6284326417183513369, 0.02518258341035289893, 1.814510055229779040 ) ) ;
#8893=EDGE_CURVE ( 'NONE', #25998, #48706, #43091, .T. ) ;
#8894=EDGE_LOOP ( 'NONE', ( #3639, #18262, #34261, #18056 ) ) ;
#8898=ORIENTED_EDGE ( 'NONE', *, *, #13737, .T. ) ;
#8900=FACE_OUTER_BOUND ( 'NONE', #33415, .T. ) ;
#8912=CARTESIAN_POINT ( 'NONE',  ( -0.4788131938641531637, 1.205361022782829114E-17, 2.914091152102186388 ) ) ;
#8915=EDGE_CURVE ( 'NONE', #25006, #24163, #33466, .T. ) ;
#8919=ORIENTED_EDGE ( 'NONE', *, *, #19065, .T. ) ;
#8920=CARTESIAN_POINT ( 'NONE',  ( -1.281152772984899491, 0.000000000000000000, -2.660341145381166506 ) ) ;
#8922=ORIENTED_EDGE ( 'NONE', *, *, #43509, .F. ) ;
#8926=ORIENTED_EDGE ( 'NONE', *, *, #42071, .T. ) ;
#8927=AXIS2_PLACEMENT_3D ( 'NONE', #17892, #49084, #17132 ) ;
#8931=CARTESIAN_POINT ( 'NONE',  ( 2.073577001504950168, 0.9922959628731219395, 1.590677202529814593 ) ) ;
#8932=DIRECTION ( 'NONE',  ( 0.3513748240813434620, 0.000000000000000000, -0.9362348706397368714 ) ) ;
#8940=CARTESIAN_POINT ( 'NONE',  ( 1.131369771556057113, 1.631181450708906411, -2.235890070012082731 ) ) ;
#8945=CARTESIAN_POINT ( 'NONE',  ( 0.1155636338427008941, -0.5222242541845523167, 0.000000000000000000 ) ) ;
#8949=FACE_OUTER_BOUND ( 'NONE', #21200, .T. ) ;
#8960=CONICAL_SURFACE ( 'NONE', #3164, 2.244934639244524632, 1.554780866114618743 ) ;
#8966=DIRECTION ( 'NONE',  ( -0.9998717552508122886, -0.01601477604151185785, 0.000000000000000000 ) ) ;
#8969=AXIS2_PLACEMENT_3D ( 'NONE', #36366, #990, #47682 ) ;
#8973=ORIENTED_EDGE ( 'NONE', *, *, #22221, .F. ) ;
#8977=CARTESIAN_POINT ( 'NONE',  ( 1.152895553066221268, 6.692913385826772199, -1.833672301139072758 ) ) ;
#8981=ORIENTED_EDGE ( 'NONE', *, *, #16332, .T. ) ;
#8990=CIRCLE ( 'NONE', #27140, 2.246510896728926010 ) ;
#8991=B_SPLINE_CURVE_WITH_KNOTS ( 'NONE', 3,
 ( #38028, #10655, #6774, #37775 ),
 .UNSPECIFIED., .F., .F.,
 ( 4, 4 ),
 ( 0.001423630509341207613, 0.04645086268844192401 ),
 .UNSPECIFIED. ) ;
#8996=CARTESIAN_POINT ( 'NONE',  ( 1.281152772984938126, 5.905511811023623991, -2.660341145381147854 ) ) ;
#9000=AXIS2_PLACEMENT_3D ( 'NONE', #31607, #15848, #43463 ) ;
#9001=CARTESIAN_POINT ( 'NONE',  ( -0.6380732109764247761, 1.697682040615038801, -2.127022210610377773 ) ) ;
#9003=PLANE ( 'NONE',  #19834 ) ;
#9007=DIRECTION ( 'NONE',  ( -0.000000000000000000, -1.000000000000000000, -0.000000000000000000 ) ) ;
#9010=ORIENTED_EDGE ( 'NONE', *, *, #18749, .T. ) ;
#9012=ADVANCED_FACE ( 'NONE', ( #22705 ), #26675, .T. ) ;
#9013=CARTESIAN_POINT ( 'NONE',  ( -1.700636463192204628, 0.000000000000000000, -0.4049693226113392219 ) ) ;
#9020=CARTESIAN_POINT ( 'NONE',  ( 1.461782879395302048, 1.205361022782829114E-17, -1.598346982901808211 ) ) ;
#9021=DIRECTION ( 'NONE',  ( 0.3513748240813304724, 0.000000000000000000, 0.9362348706397417564 ) ) ;
#9022=VERTEX_POINT ( 'NONE', #18584 ) ;
#9031=ORIENTED_EDGE ( 'NONE', *, *, #36870, .T. ) ;
#9032=LINE ( 'NONE', #40530, #2095 ) ;
#9036=CARTESIAN_POINT ( 'NONE',  ( 0.1067246931122726866, 0.02962905676920215767, 0.000000000000000000 ) ) ;
#9038=ADVANCED_FACE ( 'NONE', ( #23197 ), #33297, .F. ) ;
#9044=ORIENTED_EDGE ( 'NONE', *, *, #49482, .F. ) ;
#9048=CIRCLE ( 'NONE', #51031, 1.850107469027523432 ) ;
#9052=ORIENTED_EDGE ( 'NONE', *, *, #17304, .T. ) ;
#9053=ORIENTED_EDGE ( 'NONE', *, *, #22560, .T. ) ;
#9054=B_SPLINE_CURVE_WITH_KNOTS ( 'NONE', 3,
 ( #3115, #2866, #14745, #46202 ),
 .UNSPECIFIED., .F., .F.,
 ( 4, 4 ),
 ( 2.272220830976737561E-07, 0.01613183417298772598 ),
 .UNSPECIFIED. ) ;
#9058=CARTESIAN_POINT ( 'NONE',  ( 1.514466370292996800, 0.000000000000000000, 2.534789744887420149 ) ) ;
#9061=CARTESIAN_POINT ( 'NONE',  ( -2.307846990702095535, 2.755905511811027164, -0.8016101313716829102 ) ) ;
#9062=EDGE_CURVE ( 'NONE', #5044, #49731, #21105, .T. ) ;
#9071=CARTESIAN_POINT ( 'NONE',  ( 2.889674983507178219, 1.764288196056212454, -0.6090712660037608250 ) ) ;
#9072=CARTESIAN_POINT ( 'NONE',  ( -0.8329809839909436686, 1.706281419137876565, -2.833254665166566877 ) ) ;
#9077=CARTESIAN_POINT ( 'NONE',  ( 2.121469926805689354, 5.905511811023623991, -0.4337334748181388977 ) ) ;
#9082=VERTEX_POINT ( 'NONE', #46666 ) ;
#9094=DIRECTION ( 'NONE',  ( 0.000000000000000000, 1.160734090543304660E-16, -1.000000000000000000 ) ) ;
#9098=CARTESIAN_POINT ( 'NONE',  ( 0.08139965876239094178, 1.610780518492231694, 0.000000000000000000 ) ) ;
#9100=CARTESIAN_POINT ( 'NONE',  ( 2.867773316779195447, 1.449472587384593725, -0.7050287376752005786 ) ) ;
#9107=EDGE_CURVE ( 'NONE', #20582, #2274, #3586, .T. ) ;
#9114=CARTESIAN_POINT ( 'NONE',  ( 2.793030215715258446, 1.664308485742666877, 0.9592557174602684977 ) ) ;
#9118=ADVANCED_FACE ( 'NONE', ( #24740 ), #23965, .F. ) ;
#9121=CARTESIAN_POINT ( 'NONE',  ( -0.7145799201509074328, 1.574803149606302854, 2.044048657746648789 ) ) ;
#9122=CARTESIAN_POINT ( 'NONE',  ( 2.061875708210571201, 1.740926663775191674, 1.053657044629532802 ) ) ;
#9123=ORIENTED_EDGE ( 'NONE', *, *, #40195, .T. ) ;
#9126=DIRECTION ( 'NONE',  ( 0.000000000000000000, 1.160734090543304660E-16, -1.000000000000000000 ) ) ;
#9129=CARTESIAN_POINT ( 'NONE',  ( 0.8952071785065209841, 5.905511811023623991, 1.972340328593148007 ) ) ;
#9131=AXIS2_PLACEMENT_3D ( 'NONE', #47891, #8190, #44050 ) ;
#9133=CARTESIAN_POINT ( 'NONE',  ( 0.000000000000000000, 6.692913385826772199, 0.000000000000000000 ) ) ;
#9134=ORIENTED_EDGE ( 'NONE', *, *, #13778, .T. ) ;
#9141=VECTOR ( 'NONE', #32736, 39.37007874015748143 ) ;
#9143=ORIENTED_EDGE ( 'NONE', *, *, #39612, .F. ) ;
#9146=DIRECTION ( 'NONE',  ( -8.032339854997315857E-17, 1.000000000000000000, -1.007223559679407077E-16 ) ) ;
#9153=B_SPLINE_CURVE_WITH_KNOTS ( 'NONE', 3,
 ( #49057, #1608, #13236, #20975 ),
 .UNSPECIFIED., .F., .F.,
 ( 4, 4 ),
 ( 2.895195689601480918E-07, 0.01652376043565199903 ),
 .UNSPECIFIED. ) ;
#9160=ORIENTED_EDGE ( 'NONE', *, *, #7676, .T. ) ;
#9162=B_SPLINE_CURVE_WITH_KNOTS ( 'NONE', 3,
 ( #40103, #20473, #4731, #28464 ),
 .UNSPECIFIED., .F., .F.,
 ( 4, 4 ),
 ( 2.102951557409031314E-07, 0.002500239225155444656 ),
 .UNSPECIFIED. ) ;
#9163=CARTESIAN_POINT ( 'NONE',  ( 0.000000000000000000, 0.07874015748031502893, 0.000000000000000000 ) ) ;
#9169=VERTEX_POINT ( 'NONE', #984 ) ;
#9170=CARTESIAN_POINT ( 'NONE',  ( 0.1170985530868079300, 0.02979521312206013725, -1.850078377359382298 ) ) ;
#9173=CARTESIAN_POINT ( 'NONE',  ( -2.101391096692225791, 1.575819129783617489, -0.5301069970517552354 ) ) ;
#9177=CARTESIAN_POINT ( 'NONE',  ( 0.3129956986666029839, 1.049866565877818347, 2.000361441378088578 ) ) ;
#9179=VERTEX_POINT ( 'NONE', #31720 ) ;
#9182=B_SPLINE_CURVE_WITH_KNOTS ( 'NONE', 3,
 ( #50404, #42946, #22843, #7598 ),
 .UNSPECIFIED., .F., .F.,
 ( 4, 4 ),
 ( 0.01346820720327507846, 0.03074302814991078381 ),
 .UNSPECIFIED. ) ;
#9183=DIRECTION ( 'NONE',  ( -0.9009688679024154823, 1.288287287306305283E-16, -0.4338837391175656699 ) ) ;
#9185=ADVANCED_FACE ( 'NONE', ( #731 ), #47420, .F. ) ;
#9187=VECTOR ( 'NONE', #38602, 39.37007874015748143 ) ;
#9190=CARTESIAN_POINT ( 'NONE',  ( 0.04921259842519669359, 1.610264983814881479, 2.246280244424690320 ) ) ;
#9192=CARTESIAN_POINT ( 'NONE',  ( 0.000000000000000000, 1.574803149606302854, 0.000000000000000000 ) ) ;
#9194=ORIENTED_EDGE ( 'NONE', *, *, #30228, .T. ) ;
#9196=ADVANCED_FACE ( 'NONE', ( #32236 ), #28084, .T. ) ;
#9201=DIRECTION ( 'NONE',  ( 0.9510565162951500895, 0.000000000000000000, 0.3090169943749582204 ) ) ;
#9208=FACE_OUTER_BOUND ( 'NONE', #24919, .T. ) ;
#9210=VECTOR ( 'NONE', #40421, 39.37007874015748143 ) ;
#9211=CARTESIAN_POINT ( 'NONE',  ( 1.672606463373375485, 0.000000000000000000, 0.4917175957957914401 ) ) ;
#9213=AXIS2_PLACEMENT_3D ( 'NONE', #18988, #34742, #11249 ) ;
#9217=ORIENTED_EDGE ( 'NONE', *, *, #30917, .T. ) ;
#9223=PLANE ( 'NONE',  #4339 ) ;
#9224=B_SPLINE_CURVE_WITH_KNOTS ( 'NONE', 3,
 ( #10665, #6787, #10910, #50591 ),
 .UNSPECIFIED., .F., .F.,
 ( 4, 4 ),
 ( 2.397469164285932143E-07, 0.01629908605468858088 ),
 .UNSPECIFIED. ) ;
#9226=ORIENTED_EDGE ( 'NONE', *, *, #4174, .T. ) ;
#9234=ADVANCED_FACE ( 'NONE', ( #40488 ), #44799, .T. ) ;
#9236=ORIENTED_EDGE ( 'NONE', *, *, #37064, .T. ) ;
#9237=B_SPLINE_CURVE_WITH_KNOTS ( 'NONE', 3,
 ( #42564, #3323, #15199, #30950 ),
 .UNSPECIFIED., .F., .F.,
 ( 4, 4 ),
 ( 0.1211775127643062860, 0.1625894504277921315 ),
 .UNSPECIFIED. ) ;
#9244=EDGE_CURVE ( 'NONE', #46444, #33470, #15379, .T. ) ;
#9247=AXIS2_PLACEMENT_3D ( 'NONE', #35066, #14936, #3063 ) ;
#9255=AXIS2_PLACEMENT_3D ( 'NONE', #46375, #11039, #50472 ) ;
#9256=DIRECTION ( 'NONE',  ( 0.8805955318567391110, 0.000000000000000000, -0.4738686624729965269 ) ) ;
#9257=EDGE_CURVE ( 'NONE', #30941, #16203, #48895, .T. ) ;
#9259=DIRECTION ( 'NONE',  ( -0.01601477604151182663, 0.9998717552508123996, -0.000000000000000000 ) ) ;
#9260=CARTESIAN_POINT ( 'NONE',  ( 2.793030215715258446, 1.762782749918499814, 0.9592557174602684977 ) ) ;
#9263=EDGE_CURVE ( 'NONE', #24903, #10800, #35744, .T. ) ;
#9266=CARTESIAN_POINT ( 'NONE',  ( -2.867773316779185677, 1.674559808355669199, -0.7050287376752426560 ) ) ;
#9270=ORIENTED_EDGE ( 'NONE', *, *, #38742, .F. ) ;
#9272=CARTESIAN_POINT ( 'NONE',  ( 0.1067246931122726866, 0.02962905676920215767, 0.000000000000000000 ) ) ;
#9277=ORIENTED_EDGE ( 'NONE', *, *, #46965, .F. ) ;
#9278=CARTESIAN_POINT ( 'NONE',  ( 2.074049943651431693, 1.574803149606302854, 0.6221544894624233546 ) ) ;
#9280=AXIS2_PLACEMENT_3D ( 'NONE', #3132, #50560, #34629 ) ;
#9283=CARTESIAN_POINT ( 'NONE',  ( -2.150703319933163993, 1.607838006543269804, -0.2514661222534355645 ) ) ;
#9287=CIRCLE ( 'NONE', #15076, 1.850107469027523432 ) ;
#9290=EDGE_LOOP ( 'NONE', ( #21613, #26165, #21048, #33127 ) ) ;
#9293=LINE ( 'NONE', #48740, #5600 ) ;
#9296=B_SPLINE_CURVE_WITH_KNOTS ( 'NONE', 3,
 ( #26288, #18036, #13656, #6162 ),
 .UNSPECIFIED., .F., .F.,
 ( 4, 4 ),
 ( 0.01171354017532363727, 0.03073678216732763507 ),
 .UNSPECIFIED. ) ;
#9299=ORIENTED_EDGE ( 'NONE', *, *, #41798, .F. ) ;
#9305=DIRECTION ( 'NONE',  ( -0.01601477604151182663, 0.9998717552508123996, -0.000000000000000000 ) ) ;
#9308=EDGE_LOOP ( 'NONE', ( #35749, #2639, #25547, #19417 ) ) ;
#9309=ORIENTED_EDGE ( 'NONE', *, *, #34036, .F. ) ;
#9310=CARTESIAN_POINT ( 'NONE',  ( 0.000000000000000000, 6.692913385826772199, 0.000000000000000000 ) ) ;
#9313=CARTESIAN_POINT ( 'NONE',  ( 0.000000000000000000, 0.000000000000000000, 0.000000000000000000 ) ) ;
#9316=B_SPLINE_CURVE_WITH_KNOTS ( 'NONE', 3,
 ( #1543, #13417, #13170, #1793 ),
 .UNSPECIFIED., .F., .F.,
 ( 4, 4 ),
 ( 4.217863529357209716E-07, 0.04981117579911063797 ),
 .UNSPECIFIED. ) ;
#9318=CIRCLE ( 'NONE', #1055, 2.165354330708661568 ) ;
#9320=DIRECTION ( 'NONE',  ( 0.9998717552508121775, 0.01601477604151182663, 0.000000000000000000 ) ) ;
#9322=VERTEX_POINT ( 'NONE', #30873 ) ;
#9324=ORIENTED_EDGE ( 'NONE', *, *, #31040, .F. ) ;
#9326=DIRECTION ( 'NONE',  ( -0.9998717552508122886, -0.01601477604151180928, 0.000000000000000000 ) ) ;
#9331=VERTEX_POINT ( 'NONE', #23117 ) ;
#9334=ORIENTED_EDGE ( 'NONE', *, *, #24265, .F. ) ;
#9336=CARTESIAN_POINT ( 'NONE',  ( -1.744243240276441398, 5.905511811023623991, 1.328042291889479420 ) ) ;
#9338=ORIENTED_EDGE ( 'NONE', *, *, #39340, .F. ) ;
#9340=ORIENTED_EDGE ( 'NONE', *, *, #26647, .T. ) ;
#9342=ORIENTED_EDGE ( 'NONE', *, *, #46744, .F. ) ;
#9347=CARTESIAN_POINT ( 'NONE',  ( 0.002207914879453961969, 6.692913385826772199, 0.04916304461325451958 ) ) ;
#9349=VERTEX_POINT ( 'NONE', #19489 ) ;
#9350=CARTESIAN_POINT ( 'NONE',  ( 0.04921259842519667277, 1.720031199985617265, 2.952755905511811108 ) ) ;
#9352=B_SPLINE_CURVE_WITH_KNOTS ( 'NONE', 3,
 ( #9071, #24820, #20945, #36699 ),
 .UNSPECIFIED., .F., .F.,
 ( 4, 4 ),
 ( 2.052460249050213172E-07, 0.01602278383226833289 ),
 .UNSPECIFIED. ) ;
#9356=AXIS2_PLACEMENT_3D ( 'NONE', #11379, #38997, #31003 ) ;
#9358=CARTESIAN_POINT ( 'NONE',  ( -0.1450934409768900590, 0.000000000000000000, 2.161127057262024032 ) ) ;
#9361=EDGE_LOOP ( 'NONE', ( #19339, #13414, #24756, #26000 ) ) ;
#9372=EDGE_CURVE ( 'NONE', #38240, #43935, #45661, .T. ) ;
#9373=LINE ( 'NONE', #5753, #7761 ) ;
#9374=ORIENTED_EDGE ( 'NONE', *, *, #2503, .F. ) ;
#9375=LINE ( 'NONE', #9633, #48008 ) ;
#9387=VERTEX_POINT ( 'NONE', #16909 ) ;
#9389=CARTESIAN_POINT ( 'NONE',  ( 1.236813753895251722, 1.205361022782829114E-17, -2.681693691597563767 ) ) ;
#9393=B_SPLINE_CURVE_WITH_KNOTS ( 'NONE', 3,
 ( #43633, #27890, #4404, #8021 ),
 .UNSPECIFIED., .F., .F.,
 ( 4, 4 ),
 ( 0.1211873102087489551, 0.1625992483279400380 ),
 .UNSPECIFIED. ) ;
#9396=CARTESIAN_POINT ( 'NONE',  ( 1.365808055127285092, 0.01624875952099000959, 1.488494957536232510 ) ) ;
#9401=AXIS2_PLACEMENT_3D ( 'NONE', #10341, #50283, #37972 ) ;
#9402=LINE ( 'NONE', #48598, #2068 ) ;
#9404=CARTESIAN_POINT ( 'NONE',  ( -0.8851347855165027090, 0.009234599073057599486, 1.577415923295598876 ) ) ;
#9412=VECTOR ( 'NONE', #44423, 39.37007874015748143 ) ;
#9421=DIRECTION ( 'NONE',  ( -0.000000000000000000, 1.000000000000000000, -0.000000000000000000 ) ) ;
#9422=LINE ( 'NONE', #6813, #32401 ) ;
#9428=DIRECTION ( 'NONE',  ( 0.000000000000000000, 0.000000000000000000, 1.000000000000000000 ) ) ;
#9432=FACE_OUTER_BOUND ( 'NONE', #36316, .T. ) ;
#9433=EDGE_CURVE ( 'NONE', #43799, #30581, #48089, .T. ) ;
#9434=ORIENTED_EDGE ( 'NONE', *, *, #42071, .F. ) ;
#9447=DIRECTION ( 'NONE',  ( 5.779879058772725700E-18, 1.000000000000000000, -1.286990067732317241E-16 ) ) ;
#9449=CARTESIAN_POINT ( 'NONE',  ( -2.122900408447768505, 1.587732724264993900, -2.052396256617323278 ) ) ;
#9451=EDGE_LOOP ( 'NONE', ( #42379, #21475, #14888, #33997 ) ) ;
#9455=CARTESIAN_POINT ( 'NONE',  ( 2.136142994004097684, 1.647101463257393705, -1.351088264443995213 ) ) ;
#9463=ORIENTED_EDGE ( 'NONE', *, *, #5458, .T. ) ;
#9465=FACE_OUTER_BOUND ( 'NONE', #42317, .T. ) ;
#9469=EDGE_CURVE ( 'NONE', #39301, #44322, #44260, .T. ) ;
#9471=VERTEX_POINT ( 'NONE', #17162 ) ;
#9475=ORIENTED_EDGE ( 'NONE', *, *, #6459, .F. ) ;
#9476=AXIS2_PLACEMENT_3D ( 'NONE', #1823, #6214, #10595 ) ;
#9478=ORIENTED_EDGE ( 'NONE', *, *, #22072, .T. ) ;
#9479=EDGE_CURVE ( 'NONE', #14608, #36153, #27205, .T. ) ;
#9482=VERTEX_POINT ( 'NONE', #47586 ) ;
#9488=VERTEX_POINT ( 'NONE', #12264 ) ;
#9491=EDGE_CURVE ( 'NONE', #6407, #24742, #10430, .T. ) ;
#9494=DIRECTION ( 'NONE',  ( -0.01601477604151182663, 0.9998717552508123996, -0.000000000000000000 ) ) ;
#9497=CARTESIAN_POINT ( 'NONE',  ( -2.867773316779185677, 1.674559808355669199, -0.7050287376752426560 ) ) ;
#9505=ORIENTED_EDGE ( 'NONE', *, *, #33760, .F. ) ;
#9507=LINE ( 'NONE', #6140, #42337 ) ;
#9509=CARTESIAN_POINT ( 'NONE',  ( 2.919426793319799707, 5.118110236220475784, 0.4451252810446826302 ) ) ;
#9511=LINE ( 'NONE', #25505, #42109 ) ;
#9512=B_SPLINE_CURVE_WITH_KNOTS ( 'NONE', 3,
 ( #9753, #29628, #41497, #2518 ),
 .UNSPECIFIED., .F., .F.,
 ( 4, 4 ),
 ( 0.001413063469367606406, 0.003913248153456502960 ),
 .UNSPECIFIED. ) ;
#9513=DIRECTION ( 'NONE',  ( -0.01601477604151182663, 0.9998717552508123996, -0.000000000000000000 ) ) ;
#9519=CARTESIAN_POINT ( 'NONE',  ( -2.308557526972532692, 5.905511811023623991, 1.841013194464760305 ) ) ;
#9533=ORIENTED_EDGE ( 'NONE', *, *, #19592, .F. ) ;
#9539=DIRECTION ( 'NONE',  ( -0.000000000000000000, 1.000000000000000000, -0.000000000000000000 ) ) ;
#9540=AXIS2_PLACEMENT_3D ( 'NONE', #36624, #25504, #36370 ) ;
#9550=EDGE_CURVE ( 'NONE', #21218, #42295, #6921, .T. ) ;
#9553=B_SPLINE_CURVE_WITH_KNOTS ( 'NONE', 3,
 ( #47369, #15913, #4558, #20030 ),
 .UNSPECIFIED., .F., .F.,
 ( 4, 4 ),
 ( 0.001036764039224162678, 0.004836410851953563440 ),
 .UNSPECIFIED. ) ;
#9554=ORIENTED_EDGE ( 'NONE', *, *, #41962, .F. ) ;
#9555=CARTESIAN_POINT ( 'NONE',  ( -1.387661672111457412, 1.205361022782829114E-17, -1.663104731517942136 ) ) ;
#9561=ORIENTED_EDGE ( 'NONE', *, *, #4337, .F. ) ;
#9567=VERTEX_POINT ( 'NONE', #49119 ) ;
#9568=CARTESIAN_POINT ( 'NONE',  ( 0.000000000000000000, 0.000000000000000000, 0.000000000000000000 ) ) ;
#9574=AXIS2_PLACEMENT_3D ( 'NONE', #550, #43133, #16297 ) ;
#9577=VECTOR ( 'NONE', #38033, 39.37007874015748143 ) ;
#9583=LINE ( 'NONE', #13718, #33999 ) ;
#9584=LINE ( 'NONE', #21975, #5594 ) ;
#9589=ORIENTED_EDGE ( 'NONE', *, *, #36399, .F. ) ;
#9590=CARTESIAN_POINT ( 'NONE',  ( 2.164658444855302122, 5.905511811023623991, -0.04795272066889885720 ) ) ;
#9595=EDGE_CURVE ( 'NONE', #39853, #24587, #41416, .T. ) ;
#9600=B_SPLINE_CURVE_WITH_KNOTS ( 'NONE', 3,
 ( #18303, #13928, #37429, #48989 ),
 .UNSPECIFIED., .F., .F.,
 ( 4, 4 ),
 ( 2.136435014586510233E-07, 0.002500479660419988558 ),
 .UNSPECIFIED. ) ;
#9601=CARTESIAN_POINT ( 'NONE',  ( 0.9766252528120925591, 0.01428436922565947537, 1.730545172518233699 ) ) ;
#9607=B_SPLINE_CURVE_WITH_KNOTS ( 'NONE', 3,
 ( #2071, #2574, #14192, #5938 ),
 .UNSPECIFIED., .F., .F.,
 ( 4, 4 ),
 ( 0.1211775127643062444, 0.1625894504277921315 ),
 .UNSPECIFIED. ) ;
#9609=CARTESIAN_POINT ( 'NONE',  ( -0.8004649005966125719, 0.000000000000000000, -1.548759025234861753 ) ) ;
#9612=CARTESIAN_POINT ( 'NONE',  ( 1.723687301221656476, 1.205361022782829114E-17, -1.311649477509800876 ) ) ;
#9616=DIRECTION ( 'NONE',  ( -9.390536051998764103E-17, -1.000000000000000000, -6.822623802544789917E-17 ) ) ;
#9618=CIRCLE ( 'NONE', #24471, 2.165354330708661568 ) ;
#9620=EDGE_CURVE ( 'NONE', #12025, #44687, #1662, .T. ) ;
#9626=CARTESIAN_POINT ( 'NONE',  ( 1.693438507483599809, 1.640086946997390216, 1.863498184031233684 ) ) ;
#9631=LINE ( 'NONE', #36237, #28362 ) ;
#9633=CARTESIAN_POINT ( 'NONE',  ( -0.7145799201509080989, 6.692913385826772199, 2.044048657746648789 ) ) ;
#9640=CARTESIAN_POINT ( 'NONE',  ( -2.074656761898998170, 6.692913385826772199, -0.6223516566630905578 ) ) ;
#9643=CARTESIAN_POINT ( 'NONE',  ( 0.2810212965233879201, 1.723635030826397685, -2.939398504915932797 ) ) ;
#9647=DIRECTION ( 'NONE',  ( 0.9909497617679331460, 0.000000000000000000, 0.1342332658176667026 ) ) ;
#9648=DIRECTION ( 'NONE',  ( -0.6579387259397027066, 0.000000000000000000, -0.7530714660036196273 ) ) ;
#9649=ORIENTED_EDGE ( 'NONE', *, *, #30566, .F. ) ;
#9650=VECTOR ( 'NONE', #48900, 39.37007874015748143 ) ;
#9651=CARTESIAN_POINT ( 'NONE',  ( 0.7376647802434432855, 1.010125197387645057, -2.487884157410633179 ) ) ;
#9652=CARTESIAN_POINT ( 'NONE',  ( 1.951523201471517588, 0.05917688107560774985, -0.1369052102211298083 ) ) ;
#9655=DIRECTION ( 'NONE',  ( -0.1785568947986370392, 0.000000000000000000, 0.9839295885986295565 ) ) ;
#9656=ORIENTED_EDGE ( 'NONE', *, *, #38114, .F. ) ;
#9665=CARTESIAN_POINT ( 'NONE',  ( 0.7148041136150545816, 0.000000000000000000, -2.044646019095610168 ) ) ;
#9667=ORIENTED_EDGE ( 'NONE', *, *, #9550, .F. ) ;
#9676=CARTESIAN_POINT ( 'NONE',  ( -1.743145509346910149, 0.000000000000000000, -0.04249111949972883551 ) ) ;
#9680=CARTESIAN_POINT ( 'NONE',  ( -2.139026224642868623, 1.640833132300933972, 0.3394128413014118606 ) ) ;
#9682=ORIENTED_EDGE ( 'NONE', *, *, #11264, .T. ) ;
#9686=CARTESIAN_POINT ( 'NONE',  ( -1.263630850544466666, 0.000000000000000000, -1.276241334172347530 ) ) ;
#9693=DIRECTION ( 'NONE',  ( -0.4738686624730094055, 0.000000000000000000, 0.8805955318567321166 ) ) ;
#9699=FACE_OUTER_BOUND ( 'NONE', #30684, .T. ) ;
#9700=EDGE_CURVE ( 'NONE', #5044, #22970, #5268, .T. ) ;
#9701=( BOUNDED_CURVE ( )  B_SPLINE_CURVE ( 3, ( #22245, #33875, #26112, #34873 ),
 .UNSPECIFIED., .F., .F. ) 
 B_SPLINE_CURVE_WITH_KNOTS ( ( 4, 4 ),
 ( 2.506443096395472470, 2.557263767594603721 ),
 .UNSPECIFIED. ) 
 CURVE ( )  GEOMETRIC_REPRESENTATION_ITEM ( )  RATIONAL_B_SPLINE_CURVE ( ( 1.000000000000000000, 0.9997847831954709275, 0.9997847831954709275, 1.000000000000000000 ) ) 
 REPRESENTATION_ITEM ( '' )  );
#9702=EDGE_CURVE ( 'NONE', #31964, #7588, #40112, .T. ) ;
#9703=LINE ( 'NONE', #29577, #17355 ) ;
#9707=DIRECTION ( 'NONE',  ( -0.01601477604151182663, 0.9998717552508123996, -0.000000000000000000 ) ) ;
#9712=DIRECTION ( 'NONE',  ( -0.000000000000000000, 1.000000000000000000, -0.000000000000000000 ) ) ;
#9716=CARTESIAN_POINT ( 'NONE',  ( -2.576863348864732117, 1.568913320674888201, 1.442554885838411849 ) ) ;
#9717=B_SPLINE_CURVE_WITH_KNOTS ( 'NONE', 3,
 ( #989, #12874, #24994, #20353 ),
 .UNSPECIFIED., .F., .F.,
 ( 4, 4 ),
 ( 0.1211873102087489551, 0.1625992483279400380 ),
 .UNSPECIFIED. ) ;
#9723=CYLINDRICAL_SURFACE ( 'NONE', #34973, 2.165354330708661568 ) ;
#9724=EDGE_CURVE ( 'NONE', #26498, #17294, #39556, .T. ) ;
#9727=VECTOR ( 'NONE', #21400, 39.37007874015748143 ) ;
#9729=EDGE_CURVE ( 'NONE', #42663, #41559, #37111, .T. ) ;
#9732=CARTESIAN_POINT ( 'NONE',  ( -1.088097428176262760, 1.690474079180120492, 1.917118167796188821 ) ) ;
#9733=ADVANCED_FACE ( 'NONE', ( #4241 ), #20969, .T. ) ;
#9734=VERTEX_POINT ( 'NONE', #20503 ) ;
#9735=VECTOR ( 'NONE', #31002, 39.37007874015748143 ) ;
#9741=VECTOR ( 'NONE', #28079, 39.37007874015748143 ) ;
#9742=CARTESIAN_POINT ( 'NONE',  ( -1.481515513156636876, 0.000000000000000000, -0.9189724476880739568 ) ) ;
#9744=DIRECTION ( 'NONE',  ( -0.6089060283534990514, 0.7932423643721808748, 0.000000000000000000 ) ) ;
#9745=ORIENTED_EDGE ( 'NONE', *, *, #37514, .T. ) ;
#9746=VERTEX_POINT ( 'NONE', #28493 ) ;
#9747=VECTOR ( 'NONE', #11975, 39.37007874015748143 ) ;
#9749=ORIENTED_EDGE ( 'NONE', *, *, #8010, .T. ) ;
#9751=VERTEX_POINT ( 'NONE', #44242 ) ;
#9753=CARTESIAN_POINT ( 'NONE',  ( 1.306991306359274629, 1.630410611703223545, -1.882644677548868550 ) ) ;
#9757=EDGE_LOOP ( 'NONE', ( #28431, #34052, #29580, #15465 ) ) ;
#9759=CARTESIAN_POINT ( 'NONE',  ( -2.600183657057300035, 5.905511811023623991, 1.399218491554124144 ) ) ;
#9762=CARTESIAN_POINT ( 'NONE',  ( 1.128560816269277955, 1.725977917706353670, 1.984842472008916170 ) ) ;
#9766=CARTESIAN_POINT ( 'NONE',  ( 1.838947341486932396, 0.05737377265108637575, 0.6492553997849701553 ) ) ;
#9767=CIRCLE ( 'NONE', #50935, 2.246510896728926010 ) ;
#9770=CARTESIAN_POINT ( 'NONE',  ( 0.000000000000000000, 0.07874015748031502893, 0.000000000000000000 ) ) ;
#9772=CARTESIAN_POINT ( 'NONE',  ( -2.867773316779185677, 0.000000000000000000, -0.7050287376752425450 ) ) ;
#9779=VERTEX_POINT ( 'NONE', #33667 ) ;
#9780=CARTESIAN_POINT ( 'NONE',  ( -2.164823134740036181, 1.673228346456695492, 0.000000000000000000 ) ) ;
#9783=EDGE_CURVE ( 'NONE', #6941, #22597, #44396, .T. ) ;
#9787=EDGE_CURVE ( 'NONE', #37703, #15500, #6123, .T. ) ;
#9790=CARTESIAN_POINT ( 'NONE',  ( -2.576863348864732117, 1.580667355030889620, 1.442554885838411849 ) ) ;
#9791=EDGE_CURVE ( 'NONE', #21262, #34643, #40636, .T. ) ;
#9794=CARTESIAN_POINT ( 'NONE',  ( -1.556712866041156662, 1.548291375251236834, 2.509548638715847435 ) ) ;
#9795=ORIENTED_EDGE ( 'NONE', *, *, #25084, .F. ) ;
#9796=DIRECTION ( 'NONE',  ( 0.000000000000000000, 1.160734090543304660E-16, -1.000000000000000000 ) ) ;
#9798=DIRECTION ( 'NONE',  ( -0.08963930890344089242, -1.156025585781303350E-16, 0.9959742939952384022 ) ) ;
#9806=CIRCLE ( 'NONE', #22988, 2.165354330708661568 ) ;
#9808=CARTESIAN_POINT ( 'NONE',  ( -2.592413363271652393, 1.568516221823312629, 1.413658116983555812 ) ) ;
#9810=VERTEX_POINT ( 'NONE', #24636 ) ;
#9812=PLANE ( 'NONE',  #1868 ) ;
#9820=DIRECTION ( 'NONE',  ( -3.986037398843765983E-20, -1.000000000000000000, -1.160734090543304660E-16 ) ) ;
#9822=VERTEX_POINT ( 'NONE', #49355 ) ;
#9824=EDGE_CURVE ( 'NONE', #31188, #34410, #37537, .T. ) ;
#9831=DIRECTION ( 'NONE',  ( 7.237058681235204266E-17, -1.000000000000000000, 9.074984547606538936E-17 ) ) ;
#9835=ORIENTED_EDGE ( 'NONE', *, *, #23285, .F. ) ;
#9856=ORIENTED_EDGE ( 'NONE', *, *, #31750, .F. ) ;
#9865=CONICAL_SURFACE ( 'NONE', #32992, 2.165354330708661568, 0.2617993877991570129 ) ;
#9867=VERTEX_POINT ( 'NONE', #1128 ) ;
#9868=B_SPLINE_CURVE_WITH_KNOTS ( 'NONE', 3,
 ( #39641, #7891, #31388, #43239 ),
 .UNSPECIFIED., .F., .F.,
 ( 4, 4 ),
 ( 2.176057671437937673E-07, 0.01613016441388016517 ),
 .UNSPECIFIED. ) ;
#9869=CARTESIAN_POINT ( 'NONE',  ( 0.4521076751547876138, 1.616718085813380945, 2.215705648545971407 ) ) ;
#9872=ORIENTED_EDGE ( 'NONE', *, *, #42440, .F. ) ;
#9879=EDGE_LOOP ( 'NONE', ( #36880, #5554, #18760, #38670 ) ) ;
#9881=EDGE_CURVE ( 'NONE', #50385, #41856, #46200, .T. ) ;
#9882=CARTESIAN_POINT ( 'NONE',  ( 2.121469926805689354, 5.118110236220475784, -0.4337334748181388422 ) ) ;
#9884=B_SPLINE_CURVE_WITH_KNOTS ( 'NONE', 3,
 ( #45580, #49189, #10244, #29616 ),
 .UNSPECIFIED., .F., .F.,
 ( 4, 4 ),
 ( 2.272220335726248535E-07, 0.01624913354395895668 ),
 .UNSPECIFIED. ) ;
#9885=ORIENTED_EDGE ( 'NONE', *, *, #730, .F. ) ;
#9886=DIRECTION ( 'NONE',  ( -0.01601477604151182663, 0.9998717552508123996, -0.000000000000000000 ) ) ;
#9887=PLANE ( 'NONE',  #7795 ) ;
#9888=ADVANCED_FACE ( 'NONE', ( #36767 ), #48130, .T. ) ;
#9889=EDGE_CURVE ( 'NONE', #11672, #12924, #20349, .T. ) ;
#9894=ORIENTED_EDGE ( 'NONE', *, *, #26757, .T. ) ;
#9896=CARTESIAN_POINT ( 'NONE',  ( 0.002207914879453961535, -5.712274067634378313E-18, 0.04916304461325374242 ) ) ;
#9900=CARTESIAN_POINT ( 'NONE',  ( 1.748846139897575647, 1.475252794177884352, -2.379195924602942380 ) ) ;
#9907=ADVANCED_FACE ( 'NONE', ( #10914 ), #6547, .F. ) ;
#9909=CARTESIAN_POINT ( 'NONE',  ( 1.398572223930554026, 1.205361022782829114E-17, 1.525996566212370231 ) ) ;
#9911=ORIENTED_EDGE ( 'NONE', *, *, #27262, .T. ) ;
#9915=DIRECTION ( 'NONE',  ( -0.000000000000000000, -1.000000000000000000, -0.000000000000000000 ) ) ;
#9916=CARTESIAN_POINT ( 'NONE',  ( -1.171281348708517633, 1.623524940395525640, 1.864444939713191474 ) ) ;
#9920=VERTEX_POINT ( 'NONE', #46253 ) ;
#9929=EDGE_CURVE ( 'NONE', #12101, #20050, #4352, .T. ) ;
#9936=CARTESIAN_POINT ( 'NONE',  ( 1.598711713508005117, 6.692913385826772199, -1.460438370699377764 ) ) ;
#9938=ORIENTED_EDGE ( 'NONE', *, *, #12396, .F. ) ;
#9941=ORIENTED_EDGE ( 'NONE', *, *, #30725, .T. ) ;
#9942=ORIENTED_EDGE ( 'NONE', *, *, #50847, .F. ) ;
#9945=ORIENTED_EDGE ( 'NONE', *, *, #29104, .F. ) ;
#9951=EDGE_CURVE ( 'NONE', #50754, #380, #27103, .T. ) ;
#9954=PLANE ( 'NONE',  #19801 ) ;
#9959=PLANE ( 'NONE',  #38206 ) ;
#9962=ORIENTED_EDGE ( 'NONE', *, *, #31139, .T. ) ;
#9964=DIRECTION ( 'NONE',  ( -0.000000000000000000, 1.000000000000000000, -0.000000000000000000 ) ) ;
#9973=CARTESIAN_POINT ( 'NONE',  ( 0.07982360342473591996, 1.709180471932028711, 0.000000000000000000 ) ) ;
#9981=CARTESIAN_POINT ( 'NONE',  ( 2.164658444855302122, 5.905511811023623991, -0.04795272066889885720 ) ) ;
#9984=AXIS2_PLACEMENT_3D ( 'NONE', #49215, #25760, #29642 ) ;
#9986=CIRCLE ( 'NONE', #40499, 2.246510896728926010 ) ;
#9988=ORIENTED_EDGE ( 'NONE', *, *, #42428, .T. ) ;
#9993=EDGE_CURVE ( 'NONE', #4443, #26808, #22791, .T. ) ;
#9997=EDGE_LOOP ( 'NONE', ( #43906, #30824, #5090, #29205 ) ) ;
#9999=VECTOR ( 'NONE', #11031, 39.37007874015748854 ) ;
#10000=( BOUNDED_CURVE ( )  B_SPLINE_CURVE ( 3, ( #34778, #46617, #42259, #34281 ),
 .UNSPECIFIED., .F., .F. ) 
 B_SPLINE_CURVE_WITH_KNOTS ( ( 4, 4 ),
 ( 0.7124684239378302752, 0.7632890951369610821 ),
 .UNSPECIFIED. ) 
 CURVE ( )  GEOMETRIC_REPRESENTATION_ITEM ( )  RATIONAL_B_SPLINE_CURVE ( ( 1.000000000000000000, 0.9997847831954709275, 0.9997847831954709275, 1.000000000000000000 ) ) 
 REPRESENTATION_ITEM ( '' )  );
#10003=CARTESIAN_POINT ( 'NONE',  ( -0.2493563821447185302, 1.638291256590492129, -2.221569428308970195 ) ) ;
#10004=ORIENTED_EDGE ( 'NONE', *, *, #11552, .F. ) ;
#10006=DIRECTION ( 'NONE',  ( -0.9998717552508121775, -0.01601477604151182663, 0.000000000000000000 ) ) ;
#10008=CARTESIAN_POINT ( 'NONE',  ( 2.277873973731426638, 1.463603380278871713, 1.879489153247667632 ) ) ;
#10009=ADVANCED_FACE ( 'NONE', ( #3419 ), #27585, .T. ) ;
#10012=LINE ( 'NONE', #2521, #49202 ) ;
#10013=EDGE_CURVE ( 'NONE', #9169, #47474, #1523, .T. ) ;
#10014=VERTEX_POINT ( 'NONE', #43595 ) ;
#10018=PLANE ( 'NONE',  #41313 ) ;
#10020=CIRCLE ( 'NONE', #11661, 2.165354330708661568 ) ;
#10022=DIRECTION ( 'NONE',  ( 0.000000000000000000, 1.000000000000000000, 0.000000000000000000 ) ) ;
#10031=CARTESIAN_POINT ( 'NONE',  ( 0.2239970000120027616, 0.000000000000000000, -1.939803615689571048 ) ) ;
#10037=EDGE_LOOP ( 'NONE', ( #33180, #26613, #39451, #7785 ) ) ;
#10038=DIRECTION ( 'NONE',  ( 0.9998717552508121775, 0.01601477604151182663, 0.000000000000000000 ) ) ;
#10039=ORIENTED_EDGE ( 'NONE', *, *, #16570, .T. ) ;
#10048=LINE ( 'NONE', #45135, #26561 ) ;
#10051=CARTESIAN_POINT ( 'NONE',  ( -1.743516651958532115, 0.0004834999639498255872, 0.04168935124556687882 ) ) ;
#10056=ORIENTED_EDGE ( 'NONE', *, *, #7393, .F. ) ;
#10057=AXIS2_PLACEMENT_3D ( 'NONE', #618, #20493, #47304 ) ;
#10058=VECTOR ( 'NONE', #17109, 39.37007874015748143 ) ;
#10059=CARTESIAN_POINT ( 'NONE',  ( -2.437180031585919782, 1.566133505135788750, -1.667735833703134274 ) ) ;
#10069=EDGE_CURVE ( 'NONE', #24123, #50554, #28626, .T. ) ;
#10076=FACE_OUTER_BOUND ( 'NONE', #43788, .T. ) ;
#10083=LINE ( 'NONE', #34344, #41499 ) ;
#10086=DIRECTION ( 'NONE',  ( -3.986037398843765983E-20, -1.000000000000000000, -1.160734090543304660E-16 ) ) ;
#10089=CARTESIAN_POINT ( 'NONE',  ( 0.002207914879453961969, 6.692913385826772199, 0.04916304461325451958 ) ) ;
#10091=ORIENTED_EDGE ( 'NONE', *, *, #14181, .F. ) ;
#10092=ORIENTED_EDGE ( 'NONE', *, *, #6185, .T. ) ;
#10093=CONICAL_SURFACE ( 'NONE', #34815, 2.165354330708661568, 0.2617993877991570129 ) ;
#10097=ORIENTED_EDGE ( 'NONE', *, *, #30886, .F. ) ;
#10098=CARTESIAN_POINT ( 'NONE',  ( 1.669153017917641924, 1.205361022782829114E-17, 1.268159837793114031 ) ) ;
#10100=ORIENTED_EDGE ( 'NONE', *, *, #8314, .F. ) ;
#10101=AXIS2_PLACEMENT_3D ( 'NONE', #27987, #23867, #39617 ) ;
#10117=FACE_OUTER_BOUND ( 'NONE', #34341, .T. ) ;
#10122=PLANE ( 'NONE',  #41465 ) ;
#10123=ORIENTED_EDGE ( 'NONE', *, *, #51035, .F. ) ;
#10124=ORIENTED_EDGE ( 'NONE', *, *, #19843, .T. ) ;
#10128=DIRECTION ( 'NONE',  ( -0.000000000000000000, 1.000000000000000000, -0.000000000000000000 ) ) ;
#10129=ORIENTED_EDGE ( 'NONE', *, *, #47918, .F. ) ;
#10130=ORIENTED_EDGE ( 'NONE', *, *, #32925, .T. ) ;
#10132=ADVANCED_FACE ( 'NONE', ( #20105 ), #5137, .T. ) ;
#10135=ORIENTED_EDGE ( 'NONE', *, *, #35992, .T. ) ;
#10136=DIRECTION ( 'NONE',  ( 9.769962616701375978E-15, 0.000000000000000000, 1.000000000000000000 ) ) ;
#10139=AXIS2_PLACEMENT_3D ( 'NONE', #16551, #10834, #26331 ) ;
#10140=CYLINDRICAL_SURFACE ( 'NONE', #10177, 2.164630168518208109 ) ;
#10143=AXIS2_PLACEMENT_3D ( 'NONE', #9192, #19774, #35794 ) ;
#10144=ORIENTED_EDGE ( 'NONE', *, *, #41203, .T. ) ;
#10154=ORIENTED_EDGE ( 'NONE', *, *, #25636, .F. ) ;
#10162=CARTESIAN_POINT ( 'NONE',  ( 1.294674717756378213, 1.049866565877817681, 1.556672598441452227 ) ) ;
#10163=CONICAL_SURFACE ( 'NONE', #41493, 3.483074324928249421, 1.244861948955335196 ) ;
#10166=ORIENTED_EDGE ( 'NONE', *, *, #38524, .F. ) ;
#10167=DIRECTION ( 'NONE',  ( -0.8345732537213079727, 0.000000000000000000, 0.5508969814520945363 ) ) ;
#10168=DIRECTION ( 'NONE',  ( -0.01601477604151182663, 0.9998717552508123996, -0.000000000000000000 ) ) ;
#10170=VERTEX_POINT ( 'NONE', #497 ) ;
#10173=CARTESIAN_POINT ( 'NONE',  ( -1.557927422371237158, 0.000000000000000000, 0.7824709080581183640 ) ) ;
#10174=FACE_OUTER_BOUND ( 'NONE', #8613, .T. ) ;
#10176=AXIS2_PLACEMENT_3D ( 'NONE', #30258, #10639, #10384 ) ;
#10177=AXIS2_PLACEMENT_3D ( 'NONE', #2646, #7284, #42134 ) ;
#10178=VERTEX_POINT ( 'NONE', #37157 ) ;
#10184=EDGE_LOOP ( 'NONE', ( #48542, #42289, #17095, #31179 ) ) ;
#10188=EDGE_LOOP ( 'NONE', ( #5015, #4255, #4809, #22685 ) ) ;
#10191=EDGE_LOOP ( 'NONE', ( #9143, #30870, #26928, #16374, #39999, #14481, #27489, #29481, #44114, #33503, #94, #28203, #24306 ) ) ;
#10192=FACE_OUTER_BOUND ( 'NONE', #6192, .T. ) ;
#10194=DIRECTION ( 'NONE',  ( 0.8345732537212999791, 0.000000000000000000, 0.5508969814521065267 ) ) ;
#10196=ORIENTED_EDGE ( 'NONE', *, *, #20916, .F. ) ;
#10201=EDGE_CURVE ( 'NONE', #47505, #2009, #9296, .T. ) ;
#10205=CARTESIAN_POINT ( 'NONE',  ( 0.000000000000000000, 0.07874015748031495954, 0.000000000000000000 ) ) ;
#10206=AXIS2_PLACEMENT_3D ( 'NONE', #30447, #29933, #26056 ) ;
#10210=DIRECTION ( 'NONE',  ( 0.000000000000000000, -0.000000000000000000, 1.000000000000000000 ) ) ;
#10211=AXIS2_PLACEMENT_3D ( 'NONE', #27027, #19282, #23932 ) ;
#10214=AXIS2_PLACEMENT_3D ( 'NONE', #20605, #19824, #35591 ) ;
#10216=EDGE_LOOP ( 'NONE', ( #3297, #19434, #5687, #14168, #15419, #14399, #6493, #19048, #13097, #30800, #36500 ) ) ;
#10224=VERTEX_POINT ( 'NONE', #37668 ) ;
#10226=ORIENTED_EDGE ( 'NONE', *, *, #43148, .T. ) ;
#10227=LINE ( 'NONE', #49669, #47609 ) ;
#10228=DIRECTION ( 'NONE',  ( 0.01601477604151182663, -0.9998717552508123996, 0.000000000000000000 ) ) ;
#10231=B_SPLINE_CURVE_WITH_KNOTS ( 'NONE', 3,
 ( #39608, #8623, #48333, #32129 ),
 .UNSPECIFIED., .F., .F.,
 ( 4, 4 ),
 ( 2.019292001486067082E-07, 0.01600527235543932475 ),
 .UNSPECIFIED. ) ;
#10232=ORIENTED_EDGE ( 'NONE', *, *, #16413, .T. ) ;
#10235=B_SPLINE_CURVE_WITH_KNOTS ( 'NONE', 3,
 ( #19554, #46207, #10864, #30242 ),
 .UNSPECIFIED., .F., .F.,
 ( 4, 4 ),
 ( 0.0002843467791849443676, 0.0004991820216076624152 ),
 .UNSPECIFIED. ) ;
#10236=CARTESIAN_POINT ( 'NONE',  ( -2.519917724921192370, 1.050329523583607205, 0.3910081006951147686 ) ) ;
#10241=ORIENTED_EDGE ( 'NONE', *, *, #25741, .F. ) ;
#10243=EDGE_CURVE ( 'NONE', #19430, #49786, #45122, .T. ) ;
#10244=CARTESIAN_POINT ( 'NONE',  ( 2.201476786394565011, 1.746575479641379491, 1.240550762682156805 ) ) ;
#10258=CARTESIAN_POINT ( 'NONE',  ( -1.872964171688006996, 0.5249316497054298258, 0.2040481837739120674 ) ) ;
#10271=CARTESIAN_POINT ( 'NONE',  ( 2.171725698152134676, 1.651127248238214218, 1.668948176259438254 ) ) ;
#10277=ADVANCED_FACE ( 'NONE', ( #49229 ), #45878, .T. ) ;
#10285=PLANE ( 'NONE',  #32845 ) ;
#10287=CARTESIAN_POINT ( 'NONE',  ( 1.688048600224988149, 0.000000000000000000, -0.4357642695449466252 ) ) ;
#10290=CONICAL_SURFACE ( 'NONE', #42455, 2.244934639244524632, 1.554780866114618743 ) ;
#10291=ORIENTED_EDGE ( 'NONE', *, *, #41028, .T. ) ;
#10298=EDGE_CURVE ( 'NONE', #15130, #35692, #32728, .T. ) ;
#10300=( BOUNDED_CURVE ( )  B_SPLINE_CURVE ( 3, ( #37152, #13147, #9013, #40511 ),
 .UNSPECIFIED., .F., .F. ) 
 B_SPLINE_CURVE_WITH_KNOTS ( ( 4, 4 ),
 ( 3.318026082093744389, 3.368777294715108894 ),
 .UNSPECIFIED. ) 
 CURVE ( )  GEOMETRIC_REPRESENTATION_ITEM ( )  RATIONAL_B_SPLINE_CURVE ( ( 1.000000000000000000, 0.9997853710521733550, 0.9997853710521733550, 1.000000000000000000 ) ) 
 REPRESENTATION_ITEM ( '' )  );
#10301=LINE ( 'NONE', #50001, #39751 ) ;
#10302=EDGE_CURVE ( 'NONE', #26738, #11672, #10541, .T. ) ;
#10303=EDGE_CURVE ( 'NONE', #35318, #42095, #41781, .T. ) ;
#10305=EDGE_LOOP ( 'NONE', ( #40695, #17540, #12078, #28830 ) ) ;
#10307=DIRECTION ( 'NONE',  ( -0.1342332658176667026, 0.000000000000000000, 0.9909497617679331460 ) ) ;
#10309=ORIENTED_EDGE ( 'NONE', *, *, #42340, .T. ) ;
#10313=VERTEX_POINT ( 'NONE', #34045 ) ;
#10317=CARTESIAN_POINT ( 'NONE',  ( -1.597940118745532434, 0.5246043514710795330, -1.459700650569985214 ) ) ;
#10334=B_SPLINE_CURVE_WITH_KNOTS ( 'NONE', 3,
 ( #12859, #39453, #28594, #35583 ),
 .UNSPECIFIED., .F., .F.,
 ( 4, 4 ),
 ( 2.103352892585149584E-07, 0.002500280059082746632 ),
 .UNSPECIFIED. ) ;
#10335=DIRECTION ( 'NONE',  ( -0.7227948638273978821, 0.000000000000000000, 0.6910626489868580968 ) ) ;
#10337=CARTESIAN_POINT ( 'NONE',  ( -1.471105834599418127, 0.000000000000000000, -0.9906718873397587499 ) ) ;
#10340=ADVANCED_FACE ( 'NONE', ( #18545 ), #46134, .T. ) ;
#10341=CARTESIAN_POINT ( 'NONE',  ( 0.07982360342473591996, 1.709180471932028711, 0.000000000000000000 ) ) ;
#10344=DIRECTION ( 'NONE',  ( -0.9998717552508122886, -0.01601477604151182316, 0.000000000000000000 ) ) ;
#10345=ORIENTED_EDGE ( 'NONE', *, *, #32395, .T. ) ;
#10346=ORIENTED_EDGE ( 'NONE', *, *, #7781, .T. ) ;
#10351=AXIS2_PLACEMENT_3D ( 'NONE', #27533, #28048, #43532 ) ;
#10355=AXIS2_PLACEMENT_3D ( 'NONE', #30487, #6736, #18865 ) ;
#10357=PLANE ( 'NONE',  #4572 ) ;
#10360=ADVANCED_FACE ( 'NONE', ( #23412 ), #22918, .T. ) ;
#10361=EDGE_CURVE ( 'NONE', #16311, #4534, #34548, .T. ) ;
#10362=ORIENTED_EDGE ( 'NONE', *, *, #29537, .F. ) ;
#10363=ORIENTED_EDGE ( 'NONE', *, *, #24096, .F. ) ;
#10368=ORIENTED_EDGE ( 'NONE', *, *, #1995, .F. ) ;
#10370=DIRECTION ( 'NONE',  ( 0.1785568947986229116, -1.142151789626729957E-16, 0.9839295885986321100 ) ) ;
#10372=CARTESIAN_POINT ( 'NONE',  ( 2.600183657057280051, 0.000000000000000000, 1.399218491554161892 ) ) ;
#10374=CARTESIAN_POINT ( 'NONE',  ( 0.000000000000000000, 1.574803149606302854, 0.000000000000000000 ) ) ;
#10377=VERTEX_POINT ( 'NONE', #30925 ) ;
#10384=DIRECTION ( 'NONE',  ( 0.000000000000000000, 0.000000000000000000, 1.000000000000000000 ) ) ;
#10386=B_SPLINE_CURVE_WITH_KNOTS ( 'NONE', 3,
 ( #47766, #19666, #7804, #43154 ),
 .UNSPECIFIED., .F., .F.,
 ( 4, 4 ),
 ( 0.01189589409751768030, 0.03073709920686487629 ),
 .UNSPECIFIED. ) ;
#10391=CIRCLE ( 'NONE', #46614, 2.165354330708661568 ) ;
#10392=CARTESIAN_POINT ( 'NONE',  ( 2.947574761915768171, 1.666714435463287236, -0.1816379373804911379 ) ) ;
#10396=EDGE_CURVE ( 'NONE', #2834, #3813, #1241, .T. ) ;
#10397=VECTOR ( 'NONE', #7576, 39.37007874015748143 ) ;
#10398=CARTESIAN_POINT ( 'NONE',  ( 2.140277031474341118, 0.000000000000000000, -0.07969953553056360884 ) ) ;
#10401=CARTESIAN_POINT ( 'NONE',  ( 1.247448100859587239, 0.000000000000000000, -1.633239539486209591 ) ) ;
#10405=CARTESIAN_POINT ( 'NONE',  ( 1.775400203342704764, 1.475394431724762478, -2.359903268218703332 ) ) ;
#10408=LINE ( 'NONE', #17389, #36891 ) ;
#10409=DIRECTION ( 'NONE',  ( -0.000000000000000000, 1.000000000000000000, -0.000000000000000000 ) ) ;
#10414=EDGE_CURVE ( 'NONE', #13250, #28289, #38919, .T. ) ;
#10417=CARTESIAN_POINT ( 'NONE',  ( 0.7513820654849657776, 1.719936709731724189, 2.142107623314860376 ) ) ;
#10418=ADVANCED_FACE ( 'NONE', ( #19283 ), #35305, .F. ) ;
#10428=ADVANCED_FACE ( 'NONE', ( #3552 ), #15428, .T. ) ;
#10430=LINE ( 'NONE', #18429, #27512 ) ;
#10432=DIRECTION ( 'NONE',  ( 0.01601477604151182663, -0.9998717552508123996, 0.000000000000000000 ) ) ;
#10442=CARTESIAN_POINT ( 'NONE',  ( 2.437180031585944651, 5.905511811023623991, -1.667735833703098969 ) ) ;
#10445=ORIENTED_EDGE ( 'NONE', *, *, #33342, .F. ) ;
#10449=CARTESIAN_POINT ( 'NONE',  ( -2.164823134740035737, 1.574803149606302854, -0.04796011690018223833 ) ) ;
#10450=DIRECTION ( 'NONE',  ( -3.986037398843765983E-20, -1.000000000000000000, -1.160734090543304660E-16 ) ) ;
#10453=CARTESIAN_POINT ( 'NONE',  ( -0.04921259842519708216, 1.608688524157807498, 2.242709805336809303 ) ) ;
#10456=ORIENTED_EDGE ( 'NONE', *, *, #46972, .F. ) ;
#10458=CARTESIAN_POINT ( 'NONE',  ( -2.339241080213612545, 1.682800407567106360, 1.802537235681883843 ) ) ;
#10463=FACE_OUTER_BOUND ( 'NONE', #41959, .T. ) ;
#10464=AXIS2_PLACEMENT_3D ( 'NONE', #14646, #42510, #38650 ) ;
#10470=VERTEX_POINT ( 'NONE', #28826 ) ;
#10471=CARTESIAN_POINT ( 'NONE',  ( -2.889674983507168893, 5.905511811023623991, -0.6090712660038039017 ) ) ;
#10472=CARTESIAN_POINT ( 'NONE',  ( 2.164658444855302122, 5.905511811023623991, -0.04795272066889885720 ) ) ;
#10476=EDGE_CURVE ( 'NONE', #47415, #15540, #7461, .T. ) ;
#10477=FACE_OUTER_BOUND ( 'NONE', #15905, .T. ) ;
#10484=DIRECTION ( 'NONE',  ( -0.9998717552508122886, -0.01601477604151181275, 0.000000000000000000 ) ) ;
#10494=PLANE ( 'NONE',  #4645 ) ;
#10495=VERTEX_POINT ( 'NONE', #9211 ) ;
#10496=CARTESIAN_POINT ( 'NONE',  ( -1.556712866041156440, 1.694999912340861004, 2.509548638715847435 ) ) ;
#10500=VECTOR ( 'NONE', #48076, 39.37007874015748854 ) ;
#10501=CARTESIAN_POINT ( 'NONE',  ( 0.08139965876239094178, 1.610780518492231694, 0.000000000000000000 ) ) ;
#10503=ORIENTED_EDGE ( 'NONE', *, *, #21992, .F. ) ;
#10504=CARTESIAN_POINT ( 'NONE',  ( 0.1067246931122726866, 0.02962905676920215767, 0.000000000000000000 ) ) ;
#10505=ORIENTED_EDGE ( 'NONE', *, *, #24027, .T. ) ;
#10508=ORIENTED_EDGE ( 'NONE', *, *, #29061, .T. ) ;
#10509=EDGE_LOOP ( 'NONE', ( #7254, #138, #29791, #8883 ) ) ;
#10516=CARTESIAN_POINT ( 'NONE',  ( 1.678360014056755389, 0.9972678649800447159, 1.995835756311929110 ) ) ;
#10518=ORIENTED_EDGE ( 'NONE', *, *, #35917, .T. ) ;
#10525=VERTEX_POINT ( 'NONE', #43794 ) ;
#10530=CARTESIAN_POINT ( 'NONE',  ( 2.951990591674675368, 5.905511811023623991, -0.08331184815398307020 ) ) ;
#10541=LINE ( 'NONE', #41526, #21006 ) ;
#10545=VECTOR ( 'NONE', #22701, 39.37007874015748143 ) ;
#10551=EDGE_CURVE ( 'NONE', #40146, #40614, #12318, .T. ) ;
#10552=DIRECTION ( 'NONE',  ( -0.6579387259397138088, -8.738534663690390683E-17, 0.7530714660036099684 ) ) ;
#10557=EDGE_CURVE ( 'NONE', #31520, #18162, #49812, .T. ) ;
#10559=CARTESIAN_POINT ( 'NONE',  ( 2.919426793319799707, 0.000000000000000000, 0.4451252810446820196 ) ) ;
#10562=PLANE ( 'NONE',  #20743 ) ;
#10567=CARTESIAN_POINT ( 'NONE',  ( 2.947574761915768171, 1.666714435463287236, -0.1816379373804911379 ) ) ;
#10573=LINE ( 'NONE', #50508, #31180 ) ;
#10576=ORIENTED_EDGE ( 'NONE', *, *, #22635, .F. ) ;
#10577=CONICAL_SURFACE ( 'NONE', #24612, 3.483074324928249421, 1.244861948955335196 ) ;
#10584=CIRCLE ( 'NONE', #31215, 2.165354330708661568 ) ;
#10586=ORIENTED_EDGE ( 'NONE', *, *, #33098, .T. ) ;
#10589=B_SPLINE_CURVE_WITH_KNOTS ( 'NONE', 3,
 ( #39145, #18325, #13949, #26072 ),
 .UNSPECIFIED., .F., .F.,
 ( 4, 4 ),
 ( 2.018265806504230573E-07, 0.02001440840492994117 ),
 .UNSPECIFIED. ) ;
#10590=CARTESIAN_POINT ( 'NONE',  ( 1.083598637574782142, 1.491270273546293046, 2.747180975113346246 ) ) ;
#10592=CARTESIAN_POINT ( 'NONE',  ( -0.4462886659516242527, 1.602328624241157851, 2.183640264916793861 ) ) ;
#10593=CARTESIAN_POINT ( 'NONE',  ( -1.503492009532958695, 1.205361022782829114E-17, -0.9334790059352082725 ) ) ;
#10595=DIRECTION ( 'NONE',  ( 8.902872254219889125E-17, 1.000000000000000000, 9.311674343991287120E-17 ) ) ;
#10598=ORIENTED_EDGE ( 'NONE', *, *, #20263, .T. ) ;
#10601=ORIENTED_EDGE ( 'NONE', *, *, #45917, .T. ) ;
#10604=AXIS2_PLACEMENT_3D ( 'NONE', #31123, #19988, #35250 ) ;
#10608=CONICAL_SURFACE ( 'NONE', #30398, 2.246510896728926010, 0.01601546068027819014 ) ;
#10610=VECTOR ( 'NONE', #9421, 39.37007874015748143 ) ;
#10611=AXIS2_PLACEMENT_3D ( 'NONE', #9665, #41166, #1911 ) ;
#10616=ORIENTED_EDGE ( 'NONE', *, *, #19113, .F. ) ;
#10617=DIRECTION ( 'NONE',  ( -8.881784197001250746E-15, 0.000000000000000000, 1.000000000000000000 ) ) ;
#10621=CARTESIAN_POINT ( 'NONE',  ( -2.014599508217050250, 1.642826054184012508, -0.8075617281263232083 ) ) ;
#10624=VECTOR ( 'NONE', #44044, 39.37007874015748143 ) ;
#10627=ADVANCED_FACE ( 'NONE', ( #33231 ), #30114, .T. ) ;
#10628=LINE ( 'NONE', #41360, #37010 ) ;
#10633=LINE ( 'NONE', #14504, #13372 ) ;
#10634=DIRECTION ( 'NONE',  ( 0.01601477604151182663, -0.9998717552508123996, 0.000000000000000000 ) ) ;
#10639=DIRECTION ( 'NONE',  ( -0.000000000000000000, 1.000000000000000000, -0.000000000000000000 ) ) ;
#10651=CONICAL_SURFACE ( 'NONE', #39491, 2.165354330708661568, 0.2617993877991570129 ) ;
#10655=CARTESIAN_POINT ( 'NONE',  ( 1.286500945617783609, 0.5223259443140828573, -1.854442115480348541 ) ) ;
#10660=( CONVERSION_BASED_UNIT ( 'INCH', #19391 ) LENGTH_UNIT ( ) NAMED_UNIT ( #7980 ) );
#10661=VECTOR ( 'NONE', #30601, 39.37007874015748143 ) ;
#10665=CARTESIAN_POINT ( 'NONE',  ( 2.491402175429654253, 1.758084086496218612, -1.585592796919505609 ) ) ;
#10671=CARTESIAN_POINT ( 'NONE',  ( -1.722370577523733459, 1.205361022782829114E-17, 0.2829729990490794655 ) ) ;
#10675=FACE_OUTER_BOUND ( 'NONE', #3706, .T. ) ;
#10690=LINE ( 'NONE', #2182, #4831 ) ;
#10691=CARTESIAN_POINT ( 'NONE',  ( -1.684292108503798069, 5.905511811023623991, 1.406123411605399331 ) ) ;
#10696=EDGE_CURVE ( 'NONE', #18996, #36035, #41646, .T. ) ;
#10703=CARTESIAN_POINT ( 'NONE',  ( 0.2509731715796156282, 1.646304950397431410, -2.239533430214235121 ) ) ;
#10705=DIRECTION ( 'NONE',  ( 0.000000000000000000, 0.9659258262890662028, 0.2588190451025280114 ) ) ;
#10707=DIRECTION ( 'NONE',  ( -0.8805955318567322276, 0.000000000000000000, -0.4738686624730094610 ) ) ;
#10708=ORIENTED_EDGE ( 'NONE', *, *, #35077, .F. ) ;
#10712=CARTESIAN_POINT ( 'NONE',  ( -2.298329623231348151, 1.683429673656728465, 1.853838580093637445 ) ) ;
#10715=CARTESIAN_POINT ( 'NONE',  ( 1.733526556417521958, 0.000000000000000000, 0.1851600754179809072 ) ) ;
#10721=ADVANCED_FACE ( 'NONE', ( #39111 ), #6196, .T. ) ;
#10727=ORIENTED_EDGE ( 'NONE', *, *, #34603, .F. ) ;
#10728=CARTESIAN_POINT ( 'NONE',  ( -1.879299076992925199, 0.5249316497054292707, -0.1336616210507489411 ) ) ;
#10729=CARTESIAN_POINT ( 'NONE',  ( 0.000000000000000000, 1.574803149606302854, 0.000000000000000000 ) ) ;
#10733=EDGE_LOOP ( 'NONE', ( #45256, #39643, #35981, #17772 ) ) ;
#10734=B_SPLINE_CURVE_WITH_KNOTS ( 'NONE', 3,
 ( #15601, #11224, #22588, #34972 ),
 .UNSPECIFIED., .F., .F.,
 ( 4, 4 ),
 ( 0.03086743659920977365, 0.04894270564625235326 ),
 .UNSPECIFIED. ) ;
#10741=LINE ( 'NONE', #14106, #15574 ) ;
#10743=CARTESIAN_POINT ( 'NONE',  ( -1.721400284384397628, 0.0003482895740541699209, 0.2828415639128913361 ) ) ;
#10746=ORIENTED_EDGE ( 'NONE', *, *, #39136, .F. ) ;
#10748=DIRECTION ( 'NONE',  ( -0.01601477604151182663, 0.9998717552508123996, -0.000000000000000000 ) ) ;
#10751=EDGE_CURVE ( 'NONE', #18996, #30156, #16609, .T. ) ;
#10754=ORIENTED_EDGE ( 'NONE', *, *, #2102, .F. ) ;
#10756=AXIS2_PLACEMENT_3D ( 'NONE', #23392, #28032, #28541 ) ;
#10759=VERTEX_POINT ( 'NONE', #46324 ) ;
#10760=DIRECTION ( 'NONE',  ( 0.1785568947986370669, 0.000000000000000000, -0.9839295885986296675 ) ) ;
#10762=DIRECTION ( 'NONE',  ( -0.000000000000000000, -1.000000000000000000, -0.000000000000000000 ) ) ;
#10765=LINE ( 'NONE', #38148, #18204 ) ;
#10766=B_SPLINE_CURVE_WITH_KNOTS ( 'NONE', 3,
 ( #4412, #20149, #8027, #7775 ),
 .UNSPECIFIED., .F., .F.,
 ( 4, 4 ),
 ( 1.206284417596563428E-05, 0.002512066550552098567 ),
 .UNSPECIFIED. ) ;
#10767=DIRECTION ( 'NONE',  ( -0.01601477604151182663, 0.9998717552508123996, -0.000000000000000000 ) ) ;
#10768=CARTESIAN_POINT ( 'NONE',  ( -0.2178414669075503241, 0.5249316475426863970, -1.871410041343207542 ) ) ;
#10771=CARTESIAN_POINT ( 'NONE',  ( -0.3857230305054721864, 0.000000000000000000, 1.849896105471422025 ) ) ;
#10775=ORIENTED_EDGE ( 'NONE', *, *, #48564, .F. ) ;
#10776=CARTESIAN_POINT ( 'NONE',  ( -2.808237744966007643, 5.905511811023623991, 0.9124517550441288982 ) ) ;
#10777=CARTESIAN_POINT ( 'NONE',  ( 1.836694934015037806, 1.638894784719147513, 1.401770057403159520 ) ) ;
#10780=CARTESIAN_POINT ( 'NONE',  ( -2.165354330708661568, 1.673228346456695492, -4.271103535670736336E-20 ) ) ;
#10784=CARTESIAN_POINT ( 'NONE',  ( 0.1155636338427008941, -0.5222242541845523167, 0.000000000000000000 ) ) ;
#10791=ORIENTED_EDGE ( 'NONE', *, *, #24619, .F. ) ;
#10796=VERTEX_POINT ( 'NONE', #34738 ) ;
#10800=VERTEX_POINT ( 'NONE', #18738 ) ;
#10808=CARTESIAN_POINT ( 'NONE',  ( 0.002207914879453961535, -5.712274067634378313E-18, 0.04916304461325374242 ) ) ;
#10813=EDGE_CURVE ( 'NONE', #39458, #48829, #14451, .T. ) ;
#10817=CARTESIAN_POINT ( 'NONE',  ( 0.000000000000000000, 1.574803149606302854, 0.000000000000000000 ) ) ;
#10821=ORIENTED_EDGE ( 'NONE', *, *, #14765, .T. ) ;
#10823=AXIS2_PLACEMENT_3D ( 'NONE', #17708, #21581, #37591 ) ;
#10825=CIRCLE ( 'NONE', #90, 2.165354330708661568 ) ;
#10827=B_SPLINE_CURVE_WITH_KNOTS ( 'NONE', 3,
 ( #10392, #26138, #6526, #50087 ),
 .UNSPECIFIED., .F., .F.,
 ( 4, 4 ),
 ( 2.003042141634280194E-07, 0.01590458885791005625 ),
 .UNSPECIFIED. ) ;
#10828=B_SPLINE_CURVE_WITH_KNOTS ( 'NONE', 3,
 ( #32539, #17295, #48230, #5152 ),
 .UNSPECIFIED., .F., .F.,
 ( 4, 4 ),
 ( 0.1211873102087489551, 0.1625992483279400103 ),
 .UNSPECIFIED. ) ;
#10832=CARTESIAN_POINT ( 'NONE',  ( -2.695799277629577162, 1.677241212940233872, -1.205759334241492509 ) ) ;
#10833=LINE ( 'NONE', #6208, #23796 ) ;
#10834=DIRECTION ( 'NONE',  ( -0.01601477604151182663, 0.9998717552508123996, -0.000000000000000000 ) ) ;
#10835=ADVANCED_FACE ( 'NONE', ( #7118 ), #26780, .T. ) ;
#10840=PLANE ( 'NONE',  #11159 ) ;
#10851=ORIENTED_EDGE ( 'NONE', *, *, #20545, .T. ) ;
#10855=AXIS2_PLACEMENT_3D ( 'NONE', #38536, #50099, #42389 ) ;
#10858=VECTOR ( 'NONE', #48869, 39.37007874015748143 ) ;
#10862=ORIENTED_EDGE ( 'NONE', *, *, #44365, .T. ) ;
#10863=ORIENTED_EDGE ( 'NONE', *, *, #29515, .T. ) ;
#10864=CARTESIAN_POINT ( 'NONE',  ( -1.571896207478202800, 0.0009392905874082641340, 0.7899878318620054962 ) ) ;
#10865=CARTESIAN_POINT ( 'NONE',  ( 1.266373210783726444, 1.640528807385599697, -2.667458607414338712 ) ) ;
#10871=ORIENTED_EDGE ( 'NONE', *, *, #23687, .F. ) ;
#10872=CARTESIAN_POINT ( 'NONE',  ( 0.3847164039870727414, 0.5249316475426861750, 1.844349136158301983 ) ) ;
#10875=CARTESIAN_POINT ( 'NONE',  ( -1.743516651958532115, 0.0004834999639498430428, -4.958524412099369637E-19 ) ) ;
#10882=DIRECTION ( 'NONE',  ( -3.986037398843765983E-20, -1.000000000000000000, -1.160734090543304660E-16 ) ) ;
#10883=B_SPLINE_CURVE_WITH_KNOTS ( 'NONE', 3,
 ( #43867, #46950, #27613, #32022 ),
 .UNSPECIFIED., .F., .F.,
 ( 4, 4 ),
 ( 2.767205211280488720E-07, 0.002500421812205707271 ),
 .UNSPECIFIED. ) ;
#10885=DIRECTION ( 'NONE',  ( 0.01601477604151182663, -0.9998717552508123996, 0.000000000000000000 ) ) ;
#10890=CARTESIAN_POINT ( 'NONE',  ( 2.139229417893225627, 0.000000000000000000, -0.3394403656973398742 ) ) ;
#10891=ORIENTED_EDGE ( 'NONE', *, *, #22572, .F. ) ;
#10895=EDGE_CURVE ( 'NONE', #358, #49472, #43475, .T. ) ;
#10897=CARTESIAN_POINT ( 'NONE',  ( 1.805735793522764476, 1.049866565067838264, 0.9158222789645976691 ) ) ;
#10904=B_SPLINE_CURVE_WITH_KNOTS ( 'NONE', 3,
 ( #41968, #10728, #6607, #45057 ),
 .UNSPECIFIED., .F., .F.,
 ( 4, 4 ),
 ( 0.1211873102087489551, 0.1625992483279400103 ),
 .UNSPECIFIED. ) ;
#10905=FACE_OUTER_BOUND ( 'NONE', #15161, .T. ) ;
#10909=CARTESIAN_POINT ( 'NONE',  ( -0.1515599155143076138, 1.705474441417569320, -2.232975473887063966 ) ) ;
#10910=CARTESIAN_POINT ( 'NONE',  ( 2.134533150281098024, 1.745516327274217572, -1.350025615906367715 ) ) ;
#10914=FACE_OUTER_BOUND ( 'NONE', #44334, .T. ) ;
#10916=ORIENTED_EDGE ( 'NONE', *, *, #10243, .F. ) ;
#10917=DIRECTION ( 'NONE',  ( -0.000000000000000000, 1.000000000000000000, -0.000000000000000000 ) ) ;
#10921=EDGE_CURVE ( 'NONE', #18547, #3514, #29498, .T. ) ;
#10922=CARTESIAN_POINT ( 'NONE',  ( 0.2156685157584258827, 1.205361022782829114E-17, -2.945280361644574185 ) ) ;
#10923=CYLINDRICAL_SURFACE ( 'NONE', #46940, 2.165354330708661568 ) ;
#10925=VERTEX_POINT ( 'NONE', #47321 ) ;
#10926=ORIENTED_EDGE ( 'NONE', *, *, #18769, .F. ) ;
#10928=LINE ( 'NONE', #22547, #14186 ) ;
#10929=CARTESIAN_POINT ( 'NONE',  ( 1.551823387806912313, 1.049866565877818125, 1.300483131990376018 ) ) ;
#10933=FACE_OUTER_BOUND ( 'NONE', #36742, .T. ) ;
#10936=CIRCLE ( 'NONE', #44710, 2.165354330708661568 ) ;
#10937=ORIENTED_EDGE ( 'NONE', *, *, #32651, .T. ) ;
#10938=DIRECTION ( 'NONE',  ( 0.9362348706397368714, 1.288287287306305283E-16, 0.3513748240813434620 ) ) ;
#10942=EDGE_LOOP ( 'NONE', ( #10232, #34254, #50292, #48643 ) ) ;
#10953=AXIS2_PLACEMENT_3D ( 'NONE', #34650, #46483, #10136 ) ;
#10956=CARTESIAN_POINT ( 'NONE',  ( -0.2156685157583833057, 1.520013147563287648, -2.945280361644576850 ) ) ;
#10957=CARTESIAN_POINT ( 'NONE',  ( -1.833791099076585995, 6.692913385826772199, -1.151507526013721527 ) ) ;
#10959=EDGE_LOOP ( 'NONE', ( #30806, #26355, #4035, #11657 ) ) ;
#10961=CARTESIAN_POINT ( 'NONE',  ( -2.161044708975090156, 0.000000000000000000, 0.1463148319730351032 ) ) ;
#10963=DIRECTION ( 'NONE',  ( 0.000000000000000000, 0.000000000000000000, 1.000000000000000000 ) ) ;
#10974=CARTESIAN_POINT ( 'NONE',  ( -1.610230546471095314, 0.000000000000000000, -0.7060526055843052706 ) ) ;
#10975=EDGE_CURVE ( 'NONE', #19878, #24653, #49207, .T. ) ;
#10977=DIRECTION ( 'NONE',  ( -0.9998717552508122886, -0.01601477604151180928, 0.000000000000000000 ) ) ;
#10981=ORIENTED_EDGE ( 'NONE', *, *, #40061, .F. ) ;
#10985=AXIS2_PLACEMENT_3D ( 'NONE', #16492, #28608, #2774 ) ;
#10986=CARTESIAN_POINT ( 'NONE',  ( 0.08139965876239094178, 1.610780518492231694, 0.000000000000000000 ) ) ;
#10989=B_SPLINE_CURVE_WITH_KNOTS ( 'NONE', 3,
 ( #13878, #10003, #25744, #41492 ),
 .UNSPECIFIED., .F., .F.,
 ( 4, 4 ),
 ( 0.0007795210587999083351, 0.003279804236056507553 ),
 .UNSPECIFIED. ) ;
#10992=CARTESIAN_POINT ( 'NONE',  ( 1.833791099076603537, 1.574803149606302854, -1.151507526013694216 ) ) ;
#10993=AXIS2_PLACEMENT_3D ( 'NONE', #43774, #8679, #47363 ) ;
#10994=CARTESIAN_POINT ( 'NONE',  ( -1.327305354309126884, 0.5249316497054298258, -1.337120393289511266 ) ) ;
#10997=EDGE_CURVE ( 'NONE', #19533, #32006, #18166, .T. ) ;
#10999=DIRECTION ( 'NONE',  ( -0.01601477604151182663, 0.9998717552508123996, -0.000000000000000000 ) ) ;
#11000=EDGE_CURVE ( 'NONE', #36209, #34423, #2443, .T. ) ;
#11003=CARTESIAN_POINT ( 'NONE',  ( -1.330126866422489007, 1.653789137470381254, -1.747037097613915568 ) ) ;
#11012=ORIENTED_EDGE ( 'NONE', *, *, #39961, .T. ) ;
#11015=CIRCLE ( 'NONE', #30807, 2.244934639244525076 ) ;
#11019=AXIS2_PLACEMENT_3D ( 'NONE', #46363, #35984, #50458 ) ;
#11020=CARTESIAN_POINT ( 'NONE',  ( 2.298329729280814249, 1.755067388827460384, 1.853838447111812338 ) ) ;
#11021=CARTESIAN_POINT ( 'NONE',  ( 0.08119777152254364916, 1.623385212329073957, 0.000000000000000000 ) ) ;
#11025=B_SPLINE_CURVE_WITH_KNOTS ( 'NONE', 3,
 ( #34279, #22398, #6902, #18776 ),
 .UNSPECIFIED., .F., .F.,
 ( 4, 4 ),
 ( 0.001628790289768138272, 0.004128914707219031623 ),
 .UNSPECIFIED. ) ;
#11026=PLANE ( 'NONE',  #49678 ) ;
#11031=DIRECTION ( 'NONE',  ( -0.3090169943749447312, 1.104046895826785399E-16, -0.9510565162951544194 ) ) ;
#11035=CARTESIAN_POINT ( 'NONE',  ( -1.743145509346916588, 0.000000000000000000, 0.000000000000000000 ) ) ;
#11039=DIRECTION ( 'NONE',  ( -3.986037398843765983E-20, -1.000000000000000000, -1.160734090543304660E-16 ) ) ;
#11041=DIRECTION ( 'NONE',  ( -3.986037398843765983E-20, -1.000000000000000000, -1.160734090543304660E-16 ) ) ;
#11044=DIRECTION ( 'NONE',  ( -0.7530714660036099684, -1.160734090543304907E-16, -0.6579387259397138088 ) ) ;
#11053=CARTESIAN_POINT ( 'NONE',  ( 0.000000000000000000, 1.574803149606302854, 0.000000000000000000 ) ) ;
#11054=ORIENTED_EDGE ( 'NONE', *, *, #33732, .F. ) ;
#11062=CARTESIAN_POINT ( 'NONE',  ( -2.134236802639925212, 0.000000000000000000, -2.040539317874611847 ) ) ;
#11077=CARTESIAN_POINT ( 'NONE',  ( 1.236813753895252166, 1.738537790538875027, -2.681693691597563767 ) ) ;
#11079=CARTESIAN_POINT ( 'NONE',  ( -2.951990591674674924, 1.574803149606301744, 0.000000000000000000 ) ) ;
#11081=CARTESIAN_POINT ( 'NONE',  ( 0.1526763070133267952, 1.611922144458495687, -2.245379599360889600 ) ) ;
#11084=ORIENTED_EDGE ( 'NONE', *, *, #49811, .F. ) ;
#11086=CONICAL_SURFACE ( 'NONE', #8610, 3.483074324928249421, 1.244861948955335196 ) ;
#11090=DIRECTION ( 'NONE',  ( -0.7227948638273878901, 8.024280841161103757E-17, -0.6910626489868684219 ) ) ;
#11091=CONICAL_SURFACE ( 'NONE', #39948, 2.244934639244524632, 1.554780866114618743 ) ;
#11094=PLANE ( 'NONE',  #14109 ) ;
#11098=EDGE_CURVE ( 'NONE', #5773, #45425, #9402, .T. ) ;
#11101=CARTESIAN_POINT ( 'NONE',  ( 0.000000000000000000, 6.692913385826772199, 0.000000000000000000 ) ) ;
#11102=CARTESIAN_POINT ( 'NONE',  ( 1.645338673473796254, 0.05427277550655955352, -1.027111169014480296 ) ) ;
#11103=EDGE_CURVE ( 'NONE', #25844, #47691, #3757, .T. ) ;
#11105=EDGE_CURVE ( 'NONE', #3117, #24926, #43645, .T. ) ;
#11108=CARTESIAN_POINT ( 'NONE',  ( -1.930190994932096782, 0.000000000000000000, -0.9827944786818723077 ) ) ;
#11112=DIRECTION ( 'NONE',  ( 0.6579387259397027066, 0.000000000000000000, 0.7530714660036195163 ) ) ;
#11117=VERTEX_POINT ( 'NONE', #3429 ) ;
#11118=DIRECTION ( 'NONE',  ( -0.9998717552508121775, -0.01601477604151182663, 0.000000000000000000 ) ) ;
#11120=B_SPLINE_CURVE_WITH_KNOTS ( 'NONE', 3,
 ( #42635, #46485, #38280, #30524 ),
 .UNSPECIFIED., .F., .F.,
 ( 4, 4 ),
 ( 2.051261343427981145E-07, 0.002500229005657641102 ),
 .UNSPECIFIED. ) ;
#11122=EDGE_LOOP ( 'NONE', ( #32238, #41392, #14188, #31374 ) ) ;
#11123=EDGE_CURVE ( 'NONE', #33470, #41056, #23292, .T. ) ;
#11124=AXIS2_PLACEMENT_3D ( 'NONE', #17886, #49332, #49577 ) ;
#11126=CYLINDRICAL_SURFACE ( 'NONE', #17438, 2.164630168518208109 ) ;
#11129=VERTEX_POINT ( 'NONE', #46511 ) ;
#11133=CARTESIAN_POINT ( 'NONE',  ( -0.8238130908517355966, 1.694707076513333410, 2.054984861273213337 ) ) ;
#11134=CIRCLE ( 'NONE', #35863, 1.743387098533651480 ) ;
#11140=DIRECTION ( 'NONE',  ( -0.9195277725514544587, 0.000000000000000000, 0.3930250316539147803 ) ) ;
#11144=ORIENTED_EDGE ( 'NONE', *, *, #38901, .F. ) ;
#11149=LINE ( 'NONE', #19138, #28390 ) ;
#11153=ORIENTED_EDGE ( 'NONE', *, *, #9491, .T. ) ;
#11154=AXIS2_PLACEMENT_3D ( 'NONE', #23719, #4110, #39727 ) ;
#11156=LINE ( 'NONE', #7033, #9577 ) ;
#11157=EDGE_CURVE ( 'NONE', #26859, #50859, #31048, .T. ) ;
#11159=AXIS2_PLACEMENT_3D ( 'NONE', #15221, #46426, #38473 ) ;
#11161=VECTOR ( 'NONE', #46198, 39.37007874015748143 ) ;
#11165=DIRECTION ( 'NONE',  ( -0.01601477604151182663, 0.9998717552508123996, -0.000000000000000000 ) ) ;
#11166=CARTESIAN_POINT ( 'NONE',  ( 1.883550378546973381, 6.692913385826772199, -1.069467267250421294 ) ) ;
#11167=EDGE_CURVE ( 'NONE', #15209, #39907, #47922, .T. ) ;
#11173=DIRECTION ( 'NONE',  ( 0.000000000000000000, 0.000000000000000000, -1.000000000000000000 ) ) ;
#11175=CARTESIAN_POINT ( 'NONE',  ( 0.08139965876239094178, 1.610780518492231694, 0.000000000000000000 ) ) ;
#11178=DIRECTION ( 'NONE',  ( 0.000000000000000000, 1.160734090543304660E-16, -1.000000000000000000 ) ) ;
#11179=LINE ( 'NONE', #42662, #23535 ) ;
#11188=CARTESIAN_POINT ( 'NONE',  ( 1.646369848953919135, 1.642880493769403927, -2.182308221245992552 ) ) ;
#11190=CARTESIAN_POINT ( 'NONE',  ( 2.823445274216730638, 1.450545469922353892, 0.8656477926280681245 ) ) ;
#11191=EDGE_LOOP ( 'NONE', ( #36354, #13336, #49954, #46163 ) ) ;
#11192=VERTEX_POINT ( 'NONE', #10417 ) ;
#11193=FACE_OUTER_BOUND ( 'NONE', #44151, .T. ) ;
#11195=ADVANCED_FACE ( 'NONE', ( #30293 ), #26167, .T. ) ;
#11205=ORIENTED_EDGE ( 'NONE', *, *, #4067, .T. ) ;
#11212=FACE_OUTER_BOUND ( 'NONE', #46895, .T. ) ;
#11214=EDGE_LOOP ( 'NONE', ( #1037, #21857 ) ) ;
#11215=AXIS2_PLACEMENT_3D ( 'NONE', #43413, #35683, #8058 ) ;
#11216=EDGE_CURVE ( 'NONE', #26667, #33610, #24552, .T. ) ;
#11220=EDGE_CURVE ( 'NONE', #12966, #41924, #45786, .T. ) ;
#11222=CARTESIAN_POINT ( 'NONE',  ( 2.062746868503864572, 1.708132218730083807, 1.054125835973626968 ) ) ;
#11224=CARTESIAN_POINT ( 'NONE',  ( -0.04921259842519708910, 1.714701585914776283, 2.715578020061004683 ) ) ;
#11226=ADVANCED_FACE ( 'NONE', ( #50114 ), #14801, .T. ) ;
#11227=ORIENTED_EDGE ( 'NONE', *, *, #9824, .T. ) ;
#11229=LINE ( 'NONE', #38851, #16238 ) ;
#11230=DIRECTION ( 'NONE',  ( -9.701723960855857903E-17, 1.000000000000000000, 8.476140964546263859E-17 ) ) ;
#11231=AXIS2_PLACEMENT_3D ( 'NONE', #19959, #16876, #92 ) ;
#11234=ADVANCED_FACE ( 'NONE', ( #46262 ), #39200, .T. ) ;
#11235=DIRECTION ( 'NONE',  ( -0.01601477604151182663, 0.9998717552508123996, -0.000000000000000000 ) ) ;
#11238=ORIENTED_EDGE ( 'NONE', *, *, #12375, .T. ) ;
#11240=ORIENTED_EDGE ( 'NONE', *, *, #7026, .T. ) ;
#11246=AXIS2_PLACEMENT_3D ( 'NONE', #35505, #39120, #50679 ) ;
#11247=ORIENTED_EDGE ( 'NONE', *, *, #4359, .T. ) ;
#11249=DIRECTION ( 'NONE',  ( 0.000000000000000000, 1.160734090543304660E-16, -1.000000000000000000 ) ) ;
#11250=CARTESIAN_POINT ( 'NONE',  ( -1.891607981616729495, 1.579179190298960256, 1.073803248357834139 ) ) ;
#11254=CARTESIAN_POINT ( 'NONE',  ( 1.905671854841463952, 1.748959039950288341, 2.256015092822681645 ) ) ;
#11255=ORIENTED_EDGE ( 'NONE', *, *, #4916, .T. ) ;
#11256=CARTESIAN_POINT ( 'NONE',  ( 2.951990591674676256, 1.447429260878886348, -0.08331184815398369470 ) ) ;
#11258=EDGE_CURVE ( 'NONE', #12736, #25699, #10386, .T. ) ;
#11259=CARTESIAN_POINT ( 'NONE',  ( 0.7855418668307558860, 0.000000000000000000, -2.846347029613733870 ) ) ;
#11261=CARTESIAN_POINT ( 'NONE',  ( 2.161044708975088380, 1.205361022782829114E-17, 0.1463148319730657732 ) ) ;
#11263=ORIENTED_EDGE ( 'NONE', *, *, #44365, .F. ) ;
#11264=EDGE_CURVE ( 'NONE', #4750, #27191, #22702, .T. ) ;
#11266=ADVANCED_FACE ( 'NONE', ( #12185 ), #20441, .T. ) ;
#11268=ORIENTED_EDGE ( 'NONE', *, *, #2847, .F. ) ;
#11272=VECTOR ( 'NONE', #43699, 39.37007874015748143 ) ;
#11274=CARTESIAN_POINT ( 'NONE',  ( -2.012389709434417195, 1.049866565877818347, 0.2229346561180729214 ) ) ;
#11275=CARTESIAN_POINT ( 'NONE',  ( 0.4517796511351843680, 1.715138028758778521, 2.213898087213642007 ) ) ;
#11277=CARTESIAN_POINT ( 'NONE',  ( 2.320271282243135502, 1.712256942838378260, -0.1534657056239357720 ) ) ;
#11278=EDGE_CURVE ( 'NONE', #16625, #9331, #4805, .T. ) ;
#11281=CARTESIAN_POINT ( 'NONE',  ( 1.474379988472116487, 1.633091647787944911, 1.762361831087230213 ) ) ;
#11282=VERTEX_POINT ( 'NONE', #47510 ) ;
#11288=ORIENTED_EDGE ( 'NONE', *, *, #38947, .T. ) ;
#11289=CARTESIAN_POINT ( 'NONE',  ( -0.1071992566810134884, 0.000000000000000000, -1.740088185897663342 ) ) ;
#11292=DIRECTION ( 'NONE',  ( -0.01601477604151182663, 0.9998717552508123996, -0.000000000000000000 ) ) ;
#11294=CARTESIAN_POINT ( 'NONE',  ( -0.8783128861146038968, 0.01385187720497466773, 1.565997986929510644 ) ) ;
#11295=EDGE_CURVE ( 'NONE', #31964, #44522, #20807, .T. ) ;
#11296=DIRECTION ( 'NONE',  ( -3.986037398843765983E-20, -1.000000000000000000, -1.160734090543304660E-16 ) ) ;
#11299=DIRECTION ( 'NONE',  ( 0.3090169943749582204, 1.288287287306305283E-16, -0.9510565162951500895 ) ) ;
#11302=CARTESIAN_POINT ( 'NONE',  ( 1.779568955232893268, 1.574803149606302854, -1.233650562797287797 ) ) ;
#11304=VECTOR ( 'NONE', #42954, 39.37007874015748143 ) ;
#11307=EDGE_LOOP ( 'NONE', ( #50327, #49330, #36764, #4828 ) ) ;
#11309=ORIENTED_EDGE ( 'NONE', *, *, #12850, .T. ) ;
#11310=CYLINDRICAL_SURFACE ( 'NONE', #40320, 2.165354330708661568 ) ;
#11316=ORIENTED_EDGE ( 'NONE', *, *, #43915, .T. ) ;
#11327=EDGE_CURVE ( 'NONE', #20851, #48279, #40018, .T. ) ;
#11331=ORIENTED_EDGE ( 'NONE', *, *, #40517, .T. ) ;
#11346=EDGE_CURVE ( 'NONE', #20275, #45649, #43004, .T. ) ;
#11347=CARTESIAN_POINT ( 'NONE',  ( -0.2156685157583831947, 1.715903002249486997, -2.945280361644576850 ) ) ;
#11349=EDGE_CURVE ( 'NONE', #41298, #47368, #28474, .T. ) ;
#11353=AXIS2_PLACEMENT_3D ( 'NONE', #41704, #7850, #18720 ) ;
#11357=LINE ( 'NONE', #12367, #20097 ) ;
#11360=FACE_OUTER_BOUND ( 'NONE', #50627, .T. ) ;
#11361=ORIENTED_EDGE ( 'NONE', *, *, #51018, .T. ) ;
#11365=CARTESIAN_POINT ( 'NONE',  ( -1.294674717613570003, 1.049866565067837820, 1.556672598277949016 ) ) ;
#11370=ORIENTED_EDGE ( 'NONE', *, *, #31210, .T. ) ;
#11371=ORIENTED_EDGE ( 'NONE', *, *, #36883, .F. ) ;
#11372=CARTESIAN_POINT ( 'NONE',  ( -2.014567149787738654, 1.675634971041569443, -0.8075478974698888646 ) ) ;
#11377=VECTOR ( 'NONE', #30227, 39.37007874015748143 ) ;
#11379=CARTESIAN_POINT ( 'NONE',  ( 0.000000000000000000, 1.574803149606302854, 0.000000000000000000 ) ) ;
#11380=ORIENTED_EDGE ( 'NONE', *, *, #31958, .T. ) ;
#11385=ORIENTED_EDGE ( 'NONE', *, *, #3228, .F. ) ;
#11391=CARTESIAN_POINT ( 'NONE',  ( -1.905671854841497481, 1.591126119768930147, 2.256015092822653223 ) ) ;
#11395=VERTEX_POINT ( 'NONE', #17848 ) ;
#11399=ORIENTED_EDGE ( 'NONE', *, *, #45686, .F. ) ;
#11403=CIRCLE ( 'NONE', #40271, 2.165354330708661568 ) ;
#11407=ORIENTED_EDGE ( 'NONE', *, *, #14933, .T. ) ;
#11408=LINE ( 'NONE', #34656, #26685 ) ;
#11409=DIRECTION ( 'NONE',  ( 0.9998717552508121775, 0.01601477604151182663, 0.000000000000000000 ) ) ;
#11410=EDGE_CURVE ( 'NONE', #31480, #17017, #1143, .T. ) ;
#11411=B_SPLINE_CURVE_WITH_KNOTS ( 'NONE', 3,
 ( #38777, #10897, #26392, #22520 ),
 .UNSPECIFIED., .F., .F.,
 ( 4, 4 ),
 ( 0.1211775127643062444, 0.1625894504277921315 ),
 .UNSPECIFIED. ) ;
#11413=AXIS2_PLACEMENT_3D ( 'NONE', #27697, #43441, #8086 ) ;
#11414=VERTEX_POINT ( 'NONE', #36711 ) ;
#11415=CLOSED_SHELL ( 'NONE', ( #33734, #15141, #18164, #25221, #43792, #43732, #34483, #26474, #16471, #35080, #38995, #34658, #31981, #43609, #24204, #50596, #45882, #47407, #45310, #25716, #31995, #21348, #22353, #42459, #30358, #22661, #11195, #50949, #2308, #22949, #43727, #39515, #36433, #43257, #46547, #2118, #31283, #49688, #50714, #23133, #9907, #26029, #6676, #50219, #36815, #38656, #50722, #28645, #45212, #8040, #23103, #41165, #18256, #19935, #47099, #23348, #48492, #30634, #2203, #6830, #49073, #4772, #38056, #4289, #15532, #37888, #33915, #33696, #21007, #46837, #38619, #48632, #8817, #24569, #27243, #4021, #26615, #43414, #1560, #35308, #26440, #34040, #44029, #7659, #34252, #2483, #672, #32886, #44561, #13166, #375, #38393, #22532, #48698, #19840, #27455, #50124, #37171, #31612, #23257, #11632, #8491, #43934, #6753, #12089, #8687, #17135, #3338, #297, #50940, #7855, #4222, #12677, #11548, #43409, #11521, #19531, #12579, #36951, #7853, #50690, #31455, #28117, #38644, #48377, #7019, #32496, #748, #32605, #40862, #26793, #30818, #10132, #2035, #12122, #20417, #33661, #1845, #40872, #15687, #48655, #28059, #3830, #10340, #5520, #17231, #40243, #44223, #44123, #26260, #11472, #49064, #11266, #42114, #6332, #19300, #3975, #4566, #31335, #7196, #48527, #14986, #44344, #4008, #47717, #12801, #26577, #15900, #17716, #46103, #11226, #2444, #19877, #17596, #30117, #4810, #42228, #7387, #39993, #37464, #50231, #50023, #36152, #5215, #7246, #41426, #26787, #8238, #41035, #10418, #39901, #4514, #28295, #31426, #22094, #18765, #25977, #7413, #23328, #46559, #19201, #7750, #31637, #14895, #19028, #10360, #26563, #1957, #45819, #33082, #41657, #36766, #7156, #29366, #33085, #23186, #41864, #29144, #47836, #42326, #27946, #11842, #41604, #28331, #37988, #10277, #7341, #7252, #411, #22492, #36238, #15266, #30238, #12670, #24578, #12969, #47170, #15407, #33389, #38175, #25106, #46880, #18504, #32759, #3320, #6700, #49177, #30345, #19468, #31792, #43503, #29483, #31684, #6516, #10721, #46009, #6985, #23199, #16369, #50969, #22527, #16357, #4200, #27605, #32819, #44157, #24978, #19362, #13420, #667, #14757, #22470, #16299, #39191, #9234, #25546, #46106, #15799, #11234, #26953, #42780, #50036, #46944, #1660, #5491, #35828, #35805, #2411, #25566, #2260, #10627, #13809, #7321, #20836, #42084, #13065, #15637, #1428, #19557, #893, #5758, #37305, #923, #36599, #37408, #47081, #31268, #23589, #46640, #19677, #33032, #21636, #37282, #28349, #27049, #23966, #49399, #41766, #16933, #50005, #31686, #34765, #45717, #45750, #31710, #10835, #44510, #29098, #22139, #47175, #45926, #25067, #21254, #50780, #28483, #21207, #25074, #20432, #5577, #3744, #20130, #31979, #43071, #31925, #48373, #37217, #1049, #40381, #41661, #31851, #12995, #18812, #22207, #6546, #13177, #10009, #9012, #28655, #8294, #46579, #24496, #42446, #6715, #44959, #18335, #7250, #9038, #11625, #44089, #2634, #15890, #23391, #32012, #29634, #37749, #19141, #9888, #37527, #6869, #42133, #45708, #14947, #9733, #24102, #16943, #13578, #15704, #42968, #26988, #47400, #16334, #47950, #25060, #19429, #45535, #15403, #35219, #31747, #1493, #27939, #22872, #19184, #48956, #40081, #39835, #3700, #38147, #25577, #16423, #1813, #17187, #44989, #32400, #25517, #46670, #33011, #31973, #21732, #50298, #46411, #10428, #18964, #13107, #9185, #26080, #11741, #35279, #38776, #38624, #32660, #50091, #35368, #50657, #38792, #44953, #26602, #46461, #35400, #23807, #44356, #9196, #34425, #43269, #35261, #46145, #19021, #24153, #45113, #29533, #19785, #48177, #9118, #17182, #39586, #25708, #1181, #34420, #27548, #500, #34580, #2756, #2506, #15423, #15368 ) ) ;
#11419=DIRECTION ( 'NONE',  ( -0.01601477604151182663, 0.9998717552508123996, -0.000000000000000000 ) ) ;
#11426=CARTESIAN_POINT ( 'NONE',  ( 0.1067246931122726866, 0.02962905676920215767, 0.000000000000000000 ) ) ;
#11427=ORIENTED_EDGE ( 'NONE', *, *, #40616, .F. ) ;
#11429=CARTESIAN_POINT ( 'NONE',  ( 1.955075903006588067, 1.470442306530027832, 2.212852075800510576 ) ) ;
#11436=DIRECTION ( 'NONE',  ( -0.9998717552508122886, -0.01601477604151185785, 0.000000000000000000 ) ) ;
#11439=CARTESIAN_POINT ( 'NONE',  ( 1.517339494376257703, 1.637296765517717523, -2.004713174013318611 ) ) ;
#11443=ORIENTED_EDGE ( 'NONE', *, *, #14264, .F. ) ;
#11445=DIRECTION ( 'NONE',  ( -3.986037398843765983E-20, -1.000000000000000000, -1.160734090543304660E-16 ) ) ;
#11450=LINE ( 'NONE', #43685, #10397 ) ;
#11451=ORIENTED_EDGE ( 'NONE', *, *, #47463, .F. ) ;
#11455=EDGE_LOOP ( 'NONE', ( #23404, #30407, #24057, #7077 ) ) ;
#11458=EDGE_CURVE ( 'NONE', #6407, #22173, #16966, .T. ) ;
#11460=DIRECTION ( 'NONE',  ( -0.9998717552508122886, -0.01601477604151182316, 0.000000000000000000 ) ) ;
#11464=VECTOR ( 'NONE', #26330, 39.37007874015748143 ) ;
#11468=CIRCLE ( 'NONE', #40331, 1.850107469027523432 ) ;
#11470=CARTESIAN_POINT ( 'NONE',  ( 2.755905511811024056, 4.960629921259846142, 1.023622047244094446 ) ) ;
#11472=ADVANCED_FACE ( 'NONE', ( #13467 ), #29202, .T. ) ;
#11473=B_SPLINE_CURVE_WITH_KNOTS ( 'NONE', 3,
 ( #6998, #2872, #22746, #15248 ),
 .UNSPECIFIED., .F., .F.,
 ( 4, 4 ),
 ( 2.032912801187147383E-07, 0.002500496937475709964 ),
 .UNSPECIFIED. ) ;
#11483=CARTESIAN_POINT ( 'NONE',  ( 0.000000000000000000, 0.07874015748031502893, -0.3937007874015748254 ) ) ;
#11485=EDGE_CURVE ( 'NONE', #41810, #15466, #14685, .T. ) ;
#11490=CARTESIAN_POINT ( 'NONE',  ( -1.743268982565497449, 0.0004610889948519912205, -0.02902809809614041725 ) ) ;
#11492=DIRECTION ( 'NONE',  ( -0.9989930665413151445, 0.000000000000000000, 0.04486483035050446017 ) ) ;
#11493=EDGE_CURVE ( 'NONE', #15175, #23260, #2341, .T. ) ;
#11503=CARTESIAN_POINT ( 'NONE',  ( 1.771435203777392386, 1.736274727556916808, 1.475617711110977615 ) ) ;
#11505=DIRECTION ( 'NONE',  ( -0.01601477604151182663, 0.9998717552508123996, -0.000000000000000000 ) ) ;
#11507=ORIENTED_EDGE ( 'NONE', *, *, #5290, .F. ) ;
#11512=CARTESIAN_POINT ( 'NONE',  ( -1.776015597772149013, 0.5249316475426857309, 0.6288076367337267492 ) ) ;
#11513=EDGE_LOOP ( 'NONE', ( #35371, #36602, #28545, #23968 ) ) ;
#11517=AXIS2_PLACEMENT_3D ( 'NONE', #40527, #40784, #16781 ) ;
#11519=EDGE_LOOP ( 'NONE', ( #39414, #34696, #45526, #22041 ) ) ;
#11520=CARTESIAN_POINT ( 'NONE',  ( -2.932638728931780125, 5.905511811023623991, 0.3475908556737787314 ) ) ;
#11521=ADVANCED_FACE ( 'NONE', ( #45691 ), #10357, .T. ) ;
#11523=B_SPLINE_CURVE_WITH_KNOTS ( 'NONE', 3,
 ( #49046, #36976, #36462, #48285 ),
 .UNSPECIFIED., .F., .F.,
 ( 4, 4 ),
 ( 0.01141953369039028915, 0.03073634068572588668 ),
 .UNSPECIFIED. ) ;
#11525=CARTESIAN_POINT ( 'NONE',  ( 0.04921259842519669359, 1.621581020286960051, 2.952755905511811108 ) ) ;
#11534=CARTESIAN_POINT ( 'NONE',  ( 0.6150616064519864867, 0.03777100275179151589, 1.778883059170359493 ) ) ;
#11536=EDGE_LOOP ( 'NONE', ( #5022, #49162, #46160, #48607 ) ) ;
#11537=DIRECTION ( 'NONE',  ( 0.9749279121818259508, 0.000000000000000000, -0.2225209339563041788 ) ) ;
#11539=VERTEX_POINT ( 'NONE', #34615 ) ;
#11542=CARTESIAN_POINT ( 'NONE',  ( -1.405664884363581502, 1.586962458333645021, 1.683711065981816857 ) ) ;
#11543=CARTESIAN_POINT ( 'NONE',  ( -1.387241876633674265, 6.692913385826772199, 1.662624236931676602 ) ) ;
#11544=EDGE_LOOP ( 'NONE', ( #4723, #10092, #49757, #20224 ) ) ;
#11548=ADVANCED_FACE ( 'NONE', ( #45945 ), #34864, .T. ) ;
#11552=EDGE_CURVE ( 'NONE', #21109, #15197, #26353, .T. ) ;
#11559=CARTESIAN_POINT ( 'NONE',  ( -2.793030215715272213, 1.573188339825353665, 0.9592557174602283077 ) ) ;
#11569=DIRECTION ( 'NONE',  ( -0.9998717552508122886, -0.01601477604151181275, 0.000000000000000000 ) ) ;
#11570=ORIENTED_EDGE ( 'NONE', *, *, #27046, .T. ) ;
#11573=CARTESIAN_POINT ( 'NONE',  ( -0.3381173457103609503, 6.692913385826772199, 2.138793126519845877 ) ) ;
#11587=ORIENTED_EDGE ( 'NONE', *, *, #30685, .T. ) ;
#11591=DIRECTION ( 'NONE',  ( -1.729310098864894520E-17, 1.000000000000000000, -1.276627980444842972E-16 ) ) ;
#11593=AXIS2_PLACEMENT_3D ( 'NONE', #10205, #6840, #25955 ) ;
#11594=CIRCLE ( 'NONE', #18205, 2.244934639244525076 ) ;
#11595=CARTESIAN_POINT ( 'NONE',  ( 0.1067246931122726866, 0.02962905676920215767, 0.000000000000000000 ) ) ;
#11596=ORIENTED_EDGE ( 'NONE', *, *, #42809, .F. ) ;
#11602=ORIENTED_EDGE ( 'NONE', *, *, #27769, .F. ) ;
#11609=CARTESIAN_POINT ( 'NONE',  ( 0.000000000000000000, 6.692913385826772199, 0.000000000000000000 ) ) ;
#11610=VERTEX_POINT ( 'NONE', #22989 ) ;
#11612=VERTEX_POINT ( 'NONE', #14225 ) ;
#11613=CARTESIAN_POINT ( 'NONE',  ( 2.136190583516914820, 1.205361022782829114E-17, -0.1451986319116555235 ) ) ;
#11614=DIRECTION ( 'NONE',  ( -0.01601477604151182663, 0.9998717552508123996, -0.000000000000000000 ) ) ;
#11619=CARTESIAN_POINT ( 'NONE',  ( -0.5085650345005219286, 1.025569181085919546, 2.526811340751392354 ) ) ;
#11622=EDGE_CURVE ( 'NONE', #28528, #46686, #29974, .T. ) ;
#11623=CONICAL_SURFACE ( 'NONE', #30586, 2.165354330708661568, 0.2617993877991570129 ) ;
#11625=ADVANCED_FACE ( 'NONE', ( #12381 ), #28513, .T. ) ;
#11627=CARTESIAN_POINT ( 'NONE',  ( 0.4098391620725875262, 1.049866565067838486, 1.982786943644938793 ) ) ;
#11628=PLANE ( 'NONE',  #38225 ) ;
#11632=ADVANCED_FACE ( 'NONE', ( #47194 ), #43093, .T. ) ;
#11634=VERTEX_POINT ( 'NONE', #43860 ) ;
#11639=CARTESIAN_POINT ( 'NONE',  ( 2.623503965249849301, 1.760141956857387724, 1.355882097269874187 ) ) ;
#11642=( BOUNDED_CURVE ( )  B_SPLINE_CURVE ( 3, ( #32635, #20996, #44727, #1882 ),
 .UNSPECIFIED., .F., .F. ) 
 B_SPLINE_CURVE_WITH_KNOTS ( ( 4, 4 ),
 ( 2.670688157552317588, 2.721475174429009325 ),
 .UNSPECIFIED. ) 
 CURVE ( )  GEOMETRIC_REPRESENTATION_ITEM ( )  RATIONAL_B_SPLINE_CURVE ( ( 1.000000000000000000, 0.9997850681263177330, 0.9997850681263177330, 1.000000000000000000 ) ) 
 REPRESENTATION_ITEM ( '' )  );
#11644=CARTESIAN_POINT ( 'NONE',  ( 1.686980615242215098, -1.638433421555315900E-16, 1.408267424185159156 ) ) ;
#11647=CARTESIAN_POINT ( 'NONE',  ( -2.164823134740036181, 1.673236549936605977, -0.04796011690018290446 ) ) ;
#11648=VERTEX_POINT ( 'NONE', #51050 ) ;
#11651=LINE ( 'NONE', #32055, #32521 ) ;
#11654=ORIENTED_EDGE ( 'NONE', *, *, #38435, .F. ) ;
#11655=DIRECTION ( 'NONE',  ( 0.9989930665413144784, -5.247434042673083099E-18, 0.04486483035051863633 ) ) ;
#11656=DIRECTION ( 'NONE',  ( -0.9998717552508122886, -0.01601477604151182316, 0.000000000000000000 ) ) ;
#11657=ORIENTED_EDGE ( 'NONE', *, *, #25041, .F. ) ;
#11658=AXIS2_PLACEMENT_3D ( 'NONE', #33211, #48894, #13586 ) ;
#11660=DIRECTION ( 'NONE',  ( -0.000000000000000000, 1.000000000000000000, -0.000000000000000000 ) ) ;
#11661=AXIS2_PLACEMENT_3D ( 'NONE', #48110, #8653, #5038 ) ;
#11663=DIRECTION ( 'NONE',  ( -0.8805955318567391110, 0.000000000000000000, 0.4738686624729965269 ) ) ;
#11664=ORIENTED_EDGE ( 'NONE', *, *, #7180, .F. ) ;
#11666=CONICAL_SURFACE ( 'NONE', #24052, 2.244934639244524632, 1.554780866114618743 ) ;
#11667=B_SPLINE_CURVE_WITH_KNOTS ( 'NONE', 3,
 ( #3560, #4078, #46886, #11559 ),
 .UNSPECIFIED., .F., .F.,
 ( 4, 4 ),
 ( 4.925214732546996801E-05, 0.05034361238089160584 ),
 .UNSPECIFIED. ) ;
#11670=DIRECTION ( 'NONE',  ( -6.104789737168038204E-17, 1.000000000000000000, -1.134460028949771622E-16 ) ) ;
#11671=AXIS2_PLACEMENT_3D ( 'NONE', #44131, #48734, #49250 ) ;
#11672=VERTEX_POINT ( 'NONE', #11613 ) ;
#11673=CARTESIAN_POINT ( 'NONE',  ( 0.000000000000000000, 1.574803149606302854, 0.000000000000000000 ) ) ;
#11675=VERTEX_POINT ( 'NONE', #27100 ) ;
#11688=DIRECTION ( 'NONE',  ( -0.01601477604151182663, 0.9998717552508123996, -0.000000000000000000 ) ) ;
#11692=CARTESIAN_POINT ( 'NONE',  ( 2.347234779702823460, 1.650446160227867498, -0.9497368662867726741 ) ) ;
#11693=CARTESIAN_POINT ( 'NONE',  ( -1.556712866041156440, 1.694999912340861004, 2.509548638715847435 ) ) ;
#11704=DIRECTION ( 'NONE',  ( -0.9989930665413151445, 0.000000000000000000, 0.04486483035050446017 ) ) ;
#11712=AXIS2_PLACEMENT_3D ( 'NONE', #18561, #29920, #6433 ) ;
#11716=LINE ( 'NONE', #48066, #33363 ) ;
#11721=LINE ( 'NONE', #27460, #8514 ) ;
#11724=CARTESIAN_POINT ( 'NONE',  ( -1.205050450470247725, 0.008618577144216254052, 1.304493073717302165 ) ) ;
#11727=ORIENTED_EDGE ( 'NONE', *, *, #3130, .T. ) ;
#11736=LINE ( 'NONE', #3491, #7247 ) ;
#11740=LINE ( 'NONE', #8126, #444 ) ;
#11741=ADVANCED_FACE ( 'NONE', ( #42845 ), #43606, .F. ) ;
#11743=EDGE_LOOP ( 'NONE', ( #46911, #23339, #8851, #8659 ) ) ;
#11744=VERTEX_POINT ( 'NONE', #23231 ) ;
#11747=ORIENTED_EDGE ( 'NONE', *, *, #41706, .T. ) ;
#11753=CARTESIAN_POINT ( 'NONE',  ( -1.722315009890285964, 1.692409705881639859, -2.398471918869278241 ) ) ;
#11754=CIRCLE ( 'NONE', #43061, 1.743387098533651480 ) ;
#11758=CARTESIAN_POINT ( 'NONE',  ( 0.000000000000000000, 1.574803149606302854, 0.000000000000000000 ) ) ;
#11771=EDGE_CURVE ( 'NONE', #26516, #37629, #18492, .T. ) ;
#11772=DIRECTION ( 'NONE',  ( -0.000000000000000000, -1.000000000000000000, -0.000000000000000000 ) ) ;
#11781=CARTESIAN_POINT ( 'NONE',  ( 0.04921259842519690175, 0.02870789531899127500, 1.849213118431110914 ) ) ;
#11783=AXIS2_PLACEMENT_3D ( 'NONE', #46422, #31220, #219 ) ;
#11786=CARTESIAN_POINT ( 'NONE',  ( -0.7869067874564349419, 0.000000000000000000, -1.671666005015433276 ) ) ;
#11789=CARTESIAN_POINT ( 'NONE',  ( 2.283576142937052467, 0.5219377364620079174, -0.1518177250174685688 ) ) ;
#11790=CARTESIAN_POINT ( 'NONE',  ( 0.3015460593140593115, 0.000000000000000000, 1.937268728265797213 ) ) ;
#11791=AXIS2_PLACEMENT_3D ( 'NONE', #27779, #4047, #35539 ) ;
#11793=VERTEX_POINT ( 'NONE', #45830 ) ;
#11804=CARTESIAN_POINT ( 'NONE',  ( 1.836342932631641167, 0.000000000000000000, 1.044063857347276469 ) ) ;
#11807=DIRECTION ( 'NONE',  ( -0.000000000000000000, -1.000000000000000000, -0.000000000000000000 ) ) ;
#11814=ORIENTED_EDGE ( 'NONE', *, *, #9889, .T. ) ;
#11815=VERTEX_POINT ( 'NONE', #9278 ) ;
#11825=CARTESIAN_POINT ( 'NONE',  ( 1.771435203777392386, 1.736274727556916808, 1.475617711110977615 ) ) ;
#11827=CARTESIAN_POINT ( 'NONE',  ( -1.843472447131334624, 1.579950168977349412, -1.157898127912315944 ) ) ;
#11829=CARTESIAN_POINT ( 'NONE',  ( 0.08139965876239094178, 1.610780518492231694, 0.000000000000000000 ) ) ;
#11832=CARTESIAN_POINT ( 'NONE',  ( 2.100227814008711391, 1.467797480264206866, -2.076109931251913565 ) ) ;
#11837=LINE ( 'NONE', #3335, #4669 ) ;
#11838=CARTESIAN_POINT ( 'NONE',  ( -2.949046704851476353, 1.673284050348918583, -0.1488625813693291167 ) ) ;
#11840=EDGE_CURVE ( 'NONE', #38140, #22211, #38006, .T. ) ;
#11841=CARTESIAN_POINT ( 'NONE',  ( 2.695799277629594037, 1.662794757381320654, -1.205759334241453651 ) ) ;
#11842=ADVANCED_FACE ( 'NONE', ( #37168 ), #3791, .T. ) ;
#11848=ORIENTED_EDGE ( 'NONE', *, *, #2503, .T. ) ;
#11850=CIRCLE ( 'NONE', #10211, 1.850107469027523432 ) ;
#11857=ORIENTED_EDGE ( 'NONE', *, *, #36304, .F. ) ;
#11858=EDGE_CURVE ( 'NONE', #380, #12101, #41986, .T. ) ;
#11859=EDGE_CURVE ( 'NONE', #38271, #196, #21412, .T. ) ;
#11862=EDGE_CURVE ( 'NONE', #12327, #34870, #33047, .T. ) ;
#11869=CARTESIAN_POINT ( 'NONE',  ( 1.930249146414562578, 0.05883613814988478824, 0.3111320644955062886 ) ) ;
#11874=DIRECTION ( 'NONE',  ( 0.000000000000000000, 0.000000000000000000, -1.000000000000000000 ) ) ;
#11877=CARTESIAN_POINT ( 'NONE',  ( 2.932638728931774352, 1.447899366913586672, 0.3475908556738225297 ) ) ;
#11883=VERTEX_POINT ( 'NONE', #32791 ) ;
#11885=ORIENTED_EDGE ( 'NONE', *, *, #31265, .T. ) ;
#11900=CARTESIAN_POINT ( 'NONE',  ( -0.3136974817027967100, 1.522126940893053337, -2.936457595020224520 ) ) ;
#11902=ORIENTED_EDGE ( 'NONE', *, *, #29400, .T. ) ;
#11904=CARTESIAN_POINT ( 'NONE',  ( -1.551823387637203178, 1.049866565067837820, 1.300483131855000529 ) ) ;
#11909=CARTESIAN_POINT ( 'NONE',  ( 1.387241876633648285, 6.692913385826772199, 1.662624236931697919 ) ) ;
#11914=VERTEX_POINT ( 'NONE', #3001 ) ;
#11915=DIRECTION ( 'NONE',  ( -0.000000000000000000, 1.000000000000000000, -0.000000000000000000 ) ) ;
#11918=VERTEX_POINT ( 'NONE', #26479 ) ;
#11922=EDGE_CURVE ( 'NONE', #7866, #20944, #1695, .T. ) ;
#11925=DIRECTION ( 'NONE',  ( -0.8584487936018727616, 0.000000000000000000, 0.5128992774058948045 ) ) ;
#11926=ORIENTED_EDGE ( 'NONE', *, *, #27624, .T. ) ;
#11932=DIRECTION ( 'NONE',  ( 0.01601477604151182663, -0.9998717552508123996, 0.000000000000000000 ) ) ;
#11933=ORIENTED_EDGE ( 'NONE', *, *, #26620, .F. ) ;
#11935=ORIENTED_EDGE ( 'NONE', *, *, #6968, .F. ) ;
#11937=CARTESIAN_POINT ( 'NONE',  ( -1.662320194739477675, 5.905511811023623991, -1.388601395075574896 ) ) ;
#11940=ORIENTED_EDGE ( 'NONE', *, *, #19592, .T. ) ;
#11942=CARTESIAN_POINT ( 'NONE',  ( 0.3344856439320825214, 0.000000000000000000, 1.935533671922775145 ) ) ;
#11943=CARTESIAN_POINT ( 'NONE',  ( 0.000000000000000000, 6.692913385826772199, 0.000000000000000000 ) ) ;
#11948=CARTESIAN_POINT ( 'NONE',  ( 0.3543214468173200293, 1.713577057256821190, 2.228085083314873316 ) ) ;
#11951=CARTESIAN_POINT ( 'NONE',  ( 2.755905511811024056, 2.913385826771657250, -1.023622047244094224 ) ) ;
#11959=CARTESIAN_POINT ( 'NONE',  ( -0.4892674838277497606, 1.703934057431762739, 2.420473071843689983 ) ) ;
#11967=VECTOR ( 'NONE', #1542, 39.37007874015748143 ) ;
#11968=VECTOR ( 'NONE', #487, 39.37007874015748143 ) ;
#11972=AXIS2_PLACEMENT_3D ( 'NONE', #1650, #48848, #45005 ) ;
#11973=B_SPLINE_CURVE_WITH_KNOTS ( 'NONE', 3,
 ( #5056, #149, #15898, #43516 ),
 .UNSPECIFIED., .F., .F.,
 ( 4, 4 ),
 ( 3.418973662664240344E-07, 0.04653147169244552933 ),
 .UNSPECIFIED. ) ;
#11974=CARTESIAN_POINT ( 'NONE',  ( -1.236813753895213086, 1.601547340627394567, -2.681693691597581974 ) ) ;
#11975=DIRECTION ( 'NONE',  ( 0.9510565162951500895, -3.590656546124792943E-17, 0.3090169943749582204 ) ) ;
#11977=ORIENTED_EDGE ( 'NONE', *, *, #19942, .T. ) ;
#11979=EDGE_CURVE ( 'NONE', #19240, #6809, #14523, .T. ) ;
#11980=DIRECTION ( 'NONE',  ( -0.01601477604151182663, 0.9998717552508123996, -0.000000000000000000 ) ) ;
#11984=CARTESIAN_POINT ( 'NONE',  ( 1.942974145993213053, 1.745987691644603323, -1.925760030027876990 ) ) ;
#11985=LINE ( 'NONE', #27218, #10661 ) ;
#11986=ORIENTED_EDGE ( 'NONE', *, *, #35882, .T. ) ;
#11992=ORIENTED_EDGE ( 'NONE', *, *, #5458, .F. ) ;
#11994=ORIENTED_EDGE ( 'NONE', *, *, #26876, .F. ) ;
#11999=ORIENTED_EDGE ( 'NONE', *, *, #12739, .F. ) ;
#12005=ORIENTED_EDGE ( 'NONE', *, *, #16165, .T. ) ;
#12007=CARTESIAN_POINT ( 'NONE',  ( -2.695799277629576718, 5.905511811023623991, -1.205759334241493175 ) ) ;
#12008=CARTESIAN_POINT ( 'NONE',  ( -1.405548054723555707, 1.619772730168859365, 1.683577343699150575 ) ) ;
#12014=CARTESIAN_POINT ( 'NONE',  ( 0.000000000000000000, 2.755905511811027164, 0.000000000000000000 ) ) ;
#12020=ORIENTED_EDGE ( 'NONE', *, *, #18697, .F. ) ;
#12021=CARTESIAN_POINT ( 'NONE',  ( -2.277873973731453727, 1.562946399538843290, 1.879489153247635214 ) ) ;
#12023=ORIENTED_EDGE ( 'NONE', *, *, #37798, .T. ) ;
#12025=VERTEX_POINT ( 'NONE', #26735 ) ;
#12029=EDGE_CURVE ( 'NONE', #7052, #10796, #44741, .T. ) ;
#12032=CARTESIAN_POINT ( 'NONE',  ( 0.8329809839909850799, 1.633788288308783976, -2.833254665166554442 ) ) ;
#12033=EDGE_CURVE ( 'NONE', #15466, #48433, #4517, .T. ) ;
#12037=CARTESIAN_POINT ( 'NONE',  ( 2.734482843737263025, 0.000000000000000000, -1.115254632218672937 ) ) ;
#12038=LINE ( 'NONE', #35283, #28634 ) ;
#12048=CYLINDRICAL_SURFACE ( 'NONE', #21183, 2.165354330708661568 ) ;
#12049=ORIENTED_EDGE ( 'NONE', *, *, #50736, .T. ) ;
#12050=CARTESIAN_POINT ( 'NONE',  ( -1.740978969773838037, 0.000000000000000000, 0.09160132170885167124 ) ) ;
#12053=FACE_OUTER_BOUND ( 'NONE', #28231, .T. ) ;
#12054=AXIS2_PLACEMENT_3D ( 'NONE', #45323, #30371, #49433 ) ;
#12059=CARTESIAN_POINT ( 'NONE',  ( 1.630393911741433000, 1.635590496292660179, -1.626902725537468619 ) ) ;
#12069=EDGE_CURVE ( 'NONE', #7241, #23605, #35504, .T. ) ;
#12075=CARTESIAN_POINT ( 'NONE',  ( 0.000000000000000000, 6.692913385826772199, 0.000000000000000000 ) ) ;
#12078=ORIENTED_EDGE ( 'NONE', *, *, #28475, .F. ) ;
#12087=LINE ( 'NONE', #12595, #8351 ) ;
#12088=CONICAL_SURFACE ( 'NONE', #12946, 2.244934639244524632, 1.554780866114618743 ) ;
#12089=ADVANCED_FACE ( 'NONE', ( #8900 ), #24655, .F. ) ;
#12091=ORIENTED_EDGE ( 'NONE', *, *, #44921, .F. ) ;
#12092=CARTESIAN_POINT ( 'NONE',  ( 0.1946224253818716055, 1.718530757508495155, -2.711439145546752805 ) ) ;
#12100=ORIENTED_EDGE ( 'NONE', *, *, #50894, .F. ) ;
#12101=VERTEX_POINT ( 'NONE', #13037 ) ;
#12102=CARTESIAN_POINT ( 'NONE',  ( -1.477691947303356290, 1.684234009953186728, 1.616556376299586706 ) ) ;
#12105=FACE_OUTER_BOUND ( 'NONE', #26520, .T. ) ;
#12108=EDGE_CURVE ( 'NONE', #38164, #18815, #24138, .T. ) ;
#12112=ORIENTED_EDGE ( 'NONE', *, *, #16826, .F. ) ;
#12113=AXIS2_PLACEMENT_3D ( 'NONE', #39978, #4610, #24235 ) ;
#12116=VERTEX_POINT ( 'NONE', #47843 ) ;
#12118=LINE ( 'NONE', #39741, #45145 ) ;
#12121=ORIENTED_EDGE ( 'NONE', *, *, #32225, .F. ) ;
#12122=ADVANCED_FACE ( 'NONE', ( #15871 ), #16397, .F. ) ;
#12124=VERTEX_POINT ( 'NONE', #12007 ) ;
#12130=ORIENTED_EDGE ( 'NONE', *, *, #9620, .T. ) ;
#12132=ORIENTED_EDGE ( 'NONE', *, *, #41942, .T. ) ;
#12133=ORIENTED_EDGE ( 'NONE', *, *, #9881, .F. ) ;
#12143=CONICAL_SURFACE ( 'NONE', #31094, 2.246510896728926010, 0.01601546068027819014 ) ;
#12144=ORIENTED_EDGE ( 'NONE', *, *, #5179, .T. ) ;
#12148=ORIENTED_EDGE ( 'NONE', *, *, #14086, .F. ) ;
#12154=LINE ( 'NONE', #12930, #14004 ) ;
#12155=ORIENTED_EDGE ( 'NONE', *, *, #13034, .T. ) ;
#12161=CARTESIAN_POINT ( 'NONE',  ( -2.464291103507776359, 5.905511811023623991, -1.626664315311337594 ) ) ;
#12167=LINE ( 'NONE', #12423, #2131 ) ;
#12172=DIRECTION ( 'NONE',  ( 5.500355109725808462E-17, -1.000000000000000000, -1.022137253806221654E-16 ) ) ;
#12173=CIRCLE ( 'NONE', #39382, 2.246510896728926010 ) ;
#12181=CARTESIAN_POINT ( 'NONE',  ( 1.138972962972652603, 1.733361078862474258, -2.478525195789229585 ) ) ;
#12185=FACE_OUTER_BOUND ( 'NONE', #42986, .T. ) ;
#12188=EDGE_CURVE ( 'NONE', #32849, #40833, #35526, .T. ) ;
#12194=LINE ( 'NONE', #8319, #38119 ) ;
#12197=ORIENTED_EDGE ( 'NONE', *, *, #1824, .F. ) ;
#12199=CARTESIAN_POINT ( 'NONE',  ( -1.236813753895212642, 1.541669022091038732, -2.681693691597581974 ) ) ;
#12201=CARTESIAN_POINT ( 'NONE',  ( -2.748374859398606596, 2.755905511811027164, -0.3226306186023588096 ) ) ;
#12202=VECTOR ( 'NONE', #18146, 39.37007874015748854 ) ;
#12219=AXIS2_PLACEMENT_3D ( 'NONE', #7550, #43152, #39294 ) ;
#12223=ORIENTED_EDGE ( 'NONE', *, *, #857, .T. ) ;
#12225=EDGE_CURVE ( 'NONE', #5907, #48573, #31229, .T. ) ;
#12228=CYLINDRICAL_SURFACE ( 'NONE', #1214, 2.165354330708661568 ) ;
#12231=VECTOR ( 'NONE', #38143, 39.37007874015748143 ) ;
#12232=FACE_OUTER_BOUND ( 'NONE', #25481, .T. ) ;
#12233=CARTESIAN_POINT ( 'NONE',  ( -0.04921259842519689481, 0.000000000000000000, 2.952755905511811108 ) ) ;
#12237=DIRECTION ( 'NONE',  ( -3.986037398843765983E-20, -1.000000000000000000, -1.160734090543304660E-16 ) ) ;
#12239=DIRECTION ( 'NONE',  ( 0.000000000000000000, 0.000000000000000000, -1.000000000000000000 ) ) ;
#12244=DIRECTION ( 'NONE',  ( -3.986037398843765983E-20, -1.000000000000000000, -1.160734090543304660E-16 ) ) ;
#12248=CARTESIAN_POINT ( 'NONE',  ( 0.2810212964504857913, 1.625182864229780533, -2.939398504922494215 ) ) ;
#12252=DIRECTION ( 'NONE',  ( 0.01601477604151182663, -0.9998717552508123996, 0.000000000000000000 ) ) ;
#12260=CARTESIAN_POINT ( 'NONE',  ( 1.556712866041120469, 1.205361022782829114E-17, 2.509548638715870084 ) ) ;
#12261=B_SPLINE_CURVE_WITH_KNOTS ( 'NONE', 3,
 ( #3042, #49726, #38418, #34544 ),
 .UNSPECIFIED., .F., .F.,
 ( 4, 4 ),
 ( 0.01088822282284627151, 0.03073585682641423455 ),
 .UNSPECIFIED. ) ;
#12264=CARTESIAN_POINT ( 'NONE',  ( 1.810607833951273227, 0.05691986357332023266, -0.7203715021987137090 ) ) ;
#12265=DIRECTION ( 'NONE',  ( -1.267583980596140612E-16, 1.000000000000000000, 2.300325776299552367E-17 ) ) ;
#12270=ORIENTED_EDGE ( 'NONE', *, *, #21384, .T. ) ;
#12272=B_SPLINE_CURVE_WITH_KNOTS ( 'NONE', 3,
 ( #31692, #38928, #7435, #3304 ),
 .UNSPECIFIED., .F., .F.,
 ( 4, 4 ),
 ( 0.1211873102087489551, 0.1625992483279400103 ),
 .UNSPECIFIED. ) ;
#12274=CARTESIAN_POINT ( 'NONE',  ( -2.044241703397525978, 5.905511811023623991, -0.7159595814952903758 ) ) ;
#12285=LINE ( 'NONE', #32426, #27507 ) ;
#12287=EDGE_LOOP ( 'NONE', ( #49488, #48853, #9894, #26991 ) ) ;
#12288=ORIENTED_EDGE ( 'NONE', *, *, #13617, .T. ) ;
#12294=CARTESIAN_POINT ( 'NONE',  ( 2.134236802639954522, 5.905511811023623991, -2.040539317874580760 ) ) ;
#12296=AXIS2_PLACEMENT_3D ( 'NONE', #16068, #19169, #11436 ) ;
#12309=FACE_OUTER_BOUND ( 'NONE', #22995, .T. ) ;
#12310=CARTESIAN_POINT ( 'NONE',  ( 1.919085105436704630, 0.01897331389017133801, -0.7667369131541573735 ) ) ;
#12311=AXIS2_PLACEMENT_3D ( 'NONE', #13529, #17907, #45001 ) ;
#12313=CARTESIAN_POINT ( 'NONE',  ( -1.494044303739022972, 0.003989811691878806209, -0.9272426299426647089 ) ) ;
#12317=FACE_OUTER_BOUND ( 'NONE', #1832, .T. ) ;
#12318=LINE ( 'NONE', #27794, #23458 ) ;
#12322=ORIENTED_EDGE ( 'NONE', *, *, #9372, .F. ) ;
#12325=ORIENTED_EDGE ( 'NONE', *, *, #7438, .T. ) ;
#12326=CARTESIAN_POINT ( 'NONE',  ( 2.165460538733997353, 0.000000000000000000, 0.04798874274655835076 ) ) ;
#12327=VERTEX_POINT ( 'NONE', #42915 ) ;
#12329=CARTESIAN_POINT ( 'NONE',  ( 0.7759887336347247588, 0.04034854520891290042, -1.724780676950718794 ) ) ;
#12333=B_SPLINE_CURVE_WITH_KNOTS ( 'NONE', 3,
 ( #35995, #40631, #43971, #39607 ),
 .UNSPECIFIED., .F., .F.,
 ( 4, 4 ),
 ( 0.01470896166604594366, 0.03075119253503404149 ),
 .UNSPECIFIED. ) ;
#12338=VECTOR ( 'NONE', #2637, 39.37007874015748143 ) ;
#12343=PLANE ( 'NONE',  #4218 ) ;
#12344=CARTESIAN_POINT ( 'NONE',  ( -1.843283979527560623, 1.678378384481335139, -1.157773721536293765 ) ) ;
#12348=DIRECTION ( 'NONE',  ( -0.9998717552508122886, -0.01601477604151181275, 0.000000000000000000 ) ) ;
#12350=CARTESIAN_POINT ( 'NONE',  ( 2.592410251778310748, 1.661176152998282918, 1.413663899107065580 ) ) ;
#12351=DIRECTION ( 'NONE',  ( -1.000000000000000000, 0.000000000000000000, -0.000000000000000000 ) ) ;
#12357=CARTESIAN_POINT ( 'NONE',  ( 1.979793062125284608, 1.750113821271474857, 2.191257344206569257 ) ) ;
#12359=CARTESIAN_POINT ( 'NONE',  ( -1.662150612268487704, 1.049866565877817237, -1.156143393213623360 ) ) ;
#12360=DIRECTION ( 'NONE',  ( -0.9998717552508122886, -0.01601477604151180928, 0.000000000000000000 ) ) ;
#12367=CARTESIAN_POINT ( 'NONE',  ( -1.684292108503797181, -1.610880632035666997E-16, 1.406123411605399998 ) ) ;
#12369=DIRECTION ( 'NONE',  ( 0.01601477604151182663, -0.9998717552508123996, 0.000000000000000000 ) ) ;
#12370=DIRECTION ( 'NONE',  ( 0.9998717552508121775, 0.01601477604151182663, 0.000000000000000000 ) ) ;
#12371=ORIENTED_EDGE ( 'NONE', *, *, #42658, .F. ) ;
#12375=EDGE_CURVE ( 'NONE', #25092, #20098, #47176, .T. ) ;
#12379=ORIENTED_EDGE ( 'NONE', *, *, #7911, .T. ) ;
#12381=FACE_OUTER_BOUND ( 'NONE', #17450, .T. ) ;
#12382=CARTESIAN_POINT ( 'NONE',  ( 2.867773316779195447, 1.449472587384593725, -0.7050287376752005786 ) ) ;
#12384=EDGE_CURVE ( 'NONE', #40028, #11918, #15312, .T. ) ;
#12385=PLANE ( 'NONE',  #43631 ) ;
#12386=ORIENTED_EDGE ( 'NONE', *, *, #43057, .T. ) ;
#12388=DIRECTION ( 'NONE',  ( 0.000000000000000000, 0.000000000000000000, 1.000000000000000000 ) ) ;
#12394=EDGE_LOOP ( 'NONE', ( #21395, #45726, #8065, #16723 ) ) ;
#12396=EDGE_CURVE ( 'NONE', #37702, #25844, #27174, .T. ) ;
#12401=LINE ( 'NONE', #16021, #18550 ) ;
#12405=EDGE_CURVE ( 'NONE', #46197, #47793, #15852, .T. ) ;
#12408=ORIENTED_EDGE ( 'NONE', *, *, #11840, .T. ) ;
#12410=CARTESIAN_POINT ( 'NONE',  ( -1.528806138047155150, 0.001175590193779177828, 0.8785712512199921331 ) ) ;
#12416=DIRECTION ( 'NONE',  ( -0.01601477604151182663, 0.9998717552508123996, -0.000000000000000000 ) ) ;
#12417=CARTESIAN_POINT ( 'NONE',  ( -0.9914495361339012991, 5.905511811023623991, 2.781765111341808705 ) ) ;
#12422=CARTESIAN_POINT ( 'NONE',  ( -2.100227814008681637, 1.559371130916006543, -2.076109931251943319 ) ) ;
#12423=CARTESIAN_POINT ( 'NONE',  ( -2.949782676795219771, 5.905511811023623991, -0.1324748927672787513 ) ) ;
#12424=ORIENTED_EDGE ( 'NONE', *, *, #14378, .T. ) ;
#12428=CYLINDRICAL_SURFACE ( 'NONE', #13173, 2.165354330708661568 ) ;
#12429=VERTEX_POINT ( 'NONE', #50369 ) ;
#12431=FACE_OUTER_BOUND ( 'NONE', #35641, .T. ) ;
#12436=VECTOR ( 'NONE', #49020, 39.37007874015748143 ) ;
#12437=DIRECTION ( 'NONE',  ( -0.01601477604151182663, 0.9998717552508123996, -0.000000000000000000 ) ) ;
#12438=DIRECTION ( 'NONE',  ( -0.9998717552508122886, -0.01601477604151181275, 0.000000000000000000 ) ) ;
#12447=ORIENTED_EDGE ( 'NONE', *, *, #6590, .F. ) ;
#12454=DIRECTION ( 'NONE',  ( -3.986037398843765983E-20, -1.000000000000000000, -1.160734090543304660E-16 ) ) ;
#12463=ORIENTED_EDGE ( 'NONE', *, *, #43148, .F. ) ;
#12487=CARTESIAN_POINT ( 'NONE',  ( 0.07982360342473591996, 1.709180471932028711, 0.000000000000000000 ) ) ;
#12488=EDGE_CURVE ( 'NONE', #46309, #5934, #48195, .T. ) ;
#12491=FACE_OUTER_BOUND ( 'NONE', #16245, .T. ) ;
#12504=CARTESIAN_POINT ( 'NONE',  ( 1.068075307999460488, 1.574803149606302854, 1.883606783264653028 ) ) ;
#12507=EDGE_CURVE ( 'NONE', #36108, #810, #37638, .T. ) ;
#12509=EDGE_LOOP ( 'NONE', ( #15075, #258, #48530, #26905, #16322, #28394, #1268, #43993, #44119, #25667, #41061 ) ) ;
#12511=CARTESIAN_POINT ( 'NONE',  ( 0.000000000000000000, 0.000000000000000000, 0.000000000000000000 ) ) ;
#12512=CARTESIAN_POINT ( 'NONE',  ( -2.277873973731453727, 1.585326468414270495, 1.879489153247635214 ) ) ;
#12516=CARTESIAN_POINT ( 'NONE',  ( 0.07982360342473591996, 1.709180471932028711, 0.000000000000000000 ) ) ;
#12522=CARTESIAN_POINT ( 'NONE',  ( -1.001904449526793695, 1.691854617476330036, -1.967052558704270426 ) ) ;
#12524=CARTESIAN_POINT ( 'NONE',  ( -2.010517631316633747, 1.205361022782829114E-17, 0.8058170502102087740 ) ) ;
#12530=ORIENTED_EDGE ( 'NONE', *, *, #39249, .F. ) ;
#12534=VECTOR ( 'NONE', #21339, 39.37007874015748143 ) ;
#12539=ORIENTED_EDGE ( 'NONE', *, *, #15237, .F. ) ;
#12557=CARTESIAN_POINT ( 'NONE',  ( -0.1516866087075746383, 1.607047215343822222, -2.234383150555500297 ) ) ;
#12561=CARTESIAN_POINT ( 'NONE',  ( 1.109524193798303804, 0.000000000000000000, 1.344750771968474590 ) ) ;
#12562=FACE_OUTER_BOUND ( 'NONE', #50828, .T. ) ;
#12564=ORIENTED_EDGE ( 'NONE', *, *, #10302, .F. ) ;
#12566=CARTESIAN_POINT ( 'NONE',  ( 0.000000000000000000, 6.692913385826772199, 0.000000000000000000 ) ) ;
#12570=CARTESIAN_POINT ( 'NONE',  ( 1.695772546416037363, 1.647224322255602891, -2.417756147381349141 ) ) ;
#12573=CARTESIAN_POINT ( 'NONE',  ( 0.07982360342473591996, 1.709180471932028711, 0.000000000000000000 ) ) ;
#12577=ORIENTED_EDGE ( 'NONE', *, *, #49487, .T. ) ;
#12579=ADVANCED_FACE ( 'NONE', ( #47777 ), #31568, .T. ) ;
#12582=B_SPLINE_CURVE_WITH_KNOTS ( 'NONE', 3,
 ( #15455, #27060, #6950, #34075 ),
 .UNSPECIFIED., .F., .F.,
 ( 4, 4 ),
 ( 2.655830299951649833E-07, 0.01930353374404481653 ),
 .UNSPECIFIED. ) ;
#12591=AXIS2_PLACEMENT_3D ( 'NONE', #7958, #204, #15954 ) ;
#12595=CARTESIAN_POINT ( 'NONE',  ( 2.151809081513405442, 6.692913385826772199, 0.2418202932658665705 ) ) ;
#12605=EDGE_CURVE ( 'NONE', #21303, #209, #50244, .T. ) ;
#12606=DIRECTION ( 'NONE',  ( 0.5508969814521065267, 0.000000000000000000, -0.8345732537212999791 ) ) ;
#12611=CARTESIAN_POINT ( 'NONE',  ( 2.009025172380753066, 0.000000000000000000, 0.7045170369349440520 ) ) ;
#12620=DIRECTION ( 'NONE',  ( -0.000000000000000000, -1.000000000000000000, -0.000000000000000000 ) ) ;
#12623=EDGE_CURVE ( 'NONE', #43507, #44778, #5474, .T. ) ;
#12624=VERTEX_POINT ( 'NONE', #21990 ) ;
#12629=DIRECTION ( 'NONE',  ( 0.9749279121818259508, 0.000000000000000000, -0.2225209339563041788 ) ) ;
#12631=PLANE ( 'NONE',  #7627 ) ;
#12642=CARTESIAN_POINT ( 'NONE',  ( 1.604245399104406111, 0.5221609200332525402, -1.601902187605692918 ) ) ;
#12645=DIRECTION ( 'NONE',  ( -0.9839295885986295565, 0.000000000000000000, -0.1785568947986370392 ) ) ;
#12648=CARTESIAN_POINT ( 'NONE',  ( 1.753307453716355324, 0.9966445008960358454, 1.932023706743397184 ) ) ;
#12650=DIRECTION ( 'NONE',  ( 8.902872254219889125E-17, 1.000000000000000000, 9.311674343991287120E-17 ) ) ;
#12652=DIRECTION ( 'NONE',  ( -1.598721155460225418E-14, 0.000000000000000000, 1.000000000000000000 ) ) ;
#12654=CARTESIAN_POINT ( 'NONE',  ( -2.623503965249869729, 5.905511811023623991, 1.355882097269834663 ) ) ;
#12658=CARTESIAN_POINT ( 'NONE',  ( 2.170993901765784440, 1.749570721460282696, 1.668364588115243130 ) ) ;
#12661=CARTESIAN_POINT ( 'NONE',  ( 0.4349608091550758449, 6.692913385826772199, 2.121218629000301004 ) ) ;
#12664=CIRCLE ( 'NONE', #274, 2.165354330708661568 ) ;
#12669=AXIS2_PLACEMENT_3D ( 'NONE', #17777, #11299, #47125 ) ;
#12670=ADVANCED_FACE ( 'NONE', ( #44951 ), #41107, .T. ) ;
#12675=VECTOR ( 'NONE', #13255, 39.37007874015748143 ) ;
#12677=ADVANCED_FACE ( 'NONE', ( #5978 ), #25598, .T. ) ;
#12681=VERTEX_POINT ( 'NONE', #48544 ) ;
#12686=DIRECTION ( 'NONE',  ( 0.8805955318567391110, 5.496845023002422681E-17, -0.4738686624729965269 ) ) ;
#12691=B_SPLINE_CURVE_WITH_KNOTS ( 'NONE', 3,
 ( #24310, #36191, #36445, #39799 ),
 .UNSPECIFIED., .F., .F.,
 ( 4, 4 ),
 ( 0.1211873102087489551, 0.1625992483279400380 ),
 .UNSPECIFIED. ) ;
#12693=ORIENTED_EDGE ( 'NONE', *, *, #32991, .T. ) ;
#12698=CARTESIAN_POINT ( 'NONE',  ( 0.8318848978143555950, 1.626432784511790963, 2.356606652973837424 ) ) ;
#12701=ORIENTED_EDGE ( 'NONE', *, *, #14671, .T. ) ;
#12704=ORIENTED_EDGE ( 'NONE', *, *, #30531, .T. ) ;
#12705=CARTESIAN_POINT ( 'NONE',  ( -2.047277537895663801, 1.675111054312220515, 0.7169459839182066307 ) ) ;
#12706=AXIS2_PLACEMENT_3D ( 'NONE', #32820, #9820, #25559 ) ;
#12707=ORIENTED_EDGE ( 'NONE', *, *, #2186, .F. ) ;
#12708=ORIENTED_EDGE ( 'NONE', *, *, #21854, .F. ) ;
#12709=AXIS2_PLACEMENT_3D ( 'NONE', #28727, #20991, #48571 ) ;
#12710=CARTESIAN_POINT ( 'NONE',  ( -1.325491792074585451, 1.543512378121542961, -2.638988599164751925 ) ) ;
#12712=CARTESIAN_POINT ( 'NONE',  ( 2.932638728931774352, 1.666481914436860334, 0.3475908556738225297 ) ) ;
#12719=DIRECTION ( 'NONE',  ( -0.9998717552508122886, -0.01601477604151182316, 0.000000000000000000 ) ) ;
#12720=ORIENTED_EDGE ( 'NONE', *, *, #16570, .F. ) ;
#12721=CARTESIAN_POINT ( 'NONE',  ( -2.734482843737247038, 1.676638068352269029, -1.115254632218712016 ) ) ;
#12725=CARTESIAN_POINT ( 'NONE',  ( -2.633954527054724437, 1.575688309503748830, -0.5507047405504611470 ) ) ;
#12726=ORIENTED_EDGE ( 'NONE', *, *, #8777, .F. ) ;
#12728=CARTESIAN_POINT ( 'NONE',  ( -2.339241080213612101, 1.584370211609867685, 1.802537235681884065 ) ) ;
#12730=DIRECTION ( 'NONE',  ( -0.01601477604151182663, 0.9998717552508123996, -0.000000000000000000 ) ) ;
#12736=VERTEX_POINT ( 'NONE', #45701 ) ;
#12739=EDGE_CURVE ( 'NONE', #26290, #22720, #26111, .T. ) ;
#12740=B_SPLINE_CURVE_WITH_KNOTS ( 'NONE', 3,
 ( #2142, #32374, #22274, #42638 ),
 .UNSPECIFIED., .F., .F.,
 ( 4, 4 ),
 ( 6.194644966465025756E-07, 0.001846361613927027844 ),
 .UNSPECIFIED. ) ;
#12744=CIRCLE ( 'NONE', #42399, 2.244934639244525076 ) ;
#12752=AXIS2_PLACEMENT_3D ( 'NONE', #27030, #7675, #23672 ) ;
#12753=AXIS2_PLACEMENT_3D ( 'NONE', #36120, #750, #16500 ) ;
#12759=ORIENTED_EDGE ( 'NONE', *, *, #31958, .F. ) ;
#12762=CARTESIAN_POINT ( 'NONE',  ( -2.426831398316064980, 1.574814413673615521, -0.05972692158529400303 ) ) ;
#12767=CARTESIAN_POINT ( 'NONE',  ( 2.193564619503452828, 1.644610705845120258, 0.7644775380370429918 ) ) ;
#12769=CARTESIAN_POINT ( 'NONE',  ( 0.07982360342473591996, 1.709180471932028711, 0.000000000000000000 ) ) ;
#12773=EDGE_CURVE ( 'NONE', #36153, #18093, #36127, .T. ) ;
#12775=VERTEX_POINT ( 'NONE', #42105 ) ;
#12781=CARTESIAN_POINT ( 'NONE',  ( 2.255357468390372322, 1.645600431408117847, -0.5652488166673508285 ) ) ;
#12782=EDGE_CURVE ( 'NONE', #32538, #3117, #19392, .T. ) ;
#12783=DIRECTION ( 'NONE',  ( -0.9998717552508122886, -0.01601477604151185785, 0.000000000000000000 ) ) ;
#12785=EDGE_LOOP ( 'NONE', ( #1489, #35837, #10445, #4855, #35524, #5834, #33685, #13685, #43164, #7437, #1077 ) ) ;
#12788=CARTESIAN_POINT ( 'NONE',  ( 2.088343298084792021, 6.692913385826772199, 0.6267986818430609786 ) ) ;
#12789=B_SPLINE_CURVE_WITH_KNOTS ( 'NONE', 3,
 ( #32562, #4668, #16549, #28922 ),
 .UNSPECIFIED., .F., .F.,
 ( 4, 4 ),
 ( 0.0003468416213337044527, 0.002847000924371759830 ),
 .UNSPECIFIED. ) ;
#12790=CARTESIAN_POINT ( 'NONE',  ( 1.386843392441768241, 1.730114785850798587, -1.825100698618727257 ) ) ;
#12795=CARTESIAN_POINT ( 'NONE',  ( 0.1499993486716910962, 0.5230385143951955529, -2.215636156144062063 ) ) ;
#12796=VECTOR ( 'NONE', #39474, 39.37007874015748143 ) ;
#12801=ADVANCED_FACE ( 'NONE', ( #50304 ), #30745, .T. ) ;
#12807=CARTESIAN_POINT ( 'NONE',  ( -1.083598637574820334, 1.603934357758587614, 2.747180975113330259 ) ) ;
#12808=CARTESIAN_POINT ( 'NONE',  ( 0.7381027496705270252, 1.632310643118564997, -2.859439394060913298 ) ) ;
#12810=EDGE_CURVE ( 'NONE', #39003, #16783, #50811, .T. ) ;
#12812=EDGE_CURVE ( 'NONE', #24660, #48339, #11473, .T. ) ;
#12820=CARTESIAN_POINT ( 'NONE',  ( -0.1198125010151041281, 0.5249316497054294928, -1.880232808544963108 ) ) ;
#12821=DIRECTION ( 'NONE',  ( 9.964307797194671432E-17, -1.000000000000000000, -5.953396763000495864E-17 ) ) ;
#12824=FACE_OUTER_BOUND ( 'NONE', #16501, .T. ) ;
#12825=CARTESIAN_POINT ( 'NONE',  ( 2.308557526972506047, 0.000000000000000000, 1.841013194464792724 ) ) ;
#12826=VECTOR ( 'NONE', #19330, 39.37007874015748143 ) ;
#12828=ORIENTED_EDGE ( 'NONE', *, *, #39829, .T. ) ;
#12842=ORIENTED_EDGE ( 'NONE', *, *, #36577, .F. ) ;
#12845=EDGE_CURVE ( 'NONE', #42204, #7511, #15501, .T. ) ;
#12846=CARTESIAN_POINT ( 'NONE',  ( 0.9297740550868999199, 0.5225294794730628301, -2.044119187424908279 ) ) ;
#12848=VERTEX_POINT ( 'NONE', #27360 ) ;
#12850=EDGE_CURVE ( 'NONE', #30403, #3143, #10883, .T. ) ;
#12851=DIRECTION ( 'NONE',  ( 0.08963930890342654279, 0.000000000000000000, 0.9959742939952397345 ) ) ;
#12859=CARTESIAN_POINT ( 'NONE',  ( 2.793030215715258446, 1.451280567205322836, 0.9592557174602683867 ) ) ;
#12861=CONICAL_SURFACE ( 'NONE', #15324, 2.246510896728926010, 0.01601546068027819014 ) ;
#12863=DIRECTION ( 'NONE',  ( -1.156061316345072978E-16, -1.000000000000000000, -1.040474016969658122E-17 ) ) ;
#12867=EDGE_CURVE ( 'NONE', #9567, #32706, #44104, .T. ) ;
#12868=CARTESIAN_POINT ( 'NONE',  ( 2.164658444855302122, 5.905511811023623991, -0.04795272066889885720 ) ) ;
#12870=DIRECTION ( 'NONE',  ( -3.986037398843765983E-20, -1.000000000000000000, -1.160734090543304660E-16 ) ) ;
#12872=ORIENTED_EDGE ( 'NONE', *, *, #18724, .F. ) ;
#12874=CARTESIAN_POINT ( 'NONE',  ( 1.395323331571632020, 0.5249316497054298258, -1.265979166534827449 ) ) ;
#12876=CARTESIAN_POINT ( 'NONE',  ( 2.685792526206067343, 1.659196497464942022, -0.5625364255821559967 ) ) ;
#12879=CARTESIAN_POINT ( 'NONE',  ( -1.834323595590334977, 1.205361022782829114E-17, 1.151859023884900690 ) ) ;
#12880=DIRECTION ( 'NONE',  ( 7.237058681235334921E-17, -1.000000000000000000, -9.074984547606431700E-17 ) ) ;
#12883=CARTESIAN_POINT ( 'NONE',  ( 0.000000000000000000, 0.000000000000000000, 0.000000000000000000 ) ) ;
#12884=ORIENTED_EDGE ( 'NONE', *, *, #42863, .F. ) ;
#12885=CARTESIAN_POINT ( 'NONE',  ( 1.325491792074624087, 1.641458297549746037, -2.638988599164732385 ) ) ;
#12893=AXIS2_PLACEMENT_3D ( 'NONE', #24105, #39851, #4484 ) ;
#12900=AXIS2_PLACEMENT_3D ( 'NONE', #11943, #13988, #33874 ) ;
#12902=CARTESIAN_POINT ( 'NONE',  ( 1.355960331127249452, 0.04963785175798203497, -1.364517356352728861 ) ) ;
#12907=EDGE_CURVE ( 'NONE', #23085, #3720, #2907, .T. ) ;
#12909=CARTESIAN_POINT ( 'NONE',  ( -0.8067290215918269114, 6.692913385826772199, 2.009464521518169899 ) ) ;
#12917=CARTESIAN_POINT ( 'NONE',  ( 0.1155636338427008941, -0.5222242541845523167, 0.000000000000000000 ) ) ;
#12924=VERTEX_POINT ( 'NONE', #8774 ) ;
#12929=CARTESIAN_POINT ( 'NONE',  ( 2.932638728931774352, 1.666481914436860334, 0.3475908556738225297 ) ) ;
#12930=CARTESIAN_POINT ( 'NONE',  ( -1.775400203342670569, 1.205361022782829114E-17, -2.359903268218729089 ) ) ;
#12932=ORIENTED_EDGE ( 'NONE', *, *, #3869, .F. ) ;
#12937=EDGE_CURVE ( 'NONE', #18734, #11675, #45972, .T. ) ;
#12939=B_SPLINE_CURVE_WITH_KNOTS ( 'NONE', 3,
 ( #14647, #37901, #10768, #45352 ),
 .UNSPECIFIED., .F., .F.,
 ( 4, 4 ),
 ( 0.1211775127643062444, 0.1625894504277921315 ),
 .UNSPECIFIED. ) ;
#12941=PLANE ( 'NONE',  #17727 ) ;
#12944=AXIS2_PLACEMENT_3D ( 'NONE', #39331, #12730, #16351 ) ;
#12946=AXIS2_PLACEMENT_3D ( 'NONE', #3694, #11688, #27679 ) ;
#12948=DIRECTION ( 'NONE',  ( -0.01601477604151182663, 0.9998717552508123996, -0.000000000000000000 ) ) ;
#12954=ORIENTED_EDGE ( 'NONE', *, *, #1995, .T. ) ;
#12959=CARTESIAN_POINT ( 'NONE',  ( 0.3820226255272446414, 0.03403845698394380309, 1.829505193364920679 ) ) ;
#12961=AXIS2_PLACEMENT_3D ( 'NONE', #40084, #23561, #47019 ) ;
#12962=AXIS2_PLACEMENT_3D ( 'NONE', #14536, #18665, #26400 ) ;
#12966=VERTEX_POINT ( 'NONE', #48733 ) ;
#12967=CONICAL_SURFACE ( 'NONE', #33589, 3.033577403570480779, 1.554780866114618743 ) ;
#12969=ADVANCED_FACE ( 'NONE', ( #33055 ), #40787, .T. ) ;
#12974=DIRECTION ( 'NONE',  ( 0.9998717552508121775, 0.01601477604151182663, 0.000000000000000000 ) ) ;
#12976=ORIENTED_EDGE ( 'NONE', *, *, #4225, .F. ) ;
#12978=DIRECTION ( 'NONE',  ( -0.01601477604151182663, 0.9998717552508123996, -0.000000000000000000 ) ) ;
#12982=FACE_OUTER_BOUND ( 'NONE', #12509, .T. ) ;
#12987=LINE ( 'NONE', #8087, #35006 ) ;
#12989=DIRECTION ( 'NONE',  ( -3.986037398843765983E-20, -1.000000000000000000, -1.160734090543304660E-16 ) ) ;
#12993=ORIENTED_EDGE ( 'NONE', *, *, #35879, .F. ) ;
#12994=ORIENTED_EDGE ( 'NONE', *, *, #43663, .T. ) ;
#12995=ADVANCED_FACE ( 'NONE', ( #36400 ), #35079, .T. ) ;
#13000=CARTESIAN_POINT ( 'NONE',  ( 2.010517631316622644, 0.000000000000000000, 0.8058170502102376398 ) ) ;
#13003=CARTESIAN_POINT ( 'NONE',  ( 2.928234753086316644, 1.666404349079314562, 0.3801023109252803511 ) ) ;
#13008=CONICAL_SURFACE ( 'NONE', #41861, 3.483074324928249421, 1.244861948955335196 ) ;
#13009=LINE ( 'NONE', #6016, #6735 ) ;
#13010=EDGE_LOOP ( 'NONE', ( #14428, #574, #35620, #27438 ) ) ;
#13012=CARTESIAN_POINT ( 'NONE',  ( 1.628466770324754176, 1.733984826446373750, -1.625060189682509870 ) ) ;
#13015=DIRECTION ( 'NONE',  ( -0.000000000000000000, -1.000000000000000000, -0.000000000000000000 ) ) ;
#13016=CIRCLE ( 'NONE', #33666, 1.850107469027523432 ) ;
#13017=CARTESIAN_POINT ( 'NONE',  ( 2.437180031585944207, 1.459818316683583639, -1.667735833703099191 ) ) ;
#13018=VERTEX_POINT ( 'NONE', #29155 ) ;
#13020=CARTESIAN_POINT ( 'NONE',  ( 0.000000000000000000, 2.755905511811027164, 0.000000000000000000 ) ) ;
#13021=ORIENTED_EDGE ( 'NONE', *, *, #39704, .F. ) ;
#13025=B_SPLINE_CURVE_WITH_KNOTS ( 'NONE', 3,
 ( #13660, #32786, #17529, #8760 ),
 .UNSPECIFIED., .F., .F.,
 ( 4, 4 ),
 ( 2.075195358405174660E-07, 0.01744788363431542047 ),
 .UNSPECIFIED. ) ;
#13030=VERTEX_POINT ( 'NONE', #44388 ) ;
#13034=EDGE_CURVE ( 'NONE', #39521, #30165, #36918, .T. ) ;
#13037=CARTESIAN_POINT ( 'NONE',  ( -2.491402175429631605, 1.581999109372839385, -1.585592796919542025 ) ) ;
#13038=LINE ( 'NONE', #40413, #7157 ) ;
#13039=EDGE_CURVE ( 'NONE', #4194, #3720, #10828, .T. ) ;
#13040=FACE_OUTER_BOUND ( 'NONE', #35022, .T. ) ;
#13048=CARTESIAN_POINT ( 'NONE',  ( 0.01640433696702632560, 1.621061233670012758, 2.952755905511811108 ) ) ;
#13049=EDGE_CURVE ( 'NONE', #8816, #47610, #9032, .T. ) ;
#13051=DIRECTION ( 'NONE',  ( 0.9998717552508121775, 0.01601477604151182663, 0.000000000000000000 ) ) ;
#13053=ORIENTED_EDGE ( 'NONE', *, *, #13034, .F. ) ;
#13055=EDGE_LOOP ( 'NONE', ( #32488, #21428, #50151, #36205 ) ) ;
#13058=CARTESIAN_POINT ( 'NONE',  ( 0.002207914879453961535, -5.712274067634378313E-18, 0.04916304461325374242 ) ) ;
#13059=VECTOR ( 'NONE', #4693, 39.37007874015748143 ) ;
#13065=ADVANCED_FACE ( 'NONE', ( #12053 ), #26014, .T. ) ;
#13068=DIRECTION ( 'NONE',  ( 3.986037398843765983E-20, 1.000000000000000000, 1.160734090543304660E-16 ) ) ;
#13069=DIRECTION ( 'NONE',  ( 9.964307797194671432E-17, -1.000000000000000000, -5.953396763000495864E-17 ) ) ;
#13070=EDGE_CURVE ( 'NONE', #17742, #782, #33448, .T. ) ;
#13075=DIRECTION ( 'NONE',  ( -0.01601477604151182663, 0.9998717552508123996, -0.000000000000000000 ) ) ;
#13077=CARTESIAN_POINT ( 'NONE',  ( 0.1155636338427008941, -0.5222242541845523167, 0.000000000000000000 ) ) ;
#13085=CARTESIAN_POINT ( 'NONE',  ( 2.138597145901430352, 6.692913385826772199, 0.3393547186367261159 ) ) ;
#13097=ORIENTED_EDGE ( 'NONE', *, *, #4067, .F. ) ;
#13107=ADVANCED_FACE ( 'NONE', ( #31418 ), #47376, .T. ) ;
#13110=CARTESIAN_POINT ( 'NONE',  ( 2.695799277629594037, 1.662794757381320654, -1.205759334241453651 ) ) ;
#13113=B_SPLINE_CURVE_WITH_KNOTS ( 'NONE', 3,
 ( #42464, #6152, #46812, #15609 ),
 .UNSPECIFIED., .F., .F.,
 ( 4, 4 ),
 ( 0.01129884938030837997, 0.03073620617781123304 ),
 .UNSPECIFIED. ) ;
#13117=CARTESIAN_POINT ( 'NONE',  ( -1.748867201173968100, 1.551518886663849628, -2.379180622689949676 ) ) ;
#13118=ORIENTED_EDGE ( 'NONE', *, *, #43000, .F. ) ;
#13121=CARTESIAN_POINT ( 'NONE',  ( 0.1067246931122726866, 0.02962905676920215767, 0.000000000000000000 ) ) ;
#13127=VERTEX_POINT ( 'NONE', #11790 ) ;
#13129=CARTESIAN_POINT ( 'NONE',  ( -1.798309077365525477, 1.584767851350155743, -1.651272990452771872 ) ) ;
#13130=CARTESIAN_POINT ( 'NONE',  ( 0.000000000000000000, 1.574803149606302854, 0.000000000000000000 ) ) ;
#13136=CARTESIAN_POINT ( 'NONE',  ( -2.600183657057300923, 0.000000000000000000, 1.399218491554123700 ) ) ;
#13141=ORIENTED_EDGE ( 'NONE', *, *, #25550, .T. ) ;
#13142=CARTESIAN_POINT ( 'NONE',  ( 1.528535732727733132, 1.480350918634800728, 2.526383692155887317 ) ) ;
#13144=ORIENTED_EDGE ( 'NONE', *, *, #34036, .T. ) ;
#13147=CARTESIAN_POINT ( 'NONE',  ( -1.707223610577860429, 0.000000000000000000, -0.3728134436854625422 ) ) ;
#13148=CARTESIAN_POINT ( 'NONE',  ( 0.2646829987306326126, 5.905511811023623991, -2.940868978332396910 ) ) ;
#13151=VECTOR ( 'NONE', #26107, 39.37007874015748143 ) ;
#13155=B_SPLINE_CURVE_WITH_KNOTS ( 'NONE', 3,
 ( #48376, #37577, #9177, #33711 ),
 .UNSPECIFIED., .F., .F.,
 ( 4, 4 ),
 ( 0.1211873102087489551, 0.1625992483279400380 ),
 .UNSPECIFIED. ) ;
#13158=ORIENTED_EDGE ( 'NONE', *, *, #10551, .F. ) ;
#13159=EDGE_CURVE ( 'NONE', #43500, #30156, #5310, .T. ) ;
#13160=CONICAL_SURFACE ( 'NONE', #32140, 3.033577403570480779, 1.554780866114618743 ) ;
#13166=ADVANCED_FACE ( 'NONE', ( #4304 ), #35804, .F. ) ;
#13169=CARTESIAN_POINT ( 'NONE',  ( 0.07982360342473591996, 1.709180471932028711, 0.000000000000000000 ) ) ;
#13170=CARTESIAN_POINT ( 'NONE',  ( -1.719272085561387442, 0.5247476050418645732, 1.308128460514559332 ) ) ;
#13173=AXIS2_PLACEMENT_3D ( 'NONE', #4690, #47243, #39542 ) ;
#13174=CARTESIAN_POINT ( 'NONE',  ( 0.9439235339024302229, 1.657403817845428451, -2.073500882935703338 ) ) ;
#13177=ADVANCED_FACE ( 'NONE', ( #12562 ), #36704, .F. ) ;
#13179=CARTESIAN_POINT ( 'NONE',  ( 1.892591856222374469, 0.05823298773025239322, -0.4824499329568616157 ) ) ;
#13184=DIRECTION ( 'NONE',  ( 0.000000000000000000, 0.000000000000000000, -1.000000000000000000 ) ) ;
#13185=CONICAL_SURFACE ( 'NONE', #11517, 1.850107469027523210, 0.6386652850508578450 ) ;
#13188=LINE ( 'NONE', #12661, #1615 ) ;
#13190=ORIENTED_EDGE ( 'NONE', *, *, #36496, .T. ) ;
#13191=FACE_OUTER_BOUND ( 'NONE', #12287, .T. ) ;
#13194=DIRECTION ( 'NONE',  ( -1.156061316345072978E-16, -1.000000000000000000, -1.040474016969658122E-17 ) ) ;
#13196=VECTOR ( 'NONE', #32497, 39.37007874015748143 ) ;
#13197=B_SPLINE_CURVE_WITH_KNOTS ( 'NONE', 3,
 ( #38665, #34787, #19278, #27532 ),
 .UNSPECIFIED., .F., .F.,
 ( 4, 4 ),
 ( 0.03083869506961483056, 0.04878547865986578719 ),
 .UNSPECIFIED. ) ;
#13200=EDGE_CURVE ( 'NONE', #50651, #8216, #32974, .T. ) ;
#13201=DIRECTION ( 'NONE',  ( -6.104789737168205836E-17, 1.000000000000000000, 1.134460028949762747E-16 ) ) ;
#13208=ORIENTED_EDGE ( 'NONE', *, *, #1730, .T. ) ;
#13212=VERTEX_POINT ( 'NONE', #37599 ) ;
#13214=EDGE_CURVE ( 'NONE', #31073, #5934, #25600, .T. ) ;
#13215=ORIENTED_EDGE ( 'NONE', *, *, #30270, .T. ) ;
#13221=EDGE_LOOP ( 'NONE', ( #24473, #21167, #3880, #36325 ) ) ;
#13222=ORIENTED_EDGE ( 'NONE', *, *, #41580, .T. ) ;
#13224=EDGE_CURVE ( 'NONE', #596, #19294, #25078, .T. ) ;
#13226=ORIENTED_EDGE ( 'NONE', *, *, #25031, .T. ) ;
#13230=CARTESIAN_POINT ( 'NONE',  ( 2.222091332265985208, 1.743492810207595500, 0.6702560524809636489 ) ) ;
#13231=VECTOR ( 'NONE', #49707, 39.37007874015748143 ) ;
#13234=CARTESIAN_POINT ( 'NONE',  ( 0.01640433704663615821, 1.719511132758201999, 2.952755905511811108 ) ) ;
#13236=CARTESIAN_POINT ( 'NONE',  ( 1.854898449969132335, 1.741084675012395833, -1.705377970569586621 ) ) ;
#13237=ORIENTED_EDGE ( 'NONE', *, *, #27058, .T. ) ;
#13238=CARTESIAN_POINT ( 'NONE',  ( 1.929629134066521701, 6.692913385826772199, 0.9824921284572420976 ) ) ;
#13248=DIRECTION ( 'NONE',  ( 0.8345732537212999791, -6.397775707690033618E-17, 0.5508969814521065267 ) ) ;
#13250=VERTEX_POINT ( 'NONE', #22102 ) ;
#13251=CARTESIAN_POINT ( 'NONE',  ( -1.478009596860490715, 1.585803725363800210, 1.616919955472289727 ) ) ;
#13252=ORIENTED_EDGE ( 'NONE', *, *, #40325, .T. ) ;
#13255=DIRECTION ( 'NONE',  ( -0.000000000000000000, 1.000000000000000000, 0.000000000000000000 ) ) ;
#13257=DIRECTION ( 'NONE',  ( 2.866708903754326305E-17, 1.000000000000000000, 1.255987235303924321E-16 ) ) ;
#13259=ORIENTED_EDGE ( 'NONE', *, *, #18585, .F. ) ;
#13263=EDGE_CURVE ( 'NONE', #10495, #32762, #6088, .T. ) ;
#13264=B_SPLINE_CURVE_WITH_KNOTS ( 'NONE', 3,
 ( #18518, #14644, #30389, #34522 ),
 .UNSPECIFIED., .F., .F.,
 ( 4, 4 ),
 ( 0.0005256063878724909297, 0.003025860639318088061 ),
 .UNSPECIFIED. ) ;
#13266=ORIENTED_EDGE ( 'NONE', *, *, #15630, .T. ) ;
#13267=CARTESIAN_POINT ( 'NONE',  ( -2.074049943651441019, 6.692913385826772199, 0.6221544894623932676 ) ) ;
#13271=ORIENTED_EDGE ( 'NONE', *, *, #43846, .T. ) ;
#13273=DIRECTION ( 'NONE',  ( 0.01601477604151182663, -0.9998717552508123996, 0.000000000000000000 ) ) ;
#13276=AXIS2_PLACEMENT_3D ( 'NONE', #20842, #36595, #36851 ) ;
#13277=FACE_OUTER_BOUND ( 'NONE', #1212, .T. ) ;
#13281=EDGE_CURVE ( 'NONE', #38547, #6492, #1453, .T. ) ;
#13283=CARTESIAN_POINT ( 'NONE',  ( -0.6235241006192322466, 1.205361022782829114E-17, 2.074304693190349269 ) ) ;
#13287=DIRECTION ( 'NONE',  ( -0.01601477604151182663, 0.9998717552508123996, -0.000000000000000000 ) ) ;
#13297=ORIENTED_EDGE ( 'NONE', *, *, #10298, .T. ) ;
#13312=FACE_OUTER_BOUND ( 'NONE', #22302, .T. ) ;
#13315=AXIS2_PLACEMENT_3D ( 'NONE', #24907, #39888, #12783 ) ;
#13316=CARTESIAN_POINT ( 'NONE',  ( 0.08139965876239094178, 1.610780518492231694, 0.000000000000000000 ) ) ;
#13318=CARTESIAN_POINT ( 'NONE',  ( -1.321932112650661351, 0.002299539184349054001, -1.195809976494780047 ) ) ;
#13323=CARTESIAN_POINT ( 'NONE',  ( 0.04921259842519667971, 1.708690180665275005, 2.244725876464058523 ) ) ;
#13325=EDGE_CURVE ( 'NONE', #9488, #21677, #17797, .T. ) ;
#13327=CARTESIAN_POINT ( 'NONE',  ( 2.951990591674675368, 1.666783180044518087, -0.08331184815398359755 ) ) ;
#13335=CARTESIAN_POINT ( 'NONE',  ( 1.973323729629757217, 0.000000000000000000, -0.7899196136953162695 ) ) ;
#13336=ORIENTED_EDGE ( 'NONE', *, *, #30233, .T. ) ;
#13342=CONICAL_SURFACE ( 'NONE', #3414, 2.244934639244524632, 1.554780866114618743 ) ;
#13353=CARTESIAN_POINT ( 'NONE',  ( -2.867773316779184789, 5.905511811023623991, -0.7050287376752433222 ) ) ;
#13360=EDGE_LOOP ( 'NONE', ( #9885, #21696, #7696, #31786, #39811, #17185, #17259, #32681, #45301, #36860, #48015 ) ) ;
#13364=EDGE_CURVE ( 'NONE', #21109, #41720, #10391, .T. ) ;
#13365=ORIENTED_EDGE ( 'NONE', *, *, #27668, .F. ) ;
#13370=ORIENTED_EDGE ( 'NONE', *, *, #3579, .F. ) ;
#13372=VECTOR ( 'NONE', #13997, 39.37007874015748143 ) ;
#13377=CARTESIAN_POINT ( 'NONE',  ( -1.215880257433763489, 0.002872929996209854387, 1.316888785179493482 ) ) ;
#13379=CARTESIAN_POINT ( 'NONE',  ( 0.3382312733057609155, 5.905511811023623991, -2.139420919314965808 ) ) ;
#13380=CARTESIAN_POINT ( 'NONE',  ( 1.152895553066221934, 1.205361022782829114E-17, -1.833672301139072092 ) ) ;
#13387=EDGE_LOOP ( 'NONE', ( #42183, #39207, #43597, #11747, #845, #32123, #11933, #40354, #32770, #11054, #46781 ) ) ;
#13391=VERTEX_POINT ( 'NONE', #15360 ) ;
#13399=CARTESIAN_POINT ( 'NONE',  ( -2.165354330708661568, 1.574803149606301966, 0.08080958537891422266 ) ) ;
#13400=VERTEX_POINT ( 'NONE', #30604 ) ;
#13404=DIRECTION ( 'NONE',  ( -1.156061316345074457E-16, -1.000000000000000000, 1.040474016969491568E-17 ) ) ;
#13407=CARTESIAN_POINT ( 'NONE',  ( -0.2156685157583834722, 0.000000000000000000, -2.945280361644576850 ) ) ;
#13408=AXIS2_PLACEMENT_3D ( 'NONE', #40794, #5683, #41812 ) ;
#13411=CIRCLE ( 'NONE', #47967, 2.165354330708661568 ) ;
#13414=ORIENTED_EDGE ( 'NONE', *, *, #46296, .F. ) ;
#13417=CARTESIAN_POINT ( 'NONE',  ( -2.029281105070185109, 1.044437984162145394, 1.555352403886350432 ) ) ;
#13420=ADVANCED_FACE ( 'NONE', ( #46566 ), #44167, .T. ) ;
#13421=CONICAL_SURFACE ( 'NONE', #27398, 2.165354330708661568, 0.2617993877991570129 ) ;
#13422=AXIS2_PLACEMENT_3D ( 'NONE', #29180, #32565, #20667 ) ;
#13426=B_SPLINE_CURVE_WITH_KNOTS ( 'NONE', 3,
 ( #41412, #32923, #33683, #25156 ),
 .UNSPECIFIED., .F., .F.,
 ( 4, 4 ),
 ( 0.0005438425946845861902, 0.0009539043374978324087 ),
 .UNSPECIFIED. ) ;
#13436=CARTESIAN_POINT ( 'NONE',  ( -2.708695948734475500, 1.570819970757063144, -1.175586072237004176 ) ) ;
#13443=PLANE ( 'NONE',  #36536 ) ;
#13444=B_SPLINE_CURVE_WITH_KNOTS ( 'NONE', 3,
 ( #35838, #465, #24734, #16477 ),
 .UNSPECIFIED., .F., .F.,
 ( 4, 4 ),
 ( 0.01165461794221865459, 0.03073677718705081913 ),
 .UNSPECIFIED. ) ;
#13445=PLANE ( 'NONE',  #41640 ) ;
#13446=CARTESIAN_POINT ( 'NONE',  ( -0.1204783766914112736, 0.008687915765946812099, -1.887631293257881815 ) ) ;
#13448=LINE ( 'NONE', #29186, #2870 ) ;
#13449=EDGE_CURVE ( 'NONE', #48162, #14514, #45876, .T. ) ;
#13453=ORIENTED_EDGE ( 'NONE', *, *, #13049, .F. ) ;
#13455=CYLINDRICAL_SURFACE ( 'NONE', #39227, 2.164630168518208109 ) ;
#13457=AXIS2_PLACEMENT_3D ( 'NONE', #8277, #8533, #13184 ) ;
#13467=FACE_OUTER_BOUND ( 'NONE', #24199, .T. ) ;
#13470=ORIENTED_EDGE ( 'NONE', *, *, #40455, .F. ) ;
#13471=ORIENTED_EDGE ( 'NONE', *, *, #22572, .T. ) ;
#13472=VERTEX_POINT ( 'NONE', #42213 ) ;
#13478=CARTESIAN_POINT ( 'NONE',  ( 0.7937023274952557106, 0.02690111800290191299, -1.761563333612303106 ) ) ;
#13486=ORIENTED_EDGE ( 'NONE', *, *, #7381, .F. ) ;
#13487=CARTESIAN_POINT ( 'NONE',  ( -2.055928985459924530, 6.692913385826772199, 0.7197570096327609024 ) ) ;
#13496=AXIS2_PLACEMENT_3D ( 'NONE', #21763, #48826, #21505 ) ;
#13501=ORIENTED_EDGE ( 'NONE', *, *, #28280, .T. ) ;
#13505=LINE ( 'NONE', #17377, #48824 ) ;
#13506=CARTESIAN_POINT ( 'NONE',  ( 2.437180031585944207, 1.459818316683583639, -1.667735833703099191 ) ) ;
#13507=EDGE_CURVE ( 'NONE', #2179, #43511, #49884, .T. ) ;
#13510=CARTESIAN_POINT ( 'NONE',  ( 2.932638728931774352, 1.666481914436860334, 0.3475908556738225297 ) ) ;
#13512=CYLINDRICAL_SURFACE ( 'NONE', #37796, 2.165354330708661568 ) ;
#13515=DIRECTION ( 'NONE',  ( 0.000000000000000000, 0.000000000000000000, 1.000000000000000000 ) ) ;
#13520=DIRECTION ( 'NONE',  ( 0.01601477604151182663, -0.9998717552508123996, 0.000000000000000000 ) ) ;
#13523=CARTESIAN_POINT ( 'NONE',  ( 1.723188456408574432, 1.574803149606302854, 1.311251662046225785 ) ) ;
#13527=ORIENTED_EDGE ( 'NONE', *, *, #1908, .T. ) ;
#13528=AXIS2_PLACEMENT_3D ( 'NONE', #28877, #1771, #1263 ) ;
#13529=CARTESIAN_POINT ( 'NONE',  ( 2.808237744965994320, 0.000000000000000000, 0.9124517550441679781 ) ) ;
#13534=CIRCLE ( 'NONE', #42370, 2.164630168518208109 ) ;
#13547=CARTESIAN_POINT ( 'NONE',  ( 2.867773316779195447, 1.665472095473279790, -0.7050287376752005786 ) ) ;
#13553=CARTESIAN_POINT ( 'NONE',  ( -2.275425600868766995, 1.581315431065779542, -1.443027908266066639 ) ) ;
#13556=EDGE_CURVE ( 'NONE', #21355, #17854, #9607, .T. ) ;
#13559=CARTESIAN_POINT ( 'NONE',  ( 2.109061063546357584, 1.748596092898957233, 1.744865349675275956 ) ) ;
#13565=CARTESIAN_POINT ( 'NONE',  ( 0.7722537565518702296, 1.629158966512215923, -2.613214498325589386 ) ) ;
#13572=DIRECTION ( 'NONE',  ( 0.000000000000000000, 0.000000000000000000, 1.000000000000000000 ) ) ;
#13574=VECTOR ( 'NONE', #50728, 39.37007874015748143 ) ;
#13576=EDGE_CURVE ( 'NONE', #31520, #2997, #37968, .T. ) ;
#13577=CARTESIAN_POINT ( 'NONE',  ( 2.623970503359832840, 1.658226141870901227, 0.8008345106751136866 ) ) ;
#13578=ADVANCED_FACE ( 'NONE', ( #37192 ), #12861, .T. ) ;
#13580=CARTESIAN_POINT ( 'NONE',  ( -0.2134117707794043750, 0.02450148541315291459, -1.822192086320855164 ) ) ;
#13582=ORIENTED_EDGE ( 'NONE', *, *, #1953, .T. ) ;
#13583=LINE ( 'NONE', #14083, #45571 ) ;
#13586=DIRECTION ( 'NONE',  ( 0.000000000000000000, 0.000000000000000000, -1.000000000000000000 ) ) ;
#13587=ORIENTED_EDGE ( 'NONE', *, *, #18395, .T. ) ;
#13593=DIRECTION ( 'NONE',  ( -0.9998717552508122886, -0.01601477604151182316, 0.000000000000000000 ) ) ;
#13595=CARTESIAN_POINT ( 'NONE',  ( 2.074049943651431693, 5.118110236220475784, 0.6221544894624241318 ) ) ;
#13598=FACE_OUTER_BOUND ( 'NONE', #30066, .T. ) ;
#13603=VECTOR ( 'NONE', #43329, 39.37007874015748143 ) ;
#13613=CARTESIAN_POINT ( 'NONE',  ( -0.6381684359064370149, 1.664872118777908527, -2.127367250395180598 ) ) ;
#13614=EDGE_CURVE ( 'NONE', #9471, #16563, #21690, .T. ) ;
#13617=EDGE_CURVE ( 'NONE', #36555, #16654, #37601, .T. ) ;
#13628=CARTESIAN_POINT ( 'NONE',  ( -2.076715649576790224, 1.576214352228098470, 0.6230206298219045369 ) ) ;
#13629=EDGE_CURVE ( 'NONE', #27405, #47107, #24424, .T. ) ;
#13636=CARTESIAN_POINT ( 'NONE',  ( -1.936609506549060722, 1.676883605369557051, 0.9862484270667263297 ) ) ;
#13638=EDGE_CURVE ( 'NONE', #20465, #10525, #2831, .T. ) ;
#13639=VECTOR ( 'NONE', #28611, 39.37007874015748854 ) ;
#13642=DIRECTION ( 'NONE',  ( 0.000000000000000000, 0.000000000000000000, 1.000000000000000000 ) ) ;
#13643=DIRECTION ( 'NONE',  ( 1.142080616180681165E-16, -1.000000000000000000, -2.072570748943160811E-17 ) ) ;
#13651=ORIENTED_EDGE ( 'NONE', *, *, #1328, .T. ) ;
#13654=DIRECTION ( 'NONE',  ( -0.04486483035051863633, 1.288287287306305283E-16, 0.9989930665413144784 ) ) ;
#13656=CARTESIAN_POINT ( 'NONE',  ( -1.344179059205499849, 1.694369366911352204, 2.345726623500195451 ) ) ;
#13660=CARTESIAN_POINT ( 'NONE',  ( 0.8329809839909850799, 1.732245219823249638, -2.833254665166554442 ) ) ;
#13661=DIRECTION ( 'NONE',  ( 0.000000000000000000, 1.000000000000000000, 0.000000000000000000 ) ) ;
#13666=CARTESIAN_POINT ( 'NONE',  ( 2.437180031585944207, 1.658768335924418080, -1.667735833703099191 ) ) ;
#13669=AXIS2_PLACEMENT_3D ( 'NONE', #2906, #34657, #11409 ) ;
#13670=VERTEX_POINT ( 'NONE', #7709 ) ;
#13677=VECTOR ( 'NONE', #40269, 39.37007874015748854 ) ;
#13679=CARTESIAN_POINT ( 'NONE',  ( 0.08139965876239094178, 1.610780518492231694, 0.000000000000000000 ) ) ;
#13681=EDGE_CURVE ( 'NONE', #36107, #24851, #7143, .T. ) ;
#13685=ORIENTED_EDGE ( 'NONE', *, *, #9724, .F. ) ;
#13686=CARTESIAN_POINT ( 'NONE',  ( 0.08139965876239094178, 1.610780518492231694, 0.000000000000000000 ) ) ;
#13687=CONICAL_SURFACE ( 'NONE', #42529, 1.850107469027523210, 0.6386652850508578450 ) ;
#13688=CARTESIAN_POINT ( 'NONE',  ( -2.076656781855024114, 1.674640491952791077, 0.6230015025396302697 ) ) ;
#13689=VERTEX_POINT ( 'NONE', #11081 ) ;
#13700=B_SPLINE_CURVE_WITH_KNOTS ( 'NONE', 3,
 ( #27448, #16608, #23837, #28209 ),
 .UNSPECIFIED., .F., .F.,
 ( 4, 4 ),
 ( 2.655965292660759762E-07, 0.002500437883007026758 ),
 .UNSPECIFIED. ) ;
#13706=EDGE_CURVE ( 'NONE', #28139, #22211, #41612, .T. ) ;
#13709=ORIENTED_EDGE ( 'NONE', *, *, #21364, .F. ) ;
#13718=CARTESIAN_POINT ( 'NONE',  ( -1.461782879395278290, 0.000000000000000000, -1.598346982901829527 ) ) ;
#13721=ORIENTED_EDGE ( 'NONE', *, *, #25204, .F. ) ;
#13724=ORIENTED_EDGE ( 'NONE', *, *, #25636, .T. ) ;
#13729=VERTEX_POINT ( 'NONE', #27315 ) ;
#13735=DIRECTION ( 'NONE',  ( -1.267583980596137654E-16, 1.000000000000000000, -2.300325776299734791E-17 ) ) ;
#13737=EDGE_CURVE ( 'NONE', #975, #10759, #47158, .T. ) ;
#13738=VERTEX_POINT ( 'NONE', #16740 ) ;
#13747=CONICAL_SURFACE ( 'NONE', #36044, 3.033577403570480779, 1.554780866114618743 ) ;
#13749=LINE ( 'NONE', #5991, #28251 ) ;
#13750=VERTEX_POINT ( 'NONE', #24483 ) ;
#13755=CARTESIAN_POINT ( 'NONE',  ( -2.473328087603087866, 1.680701298296960688, -1.612973869594296783 ) ) ;
#13756=EDGE_LOOP ( 'NONE', ( #37189, #3211, #22136, #3054 ) ) ;
#13757=ORIENTED_EDGE ( 'NONE', *, *, #32233, .T. ) ;
#13758=AXIS2_PLACEMENT_3D ( 'NONE', #12516, #36532, #17414 ) ;
#13760=ORIENTED_EDGE ( 'NONE', *, *, #19942, .F. ) ;
#13766=CARTESIAN_POINT ( 'NONE',  ( -1.528559409259449442, 1.546995005732493711, 2.526369546086722373 ) ) ;
#13769=CARTESIAN_POINT ( 'NONE',  ( -0.6584127755596833609, 0.000000000000000000, 1.614277297217976859 ) ) ;
#13770=DIRECTION ( 'NONE',  ( 0.5877852522924802425, 9.388193118000637501E-17, -0.8090169943749422332 ) ) ;
#13772=ORIENTED_EDGE ( 'NONE', *, *, #36886, .T. ) ;
#13773=DIRECTION ( 'NONE',  ( 0.4338837391175526803, -1.045958227173635857E-16, 0.9009688679024218105 ) ) ;
#13774=EDGE_CURVE ( 'NONE', #18870, #13250, #44085, .T. ) ;
#13778=EDGE_CURVE ( 'NONE', #31200, #9169, #8224, .T. ) ;
#13781=DIRECTION ( 'NONE',  ( -1.598721155460225418E-14, 0.000000000000000000, 1.000000000000000000 ) ) ;
#13784=VERTEX_POINT ( 'NONE', #40233 ) ;
#13786=DIRECTION ( 'NONE',  ( 2.866708903754326305E-17, 1.000000000000000000, 1.255987235303924321E-16 ) ) ;
#13788=CARTESIAN_POINT ( 'NONE',  ( -0.9043257427339754795, 0.5245521110397223241, -1.991275222317478999 ) ) ;
#13793=LINE ( 'NONE', #5787, #17218 ) ;
#13798=ORIENTED_EDGE ( 'NONE', *, *, #6762, .T. ) ;
#13804=ORIENTED_EDGE ( 'NONE', *, *, #14671, .F. ) ;
#13808=DIRECTION ( 'NONE',  ( 0.000000000000000000, 0.000000000000000000, -1.000000000000000000 ) ) ;
#13809=ADVANCED_FACE ( 'NONE', ( #39459 ), #40091, .T. ) ;
#13810=VERTEX_POINT ( 'NONE', #48186 ) ;
#13812=CARTESIAN_POINT ( 'NONE',  ( -1.461363083917493810, 6.692913385826772199, 1.597866488315562439 ) ) ;
#13816=ORIENTED_EDGE ( 'NONE', *, *, #43972, .T. ) ;
#13822=CARTESIAN_POINT ( 'NONE',  ( 2.823445274216730638, 1.763256531483745837, 0.8656477926280683466 ) ) ;
#13824=ORIENTED_EDGE ( 'NONE', *, *, #4699, .F. ) ;
#13828=CARTESIAN_POINT ( 'NONE',  ( 1.081562861160096700, 0.04524287409729283588, -1.572369041216798768 ) ) ;
#13833=VECTOR ( 'NONE', #14081, 39.37007874015748143 ) ;
#13835=ORIENTED_EDGE ( 'NONE', *, *, #36522, .T. ) ;
#13838=CARTESIAN_POINT ( 'NONE',  ( -0.3136974817027967100, 1.615928078135840051, -2.936457595020224520 ) ) ;
#13845=ORIENTED_EDGE ( 'NONE', *, *, #15134, .F. ) ;
#13848=B_SPLINE_CURVE_WITH_KNOTS ( 'NONE', 3,
 ( #38597, #27209, #34718, #7601 ),
 .UNSPECIFIED., .F., .F.,
 ( 4, 4 ),
 ( 4.389659793852969620E-07, 0.04940888453222644361 ),
 .UNSPECIFIED. ) ;
#13860=EDGE_CURVE ( 'NONE', #11675, #42907, #40911, .T. ) ;
#13862=ORIENTED_EDGE ( 'NONE', *, *, #5472, .F. ) ;
#13868=CONICAL_SURFACE ( 'NONE', #42703, 2.246510896728926010, 0.01601546068027819014 ) ;
#13870=ORIENTED_EDGE ( 'NONE', *, *, #41516, .F. ) ;
#13871=EDGE_CURVE ( 'NONE', #17434, #25112, #7038, .T. ) ;
#13872=LINE ( 'NONE', #25738, #33193 ) ;
#13875=VECTOR ( 'NONE', #37912, 39.37007874015748143 ) ;
#13878=CARTESIAN_POINT ( 'NONE',  ( -0.2493966119946618154, 1.605482210820551758, -2.222016418551142181 ) ) ;
#13879=ORIENTED_EDGE ( 'NONE', *, *, #43770, .T. ) ;
#13883=DIRECTION ( 'NONE',  ( 0.000000000000000000, 0.000000000000000000, 1.000000000000000000 ) ) ;
#13885=B_SPLINE_CURVE_WITH_KNOTS ( 'NONE', 3,
 ( #39877, #43729, #3051, #32397 ),
 .UNSPECIFIED., .F., .F.,
 ( 4, 4 ),
 ( 0.01116762523142644965, 0.03073605728027439810 ),
 .UNSPECIFIED. ) ;
#13886=CARTESIAN_POINT ( 'NONE',  ( 0.07982360342473591996, 1.709180471932028711, 0.000000000000000000 ) ) ;
#13888=ORIENTED_EDGE ( 'NONE', *, *, #14202, .T. ) ;
#13889=CARTESIAN_POINT ( 'NONE',  ( 0.5756566573088583993, 1.629780628454260194, 2.896516654582643291 ) ) ;
#13895=LINE ( 'NONE', #21899, #34348 ) ;
#13897=DIRECTION ( 'NONE',  ( -0.01601477604151182663, 0.9998717552508123996, -0.000000000000000000 ) ) ;
#13901=B_SPLINE_CURVE_WITH_KNOTS ( 'NONE', 3,
 ( #3879, #50301, #47199, #11869 ),
 .UNSPECIFIED., .F., .F.,
 ( 4, 4 ),
 ( 3.459388077773027594E-07, 0.04345450118629323039 ),
 .UNSPECIFIED. ) ;
#13903=DIRECTION ( 'NONE',  ( -0.9998717552508122886, -0.01601477604151185785, 0.000000000000000000 ) ) ;
#13904=EDGE_CURVE ( 'NONE', #18049, #9822, #25506, .T. ) ;
#13908=EDGE_CURVE ( 'NONE', #5433, #38240, #9512, .T. ) ;
#13914=VERTEX_POINT ( 'NONE', #44845 ) ;
#13925=( BOUNDED_CURVE ( )  B_SPLINE_CURVE ( 3, ( #44328, #1731, #48171, #21612 ),
 .UNSPECIFIED., .F., .F. ) 
 B_SPLINE_CURVE_WITH_KNOTS ( ( 4, 4 ),
 ( 5.423165295728897384, 5.474004202337919622 ),
 .UNSPECIFIED. ) 
 CURVE ( )  GEOMETRIC_REPRESENTATION_ITEM ( )  RATIONAL_B_SPLINE_CURVE ( ( 1.000000000000000000, 0.9997846287284284372, 0.9997846287284284372, 1.000000000000000000 ) ) 
 REPRESENTATION_ITEM ( '' )  );
#13928=CARTESIAN_POINT ( 'NONE',  ( 1.022166022771838767, 1.735184344206899487, 2.770237021086607410 ) ) ;
#13936=VECTOR ( 'NONE', #6679, 39.37007874015748143 ) ;
#13937=CARTESIAN_POINT ( 'NONE',  ( -2.105608695257993102, 1.045687859213095594, -1.448867510875124776 ) ) ;
#13940=ORIENTED_EDGE ( 'NONE', *, *, #50630, .F. ) ;
#13942=CARTESIAN_POINT ( 'NONE',  ( -2.076696040374840901, 1.609023065478501602, 0.6230142584059638056 ) ) ;
#13945=VECTOR ( 'NONE', #40, 39.37007874015748143 ) ;
#13946=EDGE_LOOP ( 'NONE', ( #10775, #21237, #27542, #39302 ) ) ;
#13949=CARTESIAN_POINT ( 'NONE',  ( -2.412085630707005990, 1.673474101395583835, 0.2770771474091495157 ) ) ;
#13950=CARTESIAN_POINT ( 'NONE',  ( 0.08119777152254364916, 1.623385212329073957, 0.000000000000000000 ) ) ;
#13956=DIRECTION ( 'NONE',  ( -0.8584487936018727616, 0.000000000000000000, 0.5128992774058948045 ) ) ;
#13957=CARTESIAN_POINT ( 'NONE',  ( 1.215807329263347114, 1.628950133432788494, 1.938968878379255578 ) ) ;
#13958=PLANE ( 'NONE',  #9476 ) ;
#13959=CIRCLE ( 'NONE', #759, 2.244934639244525076 ) ;
#13963=FACE_OUTER_BOUND ( 'NONE', #50085, .T. ) ;
#13965=EDGE_CURVE ( 'NONE', #33353, #2321, #26877, .T. ) ;
#13966=VERTEX_POINT ( 'NONE', #17497 ) ;
#13969=AXIS2_PLACEMENT_3D ( 'NONE', #46541, #15830, #47290 ) ;
#13974=EDGE_LOOP ( 'NONE', ( #27458, #13021, #49481, #5738 ) ) ;
#13975=DIRECTION ( 'NONE',  ( -3.986037398843765983E-20, -1.000000000000000000, -1.160734090543304660E-16 ) ) ;
#13977=ORIENTED_EDGE ( 'NONE', *, *, #12225, .F. ) ;
#13983=DIRECTION ( 'NONE',  ( -0.9009688679024218105, 1.288287287306305530E-16, 0.4338837391175526803 ) ) ;
#13986=EDGE_CURVE ( 'NONE', #24851, #1464, #25240, .T. ) ;
#13988=DIRECTION ( 'NONE',  ( -0.000000000000000000, -1.000000000000000000, -0.000000000000000000 ) ) ;
#13989=DIRECTION ( 'NONE',  ( -1.118904554427321068E-16, -1.000000000000000000, -3.087980359898530052E-17 ) ) ;
#13990=ORIENTED_EDGE ( 'NONE', *, *, #34521, .T. ) ;
#13992=CARTESIAN_POINT ( 'NONE',  ( 1.327305353890115169, 0.5249316475426857309, -1.337120392888858422 ) ) ;
#13997=DIRECTION ( 'NONE',  ( 8.902872254220023478E-17, 1.000000000000000000, -9.311674343991161395E-17 ) ) ;
#13999=DIRECTION ( 'NONE',  ( 0.9009688679024218105, 0.000000000000000000, -0.4338837391175526803 ) ) ;
#14004=VECTOR ( 'NONE', #8280, 39.37007874015748143 ) ;
#14010=CARTESIAN_POINT ( 'NONE',  ( 2.043634885149959057, 6.692913385826772199, 0.7157624142946238388 ) ) ;
#14013=CARTESIAN_POINT ( 'NONE',  ( 0.1067246931122726866, 0.02962905676920215767, 0.000000000000000000 ) ) ;
#14014=CARTESIAN_POINT ( 'NONE',  ( 2.491402175429654253, 0.000000000000000000, -1.585592796919505831 ) ) ;
#14016=CARTESIAN_POINT ( 'NONE',  ( -0.6157060063382256976, 0.5249316475426859530, 1.780600056526914443 ) ) ;
#14020=CARTESIAN_POINT ( 'NONE',  ( -1.556712866041156440, 0.000000000000000000, 2.509548638715847435 ) ) ;
#14022=EDGE_CURVE ( 'NONE', #16438, #810, #23671, .T. ) ;
#14026=DIRECTION ( 'NONE',  ( -0.9998717552508122886, -0.01601477604151181275, 0.000000000000000000 ) ) ;
#14030=CARTESIAN_POINT ( 'NONE',  ( 1.723188456408574210, 6.692913385826772199, 1.311251662046226452 ) ) ;
#14033=CARTESIAN_POINT ( 'NONE',  ( 0.9360721529196784907, 0.000000000000000000, 1.470771056236116481 ) ) ;
#14034=VERTEX_POINT ( 'NONE', #11525 ) ;
#14035=DIRECTION ( 'NONE',  ( -0.9998717552508121775, -0.01601477604151182663, 0.000000000000000000 ) ) ;
#14038=DIRECTION ( 'NONE',  ( 0.000000000000000000, 0.000000000000000000, -1.000000000000000000 ) ) ;
#14040=VECTOR ( 'NONE', #7584, 39.37007874015748143 ) ;
#14044=FACE_OUTER_BOUND ( 'NONE', #10733, .T. ) ;
#14045=CARTESIAN_POINT ( 'NONE',  ( 0.08139965876239094178, 1.610780518492231694, 0.000000000000000000 ) ) ;
#14049=AXIS2_PLACEMENT_3D ( 'NONE', #24775, #29149, #9796 ) ;
#14053=CARTESIAN_POINT ( 'NONE',  ( 1.426808618753927282, 0.05077261674489902399, -1.296082183384024811 ) ) ;
#14057=ORIENTED_EDGE ( 'NONE', *, *, #25936, .F. ) ;
#14058=CARTESIAN_POINT ( 'NONE',  ( -1.675546303352015709, 1.681065010344670041, 1.399148864732502995 ) ) ;
#14062=ORIENTED_EDGE ( 'NONE', *, *, #27668, .T. ) ;
#14064=CARTESIAN_POINT ( 'NONE',  ( 2.015507221693567885, 1.674567190253306803, 1.140476272524640455 ) ) ;
#14067=CARTESIAN_POINT ( 'NONE',  ( -1.738823649205010868, 4.685061407880516032E-05, -0.1273528623143732053 ) ) ;
#14070=CARTESIAN_POINT ( 'NONE',  ( 1.841876542152869556, 1.049866565067837820, -0.8407752411460415187 ) ) ;
#14072=ORIENTED_EDGE ( 'NONE', *, *, #22408, .T. ) ;
#14078=AXIS2_PLACEMENT_3D ( 'NONE', #26285, #6416, #37916 ) ;
#14081=DIRECTION ( 'NONE',  ( -0.5877852522924802425, -9.388193118000637501E-17, 0.8090169943749422332 ) ) ;
#14082=ORIENTED_EDGE ( 'NONE', *, *, #22577, .F. ) ;
#14083=CARTESIAN_POINT ( 'NONE',  ( -0.7303501086101925610, -2.370459731021293560E-16, 2.086068174627930816 ) ) ;
#14084=CONICAL_SURFACE ( 'NONE', #5864, 2.244934639244524632, 1.554780866114618743 ) ;
#14086=EDGE_CURVE ( 'NONE', #45769, #21117, #39144, .T. ) ;
#14087=ORIENTED_EDGE ( 'NONE', *, *, #4749, .T. ) ;
#14089=DIRECTION ( 'NONE',  ( -0.9510565162951544194, 0.000000000000000000, 0.3090169943749447312 ) ) ;
#14093=DIRECTION ( 'NONE',  ( 0.000000000000000000, 0.000000000000000000, 1.000000000000000000 ) ) ;
#14100=DIRECTION ( 'NONE',  ( -0.9909497617679331460, 1.562041240006052286E-17, -0.1342332658176667026 ) ) ;
#14104=EDGE_LOOP ( 'NONE', ( #10363, #45341, #39107, #14450, #34690, #15444, #7789, #20422, #9795, #11654, #34573 ) ) ;
#14106=CARTESIAN_POINT ( 'NONE',  ( -2.867773316779185677, 0.000000000000000000, -0.7050287376752425450 ) ) ;
#14109=AXIS2_PLACEMENT_3D ( 'NONE', #43072, #27080, #15475 ) ;
#14110=LINE ( 'NONE', #49684, #26458 ) ;
#14114=EDGE_CURVE ( 'NONE', #5907, #36192, #38890, .T. ) ;
#14116=VERTEX_POINT ( 'NONE', #15146 ) ;
#14118=ORIENTED_EDGE ( 'NONE', *, *, #7056, .T. ) ;
#14131=LINE ( 'NONE', #1745, #25569 ) ;
#14132=EDGE_CURVE ( 'NONE', #643, #15782, #13264, .T. ) ;
#14133=CARTESIAN_POINT ( 'NONE',  ( 1.087963734054938625, 1.205361022782829114E-17, 1.724994741719410918 ) ) ;
#14136=CARTESIAN_POINT ( 'NONE',  ( 1.128956743970954912, 1.693175862103839746, 1.985505143361423697 ) ) ;
#14138=EDGE_CURVE ( 'NONE', #33806, #35465, #2764, .T. ) ;
#14145=CARTESIAN_POINT ( 'NONE',  ( -1.738921996492520661, 6.764728787913346618E-05, 0.1249482579781430736 ) ) ;
#14146=EDGE_LOOP ( 'NONE', ( #35203, #28457, #8194, #30105 ) ) ;
#14147=CARTESIAN_POINT ( 'NONE',  ( -1.002022727364110688, 1.659044326116128509, -1.967298165164199419 ) ) ;
#14150=EDGE_LOOP ( 'NONE', ( #4734, #8640, #25857, #21717 ) ) ;
#14152=CONICAL_SURFACE ( 'NONE', #8408, 2.244934639244524632, 1.554780866114618743 ) ;
#14158=CARTESIAN_POINT ( 'NONE',  ( -2.139020239325885253, 1.673641627049041514, 0.3394120305351381872 ) ) ;
#14162=ORIENTED_EDGE ( 'NONE', *, *, #50267, .F. ) ;
#14166=CARTESIAN_POINT ( 'NONE',  ( 0.2627480064045706332, 0.000000000000000000, 1.723473835155035605 ) ) ;
#14168=ORIENTED_EDGE ( 'NONE', *, *, #31643, .F. ) ;
#14171=LINE ( 'NONE', #18055, #32130 ) ;
#14172=EDGE_LOOP ( 'NONE', ( #4589, #6324, #16919, #8385 ) ) ;
#14174=CARTESIAN_POINT ( 'NONE',  ( 0.1526276323950742364, 1.644729766260672577, -2.244838780058033390 ) ) ;
#14178=VECTOR ( 'NONE', #49565, 39.37007874015748854 ) ;
#14179=CARTESIAN_POINT ( 'NONE',  ( -1.387241876633674265, 6.692913385826772199, 1.662624236931676602 ) ) ;
#14181=EDGE_CURVE ( 'NONE', #3351, #28908, #50154, .T. ) ;
#14184=CARTESIAN_POINT ( 'NONE',  ( -0.4369915662458470074, 0.02092044581182531462, -1.768387524372482034 ) ) ;
#14185=EDGE_CURVE ( 'NONE', #36209, #39707, #29254, .T. ) ;
#14186=VECTOR ( 'NONE', #30300, 39.37007874015748143 ) ;
#14188=ORIENTED_EDGE ( 'NONE', *, *, #50646, .F. ) ;
#14190=AXIS2_PLACEMENT_3D ( 'NONE', #39580, #31329, #34951 ) ;
#14192=CARTESIAN_POINT ( 'NONE',  ( 0.7078551077791208623, 0.5249316475426862860, 1.746015920298445767 ) ) ;
#14197=ORIENTED_EDGE ( 'NONE', *, *, #34069, .T. ) ;
#14198=ORIENTED_EDGE ( 'NONE', *, *, #19760, .T. ) ;
#14199=CARTESIAN_POINT ( 'NONE',  ( -0.9053572107128330382, 1.602824473448254405, 2.552372930600343981 ) ) ;
#14200=CARTESIAN_POINT ( 'NONE',  ( 1.692057011007029876, 0.03618185373504610031, -1.057949673616393804 ) ) ;
#14202=EDGE_CURVE ( 'NONE', #4534, #25341, #4635, .T. ) ;
#14205=EDGE_CURVE ( 'NONE', #39335, #41869, #33514, .T. ) ;
#14208=ORIENTED_EDGE ( 'NONE', *, *, #46733, .F. ) ;
#14219=EDGE_LOOP ( 'NONE', ( #17970, #5381, #36359, #23799 ) ) ;
#14224=AXIS2_PLACEMENT_3D ( 'NONE', #14459, #33588, #45415 ) ;
#14225=CARTESIAN_POINT ( 'NONE',  ( 0.7117868624172632996, 0.000000000000000000, -1.591464117667681366 ) ) ;
#14226=CARTESIAN_POINT ( 'NONE',  ( -0.7117868624172403180, 0.000000000000000000, -1.591464117667691580 ) ) ;
#14228=ORIENTED_EDGE ( 'NONE', *, *, #27063, .T. ) ;
#14229=CARTESIAN_POINT ( 'NONE',  ( 0.000000000000000000, 0.000000000000000000, 0.000000000000000000 ) ) ;
#14232=CARTESIAN_POINT ( 'NONE',  ( -0.5756566573089003658, 0.000000000000000000, 2.896516654582634853 ) ) ;
#14242=CARTESIAN_POINT ( 'NONE',  ( -1.232995795418201812, 0.000000000000000000, 1.780798594093550680 ) ) ;
#14244=EDGE_CURVE ( 'NONE', #33109, #11793, #40177, .T. ) ;
#14255=B_SPLINE_CURVE_WITH_KNOTS ( 'NONE', 3,
 ( #18388, #41377, #7020, #33642 ),
 .UNSPECIFIED., .F., .F.,
 ( 4, 4 ),
 ( 0.002100519986389839076, 0.003739631879507434968 ),
 .UNSPECIFIED. ) ;
#14262=VECTOR ( 'NONE', #11140, 39.37007874015748143 ) ;
#14264=EDGE_CURVE ( 'NONE', #5331, #20873, #47618, .T. ) ;
#14265=CARTESIAN_POINT ( 'NONE',  ( 0.2841802383804452603, 0.03247133209088205741, 1.841575167587790718 ) ) ;
#14269=ORIENTED_EDGE ( 'NONE', *, *, #21469, .F. ) ;
#14271=LINE ( 'NONE', #14020, #35922 ) ;
#14273=CARTESIAN_POINT ( 'NONE',  ( -2.339241080213612545, 1.564176246289736616, 1.802537235681883843 ) ) ;
#14277=FACE_OUTER_BOUND ( 'NONE', #44185, .T. ) ;
#14278=ORIENTED_EDGE ( 'NONE', *, *, #1344, .T. ) ;
#14280=EDGE_LOOP ( 'NONE', ( #16539, #39390, #43757, #19575 ) ) ;
#14283=ORIENTED_EDGE ( 'NONE', *, *, #37887, .T. ) ;
#14284=DIRECTION ( 'NONE',  ( 0.9998717552508121775, 0.01601477604151182663, 0.000000000000000000 ) ) ;
#14285=EDGE_CURVE ( 'NONE', #22293, #25302, #11973, .T. ) ;
#14286=DIRECTION ( 'NONE',  ( 1.283101021437938170E-16, 1.000000000000000000, 1.154811821032258155E-17 ) ) ;
#14294=ORIENTED_EDGE ( 'NONE', *, *, #10303, .T. ) ;
#14296=CARTESIAN_POINT ( 'NONE',  ( -1.744243240276440732, -1.725014817524629540E-16, 1.328042291889479865 ) ) ;
#14303=B_SPLINE_CURVE_WITH_KNOTS ( 'NONE', 3,
 ( #29139, #24513, #32264, #28631 ),
 .UNSPECIFIED., .F., .F.,
 ( 4, 4 ),
 ( 1.642879463944005381E-05, 0.05043055294521734538 ),
 .UNSPECIFIED. ) ;
#14304=CARTESIAN_POINT ( 'NONE',  ( 1.539674616754186820, 0.000000000000000000, -1.403993126671013059 ) ) ;
#14306=DIRECTION ( 'NONE',  ( -3.986037398843765983E-20, -1.000000000000000000, -1.160734090543304660E-16 ) ) ;
#14308=PLANE ( 'NONE',  #951 ) ;
#14310=CONICAL_SURFACE ( 'NONE', #47235, 2.244934639244524632, 1.554780866114618743 ) ;
#14319=CARTESIAN_POINT ( 'NONE',  ( -1.738889418803986064, 2.342530735446346105E-05, -0.1273558160304689713 ) ) ;
#14321=ORIENTED_EDGE ( 'NONE', *, *, #2655, .T. ) ;
#14322=LINE ( 'NONE', #22833, #39273 ) ;
#14323=EDGE_CURVE ( 'NONE', #26865, #33493, #21213, .T. ) ;
#14328=CARTESIAN_POINT ( 'NONE',  ( -2.119913818043088316, 1.678103251997176359, 1.196659857809422300 ) ) ;
#14335=CARTESIAN_POINT ( 'NONE',  ( 2.708690932417664232, 1.452543555714349788, -1.175597808493610952 ) ) ;
#14336=EDGE_CURVE ( 'NONE', #3944, #9810, #2215, .T. ) ;
#14339=VECTOR ( 'NONE', #23364, 39.37007874015748143 ) ;
#14343=PLANE ( 'NONE',  #39339 ) ;
#14347=CARTESIAN_POINT ( 'NONE',  ( -1.522953965282238586, 0.003526770554233742919, 0.8754220627670087351 ) ) ;
#14349=AXIS2_PLACEMENT_3D ( 'NONE', #28675, #32837, #5187 ) ;
#14351=CARTESIAN_POINT ( 'NONE',  ( -0.9146000759343694275, 1.693252956796532871, -2.012610095043610769 ) ) ;
#14352=ORIENTED_EDGE ( 'NONE', *, *, #14475, .T. ) ;
#14355=DIRECTION ( 'NONE',  ( 0.9998717552508121775, 0.01601477604151182663, 0.000000000000000000 ) ) ;
#14363=CARTESIAN_POINT ( 'NONE',  ( -1.252433315296644256, 1.589416742343778610, -1.807552045033091082 ) ) ;
#14371=CIRCLE ( 'NONE', #33332, 2.246510896728926010 ) ;
#14378=EDGE_CURVE ( 'NONE', #38642, #39685, #22808, .T. ) ;
#14393=CARTESIAN_POINT ( 'NONE',  ( 1.018961996185594021, 0.04424020667788951949, 1.609505285524495344 ) ) ;
#14394=DIRECTION ( 'NONE',  ( 0.01601477604151182663, -0.9998717552508123996, 0.000000000000000000 ) ) ;
#14399=ORIENTED_EDGE ( 'NONE', *, *, #17860, .F. ) ;
#14401=EDGE_CURVE ( 'NONE', #10925, #11129, #40939, .T. ) ;
#14406=CONICAL_SURFACE ( 'NONE', #18538, 2.165354330708661568, 0.2617993877991570129 ) ;
#14408=CARTESIAN_POINT ( 'NONE',  ( -1.217629348859213367, 1.696353326100507042, -2.415009927941460077 ) ) ;
#14412=AXIS2_PLACEMENT_3D ( 'NONE', #34730, #23100, #50662 ) ;
#14413=FACE_OUTER_BOUND ( 'NONE', #9361, .T. ) ;
#14417=ORIENTED_EDGE ( 'NONE', *, *, #26557, .T. ) ;
#14424=ORIENTED_EDGE ( 'NONE', *, *, #32560, .F. ) ;
#14426=LINE ( 'NONE', #30169, #35341 ) ;
#14428=ORIENTED_EDGE ( 'NONE', *, *, #5584, .T. ) ;
#14437=EDGE_CURVE ( 'NONE', #24910, #41415, #37070, .T. ) ;
#14438=CARTESIAN_POINT ( 'NONE',  ( 1.915720322920900331, 0.05860343245220329955, -0.3867724703730804348 ) ) ;
#14440=ORIENTED_EDGE ( 'NONE', *, *, #9791, .F. ) ;
#14442=EDGE_CURVE ( 'NONE', #23316, #640, #30218, .T. ) ;
#14445=EDGE_CURVE ( 'NONE', #640, #22920, #21061, .T. ) ;
#14447=AXIS2_PLACEMENT_3D ( 'NONE', #428, #35549, #16186 ) ;
#14450=ORIENTED_EDGE ( 'NONE', *, *, #14086, .T. ) ;
#14451=CIRCLE ( 'NONE', #45741, 2.086614173228346303 ) ;
#14452=VERTEX_POINT ( 'NONE', #45795 ) ;
#14459=CARTESIAN_POINT ( 'NONE',  ( 0.08139965876239094178, 1.610780518492231694, 0.000000000000000000 ) ) ;
#14461=CARTESIAN_POINT ( 'NONE',  ( 0.9914495361338622192, 1.493354361723550294, 2.781765111341823360 ) ) ;
#14462=CARTESIAN_POINT ( 'NONE',  ( -0.4462167695814984736, 1.635138177150359473, 2.183244083262989133 ) ) ;
#14463=CARTESIAN_POINT ( 'NONE',  ( 0.07982360342473591996, 1.709180471932028711, 0.000000000000000000 ) ) ;
#14465=DIRECTION ( 'NONE',  ( -0.9839295885986321100, -2.068648768805177565E-17, 0.1785568947986229116 ) ) ;
#14467=CARTESIAN_POINT ( 'NONE',  ( 1.971247363764868199, 6.692913385826772199, -0.8960709840011631400 ) ) ;
#14469=EDGE_LOOP ( 'NONE', ( #35871, #22062, #11247, #18472 ) ) ;
#14473=ORIENTED_EDGE ( 'NONE', *, *, #35858, .T. ) ;
#14475=EDGE_CURVE ( 'NONE', #9482, #11793, #30360, .T. ) ;
#14479=LINE ( 'NONE', #50049, #28692 ) ;
#14481=ORIENTED_EDGE ( 'NONE', *, *, #14323, .F. ) ;
#14483=CARTESIAN_POINT ( 'NONE',  ( 2.310037925956077043, 1.712093036975697258, 0.2632538465654825632 ) ) ;
#14485=VECTOR ( 'NONE', #12650, 39.37007874015748143 ) ;
#14487=ORIENTED_EDGE ( 'NONE', *, *, #34094, .F. ) ;
#14492=CARTESIAN_POINT ( 'NONE',  ( -0.2906532981117672110, 1.205361022782829114E-17, 1.877244666688175245 ) ) ;
#14499=DIRECTION ( 'NONE',  ( 0.01601477604151182663, -0.9998717552508123996, 0.000000000000000000 ) ) ;
#14500=FACE_OUTER_BOUND ( 'NONE', #29321, .T. ) ;
#14504=CARTESIAN_POINT ( 'NONE',  ( -2.168245791271168788, 1.205361022782829114E-17, -2.004968704497279486 ) ) ;
#14514=VERTEX_POINT ( 'NONE', #26203 ) ;
#14521=DIRECTION ( 'NONE',  ( 0.3090169943749447867, 1.288287287306305776E-16, 0.9510565162951545304 ) ) ;
#14523=CIRCLE ( 'NONE', #32673, 2.244934639244525076 ) ;
#14525=DIRECTION ( 'NONE',  ( 0.9998717552508121775, 0.01601477604151182663, 0.000000000000000000 ) ) ;
#14531=CARTESIAN_POINT ( 'NONE',  ( 0.000000000000000000, 6.692913385826772199, 0.000000000000000000 ) ) ;
#14532=B_SPLINE_CURVE_WITH_KNOTS ( 'NONE', 3,
 ( #33244, #29353, #4848, #9742 ),
 .UNSPECIFIED., .F., .F.,
 ( 4, 4 ),
 ( 0.1211775127643062860, 0.1625894504277921315 ),
 .UNSPECIFIED. ) ;
#14534=ORIENTED_EDGE ( 'NONE', *, *, #46347, .T. ) ;
#14536=CARTESIAN_POINT ( 'NONE',  ( 0.000000000000000000, 0.000000000000000000, 0.000000000000000000 ) ) ;
#14537=CARTESIAN_POINT ( 'NONE',  ( 2.919426793319799707, 1.448220119383965443, 0.4451252810446820196 ) ) ;
#14540=EDGE_CURVE ( 'NONE', #17362, #20582, #2707, .T. ) ;
#14545=DIRECTION ( 'NONE',  ( -0.01601477604151182663, 0.9998717552508123996, -0.000000000000000000 ) ) ;
#14548=CARTESIAN_POINT ( 'NONE',  ( 1.236813753895252166, 1.738537790538875027, -2.681693691597563767 ) ) ;
#14550=CIRCLE ( 'NONE', #2981, 2.165354330708661568 ) ;
#14552=ORIENTED_EDGE ( 'NONE', *, *, #42754, .T. ) ;
#14560=DIRECTION ( 'NONE',  ( -0.9998717552508122886, -0.01601477604151185785, 0.000000000000000000 ) ) ;
#14562=ORIENTED_EDGE ( 'NONE', *, *, #5961, .F. ) ;
#14570=DIRECTION ( 'NONE',  ( -0.000000000000000000, 1.000000000000000000, -1.156482317317871478E-16 ) ) ;
#14573=EDGE_LOOP ( 'NONE', ( #5067, #17796, #10135, #10129 ) ) ;
#14579=CARTESIAN_POINT ( 'NONE',  ( 2.014645367436137313, 1.707361785030628853, 1.140012488971987592 ) ) ;
#14581=B_SPLINE_CURVE_WITH_KNOTS ( 'NONE', 3,
 ( #42578, #3337, #30965, #46922 ),
 .UNSPECIFIED., .F., .F.,
 ( 4, 4 ),
 ( 4.306281158823199186E-05, 0.05047191582401886617 ),
 .UNSPECIFIED. ) ;
#14583=CARTESIAN_POINT ( 'NONE',  ( 2.147141360900377105, 5.905511811023623991, 0.3405121111982931659 ) ) ;
#14585=ORIENTED_EDGE ( 'NONE', *, *, #48119, .F. ) ;
#14589=CARTESIAN_POINT ( 'NONE',  ( 1.387661672111481170, 6.692913385826772199, -1.663104731517922596 ) ) ;
#14596=ORIENTED_EDGE ( 'NONE', *, *, #37594, .T. ) ;
#14606=ORIENTED_EDGE ( 'NONE', *, *, #321, .F. ) ;
#14608=VERTEX_POINT ( 'NONE', #8096 ) ;
#14622=DIRECTION ( 'NONE',  ( 1.000000000000000000, 0.000000000000000000, 0.000000000000000000 ) ) ;
#14623=DIRECTION ( 'NONE',  ( 0.000000000000000000, 0.000000000000000000, -1.000000000000000000 ) ) ;
#14627=FACE_OUTER_BOUND ( 'NONE', #1191, .T. ) ;
#14630=FACE_OUTER_BOUND ( 'NONE', #2453, .T. ) ;
#14636=ORIENTED_EDGE ( 'NONE', *, *, #2186, .T. ) ;
#14637=EDGE_CURVE ( 'NONE', #41415, #14810, #28217, .T. ) ;
#14638=ORIENTED_EDGE ( 'NONE', *, *, #19979, .F. ) ;
#14644=CARTESIAN_POINT ( 'NONE',  ( 1.033659310791692709, 1.691649499786236133, -2.032992207565942788 ) ) ;
#14646=CARTESIAN_POINT ( 'NONE',  ( 0.08139965876239094178, 1.610780518492231694, 0.000000000000000000 ) ) ;
#14647=CARTESIAN_POINT ( 'NONE',  ( -0.2430652128771645382, 1.574803149606302854, -2.151668812760861194 ) ) ;
#14648=ORIENTED_EDGE ( 'NONE', *, *, #4478, .F. ) ;
#14656=VERTEX_POINT ( 'NONE', #32369 ) ;
#14660=CARTESIAN_POINT ( 'NONE',  ( -2.164823134740036181, 1.673236549936605977, -0.04796011690018290446 ) ) ;
#14662=AXIS2_PLACEMENT_3D ( 'NONE', #22750, #50312, #18630 ) ;
#14668=DIRECTION ( 'NONE',  ( -0.9998717552508121775, -0.01601477604151182663, 0.000000000000000000 ) ) ;
#14669=CARTESIAN_POINT ( 'NONE',  ( -2.044241703397525978, 6.692913385826772199, -0.7159595814952903758 ) ) ;
#14671=EDGE_CURVE ( 'NONE', #33352, #28267, #9618, .T. ) ;
#14674=AXIS2_PLACEMENT_3D ( 'NONE', #15200, #19064, #38207 ) ;
#14677=ORIENTED_EDGE ( 'NONE', *, *, #39482, .F. ) ;
#14683=DIRECTION ( 'NONE',  ( -1.729310098865080642E-17, 1.000000000000000000, 1.276627980444840260E-16 ) ) ;
#14685=B_SPLINE_CURVE_WITH_KNOTS ( 'NONE', 3,
 ( #12959, #28693, #44439, #24829 ),
 .UNSPECIFIED., .F., .F.,
 ( 4, 4 ),
 ( 0.001075175214026108947, 0.04744591858952573737 ),
 .UNSPECIFIED. ) ;
#14686=CARTESIAN_POINT ( 'NONE',  ( 0.5544985201248122664, 1.716783259433079856, -2.194164409418295048 ) ) ;
#14688=EDGE_LOOP ( 'NONE', ( #450, #20563, #26091, #5981 ) ) ;
#14694=AXIS2_PLACEMENT_3D ( 'NONE', #45629, #13661, #36198 ) ;
#14698=CARTESIAN_POINT ( 'NONE',  ( -2.139038182717881487, 1.575216142802386754, 0.3394144611327329364 ) ) ;
#14699=DIRECTION ( 'NONE',  ( 0.000000000000000000, 0.000000000000000000, 1.000000000000000000 ) ) ;
#14700=ORIENTED_EDGE ( 'NONE', *, *, #39564, .F. ) ;
#14702=EDGE_CURVE ( 'NONE', #19859, #9471, #49004, .T. ) ;
#14706=VECTOR ( 'NONE', #11670, 39.37007874015748143 ) ;
#14708=DIRECTION ( 'NONE',  ( -0.01601477604151182663, 0.9998717552508123996, -0.000000000000000000 ) ) ;
#14710=ORIENTED_EDGE ( 'NONE', *, *, #32560, .T. ) ;
#14711=ORIENTED_EDGE ( 'NONE', *, *, #24846, .T. ) ;
#14715=EDGE_CURVE ( 'NONE', #37228, #16522, #16099, .T. ) ;
#14716=CARTESIAN_POINT ( 'NONE',  ( -1.930190994932096782, 5.905511811023623991, -0.9827944786818715306 ) ) ;
#14724=ORIENTED_EDGE ( 'NONE', *, *, #15920, .F. ) ;
#14726=EDGE_CURVE ( 'NONE', #43424, #27061, #9375, .T. ) ;
#14727=DIRECTION ( 'NONE',  ( -0.000000000000000000, 1.000000000000000000, 0.000000000000000000 ) ) ;
#14732=B_SPLINE_CURVE_WITH_KNOTS ( 'NONE', 3,
 ( #10875, #34125, #50073, #2626 ),
 .UNSPECIFIED., .F., .F.,
 ( 4, 4 ),
 ( 0.003451782018764085365, 0.004188683298192677484 ),
 .UNSPECIFIED. ) ;
#14740=CARTESIAN_POINT ( 'NONE',  ( 2.309000164489917406, 1.744884814208895296, 0.2631132722234555410 ) ) ;
#14743=AXIS2_PLACEMENT_3D ( 'NONE', #42630, #47221, #47737 ) ;
#14745=CARTESIAN_POINT ( 'NONE',  ( 2.250827373609354254, 1.648918614562027152, 1.155336271601963505 ) ) ;
#14746=EDGE_LOOP ( 'NONE', ( #10586, #27132, #31342, #31987 ) ) ;
#14747=ORIENTED_EDGE ( 'NONE', *, *, #27416, .F. ) ;
#14756=DIRECTION ( 'NONE',  ( -0.3930250316539278810, 1.288287287306305776E-16, 0.9195277725514489076 ) ) ;
#14757=ADVANCED_FACE ( 'NONE', ( #49334 ), #2699, .T. ) ;
#14759=DIRECTION ( 'NONE',  ( -0.9998717552508122886, -0.01601477604151182316, 0.000000000000000000 ) ) ;
#14762=CARTESIAN_POINT ( 'NONE',  ( 0.3960295651987776888, 1.619527252206727441, 2.457915758890707458 ) ) ;
#14764=AXIS2_PLACEMENT_3D ( 'NONE', #33617, #49306, #25850 ) ;
#14765=EDGE_CURVE ( 'NONE', #16395, #37702, #5241, .T. ) ;
#14766=CARTESIAN_POINT ( 'NONE',  ( -1.977237857982436342, 1.610616070542161049, -0.8986314441088352201 ) ) ;
#14768=ORIENTED_EDGE ( 'NONE', *, *, #10302, .T. ) ;
#14772=CARTESIAN_POINT ( 'NONE',  ( -0.7328193673159020260, 1.696164507524817511, 2.092647490920610309 ) ) ;
#14774=CARTESIAN_POINT ( 'NONE',  ( -1.695772546416001836, 1.692832103184166437, -2.417756147381374010 ) ) ;
#14792=VERTEX_POINT ( 'NONE', #32891 ) ;
#14793=EDGE_CURVE ( 'NONE', #36721, #43798, #48574, .T. ) ;
#14798=CARTESIAN_POINT ( 'NONE',  ( 0.000000000000000000, 1.574803149606302854, 0.000000000000000000 ) ) ;
#14801=PLANE ( 'NONE',  #25181 ) ;
#14804=CIRCLE ( 'NONE', #26368, 3.033577403570481668 ) ;
#14806=VERTEX_POINT ( 'NONE', #20733 ) ;
#14810=VERTEX_POINT ( 'NONE', #6005 ) ;
#14812=CARTESIAN_POINT ( 'NONE',  ( -1.843283979527560623, 1.678378384481335139, -1.157773721536293765 ) ) ;
#14815=ORIENTED_EDGE ( 'NONE', *, *, #45704, .F. ) ;
#14819=FACE_OUTER_BOUND ( 'NONE', #13387, .T. ) ;
#14824=CARTESIAN_POINT ( 'NONE',  ( 2.949046705395496737, 1.666728343919011035, -0.1488625692557980496 ) ) ;
#14827=AXIS2_PLACEMENT_3D ( 'NONE', #4175, #35495, #16388 ) ;
#14829=CARTESIAN_POINT ( 'NONE',  ( 0.07982360342473591996, 1.709180471932028711, 0.000000000000000000 ) ) ;
#14830=CARTESIAN_POINT ( 'NONE',  ( -1.722324667924217456, 1.550974602593178764, -2.398464901896889767 ) ) ;
#14833=DIRECTION ( 'NONE',  ( -0.9998717552508121775, -0.01601477604151182663, 0.000000000000000000 ) ) ;
#14836=EDGE_CURVE ( 'NONE', #1706, #33976, #13505, .T. ) ;
#14840=CARTESIAN_POINT ( 'NONE',  ( 2.010517631316623088, 5.905511811023623991, 0.8058170502102370847 ) ) ;
#14844=CARTESIAN_POINT ( 'NONE',  ( -1.984304711380529218, 1.049866565067837820, -0.4024264094840596662 ) ) ;
#14847=EDGE_CURVE ( 'NONE', #48407, #22473, #37365, .T. ) ;
#14852=EDGE_CURVE ( 'NONE', #46686, #13400, #38527, .T. ) ;
#14853=B_SPLINE_CURVE_WITH_KNOTS ( 'NONE', 3,
 ( #7433, #34051, #3302, #49736 ),
 .UNSPECIFIED., .F., .F.,
 ( 4, 4 ),
 ( 5.977740162239111428E-07, 0.0001168434444380691303 ),
 .UNSPECIFIED. ) ;
#14854=CIRCLE ( 'NONE', #29706, 2.246510896728926010 ) ;
#14856=DIRECTION ( 'NONE',  ( -0.9749279121818259508, 0.000000000000000000, 0.2225209339563041788 ) ) ;
#14857=DIRECTION ( 'NONE',  ( -0.9998717552508121775, -0.01601477604151182316, 0.000000000000000000 ) ) ;
#14862=DIRECTION ( 'NONE',  ( -0.9998717552508122886, -0.01601477604151180928, 0.000000000000000000 ) ) ;
#14864=ORIENTED_EDGE ( 'NONE', *, *, #24991, .F. ) ;
#14866=DIRECTION ( 'NONE',  ( -0.01601477604151182663, 0.9998717552508123996, -0.000000000000000000 ) ) ;
#14867=DIRECTION ( 'NONE',  ( -0.8805955318567391110, 0.000000000000000000, 0.4738686624729965269 ) ) ;
#14869=ORIENTED_EDGE ( 'NONE', *, *, #46733, .T. ) ;
#14880=ORIENTED_EDGE ( 'NONE', *, *, #41255, .F. ) ;
#14881=B_SPLINE_CURVE_WITH_KNOTS ( 'NONE', 3,
 ( #16684, #150, #32698, #15899 ),
 .UNSPECIFIED., .F., .F.,
 ( 4, 4 ),
 ( 0.0002245599449170471845, 0.002724693314481170959 ),
 .UNSPECIFIED. ) ;
#14882=DIRECTION ( 'NONE',  ( -0.01601477604151182663, 0.9998717552508123996, -0.000000000000000000 ) ) ;
#14883=ORIENTED_EDGE ( 'NONE', *, *, #19697, .F. ) ;
#14888=ORIENTED_EDGE ( 'NONE', *, *, #32106, .T. ) ;
#14895=ADVANCED_FACE ( 'NONE', ( #2897 ), #42131, .T. ) ;
#14898=B_SPLINE_CURVE_WITH_KNOTS ( 'NONE', 3,
 ( #36489, #44473, #1108, #9114 ),
 .UNSPECIFIED., .F., .F.,
 ( 4, 4 ),
 ( 0.01473299879128477791, 0.03075082650797690206 ),
 .UNSPECIFIED. ) ;
#14899=CARTESIAN_POINT ( 'NONE',  ( 0.000000000000000000, 1.595182601976580683, 0.000000000000000000 ) ) ;
#14900=CARTESIAN_POINT ( 'NONE',  ( 0.000000000000000000, 1.574803149606302854, 0.000000000000000000 ) ) ;
#14903=LINE ( 'NONE', #42515, #15949 ) ;
#14910=ORIENTED_EDGE ( 'NONE', *, *, #24504, .T. ) ;
#14911=LINE ( 'NONE', #9772, #22162 ) ;
#14917=CARTESIAN_POINT ( 'NONE',  ( 1.306991306359274629, 1.630410611703223545, -1.882644677548868550 ) ) ;
#14918=PLANE ( 'NONE',  #12669 ) ;
#14919=AXIS2_PLACEMENT_3D ( 'NONE', #12879, #486, #16234 ) ;
#14921=VECTOR ( 'NONE', #49942, 39.37007874015748143 ) ;
#14924=VERTEX_POINT ( 'NONE', #18897 ) ;
#14929=EDGE_LOOP ( 'NONE', ( #32627, #4088, #47404, #33522 ) ) ;
#14933=EDGE_CURVE ( 'NONE', #30628, #7819, #33229, .T. ) ;
#14936=DIRECTION ( 'NONE',  ( -0.01601477604151182663, 0.9998717552508123996, -0.000000000000000000 ) ) ;
#14940=FACE_OUTER_BOUND ( 'NONE', #2600, .T. ) ;
#14942=ORIENTED_EDGE ( 'NONE', *, *, #31139, .F. ) ;
#14947=ADVANCED_FACE ( 'NONE', ( #34898 ), #3536, .F. ) ;
#14953=DIRECTION ( 'NONE',  ( 5.779879058770898378E-18, 1.000000000000000000, 1.286990067732318227E-16 ) ) ;
#14961=ORIENTED_EDGE ( 'NONE', *, *, #32815, .T. ) ;
#14969=CARTESIAN_POINT ( 'NONE',  ( -2.165354330708661568, 1.574803149606301966, -1.520079223026944511E-17 ) ) ;
#14978=ORIENTED_EDGE ( 'NONE', *, *, #14185, .T. ) ;
#14980=LINE ( 'NONE', #25388, #39053 ) ;
#14985=LINE ( 'NONE', #49794, #25426 ) ;
#14986=ADVANCED_FACE ( 'NONE', ( #28347 ), #13421, .T. ) ;
#14987=ORIENTED_EDGE ( 'NONE', *, *, #41702, .T. ) ;
#14991=CONICAL_SURFACE ( 'NONE', #40568, 1.850107469027523210, 0.6386652850508578450 ) ;
#14993=AXIS2_PLACEMENT_3D ( 'NONE', #577, #25285, #19920 ) ;
#14994=LINE ( 'NONE', #19857, #37073 ) ;
#15001=CARTESIAN_POINT ( 'NONE',  ( 2.255357468390372322, 1.645600431408117847, -0.5652488166673508285 ) ) ;
#15004=ORIENTED_EDGE ( 'NONE', *, *, #50525, .F. ) ;
#15010=ORIENTED_EDGE ( 'NONE', *, *, #24499, .T. ) ;
#15012=EDGE_CURVE ( 'NONE', #28976, #17224, #38535, .T. ) ;
#15014=CARTESIAN_POINT ( 'NONE',  ( -2.047303704428026006, 1.642302236560388540, 0.7169544859399534786 ) ) ;
#15021=CARTESIAN_POINT ( 'NONE',  ( -0.7032328421997132706, 1.602112857160477688, -2.363122831868675444 ) ) ;
#15023=CARTESIAN_POINT ( 'NONE',  ( 0.08119777152254364916, 1.623385212329073957, 0.000000000000000000 ) ) ;
#15025=CONICAL_SURFACE ( 'NONE', #48777, 1.850107469027523210, 0.6386652850508578450 ) ;
#15026=CARTESIAN_POINT ( 'NONE',  ( -2.339241080213612545, 1.682800407567106360, 1.802537235681883843 ) ) ;
#15027=CARTESIAN_POINT ( 'NONE',  ( 1.528548638478742783, 1.644611471120091872, 2.526375981328617737 ) ) ;
#15029=DIRECTION ( 'NONE',  ( -0.000000000000000000, -1.000000000000000000, -0.000000000000000000 ) ) ;
#15031=CARTESIAN_POINT ( 'NONE',  ( -0.7381027496704857249, 1.531192278308824539, -2.859439394060923068 ) ) ;
#15035=ORIENTED_EDGE ( 'NONE', *, *, #23246, .F. ) ;
#15043=ORIENTED_EDGE ( 'NONE', *, *, #32645, .T. ) ;
#15044=FACE_OUTER_BOUND ( 'NONE', #9451, .T. ) ;
#15053=EDGE_CURVE ( 'NONE', #37182, #38821, #48371, .T. ) ;
#15054=ORIENTED_EDGE ( 'NONE', *, *, #41257, .F. ) ;
#15055=ORIENTED_EDGE ( 'NONE', *, *, #48701, .T. ) ;
#15057=DIRECTION ( 'NONE',  ( -0.1342332658176522420, -1.160734090543305153E-16, -0.9909497617679352555 ) ) ;
#15060=CARTESIAN_POINT ( 'NONE',  ( 0.1067246931122726866, 0.02962905676920215767, 0.000000000000000000 ) ) ;
#15065=CARTESIAN_POINT ( 'NONE',  ( -1.723687301221637380, 0.000000000000000000, -1.311649477509825745 ) ) ;
#15070=CARTESIAN_POINT ( 'NONE',  ( -2.708693778652362827, 1.677031621480801649, -1.175591149396500779 ) ) ;
#15073=ORIENTED_EDGE ( 'NONE', *, *, #12623, .T. ) ;
#15075=ORIENTED_EDGE ( 'NONE', *, *, #39705, .F. ) ;
#15076=AXIS2_PLACEMENT_3D ( 'NONE', #7578, #23315, #27439 ) ;
#15079=CARTESIAN_POINT ( 'NONE',  ( 1.871024688710137163, 0.05788755007212831316, 0.5561875852992870239 ) ) ;
#15083=FACE_OUTER_BOUND ( 'NONE', #14219, .T. ) ;
#15087=LINE ( 'NONE', #83, #23024 ) ;
#15089=AXIS2_PLACEMENT_3D ( 'NONE', #21836, #41207, #37590 ) ;
#15092=CARTESIAN_POINT ( 'NONE',  ( 1.723687301221656032, 6.692913385826772199, -1.311649477509801320 ) ) ;
#15093=CARTESIAN_POINT ( 'NONE',  ( 1.387241876633648729, 1.574803149606302854, 1.662624236931697475 ) ) ;
#15094=CARTESIAN_POINT ( 'NONE',  ( -1.847133429833641927, 0.5249316475426858419, -0.3711179595972480261 ) ) ;
#15100=CARTESIAN_POINT ( 'NONE',  ( 1.738729679588007171, 0.000000000000000000, -0.1273486421339826147 ) ) ;
#15110=AXIS2_PLACEMENT_3D ( 'NONE', #5940, #21436, #33581 ) ;
#15111=CONICAL_SURFACE ( 'NONE', #10139, 3.033577403570480779, 1.554780866114618743 ) ;
#15112=DIRECTION ( 'NONE',  ( -0.000000000000000000, 1.000000000000000000, -0.000000000000000000 ) ) ;
#15119=AXIS2_PLACEMENT_3D ( 'NONE', #49087, #17383, #21259 ) ;
#15121=DIRECTION ( 'NONE',  ( 0.000000000000000000, 0.000000000000000000, 1.000000000000000000 ) ) ;
#15130=VERTEX_POINT ( 'NONE', #2523 ) ;
#15131=CARTESIAN_POINT ( 'NONE',  ( -0.7303501086101937823, 6.692913385826772199, 2.086068174627930816 ) ) ;
#15134=EDGE_CURVE ( 'NONE', #48433, #7184, #18139, .T. ) ;
#15137=ORIENTED_EDGE ( 'NONE', *, *, #33572, .F. ) ;
#15139=EDGE_CURVE ( 'NONE', #42832, #47610, #21632, .T. ) ;
#15141=ADVANCED_FACE ( 'NONE', ( #49458 ), #29117, .F. ) ;
#15142=CONICAL_SURFACE ( 'NONE', #13528, 2.165354330708661568, 0.2617993877991570129 ) ;
#15144=B_SPLINE_CURVE_WITH_KNOTS ( 'NONE', 3,
 ( #21961, #25568, #2587, #48767 ),
 .UNSPECIFIED., .F., .F.,
 ( 4, 4 ),
 ( 0.001281067059624506604, 0.003781316473414019635 ),
 .UNSPECIFIED. ) ;
#15146=CARTESIAN_POINT ( 'NONE',  ( -2.823445274216743073, 1.573787237234608005, 0.8656477926280277124 ) ) ;
#15147=CARTESIAN_POINT ( 'NONE',  ( -2.271515265785818194, 1.047404546102530754, 1.166468901101386901 ) ) ;
#15149=PLANE ( 'NONE',  #30545 ) ;
#15151=CARTESIAN_POINT ( 'NONE',  ( 1.630393911741433000, 1.635590496292660179, -1.626902725537468619 ) ) ;
#15153=ORIENTED_EDGE ( 'NONE', *, *, #9257, .F. ) ;
#15155=DIRECTION ( 'NONE',  ( -0.1342332658176667026, -0.000000000000000000, 0.9909497617679331460 ) ) ;
#15157=DIRECTION ( 'NONE',  ( 1.000000000000000000, -0.000000000000000000, -0.000000000000000000 ) ) ;
#15161=EDGE_LOOP ( 'NONE', ( #19167, #16420, #43671, #15748 ) ) ;
#15162=CARTESIAN_POINT ( 'NONE',  ( 0.08119777152254364916, 1.623385212329073957, 0.000000000000000000 ) ) ;
#15164=FACE_OUTER_BOUND ( 'NONE', #38555, .T. ) ;
#15167=CARTESIAN_POINT ( 'NONE',  ( 0.000000000000000000, 6.692913385826772199, 0.000000000000000000 ) ) ;
#15172=CIRCLE ( 'NONE', #5260, 2.164630168518208109 ) ;
#15173=EDGE_CURVE ( 'NONE', #41147, #41613, #47075, .T. ) ;
#15175=VERTEX_POINT ( 'NONE', #21386 ) ;
#15179=ORIENTED_EDGE ( 'NONE', *, *, #36290, .T. ) ;
#15180=FACE_OUTER_BOUND ( 'NONE', #30778, .T. ) ;
#15185=AXIS2_PLACEMENT_3D ( 'NONE', #20235, #16381, #47826 ) ;
#15187=CARTESIAN_POINT ( 'NONE',  ( -2.277873973731454171, 5.905511811023623991, 1.879489153247634992 ) ) ;
#15190=VERTEX_POINT ( 'NONE', #13636 ) ;
#15191=ORIENTED_EDGE ( 'NONE', *, *, #29603, .T. ) ;
#15192=CARTESIAN_POINT ( 'NONE',  ( 1.461782879395301160, 5.905511811023623991, -1.598346982901808211 ) ) ;
#15194=ORIENTED_EDGE ( 'NONE', *, *, #13576, .T. ) ;
#15197=VERTEX_POINT ( 'NONE', #25756 ) ;
#15199=CARTESIAN_POINT ( 'NONE',  ( -0.5484938307913003186, 0.5249316475426858419, -1.802438616188773990 ) ) ;
#15200=CARTESIAN_POINT ( 'NONE',  ( 1.780101451746606722, 1.205361022782829114E-17, 1.234002060668519585 ) ) ;
#15205=DIRECTION ( 'NONE',  ( 0.000000000000000000, 0.000000000000000000, 1.000000000000000000 ) ) ;
#15206=DIRECTION ( 'NONE',  ( -0.9998717552508122886, -0.01601477604151181275, 0.000000000000000000 ) ) ;
#15207=CARTESIAN_POINT ( 'NONE',  ( -1.780101451746625152, 5.905511811023623991, 1.234002060668494716 ) ) ;
#15208=ORIENTED_EDGE ( 'NONE', *, *, #48197, .T. ) ;
#15209=VERTEX_POINT ( 'NONE', #37649 ) ;
#15214=CARTESIAN_POINT ( 'NONE',  ( 0.8069532150559728390, 6.692913385826772199, -2.010061882867131722 ) ) ;
#15217=CARTESIAN_POINT ( 'NONE',  ( 0.2510238314733705400, 1.613497360050089036, -2.240096307734528835 ) ) ;
#15218=AXIS2_PLACEMENT_3D ( 'NONE', #39426, #50984, #30419 ) ;
#15219=FACE_OUTER_BOUND ( 'NONE', #49949, .T. ) ;
#15220=CONICAL_SURFACE ( 'NONE', #12753, 2.246510896728926010, 0.01601546068027819014 ) ;
#15221=CARTESIAN_POINT ( 'NONE',  ( 0.04921259842519689481, 1.205361022782829114E-17, -2.165433070866142007 ) ) ;
#15222=DIRECTION ( 'NONE',  ( -0.9998717552508121775, -0.01601477604151182663, 0.000000000000000000 ) ) ;
#15223=AXIS2_PLACEMENT_3D ( 'NONE', #15980, #19588, #15480 ) ;
#15225=DIRECTION ( 'NONE',  ( 0.000000000000000000, 1.000000000000000000, 0.000000000000000000 ) ) ;
#15229=LINE ( 'NONE', #23988, #48928 ) ;
#15232=CARTESIAN_POINT ( 'NONE',  ( 1.871024688710137163, 0.05788755007212831316, 0.5561875852992870239 ) ) ;
#15233=EDGE_CURVE ( 'NONE', #44818, #19371, #34867, .T. ) ;
#15234=VERTEX_POINT ( 'NONE', #22396 ) ;
#15237=EDGE_CURVE ( 'NONE', #22113, #37228, #33017, .T. ) ;
#15246=EDGE_LOOP ( 'NONE', ( #11885, #24819, #8315, #44542 ) ) ;
#15248=CARTESIAN_POINT ( 'NONE',  ( -0.5756566573089003658, 1.611847391933241669, 2.896516654582634853 ) ) ;
#15252=ORIENTED_EDGE ( 'NONE', *, *, #1917, .T. ) ;
#15261=ORIENTED_EDGE ( 'NONE', *, *, #34069, .F. ) ;
#15266=ADVANCED_FACE ( 'NONE', ( #50966 ), #1066, .T. ) ;
#15269=EDGE_LOOP ( 'NONE', ( #24836, #26494, #23562, #5196 ) ) ;
#15271=CARTESIAN_POINT ( 'NONE',  ( -1.331808205664968492, 0.000000000000000000, 1.125026879082024367 ) ) ;
#15278=CARTESIAN_POINT ( 'NONE',  ( 1.472219874544873131, 1.643743200001983151, 2.560030851058970214 ) ) ;
#15280=EDGE_LOOP ( 'NONE', ( #27056, #7889, #26178, #648 ) ) ;
#15292=ORIENTED_EDGE ( 'NONE', *, *, #22581, .F. ) ;
#15295=DIRECTION ( 'NONE',  ( 3.586865599282270385E-17, -1.000000000000000000, 1.103923720497139891E-16 ) ) ;
#15298=ORIENTED_EDGE ( 'NONE', *, *, #41563, .T. ) ;
#15305=ORIENTED_EDGE ( 'NONE', *, *, #45428, .T. ) ;
#15307=FACE_OUTER_BOUND ( 'NONE', #14104, .T. ) ;
#15312=LINE ( 'NONE', #6565, #15367 ) ;
#15313=CARTESIAN_POINT ( 'NONE',  ( 1.871024688710137163, 0.05788755007212831316, 0.5561875852992870239 ) ) ;
#15314=ORIENTED_EDGE ( 'NONE', *, *, #44369, .F. ) ;
#15315=VERTEX_POINT ( 'NONE', #38653 ) ;
#15317=CARTESIAN_POINT ( 'NONE',  ( 0.2430652128771965126, 6.692913385826772199, -2.151668812760857197 ) ) ;
#15322=VECTOR ( 'NONE', #46740, 39.37007874015748854 ) ;
#15324=AXIS2_PLACEMENT_3D ( 'NONE', #29167, #44906, #22453 ) ;
#15329=CARTESIAN_POINT ( 'NONE',  ( -2.150793259809249847, 1.575027863729615341, -0.2506944975021367372 ) ) ;
#15330=AXIS2_PLACEMENT_3D ( 'NONE', #23998, #7492, #19349 ) ;
#15334=LINE ( 'NONE', #30833, #3023 ) ;
#15338=VECTOR ( 'NONE', #26042, 39.37007874015748143 ) ;
#15346=FACE_OUTER_BOUND ( 'NONE', #28509, .T. ) ;
#15353=VERTEX_POINT ( 'NONE', #50457 ) ;
#15354=CARTESIAN_POINT ( 'NONE',  ( -0.1516021625288302144, 1.672665368615215975, -2.233444876663337908 ) ) ;
#15356=CARTESIAN_POINT ( 'NONE',  ( -1.221295136473707243, 0.000000000000000000, 1.323086612934683215 ) ) ;
#15360=CARTESIAN_POINT ( 'NONE',  ( 2.695799277629594037, 1.453624836071520265, -1.205759334241453651 ) ) ;
#15361=AXIS2_PLACEMENT_3D ( 'NONE', #48684, #17492, #41250 ) ;
#15362=VECTOR ( 'NONE', #8164, 39.37007874015748143 ) ;
#15366=PLANE ( 'NONE',  #41054 ) ;
#15367=VECTOR ( 'NONE', #22307, 39.37007874015748143 ) ;
#15368=ADVANCED_FACE ( 'NONE', ( #46362 ), #11026, .F. ) ;
#15371=CONICAL_SURFACE ( 'NONE', #36013, 3.483074324928249421, 1.244861948955335196 ) ;
#15376=CARTESIAN_POINT ( 'NONE',  ( -1.023703982469668539, 0.003911508537882584999, -1.492733126648604136 ) ) ;
#15379=LINE ( 'NONE', #46582, #14339 ) ;
#15381=CARTESIAN_POINT ( 'NONE',  ( 0.3136974817028393425, 1.724153038295522800, -2.936457595020219635 ) ) ;
#15382=CARTESIAN_POINT ( 'NONE',  ( -1.695772546416001836, 1.692832103184166437, -2.417756147381374010 ) ) ;
#15384=ORIENTED_EDGE ( 'NONE', *, *, #28234, .T. ) ;
#15387=ORIENTED_EDGE ( 'NONE', *, *, #46450, .F. ) ;
#15391=B_SPLINE_CURVE_WITH_KNOTS ( 'NONE', 3,
 ( #32073, #5660, #21407, #47763 ),
 .UNSPECIFIED., .F., .F.,
 ( 4, 4 ),
 ( 0.001762245066137694887, 0.04551044212210949430 ),
 .UNSPECIFIED. ) ;
#15393=ORIENTED_EDGE ( 'NONE', *, *, #41242, .T. ) ;
#15394=ORIENTED_EDGE ( 'NONE', *, *, #7683, .F. ) ;
#15397=CIRCLE ( 'NONE', #28582, 2.165354330708661568 ) ;
#15399=B_SPLINE_CURVE_WITH_KNOTS ( 'NONE', 3,
 ( #19014, #42511, #50455, #4045 ),
 .UNSPECIFIED., .F., .F.,
 ( 4, 4 ),
 ( 2.472935563822449734E-07, 0.01679640739751839945 ),
 .UNSPECIFIED. ) ;
#15403=ADVANCED_FACE ( 'NONE', ( #28807 ), #28266, .T. ) ;
#15407=ADVANCED_FACE ( 'NONE', ( #31667 ), #35718, .T. ) ;
#15408=AXIS2_PLACEMENT_3D ( 'NONE', #16657, #32410, #48102 ) ;
#15410=CARTESIAN_POINT ( 'NONE',  ( 2.288146023452536149, 0.5219625294164390583, -0.05349855421841626796 ) ) ;
#15413=CARTESIAN_POINT ( 'NONE',  ( -1.936656578200692369, 1.644074453030845762, 0.9862737574026090304 ) ) ;
#15414=CARTESIAN_POINT ( 'NONE',  ( 1.214590356376888280, 1.727355838235203667, 1.936932008856820930 ) ) ;
#15415=CARTESIAN_POINT ( 'NONE',  ( 1.236813753895252166, 1.640077341046696890, -2.681693691597563767 ) ) ;
#15418=CARTESIAN_POINT ( 'NONE',  ( 0.2646829987306325571, 0.000000000000000000, -2.940868978332396910 ) ) ;
#15419=ORIENTED_EDGE ( 'NONE', *, *, #41833, .F. ) ;
#15422=LINE ( 'NONE', #31419, #38129 ) ;
#15423=ADVANCED_FACE ( 'NONE', ( #23917 ), #24939, .T. ) ;
#15425=CARTESIAN_POINT ( 'NONE',  ( -0.2708302372837931293, 1.608962593404075214, -2.460163500185826635 ) ) ;
#15426=DIRECTION ( 'NONE',  ( -0.9998717552508121775, -0.01601477604151182316, 0.000000000000000000 ) ) ;
#15428=PLANE ( 'NONE',  #15218 ) ;
#15430=ORIENTED_EDGE ( 'NONE', *, *, #9107, .T. ) ;
#15431=CIRCLE ( 'NONE', #47513, 2.164630168518208109 ) ;
#15436=EDGE_CURVE ( 'NONE', #20856, #11610, #27452, .T. ) ;
#15438=EDGE_CURVE ( 'NONE', #972, #1849, #289, .T. ) ;
#15444=ORIENTED_EDGE ( 'NONE', *, *, #7624, .F. ) ;
#15447=ORIENTED_EDGE ( 'NONE', *, *, #6762, .F. ) ;
#15449=ORIENTED_EDGE ( 'NONE', *, *, #27515, .F. ) ;
#15450=CIRCLE ( 'NONE', #40294, 2.244934639244525076 ) ;
#15455=CARTESIAN_POINT ( 'NONE',  ( -1.905671854841497481, 1.591126119768930147, 2.256015092822653223 ) ) ;
#15457=B_SPLINE_CURVE_WITH_KNOTS ( 'NONE', 3,
 ( #6318, #29554, #9680, #33443 ),
 .UNSPECIFIED., .F., .F.,
 ( 4, 4 ),
 ( 1.069002736119642924E-05, 0.002510697369532217862 ),
 .UNSPECIFIED. ) ;
#15465=ORIENTED_EDGE ( 'NONE', *, *, #2755, .T. ) ;
#15466=VERTEX_POINT ( 'NONE', #48138 ) ;
#15468=CARTESIAN_POINT ( 'NONE',  ( 0.5469786881612729301, 0.03668053021573630668, -1.796948620166157307 ) ) ;
#15469=DIRECTION ( 'NONE',  ( -4.561975526775755056E-17, -1.000000000000000000, 1.067327232801816862E-16 ) ) ;
#15471=DIRECTION ( 'NONE',  ( -0.3513748240813434620, 0.000000000000000000, 0.9362348706397368714 ) ) ;
#15473=CARTESIAN_POINT ( 'NONE',  ( 2.152441353505198940, 1.205361022782829114E-17, -0.2419059403264799679 ) ) ;
#15475=DIRECTION ( 'NONE',  ( 1.142080616180681165E-16, -1.000000000000000000, -2.072570748943160811E-17 ) ) ;
#15476=FACE_OUTER_BOUND ( 'NONE', #15246, .T. ) ;
#15477=ORIENTED_EDGE ( 'NONE', *, *, #10476, .F. ) ;
#15480=DIRECTION ( 'NONE',  ( 0.000000000000000000, 0.000000000000000000, -1.000000000000000000 ) ) ;
#15489=EDGE_CURVE ( 'NONE', #31373, #3078, #18400, .T. ) ;
#15496=CIRCLE ( 'NONE', #2312, 2.246510896728926010 ) ;
#15500=VERTEX_POINT ( 'NONE', #44037 ) ;
#15501=LINE ( 'NONE', #20119, #8691 ) ;
#15502=CARTESIAN_POINT ( 'NONE',  ( 0.7308738700548030875, -2.448952757038419718E-16, 2.087463732006447081 ) ) ;
#15504=AXIS2_PLACEMENT_3D ( 'NONE', #13679, #5677, #21679 ) ;
#15510=AXIS2_PLACEMENT_3D ( 'NONE', #6699, #34576, #14699 ) ;
#15514=CIRCLE ( 'NONE', #32866, 1.850107469027523432 ) ;
#15521=EDGE_LOOP ( 'NONE', ( #41654, #33896, #16260, #33156 ) ) ;
#15524=EDGE_CURVE ( 'NONE', #13212, #13391, #48267, .T. ) ;
#15529=EDGE_CURVE ( 'NONE', #33353, #47061, #13583, .T. ) ;
#15532=ADVANCED_FACE ( 'NONE', ( #33970, #17957 ), #9959, .F. ) ;
#15537=DIRECTION ( 'NONE',  ( -0.01601477604151182663, 0.9998717552508123996, -0.000000000000000000 ) ) ;
#15538=CARTESIAN_POINT ( 'NONE',  ( 0.1067246931122726866, 0.02962905676920215767, 0.000000000000000000 ) ) ;
#15540=VERTEX_POINT ( 'NONE', #29056 ) ;
#15550=LINE ( 'NONE', #32070, #13059 ) ;
#15551=EDGE_LOOP ( 'NONE', ( #18171, #2151, #29318, #8973, #25134, #8595, #27695, #42772, #30319, #8155, #15932, #23707, #10124 ) ) ;
#15554=ORIENTED_EDGE ( 'NONE', *, *, #30839, .F. ) ;
#15556=PLANE ( 'NONE',  #8253 ) ;
#15557=AXIS2_PLACEMENT_3D ( 'NONE', #17503, #33263, #48949 ) ;
#15558=CARTESIAN_POINT ( 'NONE',  ( -1.738729679588005617, 0.000000000000000000, -0.1273486421340072894 ) ) ;
#15559=EDGE_LOOP ( 'NONE', ( #36134, #40167, #15888, #47646 ) ) ;
#15563=CARTESIAN_POINT ( 'NONE',  ( 0.000000000000000000, 0.000000000000000000, 0.000000000000000000 ) ) ;
#15565=ORIENTED_EDGE ( 'NONE', *, *, #25445, .T. ) ;
#15574=VECTOR ( 'NONE', #34497, 39.37007874015748143 ) ;
#15579=ORIENTED_EDGE ( 'NONE', *, *, #23681, .F. ) ;
#15581=ORIENTED_EDGE ( 'NONE', *, *, #28972, .T. ) ;
#15584=CARTESIAN_POINT ( 'NONE',  ( 1.985331756560078986, 0.01929593017201648025, 0.5933282030623656667 ) ) ;
#15586=DIRECTION ( 'NONE',  ( 0.000000000000000000, 0.000000000000000000, -1.000000000000000000 ) ) ;
#15587=CARTESIAN_POINT ( 'NONE',  ( 0.8067290215917983787, 1.574803149606302854, 2.009464521518182334 ) ) ;
#15588=VECTOR ( 'NONE', #3905, 39.37007874015748143 ) ;
#15598=LINE ( 'NONE', #18463, #34419 ) ;
#15601=CARTESIAN_POINT ( 'NONE',  ( -0.04921259842519708910, 1.718497255264965551, 2.952755905511811108 ) ) ;
#15604=FACE_OUTER_BOUND ( 'NONE', #26407, .T. ) ;
#15606=DIRECTION ( 'NONE',  ( 1.558091277195270436E-17, -1.000000000000000000, -1.150229170499806500E-16 ) ) ;
#15609=CARTESIAN_POINT ( 'NONE',  ( -2.100227814008681637, 1.588094595312779855, -2.076109931251943763 ) ) ;
#15610=CARTESIAN_POINT ( 'NONE',  ( -2.437180031585919782, 0.000000000000000000, -1.667735833703134274 ) ) ;
#15614=ORIENTED_EDGE ( 'NONE', *, *, #19065, .F. ) ;
#15616=CIRCLE ( 'NONE', #45300, 2.165354330708661568 ) ;
#15620=VECTOR ( 'NONE', #46816, 39.37007874015748143 ) ;
#15622=ORIENTED_EDGE ( 'NONE', *, *, #39092, .F. ) ;
#15624=CARTESIAN_POINT ( 'NONE',  ( 1.786266331718541878, 0.01831036388897721787, 1.017116489302096083 ) ) ;
#15629=CARTESIAN_POINT ( 'NONE',  ( 0.2927555892279174454, 1.720075335370203407, -2.703774112429984111 ) ) ;
#15630=EDGE_CURVE ( 'NONE', #11815, #21618, #40950, .T. ) ;
#15632=ORIENTED_EDGE ( 'NONE', *, *, #23638, .T. ) ;
#15633=ORIENTED_EDGE ( 'NONE', *, *, #3357, .F. ) ;
#15637=ADVANCED_FACE ( 'NONE', ( #21328 ), #30741, .T. ) ;
#15642=EDGE_CURVE ( 'NONE', #26109, #34644, #24151, .T. ) ;
#15643=AXIS2_PLACEMENT_3D ( 'NONE', #44125, #25287, #41045 ) ;
#15650=CARTESIAN_POINT ( 'NONE',  ( -0.2155737599805752913, 0.01633517799311254987, -1.846213753763441545 ) ) ;
#15654=EDGE_CURVE ( 'NONE', #21553, #8462, #22091, .T. ) ;
#15657=CARTESIAN_POINT ( 'NONE',  ( 1.787005229743228396, 1.641566817664441791, -1.776638477264515181 ) ) ;
#15661=DIRECTION ( 'NONE',  ( -1.729310098864894520E-17, 1.000000000000000000, -1.276627980444842972E-16 ) ) ;
#15663=ORIENTED_EDGE ( 'NONE', *, *, #25858, .T. ) ;
#15665=VERTEX_POINT ( 'NONE', #23336 ) ;
#15667=CARTESIAN_POINT ( 'NONE',  ( -1.629664903723128777, 0.001228770104821741253, -0.6430327822565008455 ) ) ;
#15668=PLANE ( 'NONE',  #36455 ) ;
#15669=VERTEX_POINT ( 'NONE', #38844 ) ;
#15670=CARTESIAN_POINT ( 'NONE',  ( 2.500827540798396420, 1.754748926069762405, -1.122424414593431674 ) ) ;
#15671=CARTESIAN_POINT ( 'NONE',  ( 0.08139965876239094178, 1.610780518492231694, 0.000000000000000000 ) ) ;
#15672=DIRECTION ( 'NONE',  ( 1.241861098869884156E-16, 1.000000000000000000, 3.427318860986280993E-17 ) ) ;
#15677=ORIENTED_EDGE ( 'NONE', *, *, #47918, .T. ) ;
#15680=CARTESIAN_POINT ( 'NONE',  ( 0.04921259842519683236, 0.5238019749767087729, 2.217183491882336543 ) ) ;
#15686=AXIS2_PLACEMENT_3D ( 'NONE', #24348, #40360, #5233 ) ;
#15687=ADVANCED_FACE ( 'NONE', ( #34472 ), #18467, .F. ) ;
#15690=EDGE_CURVE ( 'NONE', #42820, #38377, #25543, .T. ) ;
#15691=CARTESIAN_POINT ( 'NONE',  ( 2.273698311726526811, 0.5219991175371894165, 0.2583313113525125271 ) ) ;
#15694=LINE ( 'NONE', #15192, #28991 ) ;
#15704=ADVANCED_FACE ( 'NONE', ( #49906 ), #14310, .T. ) ;
#15716=EDGE_CURVE ( 'NONE', #34643, #22357, #10734, .T. ) ;
#15720=AXIS2_PLACEMENT_3D ( 'NONE', #6597, #43389, #10963 ) ;
#15722=DIRECTION ( 'NONE',  ( -0.01601477604151182663, 0.9998717552508123996, -0.000000000000000000 ) ) ;
#15728=DIRECTION ( 'NONE',  ( 3.986037398843765983E-20, 1.000000000000000000, 1.160734090543304660E-16 ) ) ;
#15729=CARTESIAN_POINT ( 'NONE',  ( 1.306991306359274629, 1.630410611703223545, -1.882644677548868550 ) ) ;
#15731=DIRECTION ( 'NONE',  ( -0.000000000000000000, -1.000000000000000000, -0.000000000000000000 ) ) ;
#15736=DIRECTION ( 'NONE',  ( -0.000000000000000000, -1.000000000000000000, -0.000000000000000000 ) ) ;
#15740=CARTESIAN_POINT ( 'NONE',  ( -1.599172890215280196, 1.205361022782829114E-17, 1.460879300779170498 ) ) ;
#15746=DIRECTION ( 'NONE',  ( 0.000000000000000000, 0.000000000000000000, -1.000000000000000000 ) ) ;
#15748=ORIENTED_EDGE ( 'NONE', *, *, #8032, .T. ) ;
#15749=CONICAL_SURFACE ( 'NONE', #26484, 3.483074324928249421, 1.244861948955335196 ) ;
#15754=ORIENTED_EDGE ( 'NONE', *, *, #37063, .T. ) ;
#15756=VECTOR ( 'NONE', #44762, 39.37007874015748854 ) ;
#15760=DIRECTION ( 'NONE',  ( -0.000000000000000000, -1.000000000000000000, -0.000000000000000000 ) ) ;
#15764=FACE_OUTER_BOUND ( 'NONE', #46938, .T. ) ;
#15769=EDGE_CURVE ( 'NONE', #21408, #33697, #13848, .T. ) ;
#15773=CARTESIAN_POINT ( 'NONE',  ( -1.441820560696044584, 0.5249316475426859530, 1.212758804667590784 ) ) ;
#15782=VERTEX_POINT ( 'NONE', #22845 ) ;
#15793=CARTESIAN_POINT ( 'NONE',  ( 0.9432913529151772947, 1.723010488186151878, -2.072188145589165753 ) ) ;
#15795=CARTESIAN_POINT ( 'NONE',  ( 0.000000000000000000, 6.692913385826772199, 0.000000000000000000 ) ) ;
#15799=ADVANCED_FACE ( 'NONE', ( #47561 ), #25028, .T. ) ;
#15802=CARTESIAN_POINT ( 'NONE',  ( -1.675814739737315540, 1.582635513994296250, 1.399362935606387470 ) ) ;
#15804=EDGE_CURVE ( 'NONE', #13670, #47197, #43458, .T. ) ;
#15813=CARTESIAN_POINT ( 'NONE',  ( 0.7117868624172632996, 0.000000000000000000, -1.591464117667681366 ) ) ;
#15814=CARTESIAN_POINT ( 'NONE',  ( 0.4373159485544403369, 1.722342034578614012, 2.685422482927756427 ) ) ;
#15823=EDGE_LOOP ( 'NONE', ( #19672, #3591, #21340, #29872 ) ) ;
#15824=CARTESIAN_POINT ( 'NONE',  ( -1.790681247139289889, 1.679220913509628543, -1.240985722462402352 ) ) ;
#15827=VECTOR ( 'NONE', #44703, 39.37007874015748143 ) ;
#15830=DIRECTION ( 'NONE',  ( -0.01601477604151182663, 0.9998717552508123996, -0.000000000000000000 ) ) ;
#15831=ORIENTED_EDGE ( 'NONE', *, *, #235, .T. ) ;
#15832=ORIENTED_EDGE ( 'NONE', *, *, #38457, .T. ) ;
#15834=EDGE_CURVE ( 'NONE', #619, #42300, #353, .T. ) ;
#15838=PLANE ( 'NONE',  #35008 ) ;
#15840=CARTESIAN_POINT ( 'NONE',  ( -1.942732458483407365, 0.000000000000000000, 2.223636218514596585 ) ) ;
#15841=ORIENTED_EDGE ( 'NONE', *, *, #50894, .T. ) ;
#15842=DIRECTION ( 'NONE',  ( -0.000000000000000000, 1.000000000000000000, 0.000000000000000000 ) ) ;
#15845=ORIENTED_EDGE ( 'NONE', *, *, #31089, .F. ) ;
#15848=DIRECTION ( 'NONE',  ( -0.000000000000000000, -1.000000000000000000, -0.000000000000000000 ) ) ;
#15852=B_SPLINE_CURVE_WITH_KNOTS ( 'NONE', 3,
 ( #14812, #50867, #26673, #7064 ),
 .UNSPECIFIED., .F., .F.,
 ( 4, 4 ),
 ( 0.01101059834352955021, 0.03073596030694578790 ),
 .UNSPECIFIED. ) ;
#15864=ORIENTED_EDGE ( 'NONE', *, *, #28274, .T. ) ;
#15867=EDGE_CURVE ( 'NONE', #21112, #9779, #8871, .T. ) ;
#15871=FACE_OUTER_BOUND ( 'NONE', #46592, .T. ) ;
#15875=CARTESIAN_POINT ( 'NONE',  ( 1.930190994932111215, 1.205361022782829114E-17, -0.9827944786818438860 ) ) ;
#15879=EDGE_CURVE ( 'NONE', #34103, #49753, #4998, .T. ) ;
#15885=EDGE_LOOP ( 'NONE', ( #33064, #17851, #2880, #16040 ) ) ;
#15886=CARTESIAN_POINT ( 'NONE',  ( -1.659559921305661101, 0.5251570559280069883, 1.386400150466028158 ) ) ;
#15888=ORIENTED_EDGE ( 'NONE', *, *, #48885, .T. ) ;
#15890=ADVANCED_FACE ( 'NONE', ( #20490 ), #1968, .T. ) ;
#15898=CARTESIAN_POINT ( 'NONE',  ( 0.3491433680425106156, 0.5228997897064754374, 2.199551517448510740 ) ) ;
#15899=CARTESIAN_POINT ( 'NONE',  ( -1.613060539954027872, 1.682065834201676324, -1.474157253483306507 ) ) ;
#15900=ADVANCED_FACE ( 'NONE', ( #3983 ), #16626, .T. ) ;
#15905=EDGE_LOOP ( 'NONE', ( #5074, #8339, #12020, #1918 ) ) ;
#15906=CARTESIAN_POINT ( 'NONE',  ( 1.325491792074623643, 1.485765544018708750, -2.638988599164732385 ) ) ;
#15913=CARTESIAN_POINT ( 'NONE',  ( 1.191741137761282321, 0.03104109646116221324, -1.556565482633349928 ) ) ;
#15914=CARTESIAN_POINT ( 'NONE',  ( 1.325491792074623643, 0.000000000000000000, -2.638988599164732385 ) ) ;
#15917=CARTESIAN_POINT ( 'NONE',  ( -1.076323050859473884, 0.5246904699002969963, 1.897411179605189790 ) ) ;
#15918=CARTESIAN_POINT ( 'NONE',  ( -1.695772546416001836, 1.594396608463251486, -2.417756147381374010 ) ) ;
#15920=EDGE_CURVE ( 'NONE', #12848, #28528, #11721, .T. ) ;
#15921=CARTESIAN_POINT ( 'NONE',  ( 0.04921259842519689481, 1.205361022782829114E-17, 1.934165248549660987 ) ) ;
#15929=ORIENTED_EDGE ( 'NONE', *, *, #9724, .T. ) ;
#15932=ORIENTED_EDGE ( 'NONE', *, *, #28067, .F. ) ;
#15933=CARTESIAN_POINT ( 'NONE',  ( 4.821444091131312140E-17, 10.31496062992126284, 0.3937007874015748254 ) ) ;
#15936=EDGE_CURVE ( 'NONE', #38951, #1805, #3578, .T. ) ;
#15938=ORIENTED_EDGE ( 'NONE', *, *, #49366, .F. ) ;
#15940=EDGE_CURVE ( 'NONE', #6661, #25341, #45483, .T. ) ;
#15946=AXIS2_PLACEMENT_3D ( 'NONE', #2482, #34232, #14093 ) ;
#15947=ORIENTED_EDGE ( 'NONE', *, *, #4932, .F. ) ;
#15949=VECTOR ( 'NONE', #866, 39.37007874015748143 ) ;
#15951=ORIENTED_EDGE ( 'NONE', *, *, #40246, .T. ) ;
#15952=VERTEX_POINT ( 'NONE', #1379 ) ;
#15954=DIRECTION ( 'NONE',  ( 1.776356839400250149E-14, 0.000000000000000000, 1.000000000000000000 ) ) ;
#15955=AXIS2_PLACEMENT_3D ( 'NONE', #41960, #26708, #38099 ) ;
#15956=CARTESIAN_POINT ( 'NONE',  ( -0.04921259842519701277, 1.049866565877818125, 2.024102350102944037 ) ) ;
#15958=DIRECTION ( 'NONE',  ( -0.01601477604151182663, 0.9998717552508123996, -0.000000000000000000 ) ) ;
#15963=LINE ( 'NONE', #47677, #13196 ) ;
#15964=ORIENTED_EDGE ( 'NONE', *, *, #42397, .T. ) ;
#15967=FACE_OUTER_BOUND ( 'NONE', #28315, .T. ) ;
#15970=EDGE_CURVE ( 'NONE', #45742, #38443, #41452, .T. ) ;
#15971=LINE ( 'NONE', #5124, #44570 ) ;
#15973=LINE ( 'NONE', #32249, #41644 ) ;
#15976=B_SPLINE_CURVE_WITH_KNOTS ( 'NONE', 3,
 ( #23075, #46533, #30572, #50631 ),
 .UNSPECIFIED., .F., .F.,
 ( 4, 4 ),
 ( 3.552899504225758744E-07, 0.04838472165043559980 ),
 .UNSPECIFIED. ) ;
#15977=DIRECTION ( 'NONE',  ( -1.118904554427325505E-16, -1.000000000000000000, 3.087980359898369198E-17 ) ) ;
#15980=CARTESIAN_POINT ( 'NONE',  ( 0.002207914879453961969, 5.905511811023623991, 0.04916304461325442243 ) ) ;
#15981=AXIS2_PLACEMENT_3D ( 'NONE', #8165, #23907, #39658 ) ;
#15983=AXIS2_PLACEMENT_3D ( 'NONE', #40258, #40766, #4883 ) ;
#15986=CARTESIAN_POINT ( 'NONE',  ( 0.4506430153629077950, 0.03513753811042658048, -1.817852439337431569 ) ) ;
#15989=CARTESIAN_POINT ( 'NONE',  ( -2.455254038445241704, 1.582553845862669784, -1.640354883688478038 ) ) ;
#15992=CARTESIAN_POINT ( 'NONE',  ( 0.8451757313534469240, 1.655822191538975918, 2.111905413333155401 ) ) ;
#15995=EDGE_LOOP ( 'NONE', ( #10346, #19563, #9988, #40840 ) ) ;
#15996=EDGE_CURVE ( 'NONE', #15197, #17350, #22565, .T. ) ;
#15998=CARTESIAN_POINT ( 'NONE',  ( -1.202103464817552592, 0.5249316475426857309, 1.450716273920663824 ) ) ;
#16000=ORIENTED_EDGE ( 'NONE', *, *, #4406, .T. ) ;
#16003=ORIENTED_EDGE ( 'NONE', *, *, #29109, .F. ) ;
#16010=DIRECTION ( 'NONE',  ( -0.000000000000000000, -1.000000000000000000, -0.000000000000000000 ) ) ;
#16015=EDGE_LOOP ( 'NONE', ( #19407, #24069, #12023, #4155, #46929, #34101, #33587, #2893, #41249, #6371, #11399, #31648, #45473 ) ) ;
#16016=CIRCLE ( 'NONE', #44865, 0.3937007874015748254 ) ;
#16021=CARTESIAN_POINT ( 'NONE',  ( -0.7148041136150271591, 6.692913385826772199, -2.044646019095620382 ) ) ;
#16024=CYLINDRICAL_SURFACE ( 'NONE', #41570, 0.3937007874015748254 ) ;
#16030=DIRECTION ( 'NONE',  ( -6.104789737168038204E-17, 1.000000000000000000, -1.134460028949771622E-16 ) ) ;
#16031=B_SPLINE_CURVE_WITH_KNOTS ( 'NONE', 3,
 ( #24236, #32241, #13129, #29114 ),
 .UNSPECIFIED., .F., .F.,
 ( 4, 4 ),
 ( 2.894122015862211124E-07, 0.01950060374906107188 ),
 .UNSPECIFIED. ) ;
#16032=VERTEX_POINT ( 'NONE', #48327 ) ;
#16033=DIRECTION ( 'NONE',  ( 0.5508969814521065267, 9.684980370528620210E-17, -0.8345732537212999791 ) ) ;
#16036=EDGE_CURVE ( 'NONE', #40614, #42095, #5764, .T. ) ;
#16040=ORIENTED_EDGE ( 'NONE', *, *, #20932, .T. ) ;
#16048=ORIENTED_EDGE ( 'NONE', *, *, #40143, .T. ) ;
#16049=VECTOR ( 'NONE', #47686, 39.37007874015748854 ) ;
#16051=AXIS2_PLACEMENT_3D ( 'NONE', #39524, #38769, #3653 ) ;
#16057=EDGE_LOOP ( 'NONE', ( #39133, #40809, #8794, #20164 ) ) ;
#16068=CARTESIAN_POINT ( 'NONE',  ( 0.08119777152254364916, 1.623385212329073957, 0.000000000000000000 ) ) ;
#16072=CARTESIAN_POINT ( 'NONE',  ( -1.093343507848659524, 0.007001814219102117827, -1.421132763804449306 ) ) ;
#16074=CARTESIAN_POINT ( 'NONE',  ( -0.7148041136150268260, 5.905511811023623991, -2.044646019095619938 ) ) ;
#16075=ORIENTED_EDGE ( 'NONE', *, *, #30650, .F. ) ;
#16076=VERTEX_POINT ( 'NONE', #46241 ) ;
#16078=LINE ( 'NONE', #16336, #1912 ) ;
#16081=B_SPLINE_CURVE_WITH_KNOTS ( 'NONE', 3,
 ( #41804, #26803, #37941, #42053 ),
 .UNSPECIFIED., .F., .F.,
 ( 4, 4 ),
 ( 2.008389287922521166E-07, 0.01785224886139480382 ),
 .UNSPECIFIED. ) ;
#16082=FACE_OUTER_BOUND ( 'NONE', #16923, .T. ) ;
#16087=ORIENTED_EDGE ( 'NONE', *, *, #5644, .T. ) ;
#16091=CARTESIAN_POINT ( 'NONE',  ( 1.902660579019252562, 1.639951345248664039, -1.314902632263422966 ) ) ;
#16096=AXIS2_PLACEMENT_3D ( 'NONE', #16702, #28303, #32197 ) ;
#16097=AXIS2_PLACEMENT_3D ( 'NONE', #11595, #15722, #27333 ) ;
#16099=LINE ( 'NONE', #27966, #11272 ) ;
#16103=DIRECTION ( 'NONE',  ( 0.000000000000000000, 1.160734090543304660E-16, -1.000000000000000000 ) ) ;
#16108=CARTESIAN_POINT ( 'NONE',  ( -0.8949303405208601792, 6.692913385826772199, -1.971765468592543202 ) ) ;
#16109=DIRECTION ( 'NONE',  ( -0.7818314824680221431, 0.000000000000000000, -0.6234898018587431423 ) ) ;
#16115=ORIENTED_EDGE ( 'NONE', *, *, #10997, .T. ) ;
#16123=LINE ( 'NONE', #4506, #652 ) ;
#16131=CONICAL_SURFACE ( 'NONE', #9540, 2.244934639244524632, 1.554780866114618743 ) ;
#16132=CARTESIAN_POINT ( 'NONE',  ( 1.836342932631641167, 0.000000000000000000, 1.044063857347276469 ) ) ;
#16136=CARTESIAN_POINT ( 'NONE',  ( 1.305557278495039775, 1.728812839972934334, -1.880670907523083191 ) ) ;
#16139=B_SPLINE_CURVE_WITH_KNOTS ( 'NONE', 3,
 ( #39656, #2894, #32955, #29312 ),
 .UNSPECIFIED., .F., .F.,
 ( 4, 4 ),
 ( 0.1211775127643062444, 0.1625894504277921315 ),
 .UNSPECIFIED. ) ;
#16140=AXIS2_PLACEMENT_3D ( 'NONE', #47706, #7740, #35115 ) ;
#16145=DIRECTION ( 'NONE',  ( -0.01601477604151182663, 0.9998717552508123996, -0.000000000000000000 ) ) ;
#16147=DIRECTION ( 'NONE',  ( 0.9195277725514544587, 0.000000000000000000, -0.3930250316539147803 ) ) ;
#16153=EDGE_LOOP ( 'NONE', ( #6822, #19662, #30290, #30422, #13804 ) ) ;
#16155=CARTESIAN_POINT ( 'NONE',  ( 0.002207914879453961969, 5.905511811023623991, 0.04916304461325442243 ) ) ;
#16158=DIRECTION ( 'NONE',  ( -1.045785279492548401E-16, -1.000000000000000000, 5.036236473261409814E-17 ) ) ;
#16159=ORIENTED_EDGE ( 'NONE', *, *, #15438, .T. ) ;
#16161=DIRECTION ( 'NONE',  ( -0.08963930890342654279, 0.000000000000000000, -0.9959742939952397345 ) ) ;
#16165=EDGE_CURVE ( 'NONE', #17400, #34114, #11408, .T. ) ;
#16169=ORIENTED_EDGE ( 'NONE', *, *, #49969, .T. ) ;
#16175=DIRECTION ( 'NONE',  ( -0.9998717552508122886, -0.01601477604151182316, 0.000000000000000000 ) ) ;
#16177=ORIENTED_EDGE ( 'NONE', *, *, #14726, .F. ) ;
#16180=CARTESIAN_POINT ( 'NONE',  ( 1.034308760555261886, 1.626043101691516890, -2.034340803895991812 ) ) ;
#16186=DIRECTION ( 'NONE',  ( -0.9998717552508122886, -0.01601477604151185785, 0.000000000000000000 ) ) ;
#16187=VECTOR ( 'NONE', #47651, 39.37007874015748143 ) ;
#16188=CARTESIAN_POINT ( 'NONE',  ( -1.500342777408262496, 0.001329947905571405567, -0.9314002160103560524 ) ) ;
#16190=CARTESIAN_POINT ( 'NONE',  ( 2.305855796294430160, 1.748229977355783005, -1.039089491665910359 ) ) ;
#16195=VERTEX_POINT ( 'NONE', #15031 ) ;
#16199=EDGE_CURVE ( 'NONE', #44259, #21303, #35327, .T. ) ;
#16201=EDGE_LOOP ( 'NONE', ( #18273, #36802, #44339, #34799 ) ) ;
#16203=VERTEX_POINT ( 'NONE', #46490 ) ;
#16211=CARTESIAN_POINT ( 'NONE',  ( 0.1067246931122726866, 0.02962905676920215767, 0.000000000000000000 ) ) ;
#16213=B_SPLINE_CURVE_WITH_KNOTS ( 'NONE', 3,
 ( #25575, #32574, #48263, #41333 ),
 .UNSPECIFIED., .F., .F.,
 ( 4, 4 ),
 ( 0.001512128760873999826, 0.004012308088711828702 ),
 .UNSPECIFIED. ) ;
#16215=DIRECTION ( 'NONE',  ( -0.5128992774059071280, 0.000000000000000000, 0.8584487936018655452 ) ) ;
#16216=AXIS2_PLACEMENT_3D ( 'NONE', #41946, #31085, #46788 ) ;
#16217=ORIENTED_EDGE ( 'NONE', *, *, #43855, .T. ) ;
#16218=ORIENTED_EDGE ( 'NONE', *, *, #38733, .F. ) ;
#16220=CONICAL_SURFACE ( 'NONE', #47495, 1.850107469027523210, 0.6386652850508578450 ) ;
#16221=CARTESIAN_POINT ( 'NONE',  ( -0.5284761224300580373, 1.574803149606302854, -2.099874368989736784 ) ) ;
#16223=DIRECTION ( 'NONE',  ( 0.000000000000000000, 0.000000000000000000, 1.000000000000000000 ) ) ;
#16224=ORIENTED_EDGE ( 'NONE', *, *, #33665, .F. ) ;
#16226=DIRECTION ( 'NONE',  ( 0.000000000000000000, 1.160734090543304660E-16, -1.000000000000000000 ) ) ;
#16227=CARTESIAN_POINT ( 'NONE',  ( 0.002207914879453961535, 2.455437289341238936E-16, -2.115467123904954505 ) ) ;
#16231=CARTESIAN_POINT ( 'NONE',  ( 1.882988517681382756, 6.692913385826772199, 1.069164917025817951 ) ) ;
#16232=FACE_OUTER_BOUND ( 'NONE', #14688, .T. ) ;
#16234=DIRECTION ( 'NONE',  ( 7.097135778201508621E-17, 1.000000000000000000, 1.075170113095020677E-16 ) ) ;
#16238=VECTOR ( 'NONE', #19216, 39.37007874015748143 ) ;
#16242=ORIENTED_EDGE ( 'NONE', *, *, #2609, .T. ) ;
#16245=EDGE_LOOP ( 'NONE', ( #15153, #42120, #46059, #21967 ) ) ;
#16249=VECTOR ( 'NONE', #37000, 39.37007874015748143 ) ;
#16254=VERTEX_POINT ( 'NONE', #11909 ) ;
#16258=CARTESIAN_POINT ( 'NONE',  ( 1.064142702668988694, 0.000000000000000000, -1.380941303491905359 ) ) ;
#16260=ORIENTED_EDGE ( 'NONE', *, *, #47463, .T. ) ;
#16261=DIRECTION ( 'NONE',  ( -0.000000000000000000, 1.000000000000000000, -0.000000000000000000 ) ) ;
#16266=PLANE ( 'NONE',  #7691 ) ;
#16271=CARTESIAN_POINT ( 'NONE',  ( -1.929629134066536134, 6.692913385826772199, 0.9824921284572121216 ) ) ;
#16274=ORIENTED_EDGE ( 'NONE', *, *, #49487, .F. ) ;
#16275=ORIENTED_EDGE ( 'NONE', *, *, #1533, .F. ) ;
#16285=DIRECTION ( 'NONE',  ( -1.105928667600717569E-16, 1.000000000000000000, -6.607616187506203079E-17 ) ) ;
#16286=CARTESIAN_POINT ( 'NONE',  ( -0.3136974817027967100, 1.615928078135840051, -2.936457595020224520 ) ) ;
#16293=DIRECTION ( 'NONE',  ( 0.000000000000000000, 0.000000000000000000, -1.000000000000000000 ) ) ;
#16295=EDGE_CURVE ( 'NONE', #27405, #5605, #22973, .T. ) ;
#16297=DIRECTION ( 'NONE',  ( 0.9009688679024154823, 0.000000000000000000, 0.4338837391175656699 ) ) ;
#16298=ORIENTED_EDGE ( 'NONE', *, *, #32265, .F. ) ;
#16299=ADVANCED_FACE ( 'NONE', ( #8037 ), #7735, .T. ) ;
#16305=CARTESIAN_POINT ( 'NONE',  ( -2.134236802639925656, 5.905511811023623991, -2.040539317874611402 ) ) ;
#16308=ORIENTED_EDGE ( 'NONE', *, *, #7180, .T. ) ;
#16309=AXIS2_PLACEMENT_3D ( 'NONE', #35741, #40397, #372 ) ;
#16311=VERTEX_POINT ( 'NONE', #39533 ) ;
#16313=CONICAL_SURFACE ( 'NONE', #15504, 2.246510896728926010, 0.01601546068027819014 ) ;
#16314=VERTEX_POINT ( 'NONE', #3917 ) ;
#16315=DIRECTION ( 'NONE',  ( -0.9998717552508122886, -0.01601477604151185785, 0.000000000000000000 ) ) ;
#16316=VERTEX_POINT ( 'NONE', #27393 ) ;
#16317=CARTESIAN_POINT ( 'NONE',  ( 0.000000000000000000, 1.574803149606302854, 0.000000000000000000 ) ) ;
#16318=FACE_OUTER_BOUND ( 'NONE', #46004, .T. ) ;
#16322=ORIENTED_EDGE ( 'NONE', *, *, #33271, .F. ) ;
#16324=EDGE_LOOP ( 'NONE', ( #20186, #1175, #27423, #45907 ) ) ;
#16326=ORIENTED_EDGE ( 'NONE', *, *, #12867, .F. ) ;
#16329=DIRECTION ( 'NONE',  ( -0.9998717552508122886, -0.01601477604151180928, 0.000000000000000000 ) ) ;
#16330=LINE ( 'NONE', #47525, #3836 ) ;
#16332=EDGE_CURVE ( 'NONE', #22069, #23247, #46983, .T. ) ;
#16334=ADVANCED_FACE ( 'NONE', ( #19645 ), #39070, .F. ) ;
#16335=CARTESIAN_POINT ( 'NONE',  ( -0.01640406435879156535, 1.718999825676433835, 2.952755905511811108 ) ) ;
#16336=CARTESIAN_POINT ( 'NONE',  ( 1.779568955232893712, 6.692913385826772199, -1.233650562797287353 ) ) ;
#16341=EDGE_CURVE ( 'NONE', #4498, #50396, #44669, .T. ) ;
#16346=VERTEX_POINT ( 'NONE', #28932 ) ;
#16349=CARTESIAN_POINT ( 'NONE',  ( -0.9845150457423005319, 0.000000000000000000, -1.438794182654565601 ) ) ;
#16351=DIRECTION ( 'NONE',  ( -0.9998717552508122886, -0.01601477604151181275, 0.000000000000000000 ) ) ;
#16354=ORIENTED_EDGE ( 'NONE', *, *, #32067, .F. ) ;
#16357=ADVANCED_FACE ( 'NONE', ( #4937 ), #29188, .T. ) ;
#16363=EDGE_CURVE ( 'NONE', #24535, #7807, #28336, .T. ) ;
#16369=ADVANCED_FACE ( 'NONE', ( #13963 ), #20109, .T. ) ;
#16374=ORIENTED_EDGE ( 'NONE', *, *, #42206, .F. ) ;
#16380=CARTESIAN_POINT ( 'NONE',  ( -1.364345965745727973, 1.205361022782829114E-17, 1.150974876880269893 ) ) ;
#16381=DIRECTION ( 'NONE',  ( 0.01601477604151182663, -0.9998717552508123996, 0.000000000000000000 ) ) ;
#16385=EDGE_LOOP ( 'NONE', ( #2611, #48613, #50956, #5285 ) ) ;
#16388=DIRECTION ( 'NONE',  ( 0.000000000000000000, 0.000000000000000000, -1.000000000000000000 ) ) ;
#16389=CARTESIAN_POINT ( 'NONE',  ( 0.6551740444401462637, 0.000000000000000000, 1.885762267972743711 ) ) ;
#16394=CARTESIAN_POINT ( 'NONE',  ( -2.151809081513409438, 1.575012187087082127, 0.2418202932658340965 ) ) ;
#16395=VERTEX_POINT ( 'NONE', #17078 ) ;
#16397=PLANE ( 'NONE',  #5450 ) ;
#16404=EDGE_CURVE ( 'NONE', #10377, #35860, #34949, .T. ) ;
#16406=CARTESIAN_POINT ( 'NONE',  ( -2.161044708975090156, 0.000000000000000000, 0.1463148319730351032 ) ) ;
#16409=DIRECTION ( 'NONE',  ( -0.01601477604151182663, 0.9998717552508123996, -0.000000000000000000 ) ) ;
#16413=EDGE_CURVE ( 'NONE', #48369, #28465, #16213, .T. ) ;
#16415=EDGE_LOOP ( 'NONE', ( #38693, #860, #23640, #19378 ) ) ;
#16416=VERTEX_POINT ( 'NONE', #5445 ) ;
#16418=FACE_OUTER_BOUND ( 'NONE', #14150, .T. ) ;
#16420=ORIENTED_EDGE ( 'NONE', *, *, #37870, .F. ) ;
#16421=CARTESIAN_POINT ( 'NONE',  ( -1.790900357307437352, 1.580792207208895128, -1.241130355818072406 ) ) ;
#16423=ADVANCED_FACE ( 'NONE', ( #5953 ), #27518, .F. ) ;
#16424=CARTESIAN_POINT ( 'NONE',  ( -0.9838852166859199944, 1.205361022782829114E-17, 1.929635236160303302 ) ) ;
#16428=CIRCLE ( 'NONE', #3223, 1.743387098533651480 ) ;
#16433=DIRECTION ( 'NONE',  ( -0.000000000000000000, -1.000000000000000000, -0.000000000000000000 ) ) ;
#16438=VERTEX_POINT ( 'NONE', #33089 ) ;
#16439=LINE ( 'NONE', #23922, #45421 ) ;
#16440=CARTESIAN_POINT ( 'NONE',  ( -1.733991708815627808, 9.921953787815782565E-05, 0.1852230845914871471 ) ) ;
#16444=AXIS2_PLACEMENT_3D ( 'NONE', #45815, #46074, #38857 ) ;
#16445=DIRECTION ( 'NONE',  ( 0.01601477604151182663, -0.9998717552508123996, 0.000000000000000000 ) ) ;
#16446=VERTEX_POINT ( 'NONE', #17832 ) ;
#16450=CARTESIAN_POINT ( 'NONE',  ( -0.3136974817027967100, 1.615928078135840051, -2.936457595020224520 ) ) ;
#16451=CARTESIAN_POINT ( 'NONE',  ( 0.000000000000000000, 0.000000000000000000, 0.000000000000000000 ) ) ;
#16463=CARTESIAN_POINT ( 'NONE',  ( -1.983184043548481545, 1.684331982857502519, -1.828031556756394727 ) ) ;
#16468=DIRECTION ( 'NONE',  ( 0.000000000000000000, 1.000000000000000000, 0.000000000000000000 ) ) ;
#16471=ADVANCED_FACE ( 'NONE', ( #21969, #2344 ), #50040, .T. ) ;
#16473=CARTESIAN_POINT ( 'NONE',  ( -2.803168555496243108, 1.675558592011573644, 0.9280531160220438780 ) ) ;
#16477=CARTESIAN_POINT ( 'NONE',  ( -1.556712866041156440, 1.596563264426776207, 2.509548638715847435 ) ) ;
#16478=CARTESIAN_POINT ( 'NONE',  ( 1.944213194762889119, 0.05905979794000976862, 0.2136995197171435157 ) ) ;
#16487=VERTEX_POINT ( 'NONE', #18091 ) ;
#16492=CARTESIAN_POINT ( 'NONE',  ( 0.000000000000000000, 1.574803149606302854, 0.000000000000000000 ) ) ;
#16495=DIRECTION ( 'NONE',  ( -0.7227948638273878901, 0.000000000000000000, -0.6910626489868684219 ) ) ;
#16496=B_SPLINE_CURVE_WITH_KNOTS ( 'NONE', 3,
 ( #5914, #17792, #33559, #43041 ),
 .UNSPECIFIED., .F., .F.,
 ( 4, 4 ),
 ( 5.511647321497469134E-05, 0.004930157801157326360 ),
 .UNSPECIFIED. ) ;
#16499=ORIENTED_EDGE ( 'NONE', *, *, #27385, .T. ) ;
#16500=DIRECTION ( 'NONE',  ( 0.9998717552508121775, 0.01601477604151182663, 0.000000000000000000 ) ) ;
#16501=EDGE_LOOP ( 'NONE', ( #33829, #31054, #23249, #28944 ) ) ;
#16502=CARTESIAN_POINT ( 'NONE',  ( -0.1158910538491989134, 0.02606345816900213982, -1.836661962001401305 ) ) ;
#16503=ORIENTED_EDGE ( 'NONE', *, *, #978, .F. ) ;
#16504=B_SPLINE_CURVE_WITH_KNOTS ( 'NONE', 3,
 ( #33876, #6749, #13478, #45957 ),
 .UNSPECIFIED., .F., .F.,
 ( 4, 4 ),
 ( 6.390876033150945367E-07, 0.003275970498226882938 ),
 .UNSPECIFIED. ) ;
#16512=ORIENTED_EDGE ( 'NONE', *, *, #45287, .F. ) ;
#16513=CARTESIAN_POINT ( 'NONE',  ( -1.022165783746114442, 1.703323867449966889, 2.770237110794461444 ) ) ;
#16516=CARTESIAN_POINT ( 'NONE',  ( -1.591447364397243103, 0.002429723416550041374, -0.7337366736851151927 ) ) ;
#16517=CIRCLE ( 'NONE', #7448, 2.164630168518208109 ) ;
#16520=CARTESIAN_POINT ( 'NONE',  ( -1.171042467547485311, 1.689145562575557369, 1.864045119995098698 ) ) ;
#16522=VERTEX_POINT ( 'NONE', #49532 ) ;
#16530=DIRECTION ( 'NONE',  ( -0.000000000000000000, 1.000000000000000000, -0.000000000000000000 ) ) ;
#16532=EDGE_CURVE ( 'NONE', #46587, #22536, #34352, .T. ) ;
#16534=B_SPLINE_CURVE_WITH_KNOTS ( 'NONE', 3,
 ( #34996, #7125, #41984, #30871 ),
 .UNSPECIFIED., .F., .F.,
 ( 4, 4 ),
 ( 0.01409063418847883789, 0.03074670260773034597 ),
 .UNSPECIFIED. ) ;
#16539=ORIENTED_EDGE ( 'NONE', *, *, #5290, .T. ) ;
#16546=CARTESIAN_POINT ( 'NONE',  ( -1.883550378546958060, 5.905511811023623991, -1.069467267250447495 ) ) ;
#16548=ORIENTED_EDGE ( 'NONE', *, *, #46296, .T. ) ;
#16549=CARTESIAN_POINT ( 'NONE',  ( 1.473819267337850736, 1.665891067178861151, 1.761720034108342769 ) ) ;
#16551=CARTESIAN_POINT ( 'NONE',  ( 0.08119777152254364916, 1.623385212329073957, 0.000000000000000000 ) ) ;
#16559=CARTESIAN_POINT ( 'NONE',  ( -2.160407304981126320, 6.692913385826772199, -0.1462862061266902158 ) ) ;
#16563=VERTEX_POINT ( 'NONE', #34097 ) ;
#16569=EDGE_LOOP ( 'NONE', ( #615, #40423, #4274, #633 ) ) ;
#16570=EDGE_CURVE ( 'NONE', #48759, #20718, #30722, .T. ) ;
#16571=ORIENTED_EDGE ( 'NONE', *, *, #2070, .T. ) ;
#16572=PLANE ( 'NONE',  #32028 ) ;
#16573=ORIENTED_EDGE ( 'NONE', *, *, #42397, .F. ) ;
#16575=VERTEX_POINT ( 'NONE', #19089 ) ;
#16577=VECTOR ( 'NONE', #9831, 39.37007874015748143 ) ;
#16586=ORIENTED_EDGE ( 'NONE', *, *, #17306, .F. ) ;
#16591=DIRECTION ( 'NONE',  ( -0.1785568947986370392, 0.000000000000000000, 0.9839295885986295565 ) ) ;
#16594=ORIENTED_EDGE ( 'NONE', *, *, #11552, .T. ) ;
#16600=CARTESIAN_POINT ( 'NONE',  ( 0.8603116971394481061, 0.000000000000000000, -1.824450401507204278 ) ) ;
#16606=LINE ( 'NONE', #40605, #50895 ) ;
#16607=DIRECTION ( 'NONE',  ( 0.000000000000000000, 0.000000000000000000, -1.000000000000000000 ) ) ;
#16608=CARTESIAN_POINT ( 'NONE',  ( -1.955085917884560320, 1.688780925004493838, 2.212843326065125460 ) ) ;
#16609=B_SPLINE_CURVE_WITH_KNOTS ( 'NONE', 3,
 ( #22360, #2992, #7369, #22862 ),
 .UNSPECIFIED., .F., .F.,
 ( 4, 4 ),
 ( 0.01157806808172074861, 0.03073653090630815501 ),
 .UNSPECIFIED. ) ;
#16610=CARTESIAN_POINT ( 'NONE',  ( 0.4693945290273940363, 0.01171413463600641872, -1.885797023163377828 ) ) ;
#16612=ORIENTED_EDGE ( 'NONE', *, *, #45996, .T. ) ;
#16617=CARTESIAN_POINT ( 'NONE',  ( 0.9989521216866641407, 0.000000000000000000, 1.767914056614194651 ) ) ;
#16621=CARTESIAN_POINT ( 'NONE',  ( 2.121469926805689354, 2.755905511811027164, -0.4337334748181388422 ) ) ;
#16622=DIRECTION ( 'NONE',  ( -3.986037398843765983E-20, -1.000000000000000000, -1.160734090543304660E-16 ) ) ;
#16623=CIRCLE ( 'NONE', #35597, 2.165354330708661568 ) ;
#16625=VERTEX_POINT ( 'NONE', #4622 ) ;
#16626=CYLINDRICAL_SURFACE ( 'NONE', #48061, 2.165354330708661568 ) ;
#16629=EDGE_CURVE ( 'NONE', #21355, #47803, #23217, .T. ) ;
#16630=EDGE_LOOP ( 'NONE', ( #40509, #11986, #43628, #3394 ) ) ;
#16631=CARTESIAN_POINT ( 'NONE',  ( 2.009930929872536964, 6.692913385826772199, -0.8055662819783819817 ) ) ;
#16639=B_SPLINE_CURVE_WITH_KNOTS ( 'NONE', 3,
 ( #23035, #22530, #18407, #6543 ),
 .UNSPECIFIED., .F., .F.,
 ( 4, 4 ),
 ( 0.1211873102087489551, 0.1625992483279400103 ),
 .UNSPECIFIED. ) ;
#16640=CARTESIAN_POINT ( 'NONE',  ( 2.607952947267827781, 1.454965125674436921, 1.384780731079769289 ) ) ;
#16641=VERTEX_POINT ( 'NONE', #16502 ) ;
#16647=DIRECTION ( 'NONE',  ( 1.283101021437938170E-16, 1.000000000000000000, 1.154811821032258155E-17 ) ) ;
#16649=EDGE_CURVE ( 'NONE', #49792, #44687, #368, .T. ) ;
#16650=ORIENTED_EDGE ( 'NONE', *, *, #46539, .F. ) ;
#16652=LINE ( 'NONE', #48096, #17470 ) ;
#16654=VERTEX_POINT ( 'NONE', #23726 ) ;
#16657=CARTESIAN_POINT ( 'NONE',  ( 0.2431224069212723493, 0.000000000000000000, 2.152304290637673034 ) ) ;
#16664=DIRECTION ( 'NONE',  ( -0.000000000000000000, -1.000000000000000000, -0.000000000000000000 ) ) ;
#16666=CARTESIAN_POINT ( 'NONE',  ( -0.8329809839909438907, 1.607838722253305486, -2.833254665166566877 ) ) ;
#16675=ORIENTED_EDGE ( 'NONE', *, *, #3579, .T. ) ;
#16676=DIRECTION ( 'NONE',  ( 0.4338837391175526803, 0.000000000000000000, 0.9009688679024218105 ) ) ;
#16678=ORIENTED_EDGE ( 'NONE', *, *, #26324, .F. ) ;
#16684=CARTESIAN_POINT ( 'NONE',  ( -1.613340714851948965, 1.583636149837539975, -1.474425128113891814 ) ) ;
#16685=FACE_OUTER_BOUND ( 'NONE', #35946, .T. ) ;
#16697=ORIENTED_EDGE ( 'NONE', *, *, #21784, .F. ) ;
#16699=EDGE_CURVE ( 'NONE', #38704, #6398, #39736, .T. ) ;
#16702=CARTESIAN_POINT ( 'NONE',  ( 0.000000000000000000, 0.000000000000000000, 0.000000000000000000 ) ) ;
#16703=AXIS2_PLACEMENT_3D ( 'NONE', #28840, #20326, #1225 ) ;
#16705=VECTOR ( 'NONE', #34005, 39.37007874015748143 ) ;
#16707=ORIENTED_EDGE ( 'NONE', *, *, #23268, .T. ) ;
#16723=ORIENTED_EDGE ( 'NONE', *, *, #28121, .T. ) ;
#16724=CARTESIAN_POINT ( 'NONE',  ( 2.253340778107071785, 1.711184928431753294, -0.5647885202703215590 ) ) ;
#16726=LINE ( 'NONE', #25477, #2577 ) ;
#16729=CARTESIAN_POINT ( 'NONE',  ( -0.04921259842519708216, 1.616260271943668503, 2.716073891007743324 ) ) ;
#16730=ORIENTED_EDGE ( 'NONE', *, *, #37827, .T. ) ;
#16733=ORIENTED_EDGE ( 'NONE', *, *, #11105, .T. ) ;
#16738=CARTESIAN_POINT ( 'NONE',  ( 0.07982360342473591996, 1.709180471932028711, 0.000000000000000000 ) ) ;
#16740=CARTESIAN_POINT ( 'NONE',  ( -2.121469926805683137, 5.905511811023623991, -0.4337334748181712052 ) ) ;
#16750=CARTESIAN_POINT ( 'NONE',  ( -1.721400284384397628, 0.0003482895740541699209, 0.2828415639128913361 ) ) ;
#16752=CARTESIAN_POINT ( 'NONE',  ( -1.544727076607844474, 0.5249316497054296038, -1.078632795961144364 ) ) ;
#16753=CARTESIAN_POINT ( 'NONE',  ( 0.000000000000000000, 6.692913385826772199, 0.000000000000000000 ) ) ;
#16754=ORIENTED_EDGE ( 'NONE', *, *, #37444, .T. ) ;
#16756=CARTESIAN_POINT ( 'NONE',  ( -1.266372989455463172, 1.699517224488781064, -2.667458714000412456 ) ) ;
#16768=B_SPLINE_CURVE_WITH_KNOTS ( 'NONE', 3,
 ( #18539, #23928, #20038, #43534 ),
 .UNSPECIFIED., .F., .F.,
 ( 4, 4 ),
 ( 1.192911306398316375E-06, 0.004936895822257959809 ),
 .UNSPECIFIED. ) ;
#16778=CARTESIAN_POINT ( 'NONE',  ( 2.473328170512036461, 1.659322169655358836, -1.612973743992607956 ) ) ;
#16779=EDGE_CURVE ( 'NONE', #44880, #32877, #17518, .T. ) ;
#16781=DIRECTION ( 'NONE',  ( -0.9998717552508121775, -0.01601477604151182316, 0.000000000000000000 ) ) ;
#16783=VERTEX_POINT ( 'NONE', #12885 ) ;
#16784=EDGE_LOOP ( 'NONE', ( #20113, #31160, #23305, #16217 ) ) ;
#16789=DIRECTION ( 'NONE',  ( 0.01601477604151182663, -0.9998717552508123996, 0.000000000000000000 ) ) ;
#16794=ORIENTED_EDGE ( 'NONE', *, *, #21784, .T. ) ;
#16795=ORIENTED_EDGE ( 'NONE', *, *, #38343, .T. ) ;
#16797=CARTESIAN_POINT ( 'NONE',  ( 0.2184225803664230636, 0.02091578714757513086, -1.877866740686216618 ) ) ;
#16799=CARTESIAN_POINT ( 'NONE',  ( 2.298430379965446857, 1.646290322915411997, 0.3610056012771685197 ) ) ;
#16803=FACE_OUTER_BOUND ( 'NONE', #27434, .T. ) ;
#16806=CIRCLE ( 'NONE', #15983, 1.743387098533651480 ) ;
#16813=DIRECTION ( 'NONE',  ( 0.000000000000000000, 0.000000000000000000, 1.000000000000000000 ) ) ;
#16815=ORIENTED_EDGE ( 'NONE', *, *, #41862, .T. ) ;
#16823=FACE_OUTER_BOUND ( 'NONE', #30437, .T. ) ;
#16826=EDGE_CURVE ( 'NONE', #45425, #39932, #17271, .T. ) ;
#16835=CARTESIAN_POINT ( 'NONE',  ( -0.9602959360900468200, 0.01253876862113688373, 1.511314840084332145 ) ) ;
#16836=EDGE_CURVE ( 'NONE', #16203, #10796, #36896, .T. ) ;
#16837=ORIENTED_EDGE ( 'NONE', *, *, #6917, .F. ) ;
#16841=CARTESIAN_POINT ( 'NONE',  ( 2.695799277629594037, 1.761268146152256575, -1.205759334241453651 ) ) ;
#16845=EDGE_CURVE ( 'NONE', #39563, #9387, #30291, .T. ) ;
#16846=AXIS2_PLACEMENT_3D ( 'NONE', #33394, #48318, #25119 ) ;
#16849=CARTESIAN_POINT ( 'NONE',  ( 0.1155636338427008941, -0.5222242541845523167, 0.000000000000000000 ) ) ;
#16851=VECTOR ( 'NONE', #15977, 39.37007874015748143 ) ;
#16858=CARTESIAN_POINT ( 'NONE',  ( 2.158170387640339527, 5.905511811023623991, 0.2426819907294804068 ) ) ;
#16862=VERTEX_POINT ( 'NONE', #36633 ) ;
#16864=CARTESIAN_POINT ( 'NONE',  ( 0.000000000000000000, 5.905511811023623991, 0.000000000000000000 ) ) ;
#16870=ORIENTED_EDGE ( 'NONE', *, *, #19711, .T. ) ;
#16876=DIRECTION ( 'NONE',  ( -0.000000000000000000, -1.000000000000000000, -0.000000000000000000 ) ) ;
#16888=DIRECTION ( 'NONE',  ( -0.9998717552508122886, -0.01601477604151182316, 0.000000000000000000 ) ) ;
#16889=CARTESIAN_POINT ( 'NONE',  ( -0.4349608091551073197, 1.574803149606302854, 2.121218629000295230 ) ) ;
#16896=CARTESIAN_POINT ( 'NONE',  ( 1.300279662861326013, 0.04874602395362847423, 1.413491677621213860 ) ) ;
#16899=CARTESIAN_POINT ( 'NONE',  ( 0.04921259842519667277, 5.905511811023623991, 2.952755905511811108 ) ) ;
#16906=CARTESIAN_POINT ( 'NONE',  ( -0.8329809839909435576, 5.905511811023624880, -2.833254665166567321 ) ) ;
#16909=CARTESIAN_POINT ( 'NONE',  ( 1.556712866041120247, 1.480457248723645591, 2.509548638715870084 ) ) ;
#16913=ORIENTED_EDGE ( 'NONE', *, *, #1761, .F. ) ;
#16915=CARTESIAN_POINT ( 'NONE',  ( 2.932638728931774352, 1.205361022782829114E-17, 0.3475908556738223631 ) ) ;
#16918=CARTESIAN_POINT ( 'NONE',  ( -0.04921259842519689481, 2.794703227806734062E-17, 1.924024829198930364 ) ) ;
#16919=ORIENTED_EDGE ( 'NONE', *, *, #40220, .T. ) ;
#16923=EDGE_LOOP ( 'NONE', ( #30171, #48743, #2432, #41359 ) ) ;
#16929=DIRECTION ( 'NONE',  ( -1.509903313490212895E-14, 0.000000000000000000, 1.000000000000000000 ) ) ;
#16931=AXIS2_PLACEMENT_3D ( 'NONE', #37609, #17722, #48912 ) ;
#16933=ADVANCED_FACE ( 'NONE', ( #37661 ), #28372, .T. ) ;
#16936=DIRECTION ( 'NONE',  ( 1.142080616180681165E-16, -1.000000000000000000, -2.072570748943160811E-17 ) ) ;
#16940=CARTESIAN_POINT ( 'NONE',  ( -2.160844847978046879, 1.673297988508097855, 0.1614166014397402371 ) ) ;
#16942=CARTESIAN_POINT ( 'NONE',  ( 1.833791099076603537, 5.905511811023623991, -1.151507526013693994 ) ) ;
#16943=ADVANCED_FACE ( 'NONE', ( #38853 ), #7773, .F. ) ;
#16944=( BOUNDED_CURVE ( )  B_SPLINE_CURVE ( 3, ( #3344, #42323, #19085, #34841 ),
 .UNSPECIFIED., .F., .F. ) 
 B_SPLINE_CURVE_WITH_KNOTS ( ( 4, 4 ),
 ( 0.9053024471257524741, 0.9561597570633886267 ),
 .UNSPECIFIED. ) 
 CURVE ( )  GEOMETRIC_REPRESENTATION_ITEM ( )  RATIONAL_B_SPLINE_CURVE ( ( 1.000000000000000000, 0.9997844727828222311, 0.9997844727828222311, 1.000000000000000000 ) ) 
 REPRESENTATION_ITEM ( '' )  );
#16945=FACE_OUTER_BOUND ( 'NONE', #11536, .T. ) ;
#16951=EDGE_CURVE ( 'NONE', #25794, #46385, #13113, .T. ) ;
#16957=CARTESIAN_POINT ( 'NONE',  ( 1.864846474276733890, 0.03794660422572829900, -0.7435542096351945851 ) ) ;
#16966=CIRCLE ( 'NONE', #436, 1.743387098533651480 ) ;
#16972=ORIENTED_EDGE ( 'NONE', *, *, #6261, .T. ) ;
#16978=CARTESIAN_POINT ( 'NONE',  ( 2.734482843737263025, 0.000000000000000000, -1.115254632218672937 ) ) ;
#16979=ORIENTED_EDGE ( 'NONE', *, *, #48524, .F. ) ;
#16981=CARTESIAN_POINT ( 'NONE',  ( -0.6382636202146998450, 1.632062195274633254, -2.127712142990381139 ) ) ;
#16985=VERTEX_POINT ( 'NONE', #33791 ) ;
#16995=CARTESIAN_POINT ( 'NONE',  ( 2.882374435144376079, 1.764165479168779527, -0.6410570582911828685 ) ) ;
#16996=VECTOR ( 'NONE', #28001, 39.37007874015748143 ) ;
#16997=ORIENTED_EDGE ( 'NONE', *, *, #46796, .T. ) ;
#17002=CIRCLE ( 'NONE', #46660, 2.165354330708661568 ) ;
#17006=CARTESIAN_POINT ( 'NONE',  ( -1.722370577523733459, 1.205361022782829114E-17, 0.2829729990490794655 ) ) ;
#17009=CARTESIAN_POINT ( 'NONE',  ( 2.475065961783442514, 0.9865970136139682323, 0.8559428686598158365 ) ) ;
#17013=DIRECTION ( 'NONE',  ( -0.9998717552508122886, -0.01601477604151180928, 0.000000000000000000 ) ) ;
#17016=B_SPLINE_CURVE_WITH_KNOTS ( 'NONE', 3,
 ( #30237, #5974, #45951, #29726 ),
 .UNSPECIFIED., .F., .F.,
 ( 4, 4 ),
 ( 2.655830146740026460E-07, 0.01938437877986225882 ),
 .UNSPECIFIED. ) ;
#17017=VERTEX_POINT ( 'NONE', #28491 ) ;
#17019=EDGE_CURVE ( 'NONE', #29553, #36720, #39514, .T. ) ;
#17020=ORIENTED_EDGE ( 'NONE', *, *, #24619, .T. ) ;
#17030=DIRECTION ( 'NONE',  ( 0.000000000000000000, 0.000000000000000000, -1.000000000000000000 ) ) ;
#17031=VECTOR ( 'NONE', #38392, 39.37007874015748143 ) ;
#17033=CARTESIAN_POINT ( 'NONE',  ( -2.153807523435208093, 6.692913385826772199, 0.2420910006175677753 ) ) ;
#17035=ORIENTED_EDGE ( 'NONE', *, *, #27262, .F. ) ;
#17037=CARTESIAN_POINT ( 'NONE',  ( -1.326676825859837816, 1.205361022782829114E-17, -1.200346386814097999 ) ) ;
#17042=ORIENTED_EDGE ( 'NONE', *, *, #9257, .T. ) ;
#17047=ORIENTED_EDGE ( 'NONE', *, *, #28973, .F. ) ;
#17051=DIRECTION ( 'NONE',  ( 3.986037398843765983E-20, 1.000000000000000000, 1.160734090543304660E-16 ) ) ;
#17059=ORIENTED_EDGE ( 'NONE', *, *, #9787, .T. ) ;
#17064=CARTESIAN_POINT ( 'NONE',  ( 0.4788131938641111973, 1.628272305554966159, 2.914091152102192162 ) ) ;
#17070=CARTESIAN_POINT ( 'NONE',  ( 1.530693736245518854, 1.574803149606302854, -1.531579597454043373 ) ) ;
#17071=FACE_OUTER_BOUND ( 'NONE', #27136, .T. ) ;
#17073=CARTESIAN_POINT ( 'NONE',  ( 3.937007874015748143, 2.913385826771657250, 1.023622047244094446 ) ) ;
#17078=CARTESIAN_POINT ( 'NONE',  ( -0.4788131938641533858, 5.905511811023623991, 2.914091152102185944 ) ) ;
#17080=EDGE_CURVE ( 'NONE', #975, #41895, #44453, .T. ) ;
#17082=ORIENTED_EDGE ( 'NONE', *, *, #5961, .T. ) ;
#17083=DIRECTION ( 'NONE',  ( -0.01601477604151182663, 0.9998717552508123996, -0.000000000000000000 ) ) ;
#17085=ORIENTED_EDGE ( 'NONE', *, *, #34584, .F. ) ;
#17090=DIRECTION ( 'NONE',  ( 0.000000000000000000, 0.000000000000000000, 1.000000000000000000 ) ) ;
#17093=CIRCLE ( 'NONE', #573, 1.850107469027523432 ) ;
#17095=ORIENTED_EDGE ( 'NONE', *, *, #24879, .T. ) ;
#17097=AXIS2_PLACEMENT_3D ( 'NONE', #3214, #35221, #6598 ) ;
#17102=DIRECTION ( 'NONE',  ( 0.000000000000000000, 0.000000000000000000, -1.000000000000000000 ) ) ;
#17103=CARTESIAN_POINT ( 'NONE',  ( 2.622993961246840922, 1.756668590291742493, 0.8005172129084018318 ) ) ;
#17104=ORIENTED_EDGE ( 'NONE', *, *, #18286, .F. ) ;
#17109=DIRECTION ( 'NONE',  ( 3.986037398843765983E-20, 1.000000000000000000, 1.160734090543304660E-16 ) ) ;
#17110=CARTESIAN_POINT ( 'NONE',  ( -0.04921259842519708216, 1.608688524157807498, 2.242709805336809303 ) ) ;
#17111=EDGE_CURVE ( 'NONE', #19240, #11648, #24806, .T. ) ;
#17114=ORIENTED_EDGE ( 'NONE', *, *, #26495, .T. ) ;
#17116=LINE ( 'NONE', #43947, #23753 ) ;
#17118=DIRECTION ( 'NONE',  ( 0.000000000000000000, 0.000000000000000000, 1.000000000000000000 ) ) ;
#17120=CARTESIAN_POINT ( 'NONE',  ( -3.001271764839907430, 2.755905511811027164, 0.08552506819282471029 ) ) ;
#17122=VERTEX_POINT ( 'NONE', #43718 ) ;
#17126=CARTESIAN_POINT ( 'NONE',  ( -2.475498251075796130, 1.050049506817961831, -0.6154945137624749929 ) ) ;
#17128=AXIS2_PLACEMENT_3D ( 'NONE', #17910, #34173, #41404 ) ;
#17129=AXIS2_PLACEMENT_3D ( 'NONE', #47696, #12369, #4122 ) ;
#17132=DIRECTION ( 'NONE',  ( 0.9998717552508121775, 0.01601477604151182663, 0.000000000000000000 ) ) ;
#17134=DIRECTION ( 'NONE',  ( 0.9510565162951500895, 0.000000000000000000, 0.3090169943749582204 ) ) ;
#17135=ADVANCED_FACE ( 'NONE', ( #24116 ), #39957, .T. ) ;
#17143=CARTESIAN_POINT ( 'NONE',  ( -0.3381173457103602287, 1.574803149606302854, 2.138793126519845877 ) ) ;
#17147=CARTESIAN_POINT ( 'NONE',  ( -1.052895522975213050, 1.537105172708097767, 2.758704046758604811 ) ) ;
#17148=CARTESIAN_POINT ( 'NONE',  ( 2.191624600584984872, 1.710196431015120977, 0.7638471876793682114 ) ) ;
#17156=DIRECTION ( 'NONE',  ( 0.000000000000000000, 0.000000000000000000, 1.000000000000000000 ) ) ;
#17162=CARTESIAN_POINT ( 'NONE',  ( 2.947574761915768171, 1.765190094501404072, -0.1816379373804911379 ) ) ;
#17165=CARTESIAN_POINT ( 'NONE',  ( -1.225600105435525000, 0.000000000000000000, -1.239880218767125175 ) ) ;
#17166=ORIENTED_EDGE ( 'NONE', *, *, #14765, .F. ) ;
#17176=VERTEX_POINT ( 'NONE', #11391 ) ;
#17181=FACE_OUTER_BOUND ( 'NONE', #43683, .T. ) ;
#17182=ADVANCED_FACE ( 'NONE', ( #3642 ), #19374, .T. ) ;
#17185=ORIENTED_EDGE ( 'NONE', *, *, #37160, .F. ) ;
#17187=ADVANCED_FACE ( 'NONE', ( #23254 ), #10290, .T. ) ;
#17189=VERTEX_POINT ( 'NONE', #35393 ) ;
#17190=CIRCLE ( 'NONE', #18806, 2.244934639244525076 ) ;
#17191=CARTESIAN_POINT ( 'NONE',  ( -1.790754330931495275, 1.646411344893201845, -1.241033964651257149 ) ) ;
#17198=VERTEX_POINT ( 'NONE', #50820 ) ;
#17208=CARTESIAN_POINT ( 'NONE',  ( 2.319222573356612749, 1.745048544795088308, -0.1534186080535354380 ) ) ;
#17212=PLANE ( 'NONE',  #46081 ) ;
#17213=ORIENTED_EDGE ( 'NONE', *, *, #32145, .T. ) ;
#17218=VECTOR ( 'NONE', #1402, 39.37007874015748854 ) ;
#17221=B_SPLINE_CURVE_WITH_KNOTS ( 'NONE', 3,
 ( #50794, #35370, #31491, #239 ),
 .UNSPECIFIED., .F., .F.,
 ( 4, 4 ),
 ( 0.001744585901858061424, 0.04556827975943426173 ),
 .UNSPECIFIED. ) ;
#17224=VERTEX_POINT ( 'NONE', #11639 ) ;
#17231=ADVANCED_FACE ( 'NONE', ( #19128 ), #27125, .T. ) ;
#17233=VERTEX_POINT ( 'NONE', #31270 ) ;
#17246=EDGE_CURVE ( 'NONE', #29348, #11414, #28405, .T. ) ;
#17247=DIRECTION ( 'NONE',  ( -4.561975526775755056E-17, -1.000000000000000000, 1.067327232801816862E-16 ) ) ;
#17250=VERTEX_POINT ( 'NONE', #31521 ) ;
#17258=CARTESIAN_POINT ( 'NONE',  ( 0.000000000000000000, 6.692913385826772199, -2.086614173228346303 ) ) ;
#17259=ORIENTED_EDGE ( 'NONE', *, *, #17019, .F. ) ;
#17269=DIRECTION ( 'NONE',  ( 0.000000000000000000, 0.000000000000000000, -1.000000000000000000 ) ) ;
#17270=ORIENTED_EDGE ( 'NONE', *, *, #13049, .T. ) ;
#17271=LINE ( 'NONE', #9519, #47316 ) ;
#17279=CARTESIAN_POINT ( 'NONE',  ( -2.165354330708661568, 1.574803149606301966, -1.520079223026944511E-17 ) ) ;
#17281=ORIENTED_EDGE ( 'NONE', *, *, #48081, .T. ) ;
#17283=CARTESIAN_POINT ( 'NONE',  ( 0.9989521216866641407, 0.000000000000000000, 1.767914056614194651 ) ) ;
#17285=ORIENTED_EDGE ( 'NONE', *, *, #45541, .F. ) ;
#17286=CARTESIAN_POINT ( 'NONE',  ( -1.593548266680976155, 0.001619815658173129856, -0.7346346424156023902 ) ) ;
#17289=CARTESIAN_POINT ( 'NONE',  ( -2.491402175429631605, 1.205361022782829114E-17, -1.585592796919542025 ) ) ;
#17291=CARTESIAN_POINT ( 'NONE',  ( 2.147141360900377105, 6.692913385826772199, 0.3405121111982932769 ) ) ;
#17294=VERTEX_POINT ( 'NONE', #20139 ) ;
#17295=CARTESIAN_POINT ( 'NONE',  ( 1.146850602739119651, 0.5249316497054294928, -1.494778961828568065 ) ) ;
#17298=AXIS2_PLACEMENT_3D ( 'NONE', #28243, #19734, #22923 ) ;
#17299=EDGE_CURVE ( 'NONE', #34229, #29725, #28140, .T. ) ;
#17303=EDGE_CURVE ( 'NONE', #10313, #25755, #44106, .T. ) ;
#17304=EDGE_CURVE ( 'NONE', #11282, #39747, #1040, .T. ) ;
#17306=EDGE_CURVE ( 'NONE', #47803, #16032, #12401, .T. ) ;
#17312=CARTESIAN_POINT ( 'NONE',  ( 0.7381027496705272473, 1.730766751998747521, -2.859439394060913298 ) ) ;
#17314=B_SPLINE_CURVE_WITH_KNOTS ( 'NONE', 3,
 ( #47761, #39547, #4179, #47506 ),
 .UNSPECIFIED., .F., .F.,
 ( 4, 4 ),
 ( 0.001814792330965703596, 0.004762084017055013413 ),
 .UNSPECIFIED. ) ;
#17317=EDGE_LOOP ( 'NONE', ( #17104, #12759, #27962, #34920, #3827, #19007 ) ) ;
#17326=DIRECTION ( 'NONE',  ( -0.01601477604151182663, 0.9998717552508123996, -0.000000000000000000 ) ) ;
#17330=LINE ( 'NONE', #33090, #41749 ) ;
#17332=B_SPLINE_CURVE_WITH_KNOTS ( 'NONE', 3,
 ( #2079, #14200, #5946, #41829 ),
 .UNSPECIFIED., .F., .F.,
 ( 4, 4 ),
 ( 0.0004124273248910236846, 0.004895227329085388539 ),
 .UNSPECIFIED. ) ;
#17337=EDGE_CURVE ( 'NONE', #30710, #24910, #28993, .T. ) ;
#17341=CARTESIAN_POINT ( 'NONE',  ( 1.872964171113514320, 0.5249316475426858419, 0.2040481836961198225 ) ) ;
#17350=VERTEX_POINT ( 'NONE', #31779 ) ;
#17352=CARTESIAN_POINT ( 'NONE',  ( 1.902660579019252562, 1.639951345248664039, -1.314902632263422966 ) ) ;
#17353=DIRECTION ( 'NONE',  ( 0.9195277725514544587, 0.000000000000000000, -0.3930250316539147803 ) ) ;
#17354=EDGE_CURVE ( 'NONE', #42335, #25112, #43216, .T. ) ;
#17355=VECTOR ( 'NONE', #9447, 39.37007874015748143 ) ;
#17359=FACE_OUTER_BOUND ( 'NONE', #9290, .T. ) ;
#17362=VERTEX_POINT ( 'NONE', #24284 ) ;
#17364=FACE_OUTER_BOUND ( 'NONE', #20713, .T. ) ;
#17370=LINE ( 'NONE', #44967, #28031 ) ;
#17372=CARTESIAN_POINT ( 'NONE',  ( -2.437180031585919782, 1.681273446161504426, -1.667735833703134718 ) ) ;
#17376=EDGE_LOOP ( 'NONE', ( #27707, #25595, #42396, #40447 ) ) ;
#17377=CARTESIAN_POINT ( 'NONE',  ( -2.339241080213612545, 0.000000000000000000, 1.802537235681884065 ) ) ;
#17381=FACE_OUTER_BOUND ( 'NONE', #31128, .T. ) ;
#17383=DIRECTION ( 'NONE',  ( -0.01601477604151182663, 0.9998717552508123996, -0.000000000000000000 ) ) ;
#17384=LINE ( 'NONE', #33409, #40565 ) ;
#17389=CARTESIAN_POINT ( 'NONE',  ( 0.04921259842519689481, 1.205361022782829114E-17, 2.952755905511811108 ) ) ;
#17393=CARTESIAN_POINT ( 'NONE',  ( -1.695772546416001392, 1.551146592414875958, -2.417756147381374010 ) ) ;
#17394=EDGE_CURVE ( 'NONE', #35414, #23176, #11134, .T. ) ;
#17397=PLANE ( 'NONE',  #12311 ) ;
#17398=AXIS2_PLACEMENT_3D ( 'NONE', #46089, #42230, #1984 ) ;
#17400=VERTEX_POINT ( 'NONE', #1297 ) ;
#17405=CARTESIAN_POINT ( 'NONE',  ( -1.171042467547485311, 1.689145562575557369, 1.864045119995098698 ) ) ;
#17407=ORIENTED_EDGE ( 'NONE', *, *, #7130, .T. ) ;
#17408=VERTEX_POINT ( 'NONE', #40292 ) ;
#17409=CARTESIAN_POINT ( 'NONE',  ( 1.550261229843175492, 1.634307024739966696, 1.699618603577774945 ) ) ;
#17411=ORIENTED_EDGE ( 'NONE', *, *, #1563, .T. ) ;
#17414=DIRECTION ( 'NONE',  ( -0.9998717552508122886, -0.01601477604151181275, 0.000000000000000000 ) ) ;
#17417=ORIENTED_EDGE ( 'NONE', *, *, #50678, .F. ) ;
#17420=CARTESIAN_POINT ( 'NONE',  ( 2.576863348864710801, 0.000000000000000000, 1.442554885838449819 ) ) ;
#17427=CARTESIAN_POINT ( 'NONE',  ( -2.168245791271168343, 1.560742704294596495, -2.004968704497279486 ) ) ;
#17434=VERTEX_POINT ( 'NONE', #39170 ) ;
#17438=AXIS2_PLACEMENT_3D ( 'NONE', #26857, #7256, #38749 ) ;
#17443=VECTOR ( 'NONE', #8432, 39.37007874015748143 ) ;
#17444=CARTESIAN_POINT ( 'NONE',  ( 1.355960331127249452, 0.04963785175798203497, -1.364517356352728861 ) ) ;
#17445=CARTESIAN_POINT ( 'NONE',  ( 2.755905511811024056, 4.960629921259846142, -1.023622047244094224 ) ) ;
#17448=CARTESIAN_POINT ( 'NONE',  ( 0.000000000000000000, 0.000000000000000000, 0.000000000000000000 ) ) ;
#17450=EDGE_LOOP ( 'NONE', ( #41188, #47071, #39445, #18416 ) ) ;
#17452=DIRECTION ( 'NONE',  ( 0.000000000000000000, 0.000000000000000000, 1.000000000000000000 ) ) ;
#17462=EDGE_CURVE ( 'NONE', #38330, #4093, #31428, .T. ) ;
#17463=CARTESIAN_POINT ( 'NONE',  ( 1.163887619842433718, 0.04656145577143805392, -1.518228404148327160 ) ) ;
#17468=EDGE_CURVE ( 'NONE', #21800, #24086, #440, .T. ) ;
#17470=VECTOR ( 'NONE', #32404, 39.37007874015748143 ) ;
#17471=ORIENTED_EDGE ( 'NONE', *, *, #38672, .F. ) ;
#17488=VERTEX_POINT ( 'NONE', #23673 ) ;
#17490=ORIENTED_EDGE ( 'NONE', *, *, #32110, .F. ) ;
#17492=DIRECTION ( 'NONE',  ( -0.01601477604151182663, 0.9998717552508123996, -0.000000000000000000 ) ) ;
#17496=ORIENTED_EDGE ( 'NONE', *, *, #42141, .F. ) ;
#17497=CARTESIAN_POINT ( 'NONE',  ( 0.9442395380435398833, 1.624600478255878055, -2.074157072296122450 ) ) ;
#17498=CIRCLE ( 'NONE', #25719, 2.165354330708661568 ) ;
#17500=ORIENTED_EDGE ( 'NONE', *, *, #5447, .T. ) ;
#17503=CARTESIAN_POINT ( 'NONE',  ( 0.1155636338427008941, -0.5222242541845523167, 0.000000000000000000 ) ) ;
#17504=EDGE_LOOP ( 'NONE', ( #19936, #22605, #48001, #48939 ) ) ;
#17506=CARTESIAN_POINT ( 'NONE',  ( 1.377485945418314151, 1.001684976433488528, 2.209573301320594485 ) ) ;
#17511=DIRECTION ( 'NONE',  ( 0.000000000000000000, 0.000000000000000000, -1.000000000000000000 ) ) ;
#17513=DIRECTION ( 'NONE',  ( 0.7818314824680311359, 0.000000000000000000, -0.6234898018587319291 ) ) ;
#17515=LINE ( 'NONE', #33275, #13875 ) ;
#17516=DIRECTION ( 'NONE',  ( 1.154631945610162802E-14, 0.000000000000000000, 1.000000000000000000 ) ) ;
#17517=ORIENTED_EDGE ( 'NONE', *, *, #36072, .F. ) ;
#17518=LINE ( 'NONE', #40254, #34984 ) ;
#17524=DIRECTION ( 'NONE',  ( -0.8584487936018655452, -1.160734090543304660E-16, -0.5128992774059071280 ) ) ;
#17526=EDGE_LOOP ( 'NONE', ( #19136, #46454, #40187, #13816 ) ) ;
#17529=CARTESIAN_POINT ( 'NONE',  ( 0.7111759851608010496, 1.722959852249558388, -2.391904164000848709 ) ) ;
#17537=CARTESIAN_POINT ( 'NONE',  ( 0.3382312733057617482, 0.000000000000000000, -2.139420919314966252 ) ) ;
#17540=ORIENTED_EDGE ( 'NONE', *, *, #50002, .T. ) ;
#17543=VECTOR ( 'NONE', #49233, 39.37007874015748854 ) ;
#17546=ORIENTED_EDGE ( 'NONE', *, *, #5179, .F. ) ;
#17553=ORIENTED_EDGE ( 'NONE', *, *, #21936, .T. ) ;
#17557=ORIENTED_EDGE ( 'NONE', *, *, #3839, .T. ) ;
#17558=EDGE_CURVE ( 'NONE', #44866, #11414, #27157, .T. ) ;
#17562=EDGE_CURVE ( 'NONE', #34870, #19370, #26785, .T. ) ;
#17564=DIRECTION ( 'NONE',  ( -0.01601477604151182663, 0.9998717552508123996, -0.000000000000000000 ) ) ;
#17566=ORIENTED_EDGE ( 'NONE', *, *, #12867, .T. ) ;
#17567=B_SPLINE_CURVE_WITH_KNOTS ( 'NONE', 3,
 ( #19667, #35943, #4700, #571 ),
 .UNSPECIFIED., .F., .F.,
 ( 4, 4 ),
 ( 2.102925087030960871E-07, 0.01994480150632338758 ),
 .UNSPECIFIED. ) ;
#17576=CARTESIAN_POINT ( 'NONE',  ( -1.472219874544909768, 5.905511811023623991, 2.560030851058948453 ) ) ;
#17582=AXIS2_PLACEMENT_3D ( 'NONE', #27888, #24022, #32555 ) ;
#17588=ORIENTED_EDGE ( 'NONE', *, *, #21965, .F. ) ;
#17596=ADVANCED_FACE ( 'NONE', ( #25215 ), #28568, .T. ) ;
#17598=ORIENTED_EDGE ( 'NONE', *, *, #22695, .F. ) ;
#17603=CARTESIAN_POINT ( 'NONE',  ( 1.901865911302007106, 1.672747016891200200, -1.314378076695968511 ) ) ;
#17609=EDGE_LOOP ( 'NONE', ( #3897, #41744, #32689, #25541 ) ) ;
#17626=VERTEX_POINT ( 'NONE', #44053 ) ;
#17628=AXIS2_PLACEMENT_3D ( 'NONE', #44232, #19962, #23851 ) ;
#17629=DIRECTION ( 'NONE',  ( -0.000000000000000000, -1.000000000000000000, -0.000000000000000000 ) ) ;
#17632=DIRECTION ( 'NONE',  ( -0.9195277725514489076, 0.000000000000000000, -0.3930250316539278255 ) ) ;
#17640=CARTESIAN_POINT ( 'NONE',  ( 0.2156685157584260770, 1.722625337188476546, -2.945280361644574185 ) ) ;
#17642=FACE_OUTER_BOUND ( 'NONE', #1914, .T. ) ;
#17643=EDGE_CURVE ( 'NONE', #9082, #8114, #49821, .T. ) ;
#17650=CIRCLE ( 'NONE', #7724, 2.165354330708661568 ) ;
#17654=AXIS2_PLACEMENT_3D ( 'NONE', #48839, #41398, #44997 ) ;
#17655=CARTESIAN_POINT ( 'NONE',  ( -2.160407304981126320, 1.574879494900809584, -0.1462862061266896330 ) ) ;
#17656=CARTESIAN_POINT ( 'NONE',  ( 1.152568299495707826, 1.574803149606302854, 1.833124570921553120 ) ) ;
#17663=CARTESIAN_POINT ( 'NONE',  ( -2.122484638469143814, 1.673906474958827939, -0.4339650761337435214 ) ) ;
#17664=PLANE ( 'NONE',  #10611 ) ;
#17667=CARTESIAN_POINT ( 'NONE',  ( 0.07982360342473591996, 1.709180471932028711, 0.000000000000000000 ) ) ;
#17668=AXIS2_PLACEMENT_3D ( 'NONE', #39280, #15537, #43137 ) ;
#17674=VERTEX_POINT ( 'NONE', #36587 ) ;
#17675=ORIENTED_EDGE ( 'NONE', *, *, #29603, .F. ) ;
#17679=ORIENTED_EDGE ( 'NONE', *, *, #1723, .F. ) ;
#17685=ORIENTED_EDGE ( 'NONE', *, *, #5404, .T. ) ;
#17689=CARTESIAN_POINT ( 'NONE',  ( 1.393175312147112432, 0.000000000000000000, 1.048074961516293202 ) ) ;
#17691=ORIENTED_EDGE ( 'NONE', *, *, #16341, .F. ) ;
#17700=VECTOR ( 'NONE', #4628, 39.37007874015748143 ) ;
#17702=LINE ( 'NONE', #25696, #49475 ) ;
#17705=AXIS2_PLACEMENT_3D ( 'NONE', #39863, #42624, #8018 ) ;
#17707=CARTESIAN_POINT ( 'NONE',  ( 2.721585451156246727, 1.452232124017870607, -1.145429582200450769 ) ) ;
#17708=CARTESIAN_POINT ( 'NONE',  ( 0.000000000000000000, 5.905511811023623991, 0.000000000000000000 ) ) ;
#17716=ADVANCED_FACE ( 'NONE', ( #49427 ), #26229, .T. ) ;
#17721=FACE_OUTER_BOUND ( 'NONE', #18157, .T. ) ;
#17722=DIRECTION ( 'NONE',  ( -0.01601477604151182663, 0.9998717552508123996, -0.000000000000000000 ) ) ;
#17727=AXIS2_PLACEMENT_3D ( 'NONE', #44414, #40557, #20933 ) ;
#17728=CARTESIAN_POINT ( 'NONE',  ( 1.183645401082124904, 0.000000000000000000, 1.279993023352361980 ) ) ;
#17730=CIRCLE ( 'NONE', #22699, 2.165354330708661568 ) ;
#17738=VECTOR ( 'NONE', #50729, 39.37007874015748143 ) ;
#17740=LINE ( 'NONE', #45582, #16705 ) ;
#17742=VERTEX_POINT ( 'NONE', #21597 ) ;
#17743=ORIENTED_EDGE ( 'NONE', *, *, #23933, .T. ) ;
#17744=ORIENTED_EDGE ( 'NONE', *, *, #36865, .F. ) ;
#17754=ORIENTED_EDGE ( 'NONE', *, *, #4071, .F. ) ;
#17755=FACE_OUTER_BOUND ( 'NONE', #41403, .T. ) ;
#17763=LINE ( 'NONE', #33782, #37193 ) ;
#17764=B_SPLINE_CURVE_WITH_KNOTS ( 'NONE', 3,
 ( #35193, #31321, #50872, #15813 ),
 .UNSPECIFIED., .F., .F.,
 ( 4, 4 ),
 ( 0.1211775127643062444, 0.1625894504277921315 ),
 .UNSPECIFIED. ) ;
#17765=CARTESIAN_POINT ( 'NONE',  ( 0.7368177193319344065, 0.01309245855044433200, 1.823186522806556686 ) ) ;
#17766=EDGE_CURVE ( 'NONE', #32953, #17017, #18230, .T. ) ;
#17768=ORIENTED_EDGE ( 'NONE', *, *, #6394, .T. ) ;
#17771=AXIS2_PLACEMENT_3D ( 'NONE', #890, #4509, #27993 ) ;
#17772=ORIENTED_EDGE ( 'NONE', *, *, #10557, .T. ) ;
#17777=CARTESIAN_POINT ( 'NONE',  ( -2.044241703397525978, 1.205361022782829114E-17, -0.7159595814952911530 ) ) ;
#17778=CARTESIAN_POINT ( 'NONE',  ( -0.6094175224461334528, 1.205361022782829114E-17, 1.763844451117148271 ) ) ;
#17785=CARTESIAN_POINT ( 'NONE',  ( 1.325491792074623643, 1.485765544018708750, -2.638988599164732385 ) ) ;
#17787=CARTESIAN_POINT ( 'NONE',  ( 1.429658358381396877, 0.01654809226879937895, -1.434979885194824112 ) ) ;
#17790=EDGE_LOOP ( 'NONE', ( #6220, #42538, #9872, #13053 ) ) ;
#17791=PLANE ( 'NONE',  #33044 ) ;
#17792=CARTESIAN_POINT ( 'NONE',  ( 1.975114622544695386, 0.03906914021382532770, -0.4003288316781843936 ) ) ;
#17793=CARTESIAN_POINT ( 'NONE',  ( 2.088343298084792021, 5.905511811023623991, 0.6267986818430609786 ) ) ;
#17794=B_SPLINE_CURVE_WITH_KNOTS ( 'NONE', 3,
 ( #49460, #3031, #45863, #49214 ),
 .UNSPECIFIED., .F., .F.,
 ( 4, 4 ),
 ( 0.01212773829365105735, 0.03073793659894883193 ),
 .UNSPECIFIED. ) ;
#17796=ORIENTED_EDGE ( 'NONE', *, *, #17643, .T. ) ;
#17797=CIRCLE ( 'NONE', #35109, 1.850107469027523432 ) ;
#17805=ORIENTED_EDGE ( 'NONE', *, *, #3003, .T. ) ;
#17807=CARTESIAN_POINT ( 'NONE',  ( -0.6377510516001282381, 1.027715665865251315, -2.495823182398442697 ) ) ;
#17813=CARTESIAN_POINT ( 'NONE',  ( -2.101391096692225791, 1.575819129783617489, -0.5301069970517552354 ) ) ;
#17821=ORIENTED_EDGE ( 'NONE', *, *, #19155, .F. ) ;
#17822=CARTESIAN_POINT ( 'NONE',  ( 0.6551740444401462637, 0.000000000000000000, 1.885762267972743711 ) ) ;
#17831=AXIS2_PLACEMENT_3D ( 'NONE', #21711, #21202, #49286 ) ;
#17832=CARTESIAN_POINT ( 'NONE',  ( -0.5284761224300577043, 5.905511811023623991, -2.099874368989737228 ) ) ;
#17842=CIRCLE ( 'NONE', #35160, 1.850107469027523432 ) ;
#17843=B_SPLINE_CURVE_WITH_KNOTS ( 'NONE', 3,
 ( #654, #48109, #46397, #31907 ),
 .UNSPECIFIED., .F., .F.,
 ( 4, 4 ),
 ( 2.074264429158795827E-07, 0.002500727467959800148 ),
 .UNSPECIFIED. ) ;
#17847=ORIENTED_EDGE ( 'NONE', *, *, #6356, .F. ) ;
#17848=CARTESIAN_POINT ( 'NONE',  ( -2.889674983507169337, 1.674218314264582785, -0.6090712660038034576 ) ) ;
#17851=ORIENTED_EDGE ( 'NONE', *, *, #23638, .F. ) ;
#17853=LINE ( 'NONE', #18871, #13151 ) ;
#17854=VERTEX_POINT ( 'NONE', #41472 ) ;
#17855=ORIENTED_EDGE ( 'NONE', *, *, #22148, .F. ) ;
#17860=EDGE_CURVE ( 'NONE', #22211, #42163, #11740, .T. ) ;
#17863=DIRECTION ( 'NONE',  ( 0.000000000000000000, 0.000000000000000000, 1.000000000000000000 ) ) ;
#17865=CIRCLE ( 'NONE', #3856, 0.3937007874015748254 ) ;
#17866=ORIENTED_EDGE ( 'NONE', *, *, #18195, .F. ) ;
#17872=ORIENTED_EDGE ( 'NONE', *, *, #23109, .T. ) ;
#17874=SHAPE_REPRESENTATION_RELATIONSHIP ( 'NONE' , 'NONE' ,  #8330, #43986 ) ;
#17879=EDGE_CURVE ( 'NONE', #29609, #30462, #47065, .T. ) ;
#17881=CARTESIAN_POINT ( 'NONE',  ( -1.109524193798323788, 0.000000000000000000, 1.344750771968458380 ) ) ;
#17885=EDGE_CURVE ( 'NONE', #23291, #42847, #3494, .T. ) ;
#17886=CARTESIAN_POINT ( 'NONE',  ( 0.002207914879453961969, 6.692913385826772199, 0.04916304461325451958 ) ) ;
#17887=ORIENTED_EDGE ( 'NONE', *, *, #34299, .F. ) ;
#17889=CARTESIAN_POINT ( 'NONE',  ( -2.623503965249869729, 1.678368413758691391, 1.355882097269835107 ) ) ;
#17890=DIRECTION ( 'NONE',  ( 0.9510565162951500895, 0.000000000000000000, 0.3090169943749582204 ) ) ;
#17892=CARTESIAN_POINT ( 'NONE',  ( 0.08139965876239094178, 1.610780518492231694, 0.000000000000000000 ) ) ;
#17895=FACE_OUTER_BOUND ( 'NONE', #48579, .T. ) ;
#17902=AXIS2_PLACEMENT_3D ( 'NONE', #2719, #9964, #17452 ) ;
#17907=DIRECTION ( 'NONE',  ( -0.9510565162951500895, 0.000000000000000000, -0.3090169943749582204 ) ) ;
#17908=CARTESIAN_POINT ( 'NONE',  ( -0.01641453323182725382, 1.514958906868826061, 2.952755905511811108 ) ) ;
#17910=CARTESIAN_POINT ( 'NONE',  ( 1.037524086854322514, 0.000000000000000000, 2.764473043227584803 ) ) ;
#17912=CARTESIAN_POINT ( 'NONE',  ( 0.6160390700230953254, 1.623012950100491958, -2.417151584004514131 ) ) ;
#17913=CYLINDRICAL_SURFACE ( 'NONE', #37905, 2.165354330708661568 ) ;
#17921=CARTESIAN_POINT ( 'NONE',  ( 1.331808205664952505, 0.000000000000000000, 1.125026879082043685 ) ) ;
#17924=CARTESIAN_POINT ( 'NONE',  ( -1.083598637574820334, 1.603934357758587614, 2.747180975113330259 ) ) ;
#17926=AXIS2_PLACEMENT_3D ( 'NONE', #22394, #46111, #45600 ) ;
#17927=ORIENTED_EDGE ( 'NONE', *, *, #9244, .T. ) ;
#17936=ORIENTED_EDGE ( 'NONE', *, *, #24220, .F. ) ;
#17937=DIRECTION ( 'NONE',  ( -0.000000000000000000, 1.000000000000000000, -0.000000000000000000 ) ) ;
#17938=EDGE_LOOP ( 'NONE', ( #47291, #14978, #31411, #41623 ) ) ;
#17939=VERTEX_POINT ( 'NONE', #23611 ) ;
#17942=CARTESIAN_POINT ( 'NONE',  ( 0.000000000000000000, 5.905511811023623991, 0.000000000000000000 ) ) ;
#17946=CARTESIAN_POINT ( 'NONE',  ( 2.122900538663711867, 1.752334412280341258, -2.052396120422125048 ) ) ;
#17954=CARTESIAN_POINT ( 'NONE',  ( -1.670787592146344203, 0.000000000000000000, 0.5255918861343552573 ) ) ;
#17955=CARTESIAN_POINT ( 'NONE',  ( -1.905671854841497481, 1.555429617898292705, 2.256015092822653667 ) ) ;
#17957=FACE_OUTER_BOUND ( 'NONE', #19951, .T. ) ;
#17961=CARTESIAN_POINT ( 'NONE',  ( 0.000000000000000000, 6.692913385826772199, 0.000000000000000000 ) ) ;
#17962=DIRECTION ( 'NONE',  ( -0.000000000000000000, 1.000000000000000000, -0.000000000000000000 ) ) ;
#17968=CARTESIAN_POINT ( 'NONE',  ( -0.04921259842519708910, 1.718497255264965551, 2.952755905511811108 ) ) ;
#17969=B_SPLINE_CURVE_WITH_KNOTS ( 'NONE', 3,
 ( #16286, #38768, #35909, #3397 ),
 .UNSPECIFIED., .F., .F.,
 ( 4, 4 ),
 ( 2.008317325138464645E-07, 0.002500501682857974185 ),
 .UNSPECIFIED. ) ;
#17970=ORIENTED_EDGE ( 'NONE', *, *, #42863, .T. ) ;
#17987=VECTOR ( 'NONE', #20112, 39.37007874015748143 ) ;
#17991=CARTESIAN_POINT ( 'NONE',  ( 2.455254121199802686, 1.757512009626756244, -1.640354758320677453 ) ) ;
#17996=EDGE_CURVE ( 'NONE', #35748, #28425, #35831, .T. ) ;
#18004=CARTESIAN_POINT ( 'NONE',  ( -2.151809081513409438, 6.692913385826772199, 0.2418202932658334581 ) ) ;
#18009=B_SPLINE_CURVE_WITH_KNOTS ( 'NONE', 3,
 ( #15382, #11753, #7632, #4261 ),
 .UNSPECIFIED., .F., .F.,
 ( 4, 4 ),
 ( 2.472340750494697777E-07, 0.002500446055397966515 ),
 .UNSPECIFIED. ) ;
#18010=B_SPLINE_CURVE_WITH_KNOTS ( 'NONE', 3,
 ( #16380, #5258, #24635, #43719 ),
 .UNSPECIFIED., .F., .F.,
 ( 4, 4 ),
 ( 6.023332361526389438E-07, 0.0004818377974856800200 ),
 .UNSPECIFIED. ) ;
#18028=ORIENTED_EDGE ( 'NONE', *, *, #48936, .T. ) ;
#18033=CARTESIAN_POINT ( 'NONE',  ( -2.101347671104863313, 1.674245022174266406, -0.5300970854448181502 ) ) ;
#18035=AXIS2_PLACEMENT_3D ( 'NONE', #50769, #3336, #30964 ) ;
#18036=CARTESIAN_POINT ( 'NONE',  ( -1.216138243788243756, 1.692421698714137834, 2.131422395811148895 ) ) ;
#18037=CARTESIAN_POINT ( 'NONE',  ( 1.962403044652552442, 1.049866565067837820, -0.4983838811554699988 ) ) ;
#18038=ORIENTED_EDGE ( 'NONE', *, *, #9881, .T. ) ;
#18040=EDGE_CURVE ( 'NONE', #35466, #50600, #29014, .T. ) ;
#18042=VERTEX_POINT ( 'NONE', #19983 ) ;
#18043=EDGE_CURVE ( 'NONE', #37363, #9867, #45749, .T. ) ;
#18044=CARTESIAN_POINT ( 'NONE',  ( 1.083598637574781920, 1.736150426126270130, 2.747180975113346246 ) ) ;
#18045=ORIENTED_EDGE ( 'NONE', *, *, #13200, .F. ) ;
#18048=EDGE_CURVE ( 'NONE', #26872, #46130, #18553, .T. ) ;
#18049=VERTEX_POINT ( 'NONE', #28502 ) ;
#18055=CARTESIAN_POINT ( 'NONE',  ( 0.1450934409768589450, 1.205361022782829114E-17, 2.161127057262026252 ) ) ;
#18056=ORIENTED_EDGE ( 'NONE', *, *, #31810, .T. ) ;
#18058=CARTESIAN_POINT ( 'NONE',  ( 0.1526763070133267952, 1.611922144458495687, -2.245379599360889600 ) ) ;
#18062=CONICAL_SURFACE ( 'NONE', #42805, 3.483074324928249421, 1.244861948955335196 ) ;
#18063=DIRECTION ( 'NONE',  ( -8.032339854997315857E-17, 1.000000000000000000, -1.007223559679407077E-16 ) ) ;
#18069=DIRECTION ( 'NONE',  ( 7.105427357601001859E-15, 0.000000000000000000, 1.000000000000000000 ) ) ;
#18073=ORIENTED_EDGE ( 'NONE', *, *, #46326, .F. ) ;
#18076=CARTESIAN_POINT ( 'NONE',  ( -2.734482843737247038, 1.572033689214636709, -1.115254632218712016 ) ) ;
#18085=CARTESIAN_POINT ( 'NONE',  ( 0.2719150483610129343, 1.617565011433980793, -2.472216738435130789 ) ) ;
#18087=CARTESIAN_POINT ( 'NONE',  ( 0.000000000000000000, 5.905511811023623991, 0.000000000000000000 ) ) ;
#18091=CARTESIAN_POINT ( 'NONE',  ( -1.733853452330418987, 0.0001488292986583184614, 0.1852043564780690432 ) ) ;
#18093=VERTEX_POINT ( 'NONE', #32917 ) ;
#18095=AXIS2_PLACEMENT_3D ( 'NONE', #26133, #10128, #18134 ) ;
#18096=CARTESIAN_POINT ( 'NONE',  ( 2.592238343552378144, 1.756184615076457289, 0.8940144833510662581 ) ) ;
#18099=EDGE_CURVE ( 'NONE', #8249, #37948, #5019, .T. ) ;
#18100=ORIENTED_EDGE ( 'NONE', *, *, #36119, .T. ) ;
#18109=ORIENTED_EDGE ( 'NONE', *, *, #40000, .F. ) ;
#18111=ORIENTED_EDGE ( 'NONE', *, *, #49241, .T. ) ;
#18113=CARTESIAN_POINT ( 'NONE',  ( -2.695799277629577162, 1.677241212940233872, -1.205759334241492509 ) ) ;
#18116=ORIENTED_EDGE ( 'NONE', *, *, #34442, .T. ) ;
#18118=EDGE_CURVE ( 'NONE', #7052, #32688, #2105, .T. ) ;
#18119=DIRECTION ( 'NONE',  ( 0.01601477604151182663, -0.9998717552508123996, 0.000000000000000000 ) ) ;
#18123=DIRECTION ( 'NONE',  ( -0.01601477604151182663, 0.9998717552508123996, -0.000000000000000000 ) ) ;
#18124=CARTESIAN_POINT ( 'NONE',  ( 1.001850874905584654E-35, 5.905511811023623991, -2.165354330708661568 ) ) ;
#18134=DIRECTION ( 'NONE',  ( 0.000000000000000000, 0.000000000000000000, 1.000000000000000000 ) ) ;
#18137=CARTESIAN_POINT ( 'NONE',  ( 1.747029694980739789, -1.511962954662943480E-16, 1.330264415365524533 ) ) ;
#18138=CONICAL_SURFACE ( 'NONE', #33821, 2.244934639244524632, 1.554780866114618743 ) ;
#18139=B_SPLINE_CURVE_WITH_KNOTS ( 'NONE', 3,
 ( #13889, #41762, #45603, #6651 ),
 .UNSPECIFIED., .F., .F.,
 ( 4, 4 ),
 ( 2.033027968835072235E-07, 0.01757837248110587572 ),
 .UNSPECIFIED. ) ;
#18143=DIRECTION ( 'NONE',  ( 1.042246309067994810E-16, 1.000000000000000000, 7.572362681945316160E-17 ) ) ;
#18145=CARTESIAN_POINT ( 'NONE',  ( 0.000000000000000000, 1.574803149606302854, 0.000000000000000000 ) ) ;
#18146=DIRECTION ( 'NONE',  ( -0.9510565162951544194, -3.583074652439903135E-17, 0.3090169943749447312 ) ) ;
#18156=CARTESIAN_POINT ( 'NONE',  ( -1.478009596860490715, 1.585803725363800210, 1.616919955472289727 ) ) ;
#18157=EDGE_LOOP ( 'NONE', ( #30499, #42068, #15194, #5132 ) ) ;
#18158=DIRECTION ( 'NONE',  ( 0.01601477604151182663, -0.9998717552508123996, 0.000000000000000000 ) ) ;
#18161=CARTESIAN_POINT ( 'NONE',  ( 0.01639384210327993543, 1.514242943312319012, 2.952755905511811108 ) ) ;
#18162=VERTEX_POINT ( 'NONE', #17663 ) ;
#18163=CARTESIAN_POINT ( 'NONE',  ( 0.07982360342473591996, 1.709180471932028711, 0.000000000000000000 ) ) ;
#18164=ADVANCED_FACE ( 'NONE', ( #34179 ), #13687, .T. ) ;
#18166=LINE ( 'NONE', #21528, #42451 ) ;
#18168=DIRECTION ( 'NONE',  ( -0.9998717552508121775, -0.01601477604151182316, 0.000000000000000000 ) ) ;
#18169=VECTOR ( 'NONE', #10705, 39.37007874015748854 ) ;
#18171=ORIENTED_EDGE ( 'NONE', *, *, #47007, .F. ) ;
#18173=CARTESIAN_POINT ( 'NONE',  ( 2.099568260077707027, 6.692913385826772199, -0.5296909464895783737 ) ) ;
#18174=DIRECTION ( 'NONE',  ( -3.986037398843765983E-20, -1.000000000000000000, -1.160734090543304660E-16 ) ) ;
#18175=EDGE_LOOP ( 'NONE', ( #14552, #27874, #25518, #31874 ) ) ;
#18178=CONICAL_SURFACE ( 'NONE', #4160, 3.033577403570480779, 1.554780866114618743 ) ;
#18181=ORIENTED_EDGE ( 'NONE', *, *, #38373, .F. ) ;
#18184=CARTESIAN_POINT ( 'NONE',  ( 2.164823134740036625, 5.905511811023623991, -0.04796011690015061085 ) ) ;
#18194=CARTESIAN_POINT ( 'NONE',  ( -1.679154924913551783, 0.000000000000000000, 0.4938453199301923724 ) ) ;
#18195=EDGE_CURVE ( 'NONE', #37703, #48160, #44412, .T. ) ;
#18196=ORIENTED_EDGE ( 'NONE', *, *, #30228, .F. ) ;
#18203=CARTESIAN_POINT ( 'NONE',  ( -1.891439052599157122, 1.677607092856729709, 1.073712343777111222 ) ) ;
#18204=VECTOR ( 'NONE', #34771, 39.37007874015748143 ) ;
#18205=AXIS2_PLACEMENT_3D ( 'NONE', #27536, #24451, #19281 ) ;
#18212=DIRECTION ( 'NONE',  ( 0.000000000000000000, 1.000000000000000000, 0.000000000000000000 ) ) ;
#18213=CIRCLE ( 'NONE', #25615, 2.244934639244525076 ) ;
#18215=VERTEX_POINT ( 'NONE', #41163 ) ;
#18217=LINE ( 'NONE', #44804, #9650 ) ;
#18218=EDGE_LOOP ( 'NONE', ( #28436, #50893, #19166, #29855 ) ) ;
#18223=ORIENTED_EDGE ( 'NONE', *, *, #32230, .T. ) ;
#18224=DIRECTION ( 'NONE',  ( -0.9989930665413151445, 0.000000000000000000, 0.04486483035050446017 ) ) ;
#18227=LINE ( 'NONE', #22359, #31693 ) ;
#18228=EDGE_CURVE ( 'NONE', #45076, #3510, #29617, .T. ) ;
#18230=LINE ( 'NONE', #22610, #5385 ) ;
#18233=ORIENTED_EDGE ( 'NONE', *, *, #24027, .F. ) ;
#18239=CARTESIAN_POINT ( 'NONE',  ( -0.9914495361339011881, 1.536537968533926657, 2.781765111341808705 ) ) ;
#18243=CARTESIAN_POINT ( 'NONE',  ( 0.1450934409768597499, 5.905511811023623991, 2.161127057262026696 ) ) ;
#18244=ORIENTED_EDGE ( 'NONE', *, *, #33959, .T. ) ;
#18246=VERTEX_POINT ( 'NONE', #37548 ) ;
#18256=ADVANCED_FACE ( 'NONE', ( #33168 ), #48850, .T. ) ;
#18262=ORIENTED_EDGE ( 'NONE', *, *, #13507, .T. ) ;
#18263=DIRECTION ( 'NONE',  ( -5.207613805427244364E-18, -1.000000000000000000, -1.159565308550900415E-16 ) ) ;
#18266=DIRECTION ( 'NONE',  ( -0.000000000000000000, 1.000000000000000000, -0.000000000000000000 ) ) ;
#18269=ORIENTED_EDGE ( 'NONE', *, *, #18118, .T. ) ;
#18271=PLANE ( 'NONE',  #35569 ) ;
#18273=ORIENTED_EDGE ( 'NONE', *, *, #10476, .T. ) ;
#18274=CARTESIAN_POINT ( 'NONE',  ( -2.947574761915765063, 1.673315526576397261, -0.1816379373805333819 ) ) ;
#18279=B_SPLINE_CURVE_WITH_KNOTS ( 'NONE', 3,
 ( #49309, #29729, #37995, #45446 ),
 .UNSPECIFIED., .F., .F.,
 ( 4, 4 ),
 ( 6.133893191261082042E-07, 0.001146920647357106129 ),
 .UNSPECIFIED. ) ;
#18280=EDGE_CURVE ( 'NONE', #29782, #20718, #27415, .T. ) ;
#18285=CARTESIAN_POINT ( 'NONE',  ( 1.387661672111481836, 0.000000000000000000, -1.663104731517921930 ) ) ;
#18286=EDGE_CURVE ( 'NONE', #7103, #25998, #11179, .T. ) ;
#18296=VERTEX_POINT ( 'NONE', #23544 ) ;
#18297=CARTESIAN_POINT ( 'NONE',  ( -0.8069532150559458605, 0.000000000000000000, -2.010061882867143268 ) ) ;
#18303=CARTESIAN_POINT ( 'NONE',  ( 0.9914495361338625523, 1.734714548371065312, 2.781765111341823360 ) ) ;
#18308=ORIENTED_EDGE ( 'NONE', *, *, #41419, .T. ) ;
#18322=B_SPLINE_CURVE_WITH_KNOTS ( 'NONE', 3,
 ( #18751, #22876, #11003, #3762 ),
 .UNSPECIFIED., .F., .F.,
 ( 4, 4 ),
 ( 0.0003396899135061814587, 0.002839874597594404127 ),
 .UNSPECIFIED. ) ;
#18325=CARTESIAN_POINT ( 'NONE',  ( -2.672362179832771467, 1.673511163758323539, 0.3123340015432766736 ) ) ;
#18327=ORIENTED_EDGE ( 'NONE', *, *, #8048, .F. ) ;
#18328=VERTEX_POINT ( 'NONE', #15558 ) ;
#18332=EDGE_CURVE ( 'NONE', #47632, #42820, #22800, .T. ) ;
#18334=CARTESIAN_POINT ( 'NONE',  ( 2.134236802639954522, 0.000000000000000000, -2.040539317874581204 ) ) ;
#18335=ADVANCED_FACE ( 'NONE', ( #50117 ), #4609, .T. ) ;
#18337=DIRECTION ( 'NONE',  ( 0.000000000000000000, 1.160734090543304660E-16, -1.000000000000000000 ) ) ;
#18345=CARTESIAN_POINT ( 'NONE',  ( 1.695772546416037363, 1.647224322255602891, -2.417756147381349141 ) ) ;
#18351=ORIENTED_EDGE ( 'NONE', *, *, #12773, .T. ) ;
#18354=ORIENTED_EDGE ( 'NONE', *, *, #6234, .T. ) ;
#18359=ORIENTED_EDGE ( 'NONE', *, *, #6520, .F. ) ;
#18360=B_SPLINE_CURVE_WITH_KNOTS ( 'NONE', 3,
 ( #5265, #17148, #31885, #12767 ),
 .UNSPECIFIED., .F., .F.,
 ( 4, 4 ),
 ( 5.466635587719015859E-05, 0.002554690799234834650 ),
 .UNSPECIFIED. ) ;
#18363=VERTEX_POINT ( 'NONE', #19668 ) ;
#18364=ORIENTED_EDGE ( 'NONE', *, *, #35021, .F. ) ;
#18367=PLANE ( 'NONE',  #5895 ) ;
#18369=ORIENTED_EDGE ( 'NONE', *, *, #23046, .T. ) ;
#18376=EDGE_LOOP ( 'NONE', ( #8467, #16177, #47948, #49696 ) ) ;
#18382=ORIENTED_EDGE ( 'NONE', *, *, #5990, .F. ) ;
#18383=ORIENTED_EDGE ( 'NONE', *, *, #36304, .T. ) ;
#18388=CARTESIAN_POINT ( 'NONE',  ( -0.4369915662458470074, 0.02092044581182531462, -1.768387524372482034 ) ) ;
#18394=VECTOR ( 'NONE', #40495, 39.37007874015748143 ) ;
#18395=EDGE_CURVE ( 'NONE', #22312, #47699, #37677, .T. ) ;
#18399=DIRECTION ( 'NONE',  ( -0.9998717552508122886, -0.01601477604151182316, 0.000000000000000000 ) ) ;
#18400=CIRCLE ( 'NONE', #47198, 1.743387098533651480 ) ;
#18407=CARTESIAN_POINT ( 'NONE',  ( -1.962403044864191592, 1.049866565877817681, -0.4983838812038057786 ) ) ;
#18414=LINE ( 'NONE', #38046, #20440 ) ;
#18415=B_SPLINE_CURVE_WITH_KNOTS ( 'NONE', 3,
 ( #18962, #34716, #11222, #47044 ),
 .UNSPECIFIED., .F., .F.,
 ( 4, 4 ),
 ( 0.001721583058954078652, 0.004221656532247743121 ),
 .UNSPECIFIED. ) ;
#18416=ORIENTED_EDGE ( 'NONE', *, *, #25204, .T. ) ;
#18417=DIRECTION ( 'NONE',  ( -0.01601477604151182663, 0.9998717552508123996, -0.000000000000000000 ) ) ;
#18418=DIRECTION ( 'NONE',  ( 0.3930250316539147803, -1.160734090543304660E-16, 0.9195277725514544587 ) ) ;
#18419=DIRECTION ( 'NONE',  ( 0.000000000000000000, 0.000000000000000000, -1.000000000000000000 ) ) ;
#18422=AXIS2_PLACEMENT_3D ( 'NONE', #28710, #49317, #17863 ) ;
#18427=ORIENTED_EDGE ( 'NONE', *, *, #42782, .F. ) ;
#18428=VECTOR ( 'NONE', #44740, 39.37007874015748143 ) ;
#18429=CARTESIAN_POINT ( 'NONE',  ( 2.122091976112992828, 0.000000000000000000, 0.4338754535133130252 ) ) ;
#18441=FACE_OUTER_BOUND ( 'NONE', #16385, .T. ) ;
#18445=B_SPLINE_CURVE_WITH_KNOTS ( 'NONE', 3,
 ( #8232, #24239, #35603, #47429 ),
 .UNSPECIFIED., .F., .F.,
 ( 4, 4 ),
 ( 2.051444086415969096E-07, 0.002500220145220648053 ),
 .UNSPECIFIED. ) ;
#18448=ORIENTED_EDGE ( 'NONE', *, *, #45465, .T. ) ;
#18449=DIRECTION ( 'NONE',  ( -0.9998717552508121775, -0.01601477604151182663, 0.000000000000000000 ) ) ;
#18452=CARTESIAN_POINT ( 'NONE',  ( -2.394539146693994702, 1.677872874819792859, 1.232670874412874040 ) ) ;
#18454=DIRECTION ( 'NONE',  ( -0.01601477604151182663, 0.9998717552508123996, -0.000000000000000000 ) ) ;
#18461=EDGE_CURVE ( 'NONE', #19150, #31480, #4911, .T. ) ;
#18462=AXIS2_PLACEMENT_3D ( 'NONE', #20007, #35773, #44016 ) ;
#18463=CARTESIAN_POINT ( 'NONE',  ( -1.772999178993743152, 2.755905511811027164, -1.009977129983215649 ) ) ;
#18465=ORIENTED_EDGE ( 'NONE', *, *, #36522, .F. ) ;
#18467=PLANE ( 'NONE',  #15955 ) ;
#18468=AXIS2_PLACEMENT_3D ( 'NONE', #7986, #229, #31743 ) ;
#18471=AXIS2_PLACEMENT_3D ( 'NONE', #4679, #44667, #20418 ) ;
#18472=ORIENTED_EDGE ( 'NONE', *, *, #25611, .T. ) ;
#18484=FACE_OUTER_BOUND ( 'NONE', #5921, .T. ) ;
#18491=CARTESIAN_POINT ( 'NONE',  ( -2.168245791271168343, 1.685466330048090322, -2.004968704497279930 ) ) ;
#18492=LINE ( 'NONE', #40781, #4600 ) ;
#18493=FACE_OUTER_BOUND ( 'NONE', #2828, .T. ) ;
#18495=DIRECTION ( 'NONE',  ( -0.01601477604151182663, 0.9998717552508123996, -0.000000000000000000 ) ) ;
#18497=B_SPLINE_CURVE_WITH_KNOTS ( 'NONE', 3,
 ( #20635, #40778, #4891, #5400 ),
 .UNSPECIFIED., .F., .F.,
 ( 4, 4 ),
 ( 0.1211775127643062444, 0.1625894504277921315 ),
 .UNSPECIFIED. ) ;
#18501=CARTESIAN_POINT ( 'NONE',  ( 2.491402175429654253, 1.758084086496218612, -1.585592796919505609 ) ) ;
#18502=VECTOR ( 'NONE', #31658, 39.37007874015748143 ) ;
#18504=ADVANCED_FACE ( 'NONE', ( #27667 ), #41289, .F. ) ;
#18517=LINE ( 'NONE', #18004, #12231 ) ;
#18518=CARTESIAN_POINT ( 'NONE',  ( 1.033334490728470723, 1.724452693827607908, -2.032317711754626277 ) ) ;
#18520=CARTESIAN_POINT ( 'NONE',  ( 1.810607833951273227, 0.05691986357332023266, -0.7203715021987137090 ) ) ;
#18522=CARTESIAN_POINT ( 'NONE',  ( 2.576863348864710801, 1.660943078747768364, 1.442554885838449819 ) ) ;
#18525=ORIENTED_EDGE ( 'NONE', *, *, #27106, .T. ) ;
#18526=DIRECTION ( 'NONE',  ( -0.000000000000000000, 1.000000000000000000, -0.000000000000000000 ) ) ;
#18529=CARTESIAN_POINT ( 'NONE',  ( -1.693234526714950228, 0.000000000000000000, -0.4369479234249735167 ) ) ;
#18536=ORIENTED_EDGE ( 'NONE', *, *, #11922, .T. ) ;
#18537=CONICAL_SURFACE ( 'NONE', #5339, 1.850107469027523210, 0.6386652850508578450 ) ;
#18538=AXIS2_PLACEMENT_3D ( 'NONE', #32053, #28153, #20937 ) ;
#18539=CARTESIAN_POINT ( 'NONE',  ( 1.956192433058983493, 0.05925166736471587647, -0.03859050128386512513 ) ) ;
#18545=FACE_OUTER_BOUND ( 'NONE', #8460, .T. ) ;
#18547=VERTEX_POINT ( 'NONE', #2553 ) ;
#18550=VECTOR ( 'NONE', #36417, 39.37007874015748143 ) ;
#18553=B_SPLINE_CURVE_WITH_KNOTS ( 'NONE', 3,
 ( #24385, #40141, #9404, #48093 ),
 .UNSPECIFIED., .F., .F.,
 ( 4, 4 ),
 ( 6.098493025361481195E-07, 0.001073452918374830957 ),
 .UNSPECIFIED. ) ;
#18554=CARTESIAN_POINT ( 'NONE',  ( -2.952069331832154919, 5.118110236220475784, 1.181102362204724310 ) ) ;
#18555=EDGE_LOOP ( 'NONE', ( #39896, #14987, #3158, #36061 ) ) ;
#18560=EDGE_CURVE ( 'NONE', #7137, #7249, #34558, .T. ) ;
#18561=CARTESIAN_POINT ( 'NONE',  ( 0.07982360342473591996, 1.709180471932028711, 0.000000000000000000 ) ) ;
#18575=CONICAL_SURFACE ( 'NONE', #24312, 2.246510896728926010, 0.01601546068027819014 ) ;
#18582=ORIENTED_EDGE ( 'NONE', *, *, #28903, .F. ) ;
#18584=CARTESIAN_POINT ( 'NONE',  ( -0.9914495361339011881, 1.536537968533926657, 2.781765111341808705 ) ) ;
#18585=EDGE_CURVE ( 'NONE', #7499, #22686, #45632, .T. ) ;
#18589=ORIENTED_EDGE ( 'NONE', *, *, #32727, .T. ) ;
#18590=VECTOR ( 'NONE', #14867, 39.37007874015748143 ) ;
#18595=CARTESIAN_POINT ( 'NONE',  ( 0.3136974817028393425, 1.625700591256411531, -2.936457595020219635 ) ) ;
#18596=DIRECTION ( 'NONE',  ( 0.000000000000000000, 0.000000000000000000, 1.000000000000000000 ) ) ;
#18600=CARTESIAN_POINT ( 'NONE',  ( 1.834323595590318989, 5.905511811023623991, 1.151859023884926447 ) ) ;
#18603=EDGE_LOOP ( 'NONE', ( #28954, #48350, #28103, #48709 ) ) ;
#18604=LINE ( 'NONE', #42336, #18428 ) ;
#18605=PLANE ( 'NONE',  #26194 ) ;
#18606=ORIENTED_EDGE ( 'NONE', *, *, #45290, .T. ) ;
#18607=AXIS2_PLACEMENT_3D ( 'NONE', #9896, #8680, #6277 ) ;
#18627=DIRECTION ( 'NONE',  ( 0.000000000000000000, 0.000000000000000000, -1.000000000000000000 ) ) ;
#18630=DIRECTION ( 'NONE',  ( 0.000000000000000000, 0.000000000000000000, -1.000000000000000000 ) ) ;
#18632=CARTESIAN_POINT ( 'NONE',  ( 0.8668862056626265300, 0.04180443457634609727, -1.686684286392636789 ) ) ;
#18634=DIRECTION ( 'NONE',  ( -0.000000000000000000, -1.000000000000000000, -0.000000000000000000 ) ) ;
#18639=CARTESIAN_POINT ( 'NONE',  ( 0.4374213808359648237, 1.623899391754041854, 2.686003462684949827 ) ) ;
#18642=CARTESIAN_POINT ( 'NONE',  ( 1.930379001715699872, 1.650868500535964012, 2.234429108663295693 ) ) ;
#18643=LINE ( 'NONE', #34395, #46107 ) ;
#18646=CONICAL_SURFACE ( 'NONE', #35106, 2.244934639244524632, 1.554780866114618743 ) ;
#18649=CARTESIAN_POINT ( 'NONE',  ( 2.113646359261424745, 1.643330668647667858, -0.9569352356128659753 ) ) ;
#18655=CARTESIAN_POINT ( 'NONE',  ( 0.2957575371695307376, 0.01082520027161247393, 1.905371342176711114 ) ) ;
#18665=DIRECTION ( 'NONE',  ( -0.000000000000000000, -1.000000000000000000, -0.000000000000000000 ) ) ;
#18668=CARTESIAN_POINT ( 'NONE',  ( -2.437180031585919782, 1.566133505135788750, -1.667735833703134274 ) ) ;
#18672=LINE ( 'NONE', #25908, #50888 ) ;
#18673=CARTESIAN_POINT ( 'NONE',  ( -0.3136974817027967100, 1.714375164834789356, -2.936457595020224520 ) ) ;
#18674=DIRECTION ( 'NONE',  ( -3.986037398843765983E-20, -1.000000000000000000, -1.160734090543304660E-16 ) ) ;
#18676=VECTOR ( 'NONE', #35039, 39.37007874015748143 ) ;
#18677=ORIENTED_EDGE ( 'NONE', *, *, #6968, .T. ) ;
#18679=ORIENTED_EDGE ( 'NONE', *, *, #6739, .F. ) ;
#18687=CARTESIAN_POINT ( 'NONE',  ( 1.191535142427733174, 0.000000000000000000, -1.668040279728017605 ) ) ;
#18694=CARTESIAN_POINT ( 'NONE',  ( 2.715141060683428531, 0.000000000000000000, -1.160506983230063405 ) ) ;
#18697=EDGE_CURVE ( 'NONE', #42744, #4851, #512, .T. ) ;
#18698=ORIENTED_EDGE ( 'NONE', *, *, #42809, .T. ) ;
#18703=VERTEX_POINT ( 'NONE', #39692 ) ;
#18706=DIRECTION ( 'NONE',  ( -0.04486483035050446017, 0.000000000000000000, -0.9989930665413151445 ) ) ;
#18707=DIRECTION ( 'NONE',  ( 0.5508969814521065267, 0.000000000000000000, -0.8345732537212999791 ) ) ;
#18709=CARTESIAN_POINT ( 'NONE',  ( -0.4532322590609024759, 0.000000000000000000, -1.827234353172969561 ) ) ;
#18712=APPLICATION_CONTEXT ( 'automotive_design' ) ;
#18718=DIRECTION ( 'NONE',  ( -0.6579387259397136978, 0.000000000000000000, 0.7530714660036097463 ) ) ;
#18719=CARTESIAN_POINT ( 'NONE',  ( 0.1155636338427008941, -0.5222242541845523167, 0.000000000000000000 ) ) ;
#18720=DIRECTION ( 'NONE',  ( 0.000000000000000000, 0.000000000000000000, 1.000000000000000000 ) ) ;
#18721=VECTOR ( 'NONE', #37900, 39.37007874015748143 ) ;
#18724=EDGE_CURVE ( 'NONE', #16641, #25262, #17842, .T. ) ;
#18729=ORIENTED_EDGE ( 'NONE', *, *, #40017, .T. ) ;
#18730=CARTESIAN_POINT ( 'NONE',  ( -1.621934931400436541, 0.000000000000000000, -0.6753680165623594522 ) ) ;
#18734=VERTEX_POINT ( 'NONE', #31957 ) ;
#18735=CARTESIAN_POINT ( 'NONE',  ( -2.889674983507169337, 1.205361022782829114E-17, -0.6090712660038032356 ) ) ;
#18738=CARTESIAN_POINT ( 'NONE',  ( -1.461363083917493588, 1.574803149606302854, 1.597866488315563327 ) ) ;
#18745=FACE_OUTER_BOUND ( 'NONE', #45210, .T. ) ;
#18749=EDGE_CURVE ( 'NONE', #15665, #13810, #23685, .T. ) ;
#18750=ORIENTED_EDGE ( 'NONE', *, *, #45173, .F. ) ;
#18751=CARTESIAN_POINT ( 'NONE',  ( -1.330356682269850044, 1.588168657012911877, -1.747353411991260819 ) ) ;
#18754=EDGE_CURVE ( 'NONE', #2997, #3878, #3800, .T. ) ;
#18760=ORIENTED_EDGE ( 'NONE', *, *, #43343, .T. ) ;
#18761=EDGE_CURVE ( 'NONE', #20976, #20329, #8201, .T. ) ;
#18762=ORIENTED_EDGE ( 'NONE', *, *, #18769, .T. ) ;
#18763=ORIENTED_EDGE ( 'NONE', *, *, #50899, .F. ) ;
#18764=CARTESIAN_POINT ( 'NONE',  ( -0.5440951526915226433, 1.699187271209207983, -2.156468654116168171 ) ) ;
#18765=ADVANCED_FACE ( 'NONE', ( #43293 ), #23175, .T. ) ;
#18769=EDGE_CURVE ( 'NONE', #2318, #9779, #50737, .T. ) ;
#18772=CARTESIAN_POINT ( 'NONE',  ( -1.010509689441836390, 0.01173450346422093109, -1.474572740271697047 ) ) ;
#18775=CARTESIAN_POINT ( 'NONE',  ( -2.160407304981126764, 1.574803149606302854, -0.1462862061266896330 ) ) ;
#18776=CARTESIAN_POINT ( 'NONE',  ( 1.834499544866850851, 1.737284818394516206, 1.400019292979238772 ) ) ;
#18777=EDGE_CURVE ( 'NONE', #45538, #23634, #11667, .T. ) ;
#18778=DIRECTION ( 'NONE',  ( -0.9909497617679332571, 0.000000000000000000, -0.1342332658176667304 ) ) ;
#18786=CARTESIAN_POINT ( 'NONE',  ( 2.947574761915768171, 1.447536563168191126, -0.1816379373804911657 ) ) ;
#18799=CONICAL_SURFACE ( 'NONE', #665, 2.165354330708661568, 0.2617993877991570129 ) ;
#18800=CARTESIAN_POINT ( 'NONE',  ( 0.1155636338427008941, -0.5222242541845523167, 0.000000000000000000 ) ) ;
#18806=AXIS2_PLACEMENT_3D ( 'NONE', #19643, #9259, #17013 ) ;
#18812=ADVANCED_FACE ( 'NONE', ( #44321 ), #31030, .F. ) ;
#18815=VERTEX_POINT ( 'NONE', #13353 ) ;
#18820=CARTESIAN_POINT ( 'NONE',  ( 1.232620761116212105, 1.574803149606302854, -1.780282403660734980 ) ) ;
#18823=ORIENTED_EDGE ( 'NONE', *, *, #40143, .F. ) ;
#18825=CARTESIAN_POINT ( 'NONE',  ( 0.08139965876239094178, 1.610780518492231694, 0.000000000000000000 ) ) ;
#18828=LINE ( 'NONE', #47416, #10545 ) ;
#18829=EDGE_LOOP ( 'NONE', ( #6678, #19736, #13582, #9217 ) ) ;
#18831=CARTESIAN_POINT ( 'NONE',  ( -2.074049943651441019, 1.574803149606302854, 0.6221544894623937116 ) ) ;
#18848=CARTESIAN_POINT ( 'NONE',  ( 1.709950266952970921, 0.000000000000000000, -0.3398067978735070382 ) ) ;
#18849=ORIENTED_EDGE ( 'NONE', *, *, #1324, .F. ) ;
#18851=CARTESIAN_POINT ( 'NONE',  ( -0.2810367729153296912, 1.520692402626517170, -2.939397112015448066 ) ) ;
#18852=ORIENTED_EDGE ( 'NONE', *, *, #28685, .F. ) ;
#18856=VECTOR ( 'NONE', #4009, 39.37007874015747433 ) ;
#18859=VERTEX_POINT ( 'NONE', #40212 ) ;
#18860=CARTESIAN_POINT ( 'NONE',  ( -1.387661672111457412, 1.205361022782829114E-17, -1.663104731517942136 ) ) ;
#18863=B_SPLINE_CURVE_WITH_KNOTS ( 'NONE', 3,
 ( #19684, #15814, #31574, #11948 ),
 .UNSPECIFIED., .F., .F.,
 ( 4, 4 ),
 ( 2.033027418798480799E-07, 0.01771249989147270082 ),
 .UNSPECIFIED. ) ;
#18864=CIRCLE ( 'NONE', #27911, 1.850107469027523432 ) ;
#18865=DIRECTION ( 'NONE',  ( 2.866708903754326305E-17, 1.000000000000000000, 1.255987235303924321E-16 ) ) ;
#18870=VERTEX_POINT ( 'NONE', #24460 ) ;
#18871=CARTESIAN_POINT ( 'NONE',  ( 0.9914495361338626633, 0.000000000000000000, 2.781765111341823360 ) ) ;
#18881=DIRECTION ( 'NONE',  ( -0.08963930890344089242, 0.000000000000000000, 0.9959742939952384022 ) ) ;
#18883=CARTESIAN_POINT ( 'NONE',  ( 0.000000000000000000, 6.692913385826772199, 0.000000000000000000 ) ) ;
#18885=VERTEX_POINT ( 'NONE', #33239 ) ;
#18887=DIRECTION ( 'NONE',  ( 0.000000000000000000, 0.000000000000000000, -1.000000000000000000 ) ) ;
#18888=( BOUNDED_CURVE ( )  B_SPLINE_CURVE ( 3, ( #40752, #41012, #5378, #36884 ),
 .UNSPECIFIED., .F., .F. ) 
 B_SPLINE_CURVE_WITH_KNOTS ( ( 4, 4 ),
 ( 5.617161475044070151, 5.667964663408525894 ),
 .UNSPECIFIED. ) 
 CURVE ( )  GEOMETRIC_REPRESENTATION_ITEM ( )  RATIONAL_B_SPLINE_CURVE ( ( 1.000000000000000000, 0.9997849312356386076, 0.9997849312356386076, 1.000000000000000000 ) ) 
 REPRESENTATION_ITEM ( '' )  );
#18896=VERTEX_POINT ( 'NONE', #28316 ) ;
#18897=CARTESIAN_POINT ( 'NONE',  ( 0.2156353639037333347, 0.03137346048107473445, -1.846898229409209558 ) ) ;
#18900=EDGE_CURVE ( 'NONE', #9322, #10377, #20839, .T. ) ;
#18908=CARTESIAN_POINT ( 'NONE',  ( -1.312442655063644770, 0.006898494447474761912, -1.186737126055851022 ) ) ;
#18914=DIRECTION ( 'NONE',  ( -3.986037398843765983E-20, -1.000000000000000000, -1.160734090543304660E-16 ) ) ;
#18921=DIRECTION ( 'NONE',  ( -0.01601477604151182663, 0.9998717552508123996, -0.000000000000000000 ) ) ;
#18931=CARTESIAN_POINT ( 'NONE',  ( -1.171400696859933532, 1.590714628027123823, 1.864644694871980590 ) ) ;
#18940=CARTESIAN_POINT ( 'NONE',  ( -1.834323595590334977, 5.905511811023623991, 1.151859023884901356 ) ) ;
#18943=ORIENTED_EDGE ( 'NONE', *, *, #21625, .F. ) ;
#18948=VERTEX_POINT ( 'NONE', #46088 ) ;
#18952=LINE ( 'NONE', #46289, #19255 ) ;
#18953=CARTESIAN_POINT ( 'NONE',  ( 1.461363083917469163, 6.692913385826772199, 1.597866488315585087 ) ) ;
#18956=ORIENTED_EDGE ( 'NONE', *, *, #8032, .F. ) ;
#18958=CARTESIAN_POINT ( 'NONE',  ( -0.1227720337126170513, 0.000000000000000000, -1.913115909999223652 ) ) ;
#18959=CARTESIAN_POINT ( 'NONE',  ( -0.04921259842519706829, 1.707113721008201024, 2.241222193722145484 ) ) ;
#18960=EDGE_CURVE ( 'NONE', #2592, #22332, #20914, .T. ) ;
#18962=CARTESIAN_POINT ( 'NONE',  ( 2.064489077472676737, 1.642543324816299277, 1.055063358597729595 ) ) ;
#18964=ADVANCED_FACE ( 'NONE', ( #26238, #6872 ), #6106, .T. ) ;
#18967=EDGE_CURVE ( 'NONE', #49786, #29523, #7923, .T. ) ;
#18968=VECTOR ( 'NONE', #47163, 39.37007874015748854 ) ;
#18971=AXIS2_PLACEMENT_3D ( 'NONE', #855, #12989, #4729 ) ;
#18977=ORIENTED_EDGE ( 'NONE', *, *, #41942, .F. ) ;
#18988=CARTESIAN_POINT ( 'NONE',  ( 0.002207914879453961535, -5.712274067634378313E-18, 0.04916304461325374242 ) ) ;
#18989=CARTESIAN_POINT ( 'NONE',  ( -0.3382312733057318832, 6.692913385826772199, -2.139420919314970693 ) ) ;
#18992=CARTESIAN_POINT ( 'NONE',  ( 1.773598097765477277, 1.637884173412089250, 1.477342561509449759 ) ) ;
#18996=VERTEX_POINT ( 'NONE', #14363 ) ;
#18997=CARTESIAN_POINT ( 'NONE',  ( -2.695799277629577162, 1.578813927010291218, -1.205759334241492731 ) ) ;
#19007=ORIENTED_EDGE ( 'NONE', *, *, #27044, .T. ) ;
#19014=CARTESIAN_POINT ( 'NONE',  ( 1.775400203342704986, 1.746929418358725172, -2.359903268218703332 ) ) ;
#19020=CARTESIAN_POINT ( 'NONE',  ( 2.009930929872536964, 2.755905511811027164, -0.8055662819783819817 ) ) ;
#19021=ADVANCED_FACE ( 'NONE', ( #18493 ), #10494, .F. ) ;
#19024=EDGE_CURVE ( 'NONE', #50937, #30224, #33523, .T. ) ;
#19026=VERTEX_POINT ( 'NONE', #34500 ) ;
#19027=DIRECTION ( 'NONE',  ( -0.9998717552508122886, -0.01601477604151185785, 0.000000000000000000 ) ) ;
#19028=ADVANCED_FACE ( 'NONE', ( #18745 ), #30617, .F. ) ;
#19030=CARTESIAN_POINT ( 'NONE',  ( 2.224044434511903923, 1.677907295117183617, 0.6708906538694197064 ) ) ;
#19031=EDGE_LOOP ( 'NONE', ( #33348, #20278, #13252, #40346 ) ) ;
#19037=EDGE_CURVE ( 'NONE', #6926, #10313, #27120, .T. ) ;
#19038=DIRECTION ( 'NONE',  ( 0.000000000000000000, 1.000000000000000000, -0.000000000000000000 ) ) ;
#19040=ORIENTED_EDGE ( 'NONE', *, *, #48239, .F. ) ;
#19041=ORIENTED_EDGE ( 'NONE', *, *, #6101, .T. ) ;
#19046=VECTOR ( 'NONE', #41234, 39.37007874015748143 ) ;
#19048=ORIENTED_EDGE ( 'NONE', *, *, #35951, .F. ) ;
#19052=CARTESIAN_POINT ( 'NONE',  ( -1.775400203342670569, 1.205361022782829114E-17, -2.359903268218729089 ) ) ;
#19054=ORIENTED_EDGE ( 'NONE', *, *, #2500, .F. ) ;
#19061=ORIENTED_EDGE ( 'NONE', *, *, #23285, .T. ) ;
#19064=DIRECTION ( 'NONE',  ( -0.5508969814521065267, 1.288287287306305283E-16, 0.8345732537212999791 ) ) ;
#19065=EDGE_CURVE ( 'NONE', #44866, #18296, #17002, .T. ) ;
#19067=DIRECTION ( 'NONE',  ( 0.000000000000000000, 0.000000000000000000, 1.000000000000000000 ) ) ;
#19069=CARTESIAN_POINT ( 'NONE',  ( -2.122907315177388288, 1.559117831781008601, -2.052389032744492248 ) ) ;
#19071=DIRECTION ( 'NONE',  ( -0.01601477604151182663, 0.9998717552508123996, -0.000000000000000000 ) ) ;
#19073=CARTESIAN_POINT ( 'NONE',  ( -1.276224672482803912, 0.5249316497054298258, 1.385958525741132874 ) ) ;
#19077=CARTESIAN_POINT ( 'NONE',  ( 0.4788131938641111973, 1.504819983455083277, 2.914091152102192162 ) ) ;
#19078=DIRECTION ( 'NONE',  ( 0.3930250316539278810, -1.160734090543304907E-16, -0.9195277725514489076 ) ) ;
#19081=CARTESIAN_POINT ( 'NONE',  ( -1.743516651958532115, 0.0004834999639498430428, -4.958524412099369637E-19 ) ) ;
#19082=DIRECTION ( 'NONE',  ( -0.9998717552508121775, -0.01601477604151182663, 0.000000000000000000 ) ) ;
#19085=CARTESIAN_POINT ( 'NONE',  ( 1.346254456287517387, 0.000000000000000000, 1.565948643837855814 ) ) ;
#19089=CARTESIAN_POINT ( 'NONE',  ( 2.277873973731426194, 1.656288013650806912, 1.879489153247668076 ) ) ;
#19094=CARTESIAN_POINT ( 'NONE',  ( 2.164658444855302122, 5.905511811023623991, -0.04795272066889885720 ) ) ;
#19096=CARTESIAN_POINT ( 'NONE',  ( -1.621795816027382875, 0.000000000000000000, -0.6396693727619442438 ) ) ;
#19108=ORIENTED_EDGE ( 'NONE', *, *, #26005, .T. ) ;
#19111=FACE_OUTER_BOUND ( 'NONE', #49377, .T. ) ;
#19112=CARTESIAN_POINT ( 'NONE',  ( 0.8515791614234311524, 0.000000000000000000, 1.521253268579216167 ) ) ;
#19113=EDGE_CURVE ( 'NONE', #30581, #19191, #26489, .T. ) ;
#19115=ORIENTED_EDGE ( 'NONE', *, *, #28603, .F. ) ;
#19120=ORIENTED_EDGE ( 'NONE', *, *, #15804, .T. ) ;
#19123=ORIENTED_EDGE ( 'NONE', *, *, #13986, .T. ) ;
#19126=ORIENTED_EDGE ( 'NONE', *, *, #21092, .T. ) ;
#19128=FACE_OUTER_BOUND ( 'NONE', #8132, .T. ) ;
#19129=DIRECTION ( 'NONE',  ( -0.1342332658176667304, -1.160734090543304907E-16, 0.9909497617679332571 ) ) ;
#19130=CARTESIAN_POINT ( 'NONE',  ( 1.909828200462996062, 1.049866565877818125, 0.6722859869522012088 ) ) ;
#19132=VERTEX_POINT ( 'NONE', #28003 ) ;
#19133=ORIENTED_EDGE ( 'NONE', *, *, #39966, .T. ) ;
#19136=ORIENTED_EDGE ( 'NONE', *, *, #20545, .F. ) ;
#19138=CARTESIAN_POINT ( 'NONE',  ( 1.695772546416036919, 1.205361022782829114E-17, -2.417756147381349141 ) ) ;
#19140=VECTOR ( 'NONE', #17051, 39.37007874015748143 ) ;
#19141=ADVANCED_FACE ( 'NONE', ( #42735 ), #23617, .F. ) ;
#19150=VERTEX_POINT ( 'NONE', #44760 ) ;
#19153=CARTESIAN_POINT ( 'NONE',  ( -1.481515513156636876, 0.000000000000000000, -0.9189724476880739568 ) ) ;
#19155=EDGE_CURVE ( 'NONE', #9746, #47004, #13038, .T. ) ;
#19158=DIRECTION ( 'NONE',  ( 0.000000000000000000, 0.000000000000000000, 1.000000000000000000 ) ) ;
#19161=ORIENTED_EDGE ( 'NONE', *, *, #49429, .F. ) ;
#19163=CARTESIAN_POINT ( 'NONE',  ( 1.266373210825830764, 1.738989517266293472, -2.667458607394062486 ) ) ;
#19164=DIRECTION ( 'NONE',  ( 0.9998717552508121775, 0.01601477604151182663, 0.000000000000000000 ) ) ;
#19166=ORIENTED_EDGE ( 'NONE', *, *, #11220, .T. ) ;
#19167=ORIENTED_EDGE ( 'NONE', *, *, #17337, .T. ) ;
#19169=DIRECTION ( 'NONE',  ( -0.01601477604151182663, 0.9998717552508123996, -0.000000000000000000 ) ) ;
#19172=CARTESIAN_POINT ( 'NONE',  ( 1.388309139374679146, 1.631713065620022274, -1.827118126197171399 ) ) ;
#19175=ORIENTED_EDGE ( 'NONE', *, *, #48885, .F. ) ;
#19179=FACE_OUTER_BOUND ( 'NONE', #36850, .T. ) ;
#19180=CARTESIAN_POINT ( 'NONE',  ( -1.514466370293032993, 0.000000000000000000, 2.534789744887398388 ) ) ;
#19181=EDGE_CURVE ( 'NONE', #1516, #19985, #22741, .T. ) ;
#19182=ORIENTED_EDGE ( 'NONE', *, *, #44369, .T. ) ;
#19183=CARTESIAN_POINT ( 'NONE',  ( 0.3136974817028393425, 1.724153038295522800, -2.936457595020219635 ) ) ;
#19184=ADVANCED_FACE ( 'NONE', ( #39887 ), #36014, .T. ) ;
#19188=CARTESIAN_POINT ( 'NONE',  ( -1.901641471869980782, 5.905511811023623991, 1.079202499698819651 ) ) ;
#19191=VERTEX_POINT ( 'NONE', #28254 ) ;
#19195=VECTOR ( 'NONE', #49358, 39.37007874015748143 ) ;
#19196=CARTESIAN_POINT ( 'NONE',  ( -0.8329809839909436686, 1.533199950842965453, -2.833254665166566877 ) ) ;
#19198=CARTESIAN_POINT ( 'NONE',  ( 0.6233543567505464011, 1.574803149606302854, -2.073689640095370379 ) ) ;
#19199=ORIENTED_EDGE ( 'NONE', *, *, #23681, .T. ) ;
#19201=ADVANCED_FACE ( 'NONE', ( #1155 ), #28512, .T. ) ;
#19204=DIRECTION ( 'NONE',  ( -5.207613805427244364E-18, -1.000000000000000000, -1.159565308550900415E-16 ) ) ;
#19210=ORIENTED_EDGE ( 'NONE', *, *, #1953, .F. ) ;
#19211=CARTESIAN_POINT ( 'NONE',  ( 0.07982360342473591996, 1.709180471932028711, 0.000000000000000000 ) ) ;
#19216=DIRECTION ( 'NONE',  ( 0.000000000000000000, -1.000000000000000000, 0.000000000000000000 ) ) ;
#19218=B_SPLINE_CURVE_WITH_KNOTS ( 'NONE', 3,
 ( #27223, #35238, #34986, #14351 ),
 .UNSPECIFIED., .F., .F.,
 ( 4, 4 ),
 ( 2.219923784601946562E-07, 0.01886371725601659888 ),
 .UNSPECIFIED. ) ;
#19222=VECTOR ( 'NONE', #24529, 39.37007874015748854 ) ;
#19225=DIRECTION ( 'NONE',  ( -1.206139481778042838E-16, 1.000000000000000000, 4.526717189434675613E-17 ) ) ;
#19226=ORIENTED_EDGE ( 'NONE', *, *, #563, .F. ) ;
#19227=FACE_OUTER_BOUND ( 'NONE', #20249, .T. ) ;
#19240=VERTEX_POINT ( 'NONE', #44515 ) ;
#19244=EDGE_CURVE ( 'NONE', #22473, #18996, #46127, .T. ) ;
#19247=CARTESIAN_POINT ( 'NONE',  ( 0.2810168695315136689, 1.016046776276138708, -2.573346254327823157 ) ) ;
#19249=VERTEX_POINT ( 'NONE', #32671 ) ;
#19252=ORIENTED_EDGE ( 'NONE', *, *, #7192, .F. ) ;
#19255=VECTOR ( 'NONE', #39329, 39.37007874015748143 ) ;
#19261=AXIS2_PLACEMENT_3D ( 'NONE', #30905, #36244, #19269 ) ;
#19262=EDGE_CURVE ( 'NONE', #22025, #48160, #8646, .T. ) ;
#19263=CARTESIAN_POINT ( 'NONE',  ( 2.339241080213585899, 1.755713673067765379, 1.802537235681918037 ) ) ;
#19264=FACE_OUTER_BOUND ( 'NONE', #3178, .T. ) ;
#19269=DIRECTION ( 'NONE',  ( -0.9998717552508122886, -0.01601477604151182316, 0.000000000000000000 ) ) ;
#19272=DIRECTION ( 'NONE',  ( -0.1342332658176667026, 0.000000000000000000, 0.9909497617679331460 ) ) ;
#19278=CARTESIAN_POINT ( 'NONE',  ( 0.04921259842519669359, 1.614036899992937313, 2.481772132991067803 ) ) ;
#19281=DIRECTION ( 'NONE',  ( -0.9998717552508122886, -0.01601477604151180928, 0.000000000000000000 ) ) ;
#19282=DIRECTION ( 'NONE',  ( -0.01601477604151182663, 0.9998717552508123996, -0.000000000000000000 ) ) ;
#19283=FACE_OUTER_BOUND ( 'NONE', #24482, .T. ) ;
#19287=ORIENTED_EDGE ( 'NONE', *, *, #23545, .F. ) ;
#19289=AXIS2_PLACEMENT_3D ( 'NONE', #36421, #9305, #21692 ) ;
#19291=ORIENTED_EDGE ( 'NONE', *, *, #43343, .F. ) ;
#19292=CARTESIAN_POINT ( 'NONE',  ( 0.000000000000000000, 6.692913385826772199, 0.000000000000000000 ) ) ;
#19293=CARTESIAN_POINT ( 'NONE',  ( 0.000000000000000000, 0.000000000000000000, 0.000000000000000000 ) ) ;
#19294=VERTEX_POINT ( 'NONE', #40153 ) ;
#19300=ADVANCED_FACE ( 'NONE', ( #21291 ), #36278, .T. ) ;
#19308=CARTESIAN_POINT ( 'NONE',  ( 0.3546377434558362074, 1.615156926475952881, 2.229828021450985798 ) ) ;
#19310=ORIENTED_EDGE ( 'NONE', *, *, #4749, .F. ) ;
#19323=VECTOR ( 'NONE', #18706, 39.37007874015748143 ) ;
#19330=DIRECTION ( 'NONE',  ( 3.986037398843765983E-20, 1.000000000000000000, 1.160734090543304660E-16 ) ) ;
#19332=FACE_OUTER_BOUND ( 'NONE', #31803, .T. ) ;
#19333=VECTOR ( 'NONE', #41775, 39.37007874015748143 ) ;
#19334=DIRECTION ( 'NONE',  ( 0.2225209339563184452, 1.131543365815173240E-16, -0.9749279121818227312 ) ) ;
#19339=ORIENTED_EDGE ( 'NONE', *, *, #4004, .T. ) ;
#19341=ORIENTED_EDGE ( 'NONE', *, *, #3402, .T. ) ;
#19343=LINE ( 'NONE', #6477, #31132 ) ;
#19345=DIRECTION ( 'NONE',  ( -0.000000000000000000, 1.000000000000000000, -0.000000000000000000 ) ) ;
#19348=ORIENTED_EDGE ( 'NONE', *, *, #31656, .T. ) ;
#19349=DIRECTION ( 'NONE',  ( 1.000000000000000000, 0.000000000000000000, -0.000000000000000000 ) ) ;
#19362=ADVANCED_FACE ( 'NONE', ( #37811 ), #28595, .T. ) ;
#19364=CARTESIAN_POINT ( 'NONE',  ( -0.4349608091551079303, 6.692913385826772199, 2.121218629000294342 ) ) ;
#19368=CARTESIAN_POINT ( 'NONE',  ( -0.9970034594589531896, 1.699817861067899116, 2.516448948158077403 ) ) ;
#19370=VERTEX_POINT ( 'NONE', #49871 ) ;
#19371=VERTEX_POINT ( 'NONE', #1921 ) ;
#19373=EDGE_LOOP ( 'NONE', ( #25633, #12872, #45734, #39831 ) ) ;
#19374=CYLINDRICAL_SURFACE ( 'NONE', #49016, 2.164630168518208109 ) ;
#19376=FACE_OUTER_BOUND ( 'NONE', #8894, .T. ) ;
#19378=ORIENTED_EDGE ( 'NONE', *, *, #38559, .F. ) ;
#19379=ORIENTED_EDGE ( 'NONE', *, *, #14445, .F. ) ;
#19391=LENGTH_MEASURE_WITH_UNIT ( LENGTH_MEASURE( 0.02539999999999999897 ), #22279 );
#19392=CIRCLE ( 'NONE', #41684, 2.246510896728926010 ) ;
#19395=ORIENTED_EDGE ( 'NONE', *, *, #15654, .T. ) ;
#19396=DIRECTION ( 'NONE',  ( 0.000000000000000000, 0.000000000000000000, 1.000000000000000000 ) ) ;
#19398=CARTESIAN_POINT ( 'NONE',  ( 2.093903048064389427, 0.000000000000000000, -0.4274415146361335571 ) ) ;
#19406=CARTESIAN_POINT ( 'NONE',  ( -1.236813753895213308, 0.000000000000000000, -2.681693691597581974 ) ) ;
#19407=ORIENTED_EDGE ( 'NONE', *, *, #46856, .F. ) ;
#19408=EDGE_CURVE ( 'NONE', #42847, #16575, #4801, .T. ) ;
#19409=CARTESIAN_POINT ( 'NONE',  ( 0.000000000000000000, 5.905511811023623991, 0.000000000000000000 ) ) ;
#19411=DIRECTION ( 'NONE',  ( 3.986037398843765983E-20, 1.000000000000000000, 1.160734090543304660E-16 ) ) ;
#19417=ORIENTED_EDGE ( 'NONE', *, *, #24272, .T. ) ;
#19419=CARTESIAN_POINT ( 'NONE',  ( -2.277873973731453727, 1.683757167080951245, 1.879489153247634992 ) ) ;
#19425=DIRECTION ( 'NONE',  ( 7.237058681235334921E-17, -1.000000000000000000, -9.074984547606431700E-17 ) ) ;
#19426=DIRECTION ( 'NONE',  ( 0.3930250316539147803, 0.000000000000000000, 0.9195277725514544587 ) ) ;
#19429=ADVANCED_FACE ( 'NONE', ( #10174 ), #5499, .F. ) ;
#19430=VERTEX_POINT ( 'NONE', #30306 ) ;
#19431=DIRECTION ( 'NONE',  ( 1.000000000000000000, -0.000000000000000000, -0.000000000000000000 ) ) ;
#19434=ORIENTED_EDGE ( 'NONE', *, *, #20009, .F. ) ;
#19437=ORIENTED_EDGE ( 'NONE', *, *, #3402, .F. ) ;
#19438=ORIENTED_EDGE ( 'NONE', *, *, #23976, .T. ) ;
#19439=CARTESIAN_POINT ( 'NONE',  ( 0.000000000000000000, 6.692913385826772199, 0.000000000000000000 ) ) ;
#19440=CARTESIAN_POINT ( 'NONE',  ( 2.164823134740036625, 6.692913385826772199, -0.04796011690015051371 ) ) ;
#19444=PLANE ( 'NONE',  #8803 ) ;
#19446=CARTESIAN_POINT ( 'NONE',  ( 0.1155636338427008941, -0.5222242541845523167, 0.000000000000000000 ) ) ;
#19450=B_SPLINE_CURVE_WITH_KNOTS ( 'NONE', 3,
 ( #20221, #32121, #47809, #4743 ),
 .UNSPECIFIED., .F., .F.,
 ( 4, 4 ),
 ( 2.018269040657474853E-07, 0.002500207291903820076 ),
 .UNSPECIFIED. ) ;
#19451=B_SPLINE_CURVE_WITH_KNOTS ( 'NONE', 3,
 ( #5352, #16981, #13613, #40988 ),
 .UNSPECIFIED., .F., .F.,
 ( 4, 4 ),
 ( 0.0006212445558864886043, 0.003121509373039683521 ),
 .UNSPECIFIED. ) ;
#19455=EDGE_CURVE ( 'NONE', #34848, #42663, #6078, .T. ) ;
#19459=CARTESIAN_POINT ( 'NONE',  ( -2.685185609606552060, 1.673311766001163825, -0.1698540269626902244 ) ) ;
#19460=CARTESIAN_POINT ( 'NONE',  ( 1.836571684270173588, 0.01857023198900394079, 0.9324157793583920384 ) ) ;
#19467=ORIENTED_EDGE ( 'NONE', *, *, #44196, .F. ) ;
#19468=ADVANCED_FACE ( 'NONE', ( #39056 ), #12088, .T. ) ;
#19472=CARTESIAN_POINT ( 'NONE',  ( 2.592406080853238315, 1.455338980885439337, 1.413671649984625356 ) ) ;
#19474=VECTOR ( 'NONE', #44340, 39.37007874015748143 ) ;
#19475=VERTEX_POINT ( 'NONE', #27175 ) ;
#19484=ORIENTED_EDGE ( 'NONE', *, *, #18043, .F. ) ;
#19487=CARTESIAN_POINT ( 'NONE',  ( 1.736189279010248887, 0.03661913449923154956, 0.9901688781355542091 ) ) ;
#19489=CARTESIAN_POINT ( 'NONE',  ( -1.734268221780295827, 0.000000000000000000, 0.1852605408175444779 ) ) ;
#19495=ORIENTED_EDGE ( 'NONE', *, *, #29061, .F. ) ;
#19496=CARTESIAN_POINT ( 'NONE',  ( -2.721588301589615622, 1.578403504144545888, -1.145422913280063071 ) ) ;
#19502=DIRECTION ( 'NONE',  ( 3.986037398843765983E-20, 1.000000000000000000, 1.160734090543304660E-16 ) ) ;
#19511=CONICAL_SURFACE ( 'NONE', #26122, 2.089297179032357121, 0.2617993877991570129 ) ;
#19513=DIRECTION ( 'NONE',  ( -0.8805955318567391110, 0.000000000000000000, 0.4738686624729965269 ) ) ;
#19515=VECTOR ( 'NONE', #28723, 39.37007874015748854 ) ;
#19522=CARTESIAN_POINT ( 'NONE',  ( -2.295914061060153610, 1.576889242737733676, 0.7977328874972187123 ) ) ;
#19525=CARTESIAN_POINT ( 'NONE',  ( -0.1324246528408225543, 1.049866565877817681, -2.020365292430061022 ) ) ;
#19531=ADVANCED_FACE ( 'NONE', ( #19926 ), #37688, .T. ) ;
#19533=VERTEX_POINT ( 'NONE', #38813 ) ;
#19534=CARTESIAN_POINT ( 'NONE',  ( -2.151809081513409438, 1.673437530708463017, 0.2418202932658340965 ) ) ;
#19535=DIRECTION ( 'NONE',  ( 0.9998717552508121775, 0.01601477604151182663, 0.000000000000000000 ) ) ;
#19536=DIRECTION ( 'NONE',  ( -0.3090169943749447867, -1.160734090543305153E-16, -0.9510565162951545304 ) ) ;
#19537=CARTESIAN_POINT ( 'NONE',  ( -1.037524086854360261, 5.905511811023623991, 2.764473043227569260 ) ) ;
#19542=ORIENTED_EDGE ( 'NONE', *, *, #46770, .T. ) ;
#19543=ORIENTED_EDGE ( 'NONE', *, *, #19778, .F. ) ;
#19544=CARTESIAN_POINT ( 'NONE',  ( 2.734482843737263025, 1.761870738172414796, -1.115254632218672493 ) ) ;
#19549=EDGE_LOOP ( 'NONE', ( #15252, #17598, #41474, #22503 ) ) ;
#19551=EDGE_CURVE ( 'NONE', #1805, #7241, #493, .T. ) ;
#19554=CARTESIAN_POINT ( 'NONE',  ( -1.567214440306964107, 0.002817858044914879883, 0.7874684655159520652 ) ) ;
#19557=ADVANCED_FACE ( 'NONE', ( #10933 ), #16220, .T. ) ;
#19558=CARTESIAN_POINT ( 'NONE',  ( 0.07982360342473591996, 1.709180471932028711, 0.000000000000000000 ) ) ;
#19560=VECTOR ( 'NONE', #30646, 39.37007874015748143 ) ;
#19563=ORIENTED_EDGE ( 'NONE', *, *, #50630, .T. ) ;
#19564=CARTESIAN_POINT ( 'NONE',  ( 0.9360721529196784907, 0.000000000000000000, 1.470771056236116481 ) ) ;
#19565=LINE ( 'NONE', #25185, #9741 ) ;
#19569=CARTESIAN_POINT ( 'NONE',  ( 0.000000000000000000, 1.574803149606302854, 0.000000000000000000 ) ) ;
#19570=DIRECTION ( 'NONE',  ( 0.000000000000000000, -1.000000000000000000, 0.000000000000000000 ) ) ;
#19572=VECTOR ( 'NONE', #4689, 39.37007874015748854 ) ;
#19573=CARTESIAN_POINT ( 'NONE',  ( -1.461363083917493588, 1.574803149606302854, 1.597866488315563327 ) ) ;
#19575=ORIENTED_EDGE ( 'NONE', *, *, #23462, .F. ) ;
#19578=CARTESIAN_POINT ( 'NONE',  ( -0.7322040776173250887, 1.028380827711104617, -2.468097745819289646 ) ) ;
#19580=LINE ( 'NONE', #39214, #12826 ) ;
#19582=FACE_OUTER_BOUND ( 'NONE', #41558, .T. ) ;
#19587=EDGE_LOOP ( 'NONE', ( #17114, #3796, #34906, #21544 ) ) ;
#19588=DIRECTION ( 'NONE',  ( -3.986037398843765983E-20, -1.000000000000000000, -1.160734090543304660E-16 ) ) ;
#19592=EDGE_CURVE ( 'NONE', #23176, #40104, #16330, .T. ) ;
#19594=LINE ( 'NONE', #23472, #50846 ) ;
#19598=B_SPLINE_CURVE_WITH_KNOTS ( 'NONE', 3,
 ( #41764, #41509, #6401, #2525 ),
 .UNSPECIFIED., .F., .F.,
 ( 4, 4 ),
 ( 2.003042186605898400E-07, 0.01598066055596613841 ),
 .UNSPECIFIED. ) ;
#19599=ORIENTED_EDGE ( 'NONE', *, *, #28356, .T. ) ;
#19604=EDGE_CURVE ( 'NONE', #21767, #15175, #35612, .T. ) ;
#19608=CARTESIAN_POINT ( 'NONE',  ( 0.1197526584096238467, 0.01986475091724364955, -1.879567902740797436 ) ) ;
#19609=EDGE_LOOP ( 'NONE', ( #1392, #20449, #48228, #41883 ) ) ;
#19619=CARTESIAN_POINT ( 'NONE',  ( -1.528548437409730454, 1.695430332713048882, 2.526376101461759838 ) ) ;
#19622=DIRECTION ( 'NONE',  ( -0.000000000000000000, 1.000000000000000000, -0.000000000000000000 ) ) ;
#19628=CARTESIAN_POINT ( 'NONE',  ( -0.5286458662987743029, 0.000000000000000000, 2.100489422084707680 ) ) ;
#19629=DIRECTION ( 'NONE',  ( -0.8805955318567391110, -5.496845023002422681E-17, 0.4738686624729965269 ) ) ;
#19639=CARTESIAN_POINT ( 'NONE',  ( -1.556712866041156440, 1.596563264426776207, 2.509548638715847435 ) ) ;
#19643=CARTESIAN_POINT ( 'NONE',  ( 0.07982360342473591996, 1.709180471932028711, 0.000000000000000000 ) ) ;
#19645=FACE_OUTER_BOUND ( 'NONE', #17609, .T. ) ;
#19646=LINE ( 'NONE', #35416, #32665 ) ;
#19647=EDGE_CURVE ( 'NONE', #20944, #16575, #42999, .T. ) ;
#19651=ORIENTED_EDGE ( 'NONE', *, *, #1199, .F. ) ;
#19653=DIRECTION ( 'NONE',  ( -3.986037398843765983E-20, -1.000000000000000000, -1.160734090543304660E-16 ) ) ;
#19655=DIRECTION ( 'NONE',  ( 0.000000000000000000, 0.000000000000000000, -1.000000000000000000 ) ) ;
#19658=EDGE_CURVE ( 'NONE', #358, #50651, #40078, .T. ) ;
#19661=FACE_OUTER_BOUND ( 'NONE', #2099, .T. ) ;
#19662=ORIENTED_EDGE ( 'NONE', *, *, #44627, .T. ) ;
#19665=ORIENTED_EDGE ( 'NONE', *, *, #18960, .F. ) ;
#19666=CARTESIAN_POINT ( 'NONE',  ( -1.022258465722730714, 1.597063495466063188, -2.236165044959671278 ) ) ;
#19667=CARTESIAN_POINT ( 'NONE',  ( -2.823445274216743073, 1.675250974312822105, 0.8656477926280276014 ) ) ;
#19668=CARTESIAN_POINT ( 'NONE',  ( 2.160407304981128984, 5.905511811023623991, -0.1462862061266579361 ) ) ;
#19672=ORIENTED_EDGE ( 'NONE', *, *, #30910, .F. ) ;
#19675=ORIENTED_EDGE ( 'NONE', *, *, #18560, .F. ) ;
#19677=ADVANCED_FACE ( 'NONE', ( #1085 ), #35931, .T. ) ;
#19684=CARTESIAN_POINT ( 'NONE',  ( 0.4788131938641112528, 1.726726173772622941, 2.914091152102192162 ) ) ;
#19688=VERTEX_POINT ( 'NONE', #5214 ) ;
#19692=CARTESIAN_POINT ( 'NONE',  ( 2.950518648759406393, 1.666751258392789259, -0.1160872037100129095 ) ) ;
#19693=ORIENTED_EDGE ( 'NONE', *, *, #47232, .F. ) ;
#19696=DIRECTION ( 'NONE',  ( 0.000000000000000000, -1.000000000000000000, 0.000000000000000000 ) ) ;
#19697=EDGE_CURVE ( 'NONE', #49795, #20976, #28192, .T. ) ;
#19700=FACE_OUTER_BOUND ( 'NONE', #45630, .T. ) ;
#19704=ORIENTED_EDGE ( 'NONE', *, *, #3933, .F. ) ;
#19711=EDGE_CURVE ( 'NONE', #42971, #6865, #50685, .T. ) ;
#19717=EDGE_CURVE ( 'NONE', #39129, #25030, #320, .T. ) ;
#19718=EDGE_LOOP ( 'NONE', ( #33993, #31060, #49789, #6639 ) ) ;
#19719=CARTESIAN_POINT ( 'NONE',  ( 0.000000000000000000, 6.692913385826772199, 0.000000000000000000 ) ) ;
#19720=LINE ( 'NONE', #36254, #10500 ) ;
#19721=DIRECTION ( 'NONE',  ( -0.9998717552508121775, -0.01601477604151182316, 0.000000000000000000 ) ) ;
#19734=DIRECTION ( 'NONE',  ( -0.01601477604151182663, 0.9998717552508123996, -0.000000000000000000 ) ) ;
#19736=ORIENTED_EDGE ( 'NONE', *, *, #8783, .F. ) ;
#19738=LINE ( 'NONE', #40407, #36412 ) ;
#19739=FACE_OUTER_BOUND ( 'NONE', #44730, .T. ) ;
#19740=ORIENTED_EDGE ( 'NONE', *, *, #9702, .F. ) ;
#19741=DIRECTION ( 'NONE',  ( -0.000000000000000000, 1.000000000000000000, -0.000000000000000000 ) ) ;
#19745=CARTESIAN_POINT ( 'NONE',  ( 1.556712866041120247, 1.645058926882370542, 2.509548638715870084 ) ) ;
#19748=DIRECTION ( 'NONE',  ( -0.9510565162951500895, 3.590656546124792943E-17, -0.3090169943749582204 ) ) ;
#19753=CARTESIAN_POINT ( 'NONE',  ( 0.2156353639037333347, 0.03137346048107473445, -1.846898229409209558 ) ) ;
#19759=VECTOR ( 'NONE', #34059, 39.37007874015748143 ) ;
#19760=EDGE_CURVE ( 'NONE', #45138, #31969, #16504, .T. ) ;
#19765=EDGE_CURVE ( 'NONE', #48962, #30043, #37236, .T. ) ;
#19766=DIRECTION ( 'NONE',  ( 1.160706738777435820E-16, 1.000000000000000000, 5.589669052740852391E-17 ) ) ;
#19771=CARTESIAN_POINT ( 'NONE',  ( 0.08139965876239094178, 1.610780518492231694, 0.000000000000000000 ) ) ;
#19772=CARTESIAN_POINT ( 'NONE',  ( 0.3880746611937324064, 0.02269246980704499317, 1.862854658644473638 ) ) ;
#19774=DIRECTION ( 'NONE',  ( -0.000000000000000000, 1.000000000000000000, -0.000000000000000000 ) ) ;
#19776=CARTESIAN_POINT ( 'NONE',  ( 0.7406773873160164001, 0.5226447100659409317, 2.113585110334742279 ) ) ;
#19778=EDGE_CURVE ( 'NONE', #7505, #36292, #49558, .T. ) ;
#19779=ORIENTED_EDGE ( 'NONE', *, *, #7759, .F. ) ;
#19781=DIRECTION ( 'NONE',  ( 0.9959742939952384022, 0.000000000000000000, 0.08963930890344089242 ) ) ;
#19782=EDGE_LOOP ( 'NONE', ( #15565, #18223, #8847, #13940 ) ) ;
#19784=CARTESIAN_POINT ( 'NONE',  ( -1.472219874544909768, 1.546549606962118517, 2.560030851058948898 ) ) ;
#19785=ADVANCED_FACE ( 'NONE', ( #1856 ), #48797, .F. ) ;
#19787=DIRECTION ( 'NONE',  ( -3.986037398843765983E-20, -1.000000000000000000, -1.160734090543304660E-16 ) ) ;
#19788=VERTEX_POINT ( 'NONE', #33117 ) ;
#19793=ORIENTED_EDGE ( 'NONE', *, *, #8020, .F. ) ;
#19795=ORIENTED_EDGE ( 'NONE', *, *, #6030, .F. ) ;
#19801=AXIS2_PLACEMENT_3D ( 'NONE', #28802, #8932, #48383 ) ;
#19806=DIRECTION ( 'NONE',  ( 0.000000000000000000, 0.000000000000000000, 1.000000000000000000 ) ) ;
#19811=AXIS2_PLACEMENT_3D ( 'NONE', #11062, #29672, #41291 ) ;
#19816=ORIENTED_EDGE ( 'NONE', *, *, #38582, .F. ) ;
#19824=DIRECTION ( 'NONE',  ( -0.01601477604151182663, 0.9998717552508123996, -0.000000000000000000 ) ) ;
#19827=ORIENTED_EDGE ( 'NONE', *, *, #8184, .T. ) ;
#19832=DIRECTION ( 'NONE',  ( -0.3090169943749582204, 0.000000000000000000, 0.9510565162951500895 ) ) ;
#19834=AXIS2_PLACEMENT_3D ( 'NONE', #47430, #31733, #36371 ) ;
#19839=DIRECTION ( 'NONE',  ( 0.000000000000000000, 0.000000000000000000, -1.000000000000000000 ) ) ;
#19840=ADVANCED_FACE ( 'NONE', ( #33622 ), #41609, .F. ) ;
#19841=ORIENTED_EDGE ( 'NONE', *, *, #13507, .F. ) ;
#19843=EDGE_CURVE ( 'NONE', #5918, #15669, #6501, .T. ) ;
#19844=AXIS2_PLACEMENT_3D ( 'NONE', #33241, #711, #28063 ) ;
#19847=CARTESIAN_POINT ( 'NONE',  ( 0.7148041136150545816, 0.000000000000000000, -2.044646019095610168 ) ) ;
#19854=CARTESIAN_POINT ( 'NONE',  ( 0.08119777152254364916, 1.623385212329073957, 0.000000000000000000 ) ) ;
#19855=B_SPLINE_CURVE_WITH_KNOTS ( 'NONE', 3,
 ( #719, #32224, #16473, #32486 ),
 .UNSPECIFIED., .F., .F.,
 ( 4, 4 ),
 ( 2.102946222184170507E-07, 0.002500239313106578012 ),
 .UNSPECIFIED. ) ;
#19856=ORIENTED_EDGE ( 'NONE', *, *, #45290, .F. ) ;
#19857=CARTESIAN_POINT ( 'NONE',  ( 2.949782676795221992, 5.905511811023623991, -0.1324748927672368959 ) ) ;
#19859=VERTEX_POINT ( 'NONE', #43103 ) ;
#19866=VECTOR ( 'NONE', #49689, 39.37007874015748143 ) ;
#19875=VECTOR ( 'NONE', #23492, 39.37007874015748143 ) ;
#19877=ADVANCED_FACE ( 'NONE', ( #50806 ), #26858, .T. ) ;
#19878=VERTEX_POINT ( 'NONE', #19112 ) ;
#19892=DIRECTION ( 'NONE',  ( 0.000000000000000000, 0.000000000000000000, -1.000000000000000000 ) ) ;
#19894=VERTEX_POINT ( 'NONE', #30747 ) ;
#19895=CARTESIAN_POINT ( 'NONE',  ( 2.161044708975088380, 5.905511811023623991, 0.1463148319730650238 ) ) ;
#19898=ORIENTED_EDGE ( 'NONE', *, *, #5690, .T. ) ;
#19902=VECTOR ( 'NONE', #14570, 39.37007874015748143 ) ;
#19910=ORIENTED_EDGE ( 'NONE', *, *, #23626, .F. ) ;
#19917=ORIENTED_EDGE ( 'NONE', *, *, #33238, .F. ) ;
#19920=DIRECTION ( 'NONE',  ( -1.045785279492541006E-16, -1.000000000000000000, -5.036236473261559574E-17 ) ) ;
#19922=ORIENTED_EDGE ( 'NONE', *, *, #31221, .T. ) ;
#19926=FACE_OUTER_BOUND ( 'NONE', #238, .T. ) ;
#19927=B_SPLINE_CURVE_WITH_KNOTS ( 'NONE', 3,
 ( #14347, #33479, #45307, #9716 ),
 .UNSPECIFIED., .F., .F.,
 ( 4, 4 ),
 ( 0.0001130144768271833412, 0.05016325964078766769 ),
 .UNSPECIFIED. ) ;
#19931=CARTESIAN_POINT ( 'NONE',  ( 1.485598995959308333, 6.692913385826772199, 1.625606721701627011 ) ) ;
#19933=CARTESIAN_POINT ( 'NONE',  ( -1.330011864698828816, 1.686599376747761614, -1.746878811320646152 ) ) ;
#19935=ADVANCED_FACE ( 'NONE', ( #27113 ), #26612, .T. ) ;
#19936=ORIENTED_EDGE ( 'NONE', *, *, #29880, .T. ) ;
#19940=ORIENTED_EDGE ( 'NONE', *, *, #19658, .F. ) ;
#19941=DIRECTION ( 'NONE',  ( 0.8584487936018728726, 1.288287287306305283E-16, -0.5128992774058949156 ) ) ;
#19942=EDGE_CURVE ( 'NONE', #22594, #25844, #31257, .T. ) ;
#19951=EDGE_LOOP ( 'NONE', ( #42280, #25607, #24255, #10144, #50384, #36888, #43140, #1549, #12270, #33039, #38088, #50670, #526, #27953, #1592, #35388, #32013, #37423, #21984, #11407, #23881, #23699, #14747, #46100, #39651, #47548, #17517, #18269, #26085, #895, #2028, #31259, #7662, #13990, #19467, #34441, #11940, #25833, #109, #49436, #25186, #24966, #28445, #48169, #7002, #41732, #26059, #48732, #48794, #46685, #23725, #36261, #45320, #6331, #29164, #3069, #44078, #46765, #492, #29794, #37065, #7839, #29017, #31541, #15831, #26985, #47550, #30127, #5210, #5872, #10154, #19133, #20499, #35331, #31395, #7560, #1940, #47154, #10891, #49307, #30236, #31251, #32734, #38608, #22201, #33265, #3011, #30743, #16972, #20333, #40785, #28583, #20891, #32239, #9942, #32947, #9053, #27314, #12148, #43022, #35834, #14352, #20554, #28150, #14596, #46628, #30791, #11255, #37173, #11316, #37925, #18606, #41320, #16308, #3730, #23773, #48315, #33234, #29461, #38957, #11205, #3615, #38360, #21931, #18698, #3490, #45270, #17059, #31705, #24582, #9309, #45584, #28599, #44177, #28939, #41206, #14768, #41651, #19161, #2638 ) ) ;
#19956=CARTESIAN_POINT ( 'NONE',  ( 1.058660938151061659, 0.000000000000000000, 1.740053772717023328 ) ) ;
#19959=CARTESIAN_POINT ( 'NONE',  ( 0.000000000000000000, 0.000000000000000000, 0.000000000000000000 ) ) ;
#19960=DIRECTION ( 'NONE',  ( -0.7530714660036196273, -7.633917315840922073E-17, 0.6579387259397027066 ) ) ;
#19962=DIRECTION ( 'NONE',  ( 0.01601477604151182663, -0.9998717552508123996, 0.000000000000000000 ) ) ;
#19966=DIRECTION ( 'NONE',  ( -3.986037398843765983E-20, -1.000000000000000000, -1.160734090543304660E-16 ) ) ;
#19968=DIRECTION ( 'NONE',  ( 0.000000000000000000, 0.000000000000000000, -1.000000000000000000 ) ) ;
#19973=CARTESIAN_POINT ( 'NONE',  ( -2.950847925457031007, 1.574821451496988933, -0.08326053095501942392 ) ) ;
#19979=EDGE_CURVE ( 'NONE', #5697, #39853, #42525, .T. ) ;
#19980=AXIS2_PLACEMENT_3D ( 'NONE', #6447, #5422, #18069 ) ;
#19982=FACE_OUTER_BOUND ( 'NONE', #13974, .T. ) ;
#19983=CARTESIAN_POINT ( 'NONE',  ( 1.542217245295272932, 0.05262109711011796892, 1.166931937029544564 ) ) ;
#19985=VERTEX_POINT ( 'NONE', #15001 ) ;
#19988=DIRECTION ( 'NONE',  ( -0.01601477604151182663, 0.9998717552508123996, -0.000000000000000000 ) ) ;
#19989=VERTEX_POINT ( 'NONE', #46706 ) ;
#19994=CARTESIAN_POINT ( 'NONE',  ( -1.712991727494380223, 1.205361022782829114E-17, -0.3405009913947248945 ) ) ;
#19999=CARTESIAN_POINT ( 'NONE',  ( 2.932638728931774352, 2.755905511811027164, 0.3475908556738226962 ) ) ;
#20007=CARTESIAN_POINT ( 'NONE',  ( 2.464291103507799008, 0.000000000000000000, -1.626664315311302733 ) ) ;
#20009=EDGE_CURVE ( 'NONE', #25170, #33806, #4390, .T. ) ;
#20017=FACE_OUTER_BOUND ( 'NONE', #44386, .T. ) ;
#20020=DIRECTION ( 'NONE',  ( -0.9998717552508122886, -0.01601477604151185785, 0.000000000000000000 ) ) ;
#20027=B_SPLINE_CURVE_WITH_KNOTS ( 'NONE', 3,
 ( #46955, #19619, #43367, #35387 ),
 .UNSPECIFIED., .F., .F.,
 ( 4, 4 ),
 ( 2.329984094937993841E-07, 0.002500456841312296598 ),
 .UNSPECIFIED. ) ;
#20029=VERTEX_POINT ( 'NONE', #8002 ) ;
#20030=CARTESIAN_POINT ( 'NONE',  ( 1.247448100859587239, 0.000000000000000000, -1.633239539486209591 ) ) ;
#20031=PLANE ( 'NONE',  #7978 ) ;
#20034=EDGE_CURVE ( 'NONE', #36015, #38547, #31807, .T. ) ;
#20038=CARTESIAN_POINT ( 'NONE',  ( 2.079445128081511829, 0.01975100886603133044, -0.04412578619987858608 ) ) ;
#20040=CARTESIAN_POINT ( 'NONE',  ( -0.2493966119946618154, 1.605482210820551758, -2.222016418551142181 ) ) ;
#20044=CARTESIAN_POINT ( 'NONE',  ( 1.662150612087327728, 1.049866565067837820, -1.156143393094004601 ) ) ;
#20050=VERTEX_POINT ( 'NONE', #35633 ) ;
#20051=EDGE_CURVE ( 'NONE', #33474, #13670, #8776, .T. ) ;
#20056=ORIENTED_EDGE ( 'NONE', *, *, #21304, .F. ) ;
#20060=ORIENTED_EDGE ( 'NONE', *, *, #38036, .F. ) ;
#20062=CIRCLE ( 'NONE', #6886, 2.165354330708661568 ) ;
#20064=B_SPLINE_CURVE_WITH_KNOTS ( 'NONE', 3,
 ( #36114, #221, #746, #36625 ),
 .UNSPECIFIED., .F., .F.,
 ( 4, 4 ),
 ( 2.051433891274529492E-07, 0.01996805375819276154 ),
 .UNSPECIFIED. ) ;
#20066=EDGE_CURVE ( 'NONE', #26908, #19026, #1285, .T. ) ;
#20070=ORIENTED_EDGE ( 'NONE', *, *, #32074, .T. ) ;
#20072=DIRECTION ( 'NONE',  ( 0.000000000000000000, 1.000000000000000000, -0.000000000000000000 ) ) ;
#20075=ORIENTED_EDGE ( 'NONE', *, *, #42731, .T. ) ;
#20076=FACE_OUTER_BOUND ( 'NONE', #42901, .T. ) ;
#20078=DIRECTION ( 'NONE',  ( 0.01601477604151182663, -0.9998717552508123996, 0.000000000000000000 ) ) ;
#20082=ORIENTED_EDGE ( 'NONE', *, *, #42965, .T. ) ;
#20086=B_SPLINE_CURVE_WITH_KNOTS ( 'NONE', 3,
 ( #19172, #11439, #11188, #47267 ),
 .UNSPECIFIED., .F., .F.,
 ( 4, 4 ),
 ( 0.01401300212335106037, 0.03074580230677671083 ),
 .UNSPECIFIED. ) ;
#20089=CARTESIAN_POINT ( 'NONE',  ( 1.531154912952773284, 5.905511811023623991, 1.532020527533857424 ) ) ;
#20093=AXIS2_PLACEMENT_3D ( 'NONE', #43184, #11704, #3963 ) ;
#20096=VECTOR ( 'NONE', #21953, 39.37007874015748143 ) ;
#20097=VECTOR ( 'NONE', #15728, 39.37007874015748143 ) ;
#20098=VERTEX_POINT ( 'NONE', #6576 ) ;
#20099=EDGE_CURVE ( 'NONE', #22312, #21069, #21091, .T. ) ;
#20105=FACE_OUTER_BOUND ( 'NONE', #35988, .T. ) ;
#20106=VERTEX_POINT ( 'NONE', #13812 ) ;
#20109=CONICAL_SURFACE ( 'NONE', #6939, 1.850107469027523210, 0.6386652850508578450 ) ;
#20111=ORIENTED_EDGE ( 'NONE', *, *, #23976, .F. ) ;
#20112=DIRECTION ( 'NONE',  ( -0.9989930665413151445, -5.167793568183051143E-18, 0.04486483035050446017 ) ) ;
#20113=ORIENTED_EDGE ( 'NONE', *, *, #18960, .T. ) ;
#20115=CARTESIAN_POINT ( 'NONE',  ( 0.08119777152254364916, 1.623385212329073957, 0.000000000000000000 ) ) ;
#20116=CARTESIAN_POINT ( 'NONE',  ( 0.1224067236346046000, 0.009932954893344222297, -1.909056982598775765 ) ) ;
#20119=CARTESIAN_POINT ( 'NONE',  ( 1.312623452344845232, 5.905511811023623991, 1.722945714930923744 ) ) ;
#20122=B_SPLINE_CURVE_WITH_KNOTS ( 'NONE', 3,
 ( #48146, #5071, #47633, #20300 ),
 .UNSPECIFIED., .F., .F.,
 ( 4, 4 ),
 ( 2.018431748241431644E-07, 0.002500215118228798356 ),
 .UNSPECIFIED. ) ;
#20124=B_SPLINE_CURVE_WITH_KNOTS ( 'NONE', 3,
 ( #4586, #1475, #16724, #48170 ),
 .UNSPECIFIED., .F., .F.,
 ( 4, 4 ),
 ( 0.001799345260683910160, 0.004299357162589153257 ),
 .UNSPECIFIED. ) ;
#20125=ORIENTED_EDGE ( 'NONE', *, *, #8893, .F. ) ;
#20130=ADVANCED_FACE ( 'NONE', ( #22564 ), #7086, .T. ) ;
#20133=ORIENTED_EDGE ( 'NONE', *, *, #34847, .T. ) ;
#20135=ORIENTED_EDGE ( 'NONE', *, *, #21083, .F. ) ;
#20139=CARTESIAN_POINT ( 'NONE',  ( -0.2156685157583831947, 1.617455082123532062, -2.945280361644576850 ) ) ;
#20145=ORIENTED_EDGE ( 'NONE', *, *, #10696, .F. ) ;
#20147=CARTESIAN_POINT ( 'NONE',  ( -1.522953965282238586, 0.003526770554233742919, 0.8754220627670087351 ) ) ;
#20149=CARTESIAN_POINT ( 'NONE',  ( 2.296360773918335152, 1.711873972321264814, 0.3607252540896742632 ) ) ;
#20153=CARTESIAN_POINT ( 'NONE',  ( 0.7190704387038853174, 0.000000000000000000, 1.869489989794381080 ) ) ;
#20161=LINE ( 'NONE', #16305, #19572 ) ;
#20164=ORIENTED_EDGE ( 'NONE', *, *, #8153, .T. ) ;
#20172=FACE_OUTER_BOUND ( 'NONE', #14172, .T. ) ;
#20178=CARTESIAN_POINT ( 'NONE',  ( -1.358040552251954969, 1.036177007133961769, 2.177027195213288913 ) ) ;
#20182=CARTESIAN_POINT ( 'NONE',  ( -1.712991727494380223, 1.205361022782829114E-17, -0.3405009913947248945 ) ) ;
#20186=ORIENTED_EDGE ( 'NONE', *, *, #2784, .T. ) ;
#20187=CARTESIAN_POINT ( 'NONE',  ( -1.494044303739022972, 0.003989811691878806209, -0.9272426299426647089 ) ) ;
#20190=B_SPLINE_CURVE_WITH_KNOTS ( 'NONE', 3,
 ( #26692, #14067, #14319, #42441 ),
 .UNSPECIFIED., .F., .F.,
 ( 4, 4 ),
 ( 9.735347569733346160E-07, 6.298333608436676246E-06 ),
 .UNSPECIFIED. ) ;
#20196=DIRECTION ( 'NONE',  ( 0.08963930890344089242, 1.156025585781303350E-16, -0.9959742939952384022 ) ) ;
#20198=CARTESIAN_POINT ( 'NONE',  ( -2.399080495885657083, 1.575253574022198455, 0.3746395858504699694 ) ) ;
#20199=CARTESIAN_POINT ( 'NONE',  ( -2.793030215715272213, 1.205361022782829114E-17, 0.9592557174602285297 ) ) ;
#20204=VERTEX_POINT ( 'NONE', #71 ) ;
#20210=DIRECTION ( 'NONE',  ( -0.9998717552508121775, -0.01601477604151182663, 0.000000000000000000 ) ) ;
#20221=CARTESIAN_POINT ( 'NONE',  ( 2.919426793319799707, 1.764751637901927905, 0.4451252810446822417 ) ) ;
#20224=ORIENTED_EDGE ( 'NONE', *, *, #13706, .T. ) ;
#20227=ORIENTED_EDGE ( 'NONE', *, *, #24296, .F. ) ;
#20228=DIRECTION ( 'NONE',  ( 0.000000000000000000, 1.160734090543304660E-16, -1.000000000000000000 ) ) ;
#20229=CARTESIAN_POINT ( 'NONE',  ( -1.531154912952794378, 0.000000000000000000, 1.532020527533835441 ) ) ;
#20230=( BOUNDED_CURVE ( )  B_SPLINE_CURVE ( 3, ( #2697, #48876, #2456, #21309 ),
 .UNSPECIFIED., .F., .F. ) 
 B_SPLINE_CURVE_WITH_KNOTS ( ( 4, 4 ),
 ( 3.808740206672671214, 3.859579113281694340 ),
 .UNSPECIFIED. ) 
 CURVE ( )  GEOMETRIC_REPRESENTATION_ITEM ( )  RATIONAL_B_SPLINE_CURVE ( ( 1.000000000000000000, 0.9997846287284284372, 0.9997846287284284372, 1.000000000000000000 ) ) 
 REPRESENTATION_ITEM ( '' )  );
#20232=ORIENTED_EDGE ( 'NONE', *, *, #21446, .F. ) ;
#20235=CARTESIAN_POINT ( 'NONE',  ( 0.08139965876239094178, 1.610780518492231694, 0.000000000000000000 ) ) ;
#20236=EDGE_CURVE ( 'NONE', #35848, #31200, #46778, .T. ) ;
#20241=ORIENTED_EDGE ( 'NONE', *, *, #15867, .T. ) ;
#20242=DIRECTION ( 'NONE',  ( -0.6579387259397136978, 0.000000000000000000, 0.7530714660036097463 ) ) ;
#20243=EDGE_CURVE ( 'NONE', #26089, #40673, #20301, .T. ) ;
#20244=CARTESIAN_POINT ( 'NONE',  ( 0.9237497747831215911, 0.5249316497054298258, 1.642046528974287378 ) ) ;
#20249=EDGE_LOOP ( 'NONE', ( #35579, #50392, #6305, #7232 ) ) ;
#20250=CARTESIAN_POINT ( 'NONE',  ( -2.823445274216743073, 1.573787237234608005, 0.8656477926280277124 ) ) ;
#20261=ORIENTED_EDGE ( 'NONE', *, *, #39564, .T. ) ;
#20263=EDGE_CURVE ( 'NONE', #33586, #13738, #11450, .T. ) ;
#20268=PLANE ( 'NONE',  #36405 ) ;
#20273=CARTESIAN_POINT ( 'NONE',  ( -2.122513613727505799, 1.575480814016643638, -0.4339716895473832436 ) ) ;
#20274=EDGE_LOOP ( 'NONE', ( #37701, #585, #17691, #24962 ) ) ;
#20275=VERTEX_POINT ( 'NONE', #34695 ) ;
#20276=CARTESIAN_POINT ( 'NONE',  ( 2.491402175429654253, 1.659612532563349285, -1.585592796919505831 ) ) ;
#20278=ORIENTED_EDGE ( 'NONE', *, *, #38504, .T. ) ;
#20280=EDGE_LOOP ( 'NONE', ( #7444, #21442, #21856, #8507 ) ) ;
#20300=CARTESIAN_POINT ( 'NONE',  ( 2.932638728931774352, 1.447899366913586672, 0.3475908556738225297 ) ) ;
#20301=CIRCLE ( 'NONE', #28519, 2.244934639244525076 ) ;
#20303=DIRECTION ( 'NONE',  ( -0.6234898018587431423, 0.000000000000000000, 0.7818314824680221431 ) ) ;
#20308=DIRECTION ( 'NONE',  ( 0.000000000000000000, 1.160734090543304660E-16, -1.000000000000000000 ) ) ;
#20311=EDGE_CURVE ( 'NONE', #6610, #45728, #40601, .T. ) ;
#20321=DIRECTION ( 'NONE',  ( -0.01601477604151182663, 0.9998717552508123996, -0.000000000000000000 ) ) ;
#20323=CARTESIAN_POINT ( 'NONE',  ( -0.7381027496704849478, 5.905511811023623991, -2.859439394060923956 ) ) ;
#20324=EDGE_CURVE ( 'NONE', #22357, #21187, #35519, .T. ) ;
#20325=VERTEX_POINT ( 'NONE', #28714 ) ;
#20326=DIRECTION ( 'NONE',  ( -0.000000000000000000, 1.000000000000000000, -0.000000000000000000 ) ) ;
#20329=VERTEX_POINT ( 'NONE', #20461 ) ;
#20330=VECTOR ( 'NONE', #46303, 39.37007874015748143 ) ;
#20333=ORIENTED_EDGE ( 'NONE', *, *, #28361, .T. ) ;
#20336=EDGE_CURVE ( 'NONE', #33248, #44681, #22630, .T. ) ;
#20337=VERTEX_POINT ( 'NONE', #28966 ) ;
#20339=DIRECTION ( 'NONE',  ( 0.3930250316539147803, 0.000000000000000000, 0.9195277725514544587 ) ) ;
#20343=DIRECTION ( 'NONE',  ( -0.8345732537212999791, 0.000000000000000000, -0.5508969814521065267 ) ) ;
#20348=DIRECTION ( 'NONE',  ( 0.08963930890344089242, 0.000000000000000000, -0.9959742939952384022 ) ) ;
#20349=B_SPLINE_CURVE_WITH_KNOTS ( 'NONE', 3,
 ( #21270, #37026, #44998, #9652 ),
 .UNSPECIFIED., .F., .F.,
 ( 4, 4 ),
 ( 6.559598655537315290E-07, 0.004930659607264709435 ),
 .UNSPECIFIED. ) ;
#20351=ORIENTED_EDGE ( 'NONE', *, *, #15630, .F. ) ;
#20353=CARTESIAN_POINT ( 'NONE',  ( 1.598711713508005117, 1.574803149606302854, -1.460438370699377986 ) ) ;
#20354=CARTESIAN_POINT ( 'NONE',  ( 1.895640394390794459, 0.03825063239866469816, 0.6676760893130100349 ) ) ;
#20356=EDGE_CURVE ( 'NONE', #11815, #8216, #33520, .T. ) ;
#20357=CARTESIAN_POINT ( 'NONE',  ( 2.339241080213585899, 1.462148010760873307, 1.802537235681917815 ) ) ;
#20359=CARTESIAN_POINT ( 'NONE',  ( 0.4517796511351843680, 1.715138028758778521, 2.213898087213642007 ) ) ;
#20361=ORIENTED_EDGE ( 'NONE', *, *, #4278, .T. ) ;
#20362=AXIS2_PLACEMENT_3D ( 'NONE', #45744, #13520, #29257 ) ;
#20363=FACE_OUTER_BOUND ( 'NONE', #35875, .T. ) ;
#20375=B_SPLINE_CURVE_WITH_KNOTS ( 'NONE', 3,
 ( #20591, #48927, #16729, #32745 ),
 .UNSPECIFIED., .F., .F.,
 ( 4, 4 ),
 ( 0.04354068846991995811, 0.06157816714894258359 ),
 .UNSPECIFIED. ) ;
#20376=CARTESIAN_POINT ( 'NONE',  ( -1.410501566226150638, 6.692913385826772199, 1.689247093817288548 ) ) ;
#20378=ORIENTED_EDGE ( 'NONE', *, *, #5404, .F. ) ;
#20383=CARTESIAN_POINT ( 'NONE',  ( 2.803168581537432758, 1.762931689648581157, 0.9280530358755010312 ) ) ;
#20384=CARTESIAN_POINT ( 'NONE',  ( -0.5272349255865267370, 0.000000000000000000, 2.905303903342410621 ) ) ;
#20385=VERTEX_POINT ( 'NONE', #40857 ) ;
#20389=DIRECTION ( 'NONE',  ( -0.000000000000000000, -1.000000000000000000, -0.000000000000000000 ) ) ;
#20390=FACE_OUTER_BOUND ( 'NONE', #15521, .T. ) ;
#20397=ORIENTED_EDGE ( 'NONE', *, *, #42782, .T. ) ;
#20407=DIRECTION ( 'NONE',  ( 0.000000000000000000, 0.000000000000000000, -1.000000000000000000 ) ) ;
#20409=ORIENTED_EDGE ( 'NONE', *, *, #41088, .F. ) ;
#20410=LINE ( 'NONE', #32826, #8479 ) ;
#20412=FACE_OUTER_BOUND ( 'NONE', #15269, .T. ) ;
#20413=AXIS2_PLACEMENT_3D ( 'NONE', #21577, #40947, #37333 ) ;
#20414=DIRECTION ( 'NONE',  ( -0.9998717552508122886, -0.01601477604151182316, 0.000000000000000000 ) ) ;
#20416=CARTESIAN_POINT ( 'NONE',  ( -2.952069331832154919, 5.118110236220475784, -1.181102362204724310 ) ) ;
#20417=ADVANCED_FACE ( 'NONE', ( #12982 ), #38009, .T. ) ;
#20418=DIRECTION ( 'NONE',  ( 0.000000000000000000, 0.000000000000000000, -1.000000000000000000 ) ) ;
#20419=DIRECTION ( 'NONE',  ( 0.000000000000000000, 1.000000000000000000, 0.000000000000000000 ) ) ;
#20422=ORIENTED_EDGE ( 'NONE', *, *, #27106, .F. ) ;
#20427=DIRECTION ( 'NONE',  ( 0.000000000000000000, 0.000000000000000000, 1.000000000000000000 ) ) ;
#20429=EDGE_LOOP ( 'NONE', ( #13365, #43927, #45089, #5718 ) ) ;
#20432=ADVANCED_FACE ( 'NONE', ( #41872 ), #23576, .T. ) ;
#20435=FACE_OUTER_BOUND ( 'NONE', #32158, .T. ) ;
#20436=VECTOR ( 'NONE', #33822, 39.37007874015748143 ) ;
#20440=VECTOR ( 'NONE', #15295, 39.37007874015748143 ) ;
#20441=CYLINDRICAL_SURFACE ( 'NONE', #24360, 2.165354330708661568 ) ;
#20442=DIRECTION ( 'NONE',  ( 0.6234898018587431423, 1.288287287306305283E-16, -0.7818314824680221431 ) ) ;
#20449=ORIENTED_EDGE ( 'NONE', *, *, #47475, .T. ) ;
#20454=AXIS2_PLACEMENT_3D ( 'NONE', #25126, #41894, #6535 ) ;
#20459=ORIENTED_EDGE ( 'NONE', *, *, #27851, .T. ) ;
#20460=CARTESIAN_POINT ( 'NONE',  ( -2.919165122154194769, 1.575328909575085090, 0.4450898352768660748 ) ) ;
#20461=CARTESIAN_POINT ( 'NONE',  ( 2.823445274216730638, 2.755905511811027164, 0.8656477926280683466 ) ) ;
#20464=VERTEX_POINT ( 'NONE', #18124 ) ;
#20465=VERTEX_POINT ( 'NONE', #25609 ) ;
#20466=DIRECTION ( 'NONE',  ( 0.2660368455666687892, -1.119010597708915320E-16, 0.9639628606958549062 ) ) ;
#20467=DIRECTION ( 'NONE',  ( 0.000000000000000000, 0.000000000000000000, 1.000000000000000000 ) ) ;
#20473=CARTESIAN_POINT ( 'NONE',  ( 2.813306935135764242, 1.664615162603113818, 0.8968503919118566703 ) ) ;
#20475=ORIENTED_EDGE ( 'NONE', *, *, #25611, .F. ) ;
#20490=FACE_OUTER_BOUND ( 'NONE', #7737, .T. ) ;
#20493=DIRECTION ( 'NONE',  ( -0.000000000000000000, -1.000000000000000000, -0.000000000000000000 ) ) ;
#20497=DIRECTION ( 'NONE',  ( 0.6910626489868580968, -1.160734090543304660E-16, 0.7227948638273978821 ) ) ;
#20498=CARTESIAN_POINT ( 'NONE',  ( -0.4098391621113791072, 1.049866565877818347, 1.982786943858533268 ) ) ;
#20499=ORIENTED_EDGE ( 'NONE', *, *, #27587, .T. ) ;
#20501=LINE ( 'NONE', #37280, #25021 ) ;
#20503=CARTESIAN_POINT ( 'NONE',  ( -0.7381027496704855029, 1.707760278544290689, -2.859439394060923512 ) ) ;
#20504=EDGE_CURVE ( 'NONE', #22686, #6017, #44733, .T. ) ;
#20515=B_SPLINE_CURVE_WITH_KNOTS ( 'NONE', 3,
 ( #7605, #49091, #44991, #44488 ),
 .UNSPECIFIED., .F., .F.,
 ( 4, 4 ),
 ( 2.472189648548164523E-07, 0.01923235726777020385 ),
 .UNSPECIFIED. ) ;
#20517=ORIENTED_EDGE ( 'NONE', *, *, #10813, .F. ) ;
#20520=ORIENTED_EDGE ( 'NONE', *, *, #42560, .F. ) ;
#20524=FACE_OUTER_BOUND ( 'NONE', #43114, .T. ) ;
#20525=AXIS2_PLACEMENT_3D ( 'NONE', #15065, #43430, #19425 ) ;
#20530=CARTESIAN_POINT ( 'NONE',  ( 0.1067246931122726866, 0.02962905676920215767, 0.000000000000000000 ) ) ;
#20531=CARTESIAN_POINT ( 'NONE',  ( 1.905060681038603265, 6.692913385826772199, 1.081042454612135773 ) ) ;
#20541=ORIENTED_EDGE ( 'NONE', *, *, #7096, .F. ) ;
#20545=EDGE_CURVE ( 'NONE', #46587, #10178, #36386, .T. ) ;
#20546=CARTESIAN_POINT ( 'NONE',  ( -2.165354330708661568, 1.673228346456695492, 0.08080958544675392874 ) ) ;
#20553=DIRECTION ( 'NONE',  ( -8.021399753802077430E-17, -1.000000000000000000, -8.389726389140663754E-17 ) ) ;
#20554=ORIENTED_EDGE ( 'NONE', *, *, #14244, .F. ) ;
#20557=CARTESIAN_POINT ( 'NONE',  ( 2.074049943651431693, 1.574803149606302854, 0.6221544894624233546 ) ) ;
#20560=CARTESIAN_POINT ( 'NONE',  ( -0.04921259842519688094, 0.02713143566191717967, 1.843522435433914142 ) ) ;
#20563=ORIENTED_EDGE ( 'NONE', *, *, #8781, .F. ) ;
#20568=EDGE_CURVE ( 'NONE', #18896, #695, #26284, .T. ) ;
#20569=EDGE_CURVE ( 'NONE', #32131, #50834, #45123, .T. ) ;
#20570=ORIENTED_EDGE ( 'NONE', *, *, #38884, .F. ) ;
#20578=B_SPLINE_CURVE_WITH_KNOTS ( 'NONE', 3,
 ( #12329, #12846, #4843, #36338 ),
 .UNSPECIFIED., .F., .F.,
 ( 4, 4 ),
 ( 0.001272230606304385449, 0.04687302674643420430 ),
 .UNSPECIFIED. ) ;
#20582=VERTEX_POINT ( 'NONE', #48465 ) ;
#20583=DIRECTION ( 'NONE',  ( 3.986037398843765983E-20, 1.000000000000000000, 1.160734090543304660E-16 ) ) ;
#20586=VECTOR ( 'NONE', #34868, 39.37007874015748143 ) ;
#20589=DIRECTION ( 'NONE',  ( -0.5877852522924684742, 0.000000000000000000, -0.8090169943749506709 ) ) ;
#20591=CARTESIAN_POINT ( 'NONE',  ( -0.04921259842519708216, 1.608688524157807498, 2.242709805336809303 ) ) ;
#20593=AXIS2_PLACEMENT_3D ( 'NONE', #49516, #1814, #29173 ) ;
#20595=ORIENTED_EDGE ( 'NONE', *, *, #11278, .F. ) ;
#20604=EDGE_CURVE ( 'NONE', #17408, #36108, #25098, .T. ) ;
#20605=CARTESIAN_POINT ( 'NONE',  ( 0.1067246931122726866, 0.02962905676920215767, 0.000000000000000000 ) ) ;
#20607=B_SPLINE_CURVE_WITH_KNOTS ( 'NONE', 3,
 ( #33272, #6145, #5380, #37142 ),
 .UNSPECIFIED., .F., .F.,
 ( 4, 4 ),
 ( 0.1211873102087489551, 0.1625992483279400380 ),
 .UNSPECIFIED. ) ;
#20609=FACE_OUTER_BOUND ( 'NONE', #11743, .T. ) ;
#20611=CARTESIAN_POINT ( 'NONE',  ( 2.339241080213585899, 1.755713673067765379, 1.802537235681918037 ) ) ;
#20617=DIRECTION ( 'NONE',  ( -0.000000000000000000, 1.000000000000000000, -0.000000000000000000 ) ) ;
#20619=EDGE_LOOP ( 'NONE', ( #27606, #41554, #50237, #24041 ) ) ;
#20620=CYLINDRICAL_SURFACE ( 'NONE', #20970, 2.165354330708661568 ) ;
#20621=ORIENTED_EDGE ( 'NONE', *, *, #16413, .F. ) ;
#20625=PLANE ( 'NONE',  #5263 ) ;
#20627=CONICAL_SURFACE ( 'NONE', #2512, 2.246510896728926010, 0.01601546068027819014 ) ;
#20635=CARTESIAN_POINT ( 'NONE',  ( 1.461363083917469829, 1.574803149606302854, 1.597866488315584865 ) ) ;
#20641=CARTESIAN_POINT ( 'NONE',  ( 0.000000000000000000, 1.574803149606302854, 0.000000000000000000 ) ) ;
#20642=ORIENTED_EDGE ( 'NONE', *, *, #24420, .T. ) ;
#20643=ORIENTED_EDGE ( 'NONE', *, *, #25995, .F. ) ;
#20649=CARTESIAN_POINT ( 'NONE',  ( -1.083598637574820334, 1.538470290252458739, 2.747180975113330259 ) ) ;
#20652=EDGE_LOOP ( 'NONE', ( #10862, #4431, #22766, #44931 ) ) ;
#20654=ORIENTED_EDGE ( 'NONE', *, *, #39377, .T. ) ;
#20662=CARTESIAN_POINT ( 'NONE',  ( 2.505429192702631536, 1.652952030840073805, 0.3890454956553852650 ) ) ;
#20663=VERTEX_POINT ( 'NONE', #24510 ) ;
#20664=VERTEX_POINT ( 'NONE', #40261 ) ;
#20667=DIRECTION ( 'NONE',  ( 0.000000000000000000, 0.000000000000000000, 1.000000000000000000 ) ) ;
#20678=ORIENTED_EDGE ( 'NONE', *, *, #16363, .F. ) ;
#20681=CARTESIAN_POINT ( 'NONE',  ( 0.04921259842519689481, 1.205361022782829114E-17, 2.952755905511811108 ) ) ;
#20684=ORIENTED_EDGE ( 'NONE', *, *, #14847, .T. ) ;
#20685=DIRECTION ( 'NONE',  ( 0.000000000000000000, 1.160734090543304660E-16, -1.000000000000000000 ) ) ;
#20698=ORIENTED_EDGE ( 'NONE', *, *, #14793, .T. ) ;
#20699=CARTESIAN_POINT ( 'NONE',  ( -2.793030215715272213, 1.675725205278408403, 0.9592557174602281966 ) ) ;
#20701=ORIENTED_EDGE ( 'NONE', *, *, #36290, .F. ) ;
#20710=CARTESIAN_POINT ( 'NONE',  ( 2.138597145901430352, 6.692913385826772199, 0.3393547186367261159 ) ) ;
#20713=EDGE_LOOP ( 'NONE', ( #35074, #49414, #16815, #28076 ) ) ;
#20715=CARTESIAN_POINT ( 'NONE',  ( -0.7447559422295143561, 0.01073262845819722075, -1.659925117323180599 ) ) ;
#20718=VERTEX_POINT ( 'NONE', #29908 ) ;
#20720=CARTESIAN_POINT ( 'NONE',  ( -0.8241443283111672402, 1.596276574288824301, 2.055867440327626916 ) ) ;
#20721=B_SPLINE_CURVE_WITH_KNOTS ( 'NONE', 3,
 ( #22463, #37967, #42080, #41576 ),
 .UNSPECIFIED., .F., .F.,
 ( 4, 4 ),
 ( 2.074912098696191126E-07, 0.01852445910376516319 ),
 .UNSPECIFIED. ) ;
#20728=ORIENTED_EDGE ( 'NONE', *, *, #14022, .T. ) ;
#20733=CARTESIAN_POINT ( 'NONE',  ( 2.295325967725798222, 1.744665796922353351, 0.3605850800666594580 ) ) ;
#20735=CIRCLE ( 'NONE', #11658, 2.165354330708661568 ) ;
#20737=CARTESIAN_POINT ( 'NONE',  ( 2.951990591674675368, 1.666783180044518087, -0.08331184815398359755 ) ) ;
#20738=CARTESIAN_POINT ( 'NONE',  ( 2.165460538733997353, 0.000000000000000000, 0.04798874274655835076 ) ) ;
#20742=CARTESIAN_POINT ( 'NONE',  ( -2.043634885149970160, 6.692913385826772199, 0.7157624142945935297 ) ) ;
#20743=AXIS2_PLACEMENT_3D ( 'NONE', #49499, #3314, #10307 ) ;
#20744=CARTESIAN_POINT ( 'NONE',  ( 1.905671854841463952, 5.905511811023623991, 2.256015092822682089 ) ) ;
#20748=CARTESIAN_POINT ( 'NONE',  ( 1.083598637574782142, 1.637691314537677023, 2.747180975113346246 ) ) ;
#20751=CARTESIAN_POINT ( 'NONE',  ( -1.735354274664482110, 1.614490279294756192, 1.320953578359251424 ) ) ;
#20753=CARTESIAN_POINT ( 'NONE',  ( -1.238969615956150738, 0.5248216437167342319, -1.789020852678176121 ) ) ;
#20754=ORIENTED_EDGE ( 'NONE', *, *, #40290, .T. ) ;
#20763=B_SPLINE_CURVE_WITH_KNOTS ( 'NONE', 3,
 ( #16799, #20662, #47480, #44149 ),
 .UNSPECIFIED., .F., .F.,
 ( 4, 4 ),
 ( 0.01482598341399509086, 0.03075144114903187453 ),
 .UNSPECIFIED. ) ;
#20764=EDGE_CURVE ( 'NONE', #26292, #41090, #2727, .T. ) ;
#20768=ORIENTED_EDGE ( 'NONE', *, *, #16779, .T. ) ;
#20775=VECTOR ( 'NONE', #355, 39.37007874015748143 ) ;
#20779=ORIENTED_EDGE ( 'NONE', *, *, #43835, .T. ) ;
#20780=LINE ( 'NONE', #44268, #39461 ) ;
#20781=DIRECTION ( 'NONE',  ( -0.000000000000000000, 1.000000000000000000, -0.000000000000000000 ) ) ;
#20782=CARTESIAN_POINT ( 'NONE',  ( -0.04921259842519689481, 0.01808868210717232833, 1.870356923343539979 ) ) ;
#20792=B_SPLINE_CURVE_WITH_KNOTS ( 'NONE', 3,
 ( #40503, #44859, #21137, #48204 ),
 .UNSPECIFIED., .F., .F.,
 ( 4, 4 ),
 ( 0.1211873102087489551, 0.1625992483279400380 ),
 .UNSPECIFIED. ) ;
#20795=AXIS2_PLACEMENT_3D ( 'NONE', #44048, #48398, #170 ) ;
#20797=ORIENTED_EDGE ( 'NONE', *, *, #34828, .F. ) ;
#20804=DIRECTION ( 'NONE',  ( 0.6910626489868580968, -8.392480990704469866E-17, 0.7227948638273978821 ) ) ;
#20807=B_SPLINE_CURVE_WITH_KNOTS ( 'NONE', 3,
 ( #43411, #43664, #35941, #32076 ),
 .UNSPECIFIED., .F., .F.,
 ( 4, 4 ),
 ( 3.882109077968705590E-07, 0.04390313747348802836 ),
 .UNSPECIFIED. ) ;
#20808=DIRECTION ( 'NONE',  ( -4.561975526775602830E-17, -1.000000000000000000, -1.067327232801823148E-16 ) ) ;
#20814=AXIS2_PLACEMENT_3D ( 'NONE', #4395, #35639, #24276 ) ;
#20818=CARTESIAN_POINT ( 'NONE',  ( 2.808237744965994320, 0.000000000000000000, 0.9124517550441679781 ) ) ;
#20819=DIRECTION ( 'NONE',  ( 0.9510565162951545304, 0.000000000000000000, -0.3090169943749447867 ) ) ;
#20823=AXIS2_PLACEMENT_3D ( 'NONE', #3705, #38576, #34697 ) ;
#20832=B_SPLINE_CURVE_WITH_KNOTS ( 'NONE', 3,
 ( #43470, #48086, #48593, #4760 ),
 .UNSPECIFIED., .F., .F.,
 ( 4, 4 ),
 ( 0.1211775127643062444, 0.1625894504277921315 ),
 .UNSPECIFIED. ) ;
#20834=ORIENTED_EDGE ( 'NONE', *, *, #36592, .T. ) ;
#20836=ADVANCED_FACE ( 'NONE', ( #31397 ), #15371, .T. ) ;
#20838=ORIENTED_EDGE ( 'NONE', *, *, #21574, .T. ) ;
#20839=LINE ( 'NONE', #4841, #49928 ) ;
#20842=CARTESIAN_POINT ( 'NONE',  ( 0.08139965876239094178, 1.610780518492231694, 0.000000000000000000 ) ) ;
#20847=LINE ( 'NONE', #45087, #46301 ) ;
#20850=( BOUNDED_CURVE ( )  B_SPLINE_CURVE ( 3, ( #22531, #23531, #38786, #42648 ),
 .UNSPECIFIED., .F., .F. ) 
 B_SPLINE_CURVE_WITH_KNOTS ( ( 4, 4 ),
 ( 4.856797154144195439, 4.907729085828183457 ),
 .UNSPECIFIED. ) 
 CURVE ( )  GEOMETRIC_REPRESENTATION_ITEM ( )  RATIONAL_B_SPLINE_CURVE ( ( 1.000000000000000000, 0.9997838398768879031, 0.9997838398768879031, 1.000000000000000000 ) ) 
 REPRESENTATION_ITEM ( '' )  );
#20851=VERTEX_POINT ( 'NONE', #16421 ) ;
#20854=CIRCLE ( 'NONE', #5185, 2.246510896728926010 ) ;
#20856=VERTEX_POINT ( 'NONE', #23642 ) ;
#20857=CARTESIAN_POINT ( 'NONE',  ( 0.2156685157584260770, 1.722625337188476546, -2.945280361644574185 ) ) ;
#20859=DIRECTION ( 'NONE',  ( 0.9998717552508121775, 0.01601477604151182663, 0.000000000000000000 ) ) ;
#20861=VECTOR ( 'NONE', #15471, 39.37007874015748143 ) ;
#20862=B_SPLINE_CURVE_WITH_KNOTS ( 'NONE', 3,
 ( #20988, #16610, #47546, #1104 ),
 .UNSPECIFIED., .F., .F.,
 ( 4, 4 ),
 ( 6.340610770647737117E-07, 0.002830502821758625054 ),
 .UNSPECIFIED. ) ;
#20864=ORIENTED_EDGE ( 'NONE', *, *, #23578, .T. ) ;
#20867=VECTOR ( 'NONE', #48696, 39.37007874015748854 ) ;
#20868=CARTESIAN_POINT ( 'NONE',  ( 2.576863348864710801, 1.759415398959654819, 1.442554885838449819 ) ) ;
#20871=CARTESIAN_POINT ( 'NONE',  ( -1.427293369312925497, 0.000000000000000000, -1.001115484471666761 ) ) ;
#20872=CARTESIAN_POINT ( 'NONE',  ( -1.483604961240789333, -2.043891966111581001E-16, 1.623324365321668239 ) ) ;
#20873=VERTEX_POINT ( 'NONE', #4282 ) ;
#20875=DIRECTION ( 'NONE',  ( -0.01601477604151182663, 0.9998717552508123996, -0.000000000000000000 ) ) ;
#20878=DIRECTION ( 'NONE',  ( -0.000000000000000000, -1.000000000000000000, 0.000000000000000000 ) ) ;
#20882=CARTESIAN_POINT ( 'NONE',  ( -1.930378847111418050, 1.590732546136234937, 2.234429243736988813 ) ) ;
#20886=CARTESIAN_POINT ( 'NONE',  ( 0.8067290215917978236, 6.692913385826772199, 2.009464521518182334 ) ) ;
#20888=EDGE_CURVE ( 'NONE', #30219, #47632, #39652, .T. ) ;
#20891=ORIENTED_EDGE ( 'NONE', *, *, #14445, .T. ) ;
#20894=ORIENTED_EDGE ( 'NONE', *, *, #1471, .F. ) ;
#20902=CARTESIAN_POINT ( 'NONE',  ( -1.453832412804729302, 0.000000000000000000, -1.018633753700964428 ) ) ;
#20905=DIRECTION ( 'NONE',  ( -0.01601477604151182663, 0.9998717552508123996, -0.000000000000000000 ) ) ;
#20906=FACE_OUTER_BOUND ( 'NONE', #3104, .T. ) ;
#20908=EDGE_LOOP ( 'NONE', ( #20459, #50945, #111, #35139 ) ) ;
#20914=B_SPLINE_CURVE_WITH_KNOTS ( 'NONE', 3,
 ( #10743, #29858, #10236, #41477 ),
 .UNSPECIFIED., .F., .F.,
 ( 4, 4 ),
 ( 1.140376665250896911E-05, 0.05043874644244002864 ),
 .UNSPECIFIED. ) ;
#20915=FACE_OUTER_BOUND ( 'NONE', #26327, .T. ) ;
#20916=EDGE_CURVE ( 'NONE', #42699, #4909, #40430, .T. ) ;
#20918=ORIENTED_EDGE ( 'NONE', *, *, #50532, .F. ) ;
#20924=VERTEX_POINT ( 'NONE', #31918 ) ;
#20925=B_SPLINE_CURVE_WITH_KNOTS ( 'NONE', 3,
 ( #45431, #18096, #1835, #21206 ),
 .UNSPECIFIED., .F., .F.,
 ( 4, 4 ),
 ( 2.103951164766250122E-07, 0.01609579516997627566 ),
 .UNSPECIFIED. ) ;
#20927=AXIS2_PLACEMENT_3D ( 'NONE', #49755, #47092, #42992 ) ;
#20929=DIRECTION ( 'NONE',  ( -1.776356839400250149E-14, 0.000000000000000000, 1.000000000000000000 ) ) ;
#20931=CONICAL_SURFACE ( 'NONE', #3604, 1.850107469027523210, 0.6386652850508578450 ) ;
#20932=EDGE_CURVE ( 'NONE', #6769, #38240, #33558, .T. ) ;
#20933=DIRECTION ( 'NONE',  ( 0.3930250316539278810, 0.000000000000000000, -0.9195277725514489076 ) ) ;
#20937=DIRECTION ( 'NONE',  ( 0.000000000000000000, 0.000000000000000000, 1.000000000000000000 ) ) ;
#20938=CARTESIAN_POINT ( 'NONE',  ( 1.929629134066521923, 1.574803149606302854, 0.9824921284572415425 ) ) ;
#20941=CARTESIAN_POINT ( 'NONE',  ( 0.1067246931122726866, 0.02962905676920215767, 0.000000000000000000 ) ) ;
#20944=VERTEX_POINT ( 'NONE', #145 ) ;
#20945=CARTESIAN_POINT ( 'NONE',  ( 2.479883737258961940, 1.750989359453594130, -0.5155390881854031715 ) ) ;
#20948=EDGE_LOOP ( 'NONE', ( #10601, #34435, #11288, #41990 ) ) ;
#20949=CARTESIAN_POINT ( 'NONE',  ( 2.151809081513405886, 1.574803149606302854, 0.2418202932658659043 ) ) ;
#20953=CARTESIAN_POINT ( 'NONE',  ( -0.9726748280992547624, 0.004179766354514788743, 1.532033615445409724 ) ) ;
#20956=B_SPLINE_CURVE_WITH_KNOTS ( 'NONE', 3,
 ( #22678, #17787, #45889, #26543 ),
 .UNSPECIFIED., .F., .F.,
 ( 4, 4 ),
 ( 6.477935607884877264E-07, 0.004084871717682403425 ),
 .UNSPECIFIED. ) ;
#20958=ORIENTED_EDGE ( 'NONE', *, *, #16532, .T. ) ;
#20965=CONICAL_SURFACE ( 'NONE', #41572, 3.483074324928249421, 1.244861948955335196 ) ;
#20969=CONICAL_SURFACE ( 'NONE', #15185, 2.246510896728926010, 0.01601546068027819014 ) ;
#20970=AXIS2_PLACEMENT_3D ( 'NONE', #5129, #9007, #17269 ) ;
#20972=B_SPLINE_CURVE_WITH_KNOTS ( 'NONE', 3,
 ( #15793, #35171, #12181, #8053 ),
 .UNSPECIFIED., .F., .F.,
 ( 4, 4 ),
 ( 0.01355629821058103486, 0.03074392676604455199 ),
 .UNSPECIFIED. ) ;
#20975=CARTESIAN_POINT ( 'NONE',  ( 1.698224779224786429, 1.735102128624146811, -1.555582603516539875 ) ) ;
#20976=VERTEX_POINT ( 'NONE', #13822 ) ;
#20979=AXIS2_PLACEMENT_3D ( 'NONE', #2280, #26717, #14857 ) ;
#20981=EDGE_LOOP ( 'NONE', ( #31298, #3855, #30633, #7463 ) ) ;
#20982=ORIENTED_EDGE ( 'NONE', *, *, #11295, .T. ) ;
#20984=CARTESIAN_POINT ( 'NONE',  ( 0.000000000000000000, 0.000000000000000000, 0.000000000000000000 ) ) ;
#20985=DIRECTION ( 'NONE',  ( -0.9998717552508121775, -0.01601477604151182663, 0.000000000000000000 ) ) ;
#20988=CARTESIAN_POINT ( 'NONE',  ( 0.4787700707360283414, 1.205361022782829114E-17, -1.919768535593459724 ) ) ;
#20990=ORIENTED_EDGE ( 'NONE', *, *, #39961, .F. ) ;
#20991=DIRECTION ( 'NONE',  ( -0.01601477604151182663, 0.9998717552508123996, -0.000000000000000000 ) ) ;
#20996=CARTESIAN_POINT ( 'NONE',  ( -1.546652493784001603, 0.000000000000000000, 0.8508756243308288614 ) ) ;
#20999=ORIENTED_EDGE ( 'NONE', *, *, #11123, .F. ) ;
#21002=B_SPLINE_CURVE_WITH_KNOTS ( 'NONE', 3,
 ( #32180, #47870, #29573, #30080 ),
 .UNSPECIFIED., .F., .F.,
 ( 4, 4 ),
 ( 0.1211775127643062860, 0.1625894504277921315 ),
 .UNSPECIFIED. ) ;
#21004=VECTOR ( 'NONE', #41579, 39.37007874015748143 ) ;
#21006=VECTOR ( 'NONE', #26032, 39.37007874015748143 ) ;
#21007=ADVANCED_FACE ( 'NONE', ( #13312 ), #25429, .T. ) ;
#21009=ORIENTED_EDGE ( 'NONE', *, *, #2070, .F. ) ;
#21011=FACE_OUTER_BOUND ( 'NONE', #26622, .T. ) ;
#21012=FACE_OUTER_BOUND ( 'NONE', #20280, .T. ) ;
#21014=CARTESIAN_POINT ( 'NONE',  ( -0.2627480064045953911, 0.000000000000000000, 1.723473835155032274 ) ) ;
#21023=DIRECTION ( 'NONE',  ( -0.5128992774059071280, -9.962263361493005127E-17, 0.8584487936018655452 ) ) ;
#21030=ORIENTED_EDGE ( 'NONE', *, *, #48936, .F. ) ;
#21034=EDGE_LOOP ( 'NONE', ( #898, #27995, #33935, #42621 ) ) ;
#21035=DIRECTION ( 'NONE',  ( -0.01601477604151182663, 0.9998717552508123996, -0.000000000000000000 ) ) ;
#21039=ORIENTED_EDGE ( 'NONE', *, *, #28941, .T. ) ;
#21040=ORIENTED_EDGE ( 'NONE', *, *, #24202, .T. ) ;
#21042=CARTESIAN_POINT ( 'NONE',  ( 0.5110944797606088441, 1.727220439156562204, 2.908232962414051492 ) ) ;
#21044=ORIENTED_EDGE ( 'NONE', *, *, #30060, .F. ) ;
#21048=ORIENTED_EDGE ( 'NONE', *, *, #32115, .T. ) ;
#21049=AXIS2_PLACEMENT_3D ( 'NONE', #13169, #20905, #25033 ) ;
#21053=ORIENTED_EDGE ( 'NONE', *, *, #49366, .T. ) ;
#21056=EDGE_CURVE ( 'NONE', #25743, #25170, #47025, .T. ) ;
#21061=LINE ( 'NONE', #36813, #541 ) ;
#21069=VERTEX_POINT ( 'NONE', #17689 ) ;
#21070=CARTESIAN_POINT ( 'NONE',  ( 2.695799277629594037, 1.453624836071520265, -1.205759334241453651 ) ) ;
#21072=VERTEX_POINT ( 'NONE', #22077 ) ;
#21074=CARTESIAN_POINT ( 'NONE',  ( 1.950008968278537091, 6.692913385826772199, 0.9934589848971188131 ) ) ;
#21076=DIRECTION ( 'NONE',  ( -0.3090169943749582204, 0.000000000000000000, 0.9510565162951500895 ) ) ;
#21083=EDGE_CURVE ( 'NONE', #37126, #22293, #49142, .T. ) ;
#21088=EDGE_CURVE ( 'NONE', #36015, #41720, #13155, .T. ) ;
#21090=DIRECTION ( 'NONE',  ( 0.000000000000000000, 0.000000000000000000, -1.000000000000000000 ) ) ;
#21091=CIRCLE ( 'NONE', #49893, 1.743387098533651480 ) ;
#21092=EDGE_CURVE ( 'NONE', #48759, #15500, #29140, .T. ) ;
#21095=ORIENTED_EDGE ( 'NONE', *, *, #21056, .T. ) ;
#21102=LINE ( 'NONE', #16978, #9141 ) ;
#21105=B_SPLINE_CURVE_WITH_KNOTS ( 'NONE', 3,
 ( #3844, #50021, #30459, #18831 ),
 .UNSPECIFIED., .F., .F.,
 ( 4, 4 ),
 ( 0.1211873102087489551, 0.1625992483279400380 ),
 .UNSPECIFIED. ) ;
#21109=VERTEX_POINT ( 'NONE', #22574 ) ;
#21112=VERTEX_POINT ( 'NONE', #14583 ) ;
#21114=DIRECTION ( 'NONE',  ( -0.9998717552508121775, -0.01601477604151182663, 0.000000000000000000 ) ) ;
#21116=AXIS2_PLACEMENT_3D ( 'NONE', #13121, #35588, #473 ) ;
#21117=VERTEX_POINT ( 'NONE', #18709 ) ;
#21120=VERTEX_POINT ( 'NONE', #38335 ) ;
#21122=EDGE_CURVE ( 'NONE', #31774, #16641, #32266, .T. ) ;
#21128=CARTESIAN_POINT ( 'NONE',  ( -0.3500732549360408563, 1.603869690133923331, 2.204675616574417685 ) ) ;
#21132=DIRECTION ( 'NONE',  ( -0.9998717552508122886, -0.01601477604151185785, 0.000000000000000000 ) ) ;
#21135=CARTESIAN_POINT ( 'NONE',  ( -1.427293369312925497, 0.000000000000000000, -1.001115484471666761 ) ) ;
#21137=CARTESIAN_POINT ( 'NONE',  ( -0.8338860769296044806, 1.049866565877818125, -1.845005749107295756 ) ) ;
#21139=ORIENTED_EDGE ( 'NONE', *, *, #34847, .F. ) ;
#21144=CARTESIAN_POINT ( 'NONE',  ( 2.161044708975088380, 1.205361022782829114E-17, 0.1463148319730657732 ) ) ;
#21152=CARTESIAN_POINT ( 'NONE',  ( 1.695772546416037363, 1.647224322255602891, -2.417756147381349141 ) ) ;
#21153=VECTOR ( 'NONE', #3097, 39.37007874015748143 ) ;
#21156=EDGE_CURVE ( 'NONE', #47474, #20582, #14322, .T. ) ;
#21158=CARTESIAN_POINT ( 'NONE',  ( -1.497019770989685084, 1.049866565067838486, -1.363210918355331591 ) ) ;
#21160=ORIENTED_EDGE ( 'NONE', *, *, #17354, .F. ) ;
#21161=CARTESIAN_POINT ( 'NONE',  ( 1.852263788401641076, 0.9949518933081566985, -1.839032047933712111 ) ) ;
#21162=CARTESIAN_POINT ( 'NONE',  ( 0.8291286199751974895, 1.205361022782829114E-17, -1.835126787948130556 ) ) ;
#21163=VECTOR ( 'NONE', #34458, 39.37007874015748143 ) ;
#21164=CARTESIAN_POINT ( 'NONE',  ( -1.883550378546958060, 1.205361022782829114E-17, -1.069467267250448161 ) ) ;
#21165=AXIS2_PLACEMENT_3D ( 'NONE', #25924, #26425, #14560 ) ;
#21166=DIRECTION ( 'NONE',  ( -0.9998717552508122886, -0.01601477604151182316, 0.000000000000000000 ) ) ;
#21167=ORIENTED_EDGE ( 'NONE', *, *, #49747, .F. ) ;
#21168=ORIENTED_EDGE ( 'NONE', *, *, #50847, .T. ) ;
#21175=EDGE_LOOP ( 'NONE', ( #44062, #15384, #30194, #37469 ) ) ;
#21177=CARTESIAN_POINT ( 'NONE',  ( -2.168245791271168788, 1.205361022782829114E-17, -2.004968704497279486 ) ) ;
#21179=ORIENTED_EDGE ( 'NONE', *, *, #21542, .F. ) ;
#21182=CARTESIAN_POINT ( 'NONE',  ( 0.2239970000120027616, 0.000000000000000000, -1.939803615689571048 ) ) ;
#21183=AXIS2_PLACEMENT_3D ( 'NONE', #423, #47631, #40450 ) ;
#21187=VERTEX_POINT ( 'NONE', #10453 ) ;
#21188=EDGE_CURVE ( 'NONE', #17122, #11634, #40959, .T. ) ;
#21189=CARTESIAN_POINT ( 'NONE',  ( -2.576863348864732117, 1.568913320674888201, 1.442554885838411849 ) ) ;
#21192=EDGE_CURVE ( 'NONE', #3813, #29782, #15334, .T. ) ;
#21195=EDGE_CURVE ( 'NONE', #40833, #50445, #7342, .T. ) ;
#21200=EDGE_LOOP ( 'NONE', ( #41262, #48539, #16115, #43381 ) ) ;
#21202=DIRECTION ( 'NONE',  ( -0.000000000000000000, -1.000000000000000000, -0.000000000000000000 ) ) ;
#21203=ORIENTED_EDGE ( 'NONE', *, *, #21983, .T. ) ;
#21204=ORIENTED_EDGE ( 'NONE', *, *, #32437, .F. ) ;
#21206=CARTESIAN_POINT ( 'NONE',  ( 2.190654571063535005, 1.742989292944022939, 0.7635320059819211691 ) ) ;
#21207=ADVANCED_FACE ( 'NONE', ( #11212 ), #38485, .T. ) ;
#21208=VERTEX_POINT ( 'NONE', #30073 ) ;
#21210=ORIENTED_EDGE ( 'NONE', *, *, #22723, .T. ) ;
#21212=ORIENTED_EDGE ( 'NONE', *, *, #35696, .T. ) ;
#21213=B_SPLINE_CURVE_WITH_KNOTS ( 'NONE', 3,
 ( #41199, #37329, #29571, #48633 ),
 .UNSPECIFIED., .F., .F.,
 ( 4, 4 ),
 ( 2.136716580819921136E-07, 0.01722135198962225847 ),
 .UNSPECIFIED. ) ;
#21218=VERTEX_POINT ( 'NONE', #6831 ) ;
#21221=VECTOR ( 'NONE', #38840, 39.37007874015748143 ) ;
#21222=CARTESIAN_POINT ( 'NONE',  ( -2.295861763883067841, 1.675315707476183080, 0.7977158951143258347 ) ) ;
#21227=CARTESIAN_POINT ( 'NONE',  ( 2.277873973731426194, 1.656288013650806912, 1.879489153247668076 ) ) ;
#21228=EDGE_CURVE ( 'NONE', #22686, #15190, #6387, .T. ) ;
#21235=CARTESIAN_POINT ( 'NONE',  ( -0.04921259842519708910, 1.674305324545202867, 2.241718228789840950 ) ) ;
#21237=ORIENTED_EDGE ( 'NONE', *, *, #35425, .T. ) ;
#21238=ORIENTED_EDGE ( 'NONE', *, *, #46539, .T. ) ;
#21254=ADVANCED_FACE ( 'NONE', ( #23577 ), #3062, .T. ) ;
#21259=DIRECTION ( 'NONE',  ( -0.9998717552508122886, -0.01601477604151182316, 0.000000000000000000 ) ) ;
#21260=AXIS2_PLACEMENT_3D ( 'NONE', #9036, #24273, #780 ) ;
#21262=VERTEX_POINT ( 'NONE', #4214 ) ;
#21264=DIRECTION ( 'NONE',  ( 0.9998717552508121775, 0.01601477604151182663, 0.000000000000000000 ) ) ;
#21270=CARTESIAN_POINT ( 'NONE',  ( 2.136190583516914820, 1.205361022782829114E-17, -0.1451986319116555235 ) ) ;
#21276=CIRCLE ( 'NONE', #29531, 1.743387098533651480 ) ;
#21277=B_SPLINE_CURVE_WITH_KNOTS ( 'NONE', 3,
 ( #20557, #40186, #44299, #32190 ),
 .UNSPECIFIED., .F., .F.,
 ( 4, 4 ),
 ( 0.1211775127643062444, 0.1625894504277921315 ),
 .UNSPECIFIED. ) ;
#21283=CARTESIAN_POINT ( 'NONE',  ( 0.000000000000000000, 6.692913385826772199, 0.000000000000000000 ) ) ;
#21288=ORIENTED_EDGE ( 'NONE', *, *, #19181, .T. ) ;
#21291=FACE_OUTER_BOUND ( 'NONE', #12785, .T. ) ;
#21293=DIRECTION ( 'NONE',  ( 0.5877852522924685852, 0.000000000000000000, 0.8090169943749507819 ) ) ;
#21298=VECTOR ( 'NONE', #31183, 39.37007874015748143 ) ;
#21303=VERTEX_POINT ( 'NONE', #16091 ) ;
#21304=EDGE_CURVE ( 'NONE', #26089, #1230, #35910, .T. ) ;
#21305=CARTESIAN_POINT ( 'NONE',  ( -2.122494303567052487, 1.641097921313502184, -0.4339672821292706595 ) ) ;
#21309=CARTESIAN_POINT ( 'NONE',  ( -1.263630850544466666, 0.000000000000000000, -1.276241334172347530 ) ) ;
#21310=EDGE_CURVE ( 'NONE', #1426, #34848, #27210, .T. ) ;
#21320=CARTESIAN_POINT ( 'NONE',  ( -1.312442655063644770, 0.006898494447474761912, -1.186737126055851022 ) ) ;
#21321=EDGE_CURVE ( 'NONE', #42907, #26436, #24211, .T. ) ;
#21322=B_SPLINE_CURVE_WITH_KNOTS ( 'NONE', 3,
 ( #35029, #6893, #50452, #18520 ),
 .UNSPECIFIED., .F., .F.,
 ( 4, 4 ),
 ( 3.722988146457368422E-07, 0.04368291484730600638 ),
 .UNSPECIFIED. ) ;
#21323=CARTESIAN_POINT ( 'NONE',  ( 2.225020958752729872, 1.645114536686943296, 0.6712079458291126954 ) ) ;
#21326=CARTESIAN_POINT ( 'NONE',  ( -1.312623452344869435, 5.905511811023623991, 1.722945714930905536 ) ) ;
#21328=FACE_OUTER_BOUND ( 'NONE', #16057, .T. ) ;
#21333=EDGE_LOOP ( 'NONE', ( #48278, #4462, #2294, #38755 ) ) ;
#21339=DIRECTION ( 'NONE',  ( -1.729310098865080642E-17, 1.000000000000000000, 1.276627980444840260E-16 ) ) ;
#21340=ORIENTED_EDGE ( 'NONE', *, *, #9700, .F. ) ;
#21343=B_SPLINE_CURVE_WITH_KNOTS ( 'NONE', 3,
 ( #35194, #49876, #50873, #3698 ),
 .UNSPECIFIED., .F., .F.,
 ( 4, 4 ),
 ( 2.034061690683489341E-07, 0.002500755411796015595 ),
 .UNSPECIFIED. ) ;
#21345=AXIS2_PLACEMENT_3D ( 'NONE', #32532, #8763, #25020 ) ;
#21348=ADVANCED_FACE ( 'NONE', ( #40102 ), #19444, .T. ) ;
#21353=AXIS2_PLACEMENT_3D ( 'NONE', #21642, #13897, #19027 ) ;
#21355=VERTEX_POINT ( 'NONE', #15587 ) ;
#21359=ORIENTED_EDGE ( 'NONE', *, *, #26647, .F. ) ;
#21364=EDGE_CURVE ( 'NONE', #10525, #34229, #13700, .T. ) ;
#21365=DIRECTION ( 'NONE',  ( -0.1785568947986229116, 0.000000000000000000, -0.9839295885986321100 ) ) ;
#21368=AXIS2_PLACEMENT_3D ( 'NONE', #50613, #27169, #44189 ) ;
#21370=ORIENTED_EDGE ( 'NONE', *, *, #45917, .F. ) ;
#21371=CARTESIAN_POINT ( 'NONE',  ( 0.08139965876239094178, 1.610780518492231694, 0.000000000000000000 ) ) ;
#21372=ORIENTED_EDGE ( 'NONE', *, *, #21625, .T. ) ;
#21384=EDGE_CURVE ( 'NONE', #23897, #38926, #29749, .T. ) ;
#21386=CARTESIAN_POINT ( 'NONE',  ( 2.312113436335841321, 1.646509482104762334, 0.2635349935491774209 ) ) ;
#21388=CIRCLE ( 'NONE', #50150, 2.164630168518208109 ) ;
#21390=DIRECTION ( 'NONE',  ( 0.1785568947986229116, 0.000000000000000000, 0.9839295885986321100 ) ) ;
#21395=ORIENTED_EDGE ( 'NONE', *, *, #44054, .T. ) ;
#21397=ORIENTED_EDGE ( 'NONE', *, *, #40399, .F. ) ;
#21399=FACE_OUTER_BOUND ( 'NONE', #29039, .T. ) ;
#21400=DIRECTION ( 'NONE',  ( -9.390536051998764103E-17, -1.000000000000000000, -6.822623802544789917E-17 ) ) ;
#21406=CARTESIAN_POINT ( 'NONE',  ( -0.7148041136150262709, 1.205361022782829114E-17, -2.044646019095620826 ) ) ;
#21407=CARTESIAN_POINT ( 'NONE',  ( 2.387237949294865214, 0.9877775034572128243, -1.073873893196610751 ) ) ;
#21408=VERTEX_POINT ( 'NONE', #24859 ) ;
#21412=LINE ( 'NONE', #48223, #49079 ) ;
#21422=LINE ( 'NONE', #48231, #46257 ) ;
#21426=LINE ( 'NONE', #5419, #1948 ) ;
#21427=ORIENTED_EDGE ( 'NONE', *, *, #4108, .F. ) ;
#21428=ORIENTED_EDGE ( 'NONE', *, *, #36691, .F. ) ;
#21430=CARTESIAN_POINT ( 'NONE',  ( 2.122091976112992828, 0.000000000000000000, 0.4338754535133130252 ) ) ;
#21431=ORIENTED_EDGE ( 'NONE', *, *, #50978, .T. ) ;
#21432=VERTEX_POINT ( 'NONE', #21753 ) ;
#21435=CARTESIAN_POINT ( 'NONE',  ( -2.101376631542743567, 1.608627760585161992, -0.5301036954757798458 ) ) ;
#21436=DIRECTION ( 'NONE',  ( -0.000000000000000000, -1.000000000000000000, -0.000000000000000000 ) ) ;
#21439=CARTESIAN_POINT ( 'NONE',  ( 2.179222933086670366, 5.118110236220475784, 2.848360286204476122 ) ) ;
#21442=ORIENTED_EDGE ( 'NONE', *, *, #49539, .F. ) ;
#21443=ORIENTED_EDGE ( 'NONE', *, *, #42236, .T. ) ;
#21446=EDGE_CURVE ( 'NONE', #8605, #11744, #44711, .T. ) ;
#21450=AXIS2_PLACEMENT_3D ( 'NONE', #28602, #35846, #24486 ) ;
#21460=CARTESIAN_POINT ( 'NONE',  ( -1.905671854841497481, 1.689559879305088996, 2.256015092822653223 ) ) ;
#21462=ORIENTED_EDGE ( 'NONE', *, *, #45287, .T. ) ;
#21469=EDGE_CURVE ( 'NONE', #3514, #23810, #30342, .T. ) ;
#21474=VERTEX_POINT ( 'NONE', #40363 ) ;
#21475=ORIENTED_EDGE ( 'NONE', *, *, #40290, .F. ) ;
#21481=ORIENTED_EDGE ( 'NONE', *, *, #50377, .T. ) ;
#21483=FACE_OUTER_BOUND ( 'NONE', #49498, .T. ) ;
#21484=DIRECTION ( 'NONE',  ( -0.9998717552508121775, -0.01601477604151182663, 0.000000000000000000 ) ) ;
#21489=DIRECTION ( 'NONE',  ( 0.4338837391175526803, 0.000000000000000000, 0.9009688679024218105 ) ) ;
#21491=VERTEX_POINT ( 'NONE', #1869 ) ;
#21493=DIRECTION ( 'NONE',  ( 0.5128992774059071280, 9.962263361493005127E-17, -0.8584487936018655452 ) ) ;
#21494=EDGE_CURVE ( 'NONE', #33100, #48369, #3267, .T. ) ;
#21498=ORIENTED_EDGE ( 'NONE', *, *, #15529, .T. ) ;
#21499=B_SPLINE_CURVE_WITH_KNOTS ( 'NONE', 3,
 ( #39166, #16190, #15670, #8695 ),
 .UNSPECIFIED., .F., .F.,
 ( 4, 4 ),
 ( 0.01458567687628280554, 0.03075035112464553563 ),
 .UNSPECIFIED. ) ;
#21504=DIRECTION ( 'NONE',  ( 0.2225209339563041788, -1.160734090543304660E-16, 0.9749279121818259508 ) ) ;
#21505=DIRECTION ( 'NONE',  ( 0.9998717552508121775, 0.01601477604151182663, 0.000000000000000000 ) ) ;
#21515=AXIS2_PLACEMENT_3D ( 'NONE', #1226, #12851, #40475 ) ;
#21516=DIRECTION ( 'NONE',  ( -0.000000000000000000, -1.000000000000000000, -0.000000000000000000 ) ) ;
#21517=DIRECTION ( 'NONE',  ( -0.7530714660036196273, 0.000000000000000000, 0.6579387259397027066 ) ) ;
#21523=AXIS2_PLACEMENT_3D ( 'NONE', #15875, #43232, #43488 ) ;
#21524=B_SPLINE_CURVE_WITH_KNOTS ( 'NONE', 3,
 ( #23591, #14844, #15094, #35474 ),
 .UNSPECIFIED., .F., .F.,
 ( 4, 4 ),
 ( 0.1211775127643062860, 0.1625894504277921315 ),
 .UNSPECIFIED. ) ;
#21526=ORIENTED_EDGE ( 'NONE', *, *, #19765, .F. ) ;
#21527=FACE_OUTER_BOUND ( 'NONE', #39481, .T. ) ;
#21528=CARTESIAN_POINT ( 'NONE',  ( 1.068402561569974374, 5.905511811023623991, -1.884154513482173110 ) ) ;
#21539=DIRECTION ( 'NONE',  ( -0.9749279121818227312, 0.000000000000000000, -0.2225209339563184452 ) ) ;
#21541=CARTESIAN_POINT ( 'NONE',  ( 2.339241080213585899, 1.657243480315735873, 1.802537235681917815 ) ) ;
#21542=EDGE_CURVE ( 'NONE', #13472, #1865, #37114, .T. ) ;
#21543=ORIENTED_EDGE ( 'NONE', *, *, #40571, .F. ) ;
#21544=ORIENTED_EDGE ( 'NONE', *, *, #41543, .F. ) ;
#21546=CARTESIAN_POINT ( 'NONE',  ( -2.165460538733998241, 1.205361022782829114E-17, 0.04798874274652762534 ) ) ;
#21551=DIRECTION ( 'NONE',  ( -0.6234898018587318180, 0.000000000000000000, -0.7818314824680309139 ) ) ;
#21553=VERTEX_POINT ( 'NONE', #6763 ) ;
#21555=ORIENTED_EDGE ( 'NONE', *, *, #17246, .F. ) ;
#21558=CARTESIAN_POINT ( 'NONE',  ( 0.07982360342473591996, 1.709180471932028711, 0.000000000000000000 ) ) ;
#21561=AXIS2_PLACEMENT_3D ( 'NONE', #11259, #26990, #7388 ) ;
#21562=EDGE_CURVE ( 'NONE', #25006, #20856, #798, .T. ) ;
#21565=UNCERTAINTY_MEASURE_WITH_UNIT (LENGTH_MEASURE( 1.000000000000000082E-05 ), #25362, 'distance_accuracy_value', 'NONE');
#21568=CIRCLE ( 'NONE', #33958, 2.246510896728926010 ) ;
#21569=EDGE_CURVE ( 'NONE', #11282, #34114, #4448, .T. ) ;
#21574=EDGE_CURVE ( 'NONE', #33100, #22384, #48763, .T. ) ;
#21576=LINE ( 'NONE', #17445, #2246 ) ;
#21577=CARTESIAN_POINT ( 'NONE',  ( 0.1450934409768589450, 1.205361022782829114E-17, 2.161127057262026252 ) ) ;
#21581=DIRECTION ( 'NONE',  ( -3.986037398843765983E-20, -1.000000000000000000, -1.160734090543304660E-16 ) ) ;
#21586=CARTESIAN_POINT ( 'NONE',  ( 0.002207914879453961535, -5.712274067634378313E-18, 0.04916304461325374242 ) ) ;
#21591=ORIENTED_EDGE ( 'NONE', *, *, #27063, .F. ) ;
#21594=AXIS2_PLACEMENT_3D ( 'NONE', #12487, #11980, #27717 ) ;
#21597=CARTESIAN_POINT ( 'NONE',  ( -0.3595914698493425377, 0.000000000000000000, 1.705899337635481405 ) ) ;
#21600=ORIENTED_EDGE ( 'NONE', *, *, #12108, .T. ) ;
#21607=FACE_OUTER_BOUND ( 'NONE', #40478, .T. ) ;
#21609=ORIENTED_EDGE ( 'NONE', *, *, #22330, .F. ) ;
#21612=CARTESIAN_POINT ( 'NONE',  ( 1.539674616754186820, 0.000000000000000000, -1.403993126671013059 ) ) ;
#21613=ORIENTED_EDGE ( 'NONE', *, *, #50525, .T. ) ;
#21614=CARTESIAN_POINT ( 'NONE',  ( -0.5433753726466064027, 1.710786698518002913, 2.902374844046801350 ) ) ;
#21616=ORIENTED_EDGE ( 'NONE', *, *, #35364, .T. ) ;
#21617=B_SPLINE_CURVE_WITH_KNOTS ( 'NONE', 3,
 ( #17785, #1779, #4434, #40332 ),
 .UNSPECIFIED., .F., .F.,
 ( 4, 4 ),
 ( 3.758775566991543122E-07, 0.04545307989631656997 ),
 .UNSPECIFIED. ) ;
#21618=VERTEX_POINT ( 'NONE', #7274 ) ;
#21620=CARTESIAN_POINT ( 'NONE',  ( 2.685986181519757210, 5.118110236220475784, -1.228718213908073897 ) ) ;
#21621=VERTEX_POINT ( 'NONE', #34141 ) ;
#21622=CARTESIAN_POINT ( 'NONE',  ( -2.734482843737247926, 5.905511811023623991, -1.115254632218712683 ) ) ;
#21625=EDGE_CURVE ( 'NONE', #18215, #28527, #34630, .T. ) ;
#21629=CARTESIAN_POINT ( 'NONE',  ( 1.905671854841463952, 1.472358791367697650, 2.256015092822682089 ) ) ;
#21632=LINE ( 'NONE', #33527, #23278 ) ;
#21636=ADVANCED_FACE ( 'NONE', ( #30762 ), #32748, .T. ) ;
#21637=CARTESIAN_POINT ( 'NONE',  ( 1.979793062125284830, 1.205361022782829114E-17, 2.191257344206568813 ) ) ;
#21639=CARTESIAN_POINT ( 'NONE',  ( 0.7506868623604561197, 1.205361022782829114E-17, 1.860140722251951484 ) ) ;
#21642=CARTESIAN_POINT ( 'NONE',  ( 0.08119777152254364916, 1.623385212329073957, 0.000000000000000000 ) ) ;
#21648=ORIENTED_EDGE ( 'NONE', *, *, #36897, .T. ) ;
#21649=CARTESIAN_POINT ( 'NONE',  ( -2.318785326865331342, 1.584680398590042172, 1.828187939057640321 ) ) ;
#21652=CARTESIAN_POINT ( 'NONE',  ( -0.3742159057234073494, 0.02192591290182492950, 1.786486621533327712 ) ) ;
#21656=DIRECTION ( 'NONE',  ( -0.9998717552508122886, -0.01601477604151180928, 0.000000000000000000 ) ) ;
#21660=CARTESIAN_POINT ( 'NONE',  ( -1.293618082698012151, 0.000000000000000000, -1.168738992012460898 ) ) ;
#21661=CARTESIAN_POINT ( 'NONE',  ( 1.635196357930355893, 0.5249316497054298258, 0.9358222698459752742 ) ) ;
#21674=AXIS2_PLACEMENT_3D ( 'NONE', #9272, #5140, #1777 ) ;
#21677=VERTEX_POINT ( 'NONE', #4664 ) ;
#21679=DIRECTION ( 'NONE',  ( 0.9998717552508121775, 0.01601477604151182663, 0.000000000000000000 ) ) ;
#21685=AXIS2_PLACEMENT_3D ( 'NONE', #38401, #18526, #6900 ) ;
#21686=LINE ( 'NONE', #21177, #3938 ) ;
#21690=LINE ( 'NONE', #3329, #8725 ) ;
#21692=DIRECTION ( 'NONE',  ( -0.9998717552508122886, -0.01601477604151180928, 0.000000000000000000 ) ) ;
#21695=ORIENTED_EDGE ( 'NONE', *, *, #47814, .T. ) ;
#21696=ORIENTED_EDGE ( 'NONE', *, *, #49008, .F. ) ;
#21701=EDGE_CURVE ( 'NONE', #15234, #18703, #9393, .T. ) ;
#21710=CARTESIAN_POINT ( 'NONE',  ( 0.08119777152254364916, 1.623385212329073957, 0.000000000000000000 ) ) ;
#21711=CARTESIAN_POINT ( 'NONE',  ( 0.000000000000000000, 6.692913385826772199, 0.000000000000000000 ) ) ;
#21717=ORIENTED_EDGE ( 'NONE', *, *, #6459, .T. ) ;
#21720=ORIENTED_EDGE ( 'NONE', *, *, #24693, .F. ) ;
#21723=B_SPLINE_CURVE_WITH_KNOTS ( 'NONE', 3,
 ( #4343, #16995, #40230, #8727 ),
 .UNSPECIFIED., .F., .F.,
 ( 4, 4 ),
 ( 2.051448000182432276E-07, 0.002500220163013508554 ),
 .UNSPECIFIED. ) ;
#21732=ADVANCED_FACE ( 'NONE', ( #19376 ), #16024, .F. ) ;
#21734=ORIENTED_EDGE ( 'NONE', *, *, #2102, .T. ) ;
#21742=ORIENTED_EDGE ( 'NONE', *, *, #21701, .F. ) ;
#21743=CARTESIAN_POINT ( 'NONE',  ( 2.558651102769570803E-16, 1.595182601976580683, -2.089297179032357121 ) ) ;
#21746=DIRECTION ( 'NONE',  ( 0.3513748240813304724, -1.086859790425929286E-16, 0.9362348706397417564 ) ) ;
#21747=ORIENTED_EDGE ( 'NONE', *, *, #42689, .F. ) ;
#21749=ORIENTED_EDGE ( 'NONE', *, *, #40909, .T. ) ;
#21750=AXIS2_PLACEMENT_3D ( 'NONE', #43825, #32495, #48187 ) ;
#21753=CARTESIAN_POINT ( 'NONE',  ( -0.6383587639822442261, 1.599252270110662399, -2.128056888689588089 ) ) ;
#21757=VECTOR ( 'NONE', #11655, 39.37007874015748143 ) ;
#21758=CARTESIAN_POINT ( 'NONE',  ( -0.6383587639822442261, 1.599252270110662399, -2.128056888689588089 ) ) ;
#21761=CARTESIAN_POINT ( 'NONE',  ( 2.160407304981128984, 5.118110236220475784, -0.1462862061266579361 ) ) ;
#21763=CARTESIAN_POINT ( 'NONE',  ( 0.1155636338427008941, -0.5222242541845523167, 0.000000000000000000 ) ) ;
#21767=VERTEX_POINT ( 'NONE', #12929 ) ;
#21772=ORIENTED_EDGE ( 'NONE', *, *, #19181, .F. ) ;
#21775=CARTESIAN_POINT ( 'NONE',  ( 1.686980615242215098, 5.905511811023623991, 1.408267424185160044 ) ) ;
#21776=ORIENTED_EDGE ( 'NONE', *, *, #26005, .F. ) ;
#21778=AXIS2_PLACEMENT_3D ( 'NONE', #49391, #10450, #29301 ) ;
#21784=EDGE_CURVE ( 'NONE', #37182, #19985, #14371, .T. ) ;
#21785=VERTEX_POINT ( 'NONE', #36938 ) ;
#21788=CIRCLE ( 'NONE', #9401, 2.244934639244525076 ) ;
#21796=DIRECTION ( 'NONE',  ( -0.01601477604151182663, 0.9998717552508123996, -0.000000000000000000 ) ) ;
#21799=EDGE_CURVE ( 'NONE', #8220, #19533, #24247, .T. ) ;
#21800=VERTEX_POINT ( 'NONE', #41317 ) ;
#21804=ORIENTED_EDGE ( 'NONE', *, *, #6838, .T. ) ;
#21805=ORIENTED_EDGE ( 'NONE', *, *, #37346, .T. ) ;
#21808=CARTESIAN_POINT ( 'NONE',  ( -2.059449025298142999, 1.580632209844732960, -1.300463018946054428 ) ) ;
#21818=ORIENTED_EDGE ( 'NONE', *, *, #30500, .F. ) ;
#21819=CARTESIAN_POINT ( 'NONE',  ( 0.4788131938641113083, 0.000000000000000000, 2.914091152102192162 ) ) ;
#21823=VECTOR ( 'NONE', #17632, 39.37007874015748143 ) ;
#21824=CIRCLE ( 'NONE', #6996, 1.850107469027523432 ) ;
#21825=DIRECTION ( 'NONE',  ( -0.01601477604151182663, 0.9998717552508123996, -0.000000000000000000 ) ) ;
#21829=CARTESIAN_POINT ( 'NONE',  ( -0.2156685157583831947, 1.715903002249486997, -2.945280361644576850 ) ) ;
#21834=ORIENTED_EDGE ( 'NONE', *, *, #4105, .F. ) ;
#21836=CARTESIAN_POINT ( 'NONE',  ( 0.000000000000000000, 5.118110236220475784, 0.000000000000000000 ) ) ;
#21842=CARTESIAN_POINT ( 'NONE',  ( 2.044241703397536636, 0.000000000000000000, -0.7159595814952622872 ) ) ;
#21845=EDGE_CURVE ( 'NONE', #5208, #31969, #46466, .T. ) ;
#21849=EDGE_LOOP ( 'NONE', ( #18351, #920, #44107, #39759 ) ) ;
#21854=EDGE_CURVE ( 'NONE', #37890, #5331, #34971, .T. ) ;
#21856=ORIENTED_EDGE ( 'NONE', *, *, #7152, .F. ) ;
#21857=ORIENTED_EDGE ( 'NONE', *, *, #47230, .F. ) ;
#21863=DIRECTION ( 'NONE',  ( 0.000000000000000000, 1.160734090543304660E-16, -1.000000000000000000 ) ) ;
#21865=VECTOR ( 'NONE', #888, 39.37007874015748854 ) ;
#21868=DIRECTION ( 'NONE',  ( -0.9998717552508122886, -0.01601477604151185785, 0.000000000000000000 ) ) ;
#21869=CARTESIAN_POINT ( 'NONE',  ( -1.688048600224982154, 0.000000000000000000, -0.4357642695449713277 ) ) ;
#21872=DIRECTION ( 'NONE',  ( 1.283101021437939896E-16, 1.000000000000000000, -1.154811821032073265E-17 ) ) ;
#21882=CARTESIAN_POINT ( 'NONE',  ( -0.3465944589516567476, 5.905511811023623991, 2.185505870675810147 ) ) ;
#21887=ORIENTED_EDGE ( 'NONE', *, *, #49744, .F. ) ;
#21894=CARTESIAN_POINT ( 'NONE',  ( 2.889674983507178219, 1.665813060096536402, -0.6090712660037608250 ) ) ;
#21897=FACE_OUTER_BOUND ( 'NONE', #29277, .T. ) ;
#21898=EDGE_CURVE ( 'NONE', #38704, #970, #25305, .T. ) ;
#21899=CARTESIAN_POINT ( 'NONE',  ( -1.662320194739478119, 6.692913385826772199, -1.388601395075575118 ) ) ;
#21900=ORIENTED_EDGE ( 'NONE', *, *, #44797, .F. ) ;
#21913=EDGE_CURVE ( 'NONE', #35952, #31499, #37662, .T. ) ;
#21918=ORIENTED_EDGE ( 'NONE', *, *, #49695, .T. ) ;
#21921=EDGE_CURVE ( 'NONE', #22090, #2321, #23650, .T. ) ;
#21923=DIRECTION ( 'NONE',  ( -0.000000000000000000, 1.000000000000000000, -0.000000000000000000 ) ) ;
#21931=ORIENTED_EDGE ( 'NONE', *, *, #17246, .T. ) ;
#21936=EDGE_CURVE ( 'NONE', #45327, #5560, #10589, .T. ) ;
#21941=ORIENTED_EDGE ( 'NONE', *, *, #6739, .T. ) ;
#21942=ORIENTED_EDGE ( 'NONE', *, *, #30505, .T. ) ;
#21953=DIRECTION ( 'NONE',  ( -3.986037398843765983E-20, -1.000000000000000000, -1.160734090543304660E-16 ) ) ;
#21954=FACE_OUTER_BOUND ( 'NONE', #2938, .T. ) ;
#21957=CARTESIAN_POINT ( 'NONE',  ( 1.548545842648739956, 1.732704746525083772, 1.697655184951773810 ) ) ;
#21961=CARTESIAN_POINT ( 'NONE',  ( -0.8238130908517355966, 1.694707076513333410, 2.054984861273213337 ) ) ;
#21962=EDGE_CURVE ( 'NONE', #40673, #12848, #43200, .T. ) ;
#21965=EDGE_CURVE ( 'NONE', #36441, #38339, #33084, .T. ) ;
#21967=ORIENTED_EDGE ( 'NONE', *, *, #16836, .F. ) ;
#21969=FACE_BOUND ( 'NONE', #11214, .T. ) ;
#21970=DIRECTION ( 'NONE',  ( -0.01601477604151182663, 0.9998717552508123996, -0.000000000000000000 ) ) ;
#21972=ORIENTED_EDGE ( 'NONE', *, *, #31656, .F. ) ;
#21974=ORIENTED_EDGE ( 'NONE', *, *, #40436, .F. ) ;
#21975=CARTESIAN_POINT ( 'NONE',  ( -1.152895553066196177, 0.000000000000000000, -1.833672301139088745 ) ) ;
#21976=AXIS2_PLACEMENT_3D ( 'NONE', #36554, #36297, #921 ) ;
#21983=EDGE_CURVE ( 'NONE', #41400, #37182, #48664, .T. ) ;
#21984=ORIENTED_EDGE ( 'NONE', *, *, #34263, .F. ) ;
#21987=ORIENTED_EDGE ( 'NONE', *, *, #15524, .F. ) ;
#21990=CARTESIAN_POINT ( 'NONE',  ( -1.676283831994445306, 0.001070912127414903967, 0.4929124452910598198 ) ) ;
#21992=EDGE_CURVE ( 'NONE', #9482, #25262, #3812, .T. ) ;
#21996=CARTESIAN_POINT ( 'NONE',  ( 0.08139965876239094178, 1.610780518492231694, 0.000000000000000000 ) ) ;
#22002=CARTESIAN_POINT ( 'NONE',  ( -2.592410190524168545, 1.678844659144130613, 1.413664012936335590 ) ) ;
#22004=VECTOR ( 'NONE', #37843, 39.37007874015748143 ) ;
#22012=CARTESIAN_POINT ( 'NONE',  ( 0.7521025634872258170, 1.621523052975431867, 2.144027383376515328 ) ) ;
#22013=ORIENTED_EDGE ( 'NONE', *, *, #32288, .T. ) ;
#22023=LINE ( 'NONE', #28736, #40085 ) ;
#22025=VERTEX_POINT ( 'NONE', #16942 ) ;
#22030=ORIENTED_EDGE ( 'NONE', *, *, #1137, .F. ) ;
#22036=CARTESIAN_POINT ( 'NONE',  ( -2.491402175429631605, 1.567214198537667302, -1.585592796919542025 ) ) ;
#22037=VECTOR ( 'NONE', #20808, 39.37007874015748143 ) ;
#22040=LINE ( 'NONE', #37286, #33230 ) ;
#22041=ORIENTED_EDGE ( 'NONE', *, *, #46960, .T. ) ;
#22043=CARTESIAN_POINT ( 'NONE',  ( -1.891607981616729495, 1.579179190298960256, 1.073803248357834139 ) ) ;
#22046=ORIENTED_EDGE ( 'NONE', *, *, #35567, .F. ) ;
#22048=DIRECTION ( 'NONE',  ( 0.5508969814520945363, 0.000000000000000000, 0.8345732537213079727 ) ) ;
#22056=VERTEX_POINT ( 'NONE', #36558 ) ;
#22057=EDGE_CURVE ( 'NONE', #33804, #19688, #14881, .T. ) ;
#22058=DIRECTION ( 'NONE',  ( -0.01601477604151182663, 0.9998717552508123996, -0.000000000000000000 ) ) ;
#22062=ORIENTED_EDGE ( 'NONE', *, *, #10895, .F. ) ;
#22063=CARTESIAN_POINT ( 'NONE',  ( 1.686980615242215098, 6.692913385826772199, 1.408267424185160266 ) ) ;
#22066=ORIENTED_EDGE ( 'NONE', *, *, #6525, .F. ) ;
#22069=VERTEX_POINT ( 'NONE', #4286 ) ;
#22070=CARTESIAN_POINT ( 'NONE',  ( 2.016369045219287948, 1.641772594434526278, 1.140940039539855677 ) ) ;
#22072=EDGE_CURVE ( 'NONE', #33123, #35300, #35531, .T. ) ;
#22074=VECTOR ( 'NONE', #25355, 39.37007874015748854 ) ;
#22077=CARTESIAN_POINT ( 'NONE',  ( 0.7308738700548025324, 5.905511811023623991, 2.087463732006447525 ) ) ;
#22082=ORIENTED_EDGE ( 'NONE', *, *, #45349, .F. ) ;
#22084=CARTESIAN_POINT ( 'NONE',  ( 2.100227814008711391, 1.467797480264206866, -2.076109931251913565 ) ) ;
#22085=EDGE_CURVE ( 'NONE', #18042, #23291, #31515, .T. ) ;
#22090=VERTEX_POINT ( 'NONE', #48129 ) ;
#22091=LINE ( 'NONE', #33724, #6012 ) ;
#22092=EDGE_CURVE ( 'NONE', #40703, #16654, #43766, .T. ) ;
#22094=ADVANCED_FACE ( 'NONE', ( #40437 ), #44290, .F. ) ;
#22098=CARTESIAN_POINT ( 'NONE',  ( -0.3499974520433976055, 1.636679305949812147, 2.204257908207249095 ) ) ;
#22102=CARTESIAN_POINT ( 'NONE',  ( -2.084291548511495229, 6.692913385826772199, 0.6254821886024592992 ) ) ;
#22110=CIRCLE ( 'NONE', #49257, 2.244934639244525076 ) ;
#22112=ORIENTED_EDGE ( 'NONE', *, *, #32225, .T. ) ;
#22113=VERTEX_POINT ( 'NONE', #39913 ) ;
#22117=VERTEX_POINT ( 'NONE', #44027 ) ;
#22118=CARTESIAN_POINT ( 'NONE',  ( 0.000000000000000000, 10.31496062992126284, -0.3937007874015748254 ) ) ;
#22124=LINE ( 'NONE', #18243, #14921 ) ;
#22130=ORIENTED_EDGE ( 'NONE', *, *, #36870, .F. ) ;
#22131=CONICAL_SURFACE ( 'NONE', #8927, 2.246510896728926010, 0.01601546068027819014 ) ;
#22136=ORIENTED_EDGE ( 'NONE', *, *, #494, .F. ) ;
#22138=DIRECTION ( 'NONE',  ( -0.01601477604151182663, 0.9998717552508123996, -0.000000000000000000 ) ) ;
#22139=ADVANCED_FACE ( 'NONE', ( #20017 ), #8575, .T. ) ;
#22142=DIRECTION ( 'NONE',  ( -0.9998717552508121775, -0.01601477604151182316, 0.000000000000000000 ) ) ;
#22148=EDGE_CURVE ( 'NONE', #28307, #22970, #21002, .T. ) ;
#22150=CARTESIAN_POINT ( 'NONE',  ( -2.793030215715272213, 1.573188339825353665, 0.9592557174602283077 ) ) ;
#22151=DIRECTION ( 'NONE',  ( 1.000000000000000000, 0.000000000000000000, 0.000000000000000000 ) ) ;
#22154=ORIENTED_EDGE ( 'NONE', *, *, #8323, .T. ) ;
#22155=FACE_OUTER_BOUND ( 'NONE', #2536, .T. ) ;
#22162=VECTOR ( 'NONE', #41270, 39.37007874015748143 ) ;
#22170=ORIENTED_EDGE ( 'NONE', *, *, #45530, .F. ) ;
#22171=DIRECTION ( 'NONE',  ( 0.01601477604151182663, -0.9998717552508123996, 0.000000000000000000 ) ) ;
#22172=ORIENTED_EDGE ( 'NONE', *, *, #48344, .T. ) ;
#22173=VERTEX_POINT ( 'NONE', #48634 ) ;
#22179=FACE_OUTER_BOUND ( 'NONE', #40677, .T. ) ;
#22182=LINE ( 'NONE', #10559, #31307 ) ;
#22196=ORIENTED_EDGE ( 'NONE', *, *, #39554, .F. ) ;
#22199=DIRECTION ( 'NONE',  ( -0.9998717552508121775, -0.01601477604151182663, 0.000000000000000000 ) ) ;
#22201=ORIENTED_EDGE ( 'NONE', *, *, #38742, .T. ) ;
#22207=ADVANCED_FACE ( 'NONE', ( #9699 ), #22587, .T. ) ;
#22209=CARTESIAN_POINT ( 'NONE',  ( 0.1155636338427008941, -0.5222242541845523167, 0.000000000000000000 ) ) ;
#22211=VERTEX_POINT ( 'NONE', #22084 ) ;
#22213=CARTESIAN_POINT ( 'NONE',  ( 1.232620761116212105, 1.574803149606302854, -1.780282403660734980 ) ) ;
#22216=DIRECTION ( 'NONE',  ( -0.000000000000000000, -1.000000000000000000, -0.000000000000000000 ) ) ;
#22219=( BOUNDED_CURVE ( )  B_SPLINE_CURVE ( 3, ( #4467, #594, #29230, #45461 ),
 .UNSPECIFIED., .F., .F. ) 
 B_SPLINE_CURVE_WITH_KNOTS ( ( 4, 4 ),
 ( 6.010276100315349979, 6.061027312936714040 ),
 .UNSPECIFIED. ) 
 CURVE ( )  GEOMETRIC_REPRESENTATION_ITEM ( )  RATIONAL_B_SPLINE_CURVE ( ( 1.000000000000000000, 0.9997853710521733550, 0.9997853710521733550, 1.000000000000000000 ) ) 
 REPRESENTATION_ITEM ( '' )  );
#22220=CONICAL_SURFACE ( 'NONE', #21368, 3.033577403570480779, 1.554780866114618743 ) ;
#22221=EDGE_CURVE ( 'NONE', #24926, #6017, #46203, .T. ) ;
#22227=EDGE_CURVE ( 'NONE', #21491, #28109, #5568, .T. ) ;
#22231=ORIENTED_EDGE ( 'NONE', *, *, #34584, .T. ) ;
#22237=CARTESIAN_POINT ( 'NONE',  ( 0.07982360342473591996, 1.709180471932028711, 0.000000000000000000 ) ) ;
#22238=ORIENTED_EDGE ( 'NONE', *, *, #5101, .F. ) ;
#22239=ORIENTED_EDGE ( 'NONE', *, *, #30531, .F. ) ;
#22245=CARTESIAN_POINT ( 'NONE',  ( -1.364345965745727973, 1.205361022782829114E-17, 1.150974876880269893 ) ) ;
#22246=CARTESIAN_POINT ( 'NONE',  ( 1.930190994932110771, 6.692913385826772199, -0.9827944786818446632 ) ) ;
#22247=EDGE_CURVE ( 'NONE', #45160, #36136, #39469, .T. ) ;
#22251=VECTOR ( 'NONE', #772, 39.37007874015748143 ) ;
#22252=DIRECTION ( 'NONE',  ( 5.063291518729136385E-17, 1.000000000000000000, -1.184615939703115601E-16 ) ) ;
#22254=EDGE_LOOP ( 'NONE', ( #21204, #39599, #19543, #9160, #15579, #45719, #35769, #25592, #10727, #10937, #13453, #19041, #8036, #2568, #50994, #38810, #46494, #32035, #10362, #13798, #20999, #3840, #30550 ) ) ;
#22255=DIRECTION ( 'NONE',  ( 0.9639628606958549062, 0.000000000000000000, -0.2660368455666687892 ) ) ;
#22263=CARTESIAN_POINT ( 'NONE',  ( 1.642191404871903071, 0.000000000000000000, 0.5853255206279913692 ) ) ;
#22270=ORIENTED_EDGE ( 'NONE', *, *, #2500, .T. ) ;
#22274=CARTESIAN_POINT ( 'NONE',  ( -0.2824664041639280421, 0.01564075248451678515, 1.832131162653048095 ) ) ;
#22279=( LENGTH_UNIT ( ) NAMED_UNIT ( * ) SI_UNIT ( $, .METRE. ) );
#22283=DIRECTION ( 'NONE',  ( -0.000000000000000000, 1.000000000000000000, -0.000000000000000000 ) ) ;
#22285=CARTESIAN_POINT ( 'NONE',  ( -0.6735344408194913202, 1.606463534062856580, -2.625481381298739425 ) ) ;
#22289=CARTESIAN_POINT ( 'NONE',  ( -2.473332397914018710, 1.566147966415063486, -1.612967339752349183 ) ) ;
#22293=VERTEX_POINT ( 'NONE', #37844 ) ;
#22294=CARTESIAN_POINT ( 'NONE',  ( 0.1155636338427008941, -0.5222242541845523167, 0.000000000000000000 ) ) ;
#22299=DIRECTION ( 'NONE',  ( -0.01601477604151182663, 0.9998717552508123996, -0.000000000000000000 ) ) ;
#22302=EDGE_LOOP ( 'NONE', ( #43096, #38135, #14724, #22355, #16218, #13845, #43181, #42361, #25751, #15054, #5508, #9236, #38685 ) ) ;
#22303=DIRECTION ( 'NONE',  ( 0.9639628606958550172, -1.160734090543304660E-16, -0.2660368455666688448 ) ) ;
#22306=DIRECTION ( 'NONE',  ( -3.986037398843765983E-20, -1.000000000000000000, -1.160734090543304660E-16 ) ) ;
#22307=DIRECTION ( 'NONE',  ( 3.586865599282426309E-17, -1.000000000000000000, -1.103923720497134591E-16 ) ) ;
#22308=VECTOR ( 'NONE', #5913, 39.37007874015748854 ) ;
#22312=VERTEX_POINT ( 'NONE', #22839 ) ;
#22313=FACE_OUTER_BOUND ( 'NONE', #37393, .T. ) ;
#22318=B_SPLINE_CURVE_WITH_KNOTS ( 'NONE', 3,
 ( #10496, #41737, #6370, #30116 ),
 .UNSPECIFIED., .F., .F.,
 ( 4, 4 ),
 ( 2.329854378366125777E-07, 0.01910013319552298500 ),
 .UNSPECIFIED. ) ;
#22323=DIRECTION ( 'NONE',  ( 7.097135778201508621E-17, 1.000000000000000000, 1.075170113095020677E-16 ) ) ;
#22326=DIRECTION ( 'NONE',  ( -0.01601477604151182663, 0.9998717552508123996, -0.000000000000000000 ) ) ;
#22328=CARTESIAN_POINT ( 'NONE',  ( -1.695772546416001392, 1.551146592414875958, -2.417756147381374010 ) ) ;
#22330=EDGE_CURVE ( 'NONE', #50014, #20204, #3213, .T. ) ;
#22332=VERTEX_POINT ( 'NONE', #3722 ) ;
#22349=VERTEX_POINT ( 'NONE', #31346 ) ;
#22351=EDGE_CURVE ( 'NONE', #29652, #5773, #24758, .T. ) ;
#22352=CARTESIAN_POINT ( 'NONE',  ( -1.731130289826405155, 0.000000000000000000, 0.2179283737756174399 ) ) ;
#22353=ADVANCED_FACE ( 'NONE', ( #3470 ), #26205, .T. ) ;
#22355=ORIENTED_EDGE ( 'NONE', *, *, #21962, .F. ) ;
#22357=VERTEX_POINT ( 'NONE', #18959 ) ;
#22359=CARTESIAN_POINT ( 'NONE',  ( -2.139229417893219853, 5.905511811023623991, -0.3394403656973702388 ) ) ;
#22360=CARTESIAN_POINT ( 'NONE',  ( -1.252433315296644256, 1.589416742343778610, -1.807552045033091082 ) ) ;
#22362=ORIENTED_EDGE ( 'NONE', *, *, #8783, .T. ) ;
#22366=CARTESIAN_POINT ( 'NONE',  ( 2.100227814008711391, 1.467797480264206866, -2.076109931251913565 ) ) ;
#22377=CARTESIAN_POINT ( 'NONE',  ( 0.04921259842519689481, 1.205361022782829114E-17, 1.934165248549660987 ) ) ;
#22381=CARTESIAN_POINT ( 'NONE',  ( -0.04921259842519689481, 0.000000000000000000, -2.165433070866142007 ) ) ;
#22384=VERTEX_POINT ( 'NONE', #30333 ) ;
#22394=CARTESIAN_POINT ( 'NONE',  ( 1.883550378546973603, 0.000000000000000000, -1.069467267250420628 ) ) ;
#22396=CARTESIAN_POINT ( 'NONE',  ( 0.2052282226254518727, 0.000000000000000000, -1.731265419273307682 ) ) ;
#22398=CARTESIAN_POINT ( 'NONE',  ( 1.835963193532814008, 1.671691464651421155, 1.401186513841017778 ) ) ;
#22400=AXIS2_PLACEMENT_3D ( 'NONE', #32446, #47365, #16175 ) ;
#22408=EDGE_CURVE ( 'NONE', #20663, #12124, #34465, .T. ) ;
#22412=AXIS2_PLACEMENT_3D ( 'NONE', #16211, #35833, #8212 ) ;
#22417=CARTESIAN_POINT ( 'NONE',  ( -0.4161812636739087856, 0.000000000000000000, -1.692983086477939825 ) ) ;
#22422=ORIENTED_EDGE ( 'NONE', *, *, #16845, .F. ) ;
#22427=ORIENTED_EDGE ( 'NONE', *, *, #33812, .T. ) ;
#22430=VERTEX_POINT ( 'NONE', #24615 ) ;
#22436=ORIENTED_EDGE ( 'NONE', *, *, #13576, .F. ) ;
#22437=EDGE_CURVE ( 'NONE', #25003, #47775, #29133, .T. ) ;
#22443=CARTESIAN_POINT ( 'NONE',  ( -0.5455270741695672498, 1.205361022782829114E-17, -1.791688814994948808 ) ) ;
#22449=ORIENTED_EDGE ( 'NONE', *, *, #5121, .F. ) ;
#22453=DIRECTION ( 'NONE',  ( 0.9998717552508121775, 0.01601477604151182663, 0.000000000000000000 ) ) ;
#22463=CARTESIAN_POINT ( 'NONE',  ( -0.7381027496704855029, 1.707760278544290689, -2.859439394060923512 ) ) ;
#22464=DIRECTION ( 'NONE',  ( -0.01601477604151182663, 0.9998717552508123996, -0.000000000000000000 ) ) ;
#22465=CARTESIAN_POINT ( 'NONE',  ( 1.775400203342705430, 5.905511811023623991, -2.359903268218702888 ) ) ;
#22467=ORIENTED_EDGE ( 'NONE', *, *, #31643, .T. ) ;
#22470=ADVANCED_FACE ( 'NONE', ( #35722 ), #43237, .T. ) ;
#22473=VERTEX_POINT ( 'NONE', #23846 ) ;
#22476=CARTESIAN_POINT ( 'NONE',  ( -1.740978969773838037, 0.000000000000000000, 0.09160132170885167124 ) ) ;
#22487=EDGE_CURVE ( 'NONE', #22384, #45444, #11716, .T. ) ;
#22492=ADVANCED_FACE ( 'NONE', ( #39595 ), #15838, .F. ) ;
#22495=CARTESIAN_POINT ( 'NONE',  ( 0.1067246931122726866, 0.02962905676920215767, 0.000000000000000000 ) ) ;
#22498=DIRECTION ( 'NONE',  ( -0.3090169943749582204, -1.103800545167488837E-16, 0.9510565162951500895 ) ) ;
#22503=ORIENTED_EDGE ( 'NONE', *, *, #39126, .T. ) ;
#22504=EDGE_LOOP ( 'NONE', ( #34181, #10505, #1557, #25742 ) ) ;
#22507=( BOUNDED_CURVE ( )  B_SPLINE_CURVE ( 3, ( #50167, #42463, #22851, #15356 ),
 .UNSPECIFIED., .F., .F. ) 
 B_SPLINE_CURVE_WITH_KNOTS ( ( 4, 4 ),
 ( 2.340218168529833331, 2.391075478467469484 ),
 .UNSPECIFIED. ) 
 CURVE ( )  GEOMETRIC_REPRESENTATION_ITEM ( )  RATIONAL_B_SPLINE_CURVE ( ( 1.000000000000000000, 0.9997844727828222311, 0.9997844727828222311, 1.000000000000000000 ) ) 
 REPRESENTATION_ITEM ( '' )  );
#22512=VECTOR ( 'NONE', #28780, 39.37007874015748143 ) ;
#22513=DIRECTION ( 'NONE',  ( -0.9909497617679352555, 0.000000000000000000, 0.1342332658176522697 ) ) ;
#22514=ORIENTED_EDGE ( 'NONE', *, *, #45021, .T. ) ;
#22518=B_SPLINE_CURVE_WITH_KNOTS ( 'NONE', 3,
 ( #14265, #46237, #18655, #34403 ),
 .UNSPECIFIED., .F., .F.,
 ( 4, 4 ),
 ( 0.002149632668185018445, 0.004753995714153514546 ),
 .UNSPECIFIED. ) ;
#22520=CARTESIAN_POINT ( 'NONE',  ( 1.557927422371225612, 0.000000000000000000, 0.7824709080581413456 ) ) ;
#22525=CARTESIAN_POINT ( 'NONE',  ( 1.723687301221655810, 5.905511811023623991, -1.311649477509801098 ) ) ;
#22527=ADVANCED_FACE ( 'NONE', ( #43451 ), #18537, .T. ) ;
#22530=CARTESIAN_POINT ( 'NONE',  ( -1.825231763670859042, 0.5249316497054293817, -0.4670754313976908101 ) ) ;
#22531=CARTESIAN_POINT ( 'NONE',  ( 0.4787700707360283414, 1.205361022782829114E-17, -1.919768535593459724 ) ) ;
#22532=ADVANCED_FACE ( 'NONE', ( #47295 ), #12228, .T. ) ;
#22536=VERTEX_POINT ( 'NONE', #24359 ) ;
#22540=CARTESIAN_POINT ( 'NONE',  ( 0.000000000000000000, 1.574803149606302854, 0.000000000000000000 ) ) ;
#22547=CARTESIAN_POINT ( 'NONE',  ( 2.353959093805374377E-19, 5.905511811023623991, 2.952755905511811108 ) ) ;
#22551=CARTESIAN_POINT ( 'NONE',  ( 0.3015460593140593115, 0.000000000000000000, 1.937268728265797213 ) ) ;
#22555=VECTOR ( 'NONE', #15155, 39.37007874015748854 ) ;
#22556=ORIENTED_EDGE ( 'NONE', *, *, #14540, .F. ) ;
#22558=CARTESIAN_POINT ( 'NONE',  ( 1.502052629464437183, 0.01692425682782448815, -1.368022823756944950 ) ) ;
#22560=EDGE_CURVE ( 'NONE', #19371, #25220, #865, .T. ) ;
#22563=DIRECTION ( 'NONE',  ( -0.01601477604151182663, 0.9998717552508123996, -0.000000000000000000 ) ) ;
#22564=FACE_OUTER_BOUND ( 'NONE', #25819, .T. ) ;
#22565=CIRCLE ( 'NONE', #6898, 2.165354330708661568 ) ;
#22570=DIRECTION ( 'NONE',  ( 0.9998717552508121775, 0.01601477604151182663, 0.000000000000000000 ) ) ;
#22571=PLANE ( 'NONE',  #20093 ) ;
#22572=EDGE_CURVE ( 'NONE', #50201, #21785, #6268, .T. ) ;
#22574=CARTESIAN_POINT ( 'NONE',  ( 0.04921259842519669359, 1.574803149606302854, 2.164795024401847456 ) ) ;
#22576=ORIENTED_EDGE ( 'NONE', *, *, #6125, .T. ) ;
#22577=EDGE_CURVE ( 'NONE', #16254, #16314, #44720, .T. ) ;
#22578=ORIENTED_EDGE ( 'NONE', *, *, #24207, .T. ) ;
#22581=EDGE_CURVE ( 'NONE', #16346, #50666, #37262, .T. ) ;
#22582=FACE_OUTER_BOUND ( 'NONE', #10942, .T. ) ;
#22584=DIRECTION ( 'NONE',  ( 0.8805955318567321166, 0.000000000000000000, 0.4738686624730094055 ) ) ;
#22585=CARTESIAN_POINT ( 'NONE',  ( -1.232620761116186126, 5.905511811023623991, -1.780282403660754076 ) ) ;
#22586=ORIENTED_EDGE ( 'NONE', *, *, #21962, .T. ) ;
#22587=CONICAL_SURFACE ( 'NONE', #35780, 2.246510896728926010, 0.01601546068027819014 ) ;
#22588=CARTESIAN_POINT ( 'NONE',  ( -0.04921259842519708910, 1.710906707958852691, 2.478400121980571580 ) ) ;
#22589=AXIS2_PLACEMENT_3D ( 'NONE', #27852, #47695, #23729 ) ;
#22594=VERTEX_POINT ( 'NONE', #33397 ) ;
#22595=LINE ( 'NONE', #6347, #9187 ) ;
#22596=CARTESIAN_POINT ( 'NONE',  ( 2.326943258702977246, 1.646747008850265370, -0.05524094006260020506 ) ) ;
#22597=VERTEX_POINT ( 'NONE', #13506 ) ;
#22600=DIRECTION ( 'NONE',  ( 0.000000000000000000, 0.000000000000000000, 1.000000000000000000 ) ) ;
#22605=ORIENTED_EDGE ( 'NONE', *, *, #13871, .T. ) ;
#22610=CARTESIAN_POINT ( 'NONE',  ( 1.068402561569975484, 0.000000000000000000, -1.884154513482173554 ) ) ;
#22629=EDGE_LOOP ( 'NONE', ( #3135, #32610, #2912, #2505 ) ) ;
#22630=B_SPLINE_CURVE_WITH_KNOTS ( 'NONE', 3,
 ( #29228, #20715, #39826, #24598 ),
 .UNSPECIFIED., .F., .F.,
 ( 4, 4 ),
 ( 0.001625204961501889710, 0.002876679757166853129 ),
 .UNSPECIFIED. ) ;
#22633=AXIS2_PLACEMENT_3D ( 'NONE', #32717, #20819, #36576 ) ;
#22635=EDGE_CURVE ( 'NONE', #869, #50130, #42480, .T. ) ;
#22636=VERTEX_POINT ( 'NONE', #21761 ) ;
#22637=VERTEX_POINT ( 'NONE', #41380 ) ;
#22642=DIRECTION ( 'NONE',  ( 0.000000000000000000, -1.000000000000000000, -0.000000000000000000 ) ) ;
#22643=FACE_OUTER_BOUND ( 'NONE', #10184, .T. ) ;
#22644=DIRECTION ( 'NONE',  ( 0.2225209339563041788, 0.000000000000000000, 0.9749279121818259508 ) ) ;
#22645=EDGE_LOOP ( 'NONE', ( #1044, #23372, #47564, #30676 ) ) ;
#22653=CARTESIAN_POINT ( 'NONE',  ( -2.437180031585919782, 1.681273446161504426, -1.667735833703134718 ) ) ;
#22657=DIRECTION ( 'NONE',  ( -0.2225209339563041788, 1.288287287306305283E-16, -0.9749279121818259508 ) ) ;
#22661=ADVANCED_FACE ( 'NONE', ( #37518 ), #9887, .T. ) ;
#22662=VECTOR ( 'NONE', #25066, 39.37007874015748143 ) ;
#22664=ORIENTED_EDGE ( 'NONE', *, *, #43770, .F. ) ;
#22665=CARTESIAN_POINT ( 'NONE',  ( 1.775400203342704764, 0.000000000000000000, -2.359903268218703332 ) ) ;
#22673=AXIS2_PLACEMENT_3D ( 'NONE', #44403, #47986, #8532 ) ;
#22674=ORIENTED_EDGE ( 'NONE', *, *, #27046, .F. ) ;
#22678=CARTESIAN_POINT ( 'NONE',  ( 1.466506618346834934, 1.205361022782829114E-17, -1.470210429041567401 ) ) ;
#22681=CARTESIAN_POINT ( 'NONE',  ( 0.000000000000000000, 0.000000000000000000, 0.000000000000000000 ) ) ;
#22682=FACE_OUTER_BOUND ( 'NONE', #27343, .T. ) ;
#22684=B_SPLINE_CURVE_WITH_KNOTS ( 'NONE', 3,
 ( #16394, #34997, #8642, #24390 ),
 .UNSPECIFIED., .F., .F.,
 ( 4, 4 ),
 ( 0.01072160935731267424, 0.03072004101276351595 ),
 .UNSPECIFIED. ) ;
#22685=ORIENTED_EDGE ( 'NONE', *, *, #50400, .T. ) ;
#22686=VERTEX_POINT ( 'NONE', #17889 ) ;
#22695=EDGE_CURVE ( 'NONE', #869, #43448, #11120, .T. ) ;
#22697=DIRECTION ( 'NONE',  ( -2.582876339026174526E-17, -1.000000000000000000, -1.131632063491654496E-16 ) ) ;
#22699=AXIS2_PLACEMENT_3D ( 'NONE', #18087, #10086, #33083 ) ;
#22700=EDGE_LOOP ( 'NONE', ( #6240, #19841 ) ) ;
#22701=DIRECTION ( 'NONE',  ( -2.582876339026174526E-17, -1.000000000000000000, -1.131632063491654496E-16 ) ) ;
#22702=CIRCLE ( 'NONE', #32630, 2.165354330708661568 ) ;
#22705=FACE_OUTER_BOUND ( 'NONE', #3417, .T. ) ;
#22707=VERTEX_POINT ( 'NONE', #3401 ) ;
#22718=LINE ( 'NONE', #30213, #39098 ) ;
#22720=VERTEX_POINT ( 'NONE', #45730 ) ;
#22723=EDGE_CURVE ( 'NONE', #8328, #26516, #26637, .T. ) ;
#22724=EDGE_CURVE ( 'NONE', #20325, #31865, #11149, .T. ) ;
#22730=MECHANICAL_DESIGN_GEOMETRIC_PRESENTATION_REPRESENTATION('',(#40046),#44164);
#22731=B_SPLINE_CURVE_WITH_KNOTS ( 'NONE', 3,
 ( #3790, #31668, #19776, #11534 ),
 .UNSPECIFIED., .F., .F.,
 ( 4, 4 ),
 ( 3.606898746852332451E-07, 0.04590458542295366290 ),
 .UNSPECIFIED. ) ;
#22732=VECTOR ( 'NONE', #43316, 39.37007874015748854 ) ;
#22733=ORIENTED_EDGE ( 'NONE', *, *, #39612, .T. ) ;
#22741=B_SPLINE_CURVE_WITH_KNOTS ( 'NONE', 3,
 ( #13547, #5029, #1665, #12781 ),
 .UNSPECIFIED., .F., .F.,
 ( 4, 4 ),
 ( 2.052460024355699288E-07, 0.01596358452146435375 ),
 .UNSPECIFIED. ) ;
#22745=CARTESIAN_POINT ( 'NONE',  ( -0.3225722872767163296, 0.000000000000000000, 1.868935683883109045 ) ) ;
#22746=CARTESIAN_POINT ( 'NONE',  ( -0.5433753727366142927, 1.612341559703608596, 2.902374844030467305 ) ) ;
#22747=DIRECTION ( 'NONE',  ( 0.01601477604151182663, -0.9998717552508123996, 0.000000000000000000 ) ) ;
#22749=ORIENTED_EDGE ( 'NONE', *, *, #32074, .F. ) ;
#22750=CARTESIAN_POINT ( 'NONE',  ( 0.000000000000000000, 6.692913385826772199, 0.000000000000000000 ) ) ;
#22753=ORIENTED_EDGE ( 'NONE', *, *, #14726, .T. ) ;
#22754=B_SPLINE_CURVE_WITH_KNOTS ( 'NONE', 3,
 ( #46002, #27151, #22285, #50347 ),
 .UNSPECIFIED., .F., .F.,
 ( 4, 4 ),
 ( 0.01224259289618789825, 0.03073794493652437163 ),
 .UNSPECIFIED. ) ;
#22755=FACE_OUTER_BOUND ( 'NONE', #25848, .T. ) ;
#22756=EDGE_CURVE ( 'NONE', #32762, #39747, #38055, .T. ) ;
#22758=ORIENTED_EDGE ( 'NONE', *, *, #37827, .F. ) ;
#22764=CARTESIAN_POINT ( 'NONE',  ( -1.977197495136348460, 1.643425115977502848, -0.8986141922004805549 ) ) ;
#22766=ORIENTED_EDGE ( 'NONE', *, *, #37663, .T. ) ;
#22771=CARTESIAN_POINT ( 'NONE',  ( -2.576863348864732117, 1.205361022782829114E-17, 1.442554885838412071 ) ) ;
#22774=CARTESIAN_POINT ( 'NONE',  ( 0.8329809839909848579, 0.000000000000000000, -2.833254665166554442 ) ) ;
#22776=EDGE_CURVE ( 'NONE', #39707, #48162, #46732, .T. ) ;
#22781=AXIS2_PLACEMENT_3D ( 'NONE', #36593, #47905, #8966 ) ;
#22784=EDGE_CURVE ( 'NONE', #43935, #34736, #42132, .T. ) ;
#22788=CARTESIAN_POINT ( 'NONE',  ( -1.676283831994445306, 0.001070912127414903967, 0.4929124452910598198 ) ) ;
#22791=LINE ( 'NONE', #3165, #6935 ) ;
#22798=DIRECTION ( 'NONE',  ( -4.561975526775602830E-17, -1.000000000000000000, -1.067327232801823148E-16 ) ) ;
#22800=LINE ( 'NONE', #3431, #26852 ) ;
#22801=VECTOR ( 'NONE', #14089, 39.37007874015748143 ) ;
#22803=EDGE_LOOP ( 'NONE', ( #42242, #24975, #26437, #43830 ) ) ;
#22807=DIRECTION ( 'NONE',  ( -0.9998717552508121775, -0.01601477604151182663, 0.000000000000000000 ) ) ;
#22808=CIRCLE ( 'NONE', #1354, 1.850107469027523432 ) ;
#22813=ORIENTED_EDGE ( 'NONE', *, *, #42061, .F. ) ;
#22814=ORIENTED_EDGE ( 'NONE', *, *, #49037, .T. ) ;
#22817=VECTOR ( 'NONE', #16936, 39.37007874015748143 ) ;
#22818=DIRECTION ( 'NONE',  ( -8.021399753802198224E-17, -1.000000000000000000, 8.389726389140549123E-17 ) ) ;
#22819=ORIENTED_EDGE ( 'NONE', *, *, #30270, .F. ) ;
#22820=CARTESIAN_POINT ( 'NONE',  ( -2.695799277629577162, 1.677241212940233872, -1.205759334241492509 ) ) ;
#22833=CARTESIAN_POINT ( 'NONE',  ( 3.937007874015748143, 4.960629921259846142, -1.023622047244094224 ) ) ;
#22838=DIRECTION ( 'NONE',  ( -0.4338837391175526803, 0.000000000000000000, -0.9009688679024218105 ) ) ;
#22839=CARTESIAN_POINT ( 'NONE',  ( 1.511286805986086890, 0.000000000000000000, 0.8691436966267173103 ) ) ;
#22840=EDGE_CURVE ( 'NONE', #20337, #22536, #35913, .T. ) ;
#22841=CONICAL_SURFACE ( 'NONE', #35220, 2.165354330708661568, 0.2617993877991570129 ) ;
#22843=CARTESIAN_POINT ( 'NONE',  ( 1.003959327938112933, 1.731243926512280762, 2.534982793440925253 ) ) ;
#22845=CARTESIAN_POINT ( 'NONE',  ( 1.034308760555261886, 1.626043101691516890, -2.034340803895991812 ) ) ;
#22851=CARTESIAN_POINT ( 'NONE',  ( -1.198835066468417310, 0.000000000000000000, 1.347140709999463670 ) ) ;
#22856=CARTESIAN_POINT ( 'NONE',  ( 0.8329809839909849689, 1.496921813388997435, -2.833254665166554442 ) ) ;
#22859=ORIENTED_EDGE ( 'NONE', *, *, #15438, .F. ) ;
#22862=CARTESIAN_POINT ( 'NONE',  ( -1.695772546416001836, 1.594396608463251486, -2.417756147381374010 ) ) ;
#22863=DIRECTION ( 'NONE',  ( 8.902872254219889125E-17, 1.000000000000000000, 9.311674343991287120E-17 ) ) ;
#22864=ORIENTED_EDGE ( 'NONE', *, *, #15529, .F. ) ;
#22866=CARTESIAN_POINT ( 'NONE',  ( 2.151753172350863164, 1.709557817375465305, -0.8661840175195394398 ) ) ;
#22872=ADVANCED_FACE ( 'NONE', ( #800 ), #18575, .T. ) ;
#22876=CARTESIAN_POINT ( 'NONE',  ( -1.330241805570659519, 1.620978897557992404, -1.747195297779411627 ) ) ;
#22877=CIRCLE ( 'NONE', #32772, 1.850107469027523432 ) ;
#22884=VERTEX_POINT ( 'NONE', #39526 ) ;
#22886=B_SPLINE_CURVE_WITH_KNOTS ( 'NONE', 3,
 ( #17655, #33160, #41157, #48844 ),
 .UNSPECIFIED., .F., .F.,
 ( 4, 4 ),
 ( 2.000077559038616695E-07, 0.002660951063790191386 ),
 .UNSPECIFIED. ) ;
#22888=ORIENTED_EDGE ( 'NONE', *, *, #32930, .F. ) ;
#22891=VECTOR ( 'NONE', #20553, 39.37007874015748143 ) ;
#22895=CARTESIAN_POINT ( 'NONE',  ( 0.000000000000000000, 6.692913385826772199, 0.000000000000000000 ) ) ;
#22902=ORIENTED_EDGE ( 'NONE', *, *, #12773, .F. ) ;
#22906=LINE ( 'NONE', #27019, #47650 ) ;
#22911=FACE_OUTER_BOUND ( 'NONE', #18603, .T. ) ;
#22918=PLANE ( 'NONE',  #37494 ) ;
#22920=VERTEX_POINT ( 'NONE', #24299 ) ;
#22923=DIRECTION ( 'NONE',  ( -0.9998717552508122886, -0.01601477604151181275, 0.000000000000000000 ) ) ;
#22924=EDGE_LOOP ( 'NONE', ( #35761, #38712, #35436, #6904 ) ) ;
#22934=CARTESIAN_POINT ( 'NONE',  ( -1.064142702668968932, 0.000000000000000000, -1.380941303491921346 ) ) ;
#22935=CARTESIAN_POINT ( 'NONE',  ( 2.160407304981128984, 6.692913385826772199, -0.1462862061266579361 ) ) ;
#22938=ORIENTED_EDGE ( 'NONE', *, *, #15769, .T. ) ;
#22939=DIRECTION ( 'NONE',  ( -3.986037398843765983E-20, -1.000000000000000000, -1.160734090543304660E-16 ) ) ;
#22943=FACE_OUTER_BOUND ( 'NONE', #48614, .T. ) ;
#22945=ORIENTED_EDGE ( 'NONE', *, *, #29240, .F. ) ;
#22947=EDGE_CURVE ( 'NONE', #33248, #47415, #4530, .T. ) ;
#22949=ADVANCED_FACE ( 'NONE', ( #7778 ), #13445, .F. ) ;
#22950=DIRECTION ( 'NONE',  ( 0.01601477604151182663, -0.9998717552508123996, 0.000000000000000000 ) ) ;
#22957=AXIS2_PLACEMENT_3D ( 'NONE', #46504, #27155, #11173 ) ;
#22958=CARTESIAN_POINT ( 'NONE',  ( 0.1067246931122726866, 0.02962905676920215767, 0.000000000000000000 ) ) ;
#22959=AXIS2_PLACEMENT_3D ( 'NONE', #27259, #10762, #39143 ) ;
#22962=CARTESIAN_POINT ( 'NONE',  ( -1.693234526714950228, 0.000000000000000000, -0.4369479234249735167 ) ) ;
#22970=VERTEX_POINT ( 'NONE', #44918 ) ;
#22972=DIRECTION ( 'NONE',  ( -0.01601477604151182663, 0.9998717552508123996, -0.000000000000000000 ) ) ;
#22973=B_SPLINE_CURVE_WITH_KNOTS ( 'NONE', 3,
 ( #12422, #807, #8553, #40313 ),
 .UNSPECIFIED., .F., .F.,
 ( 4, 4 ),
 ( 4.780700947777823547E-07, 0.04951104265158085688 ),
 .UNSPECIFIED. ) ;
#22983=CARTESIAN_POINT ( 'NONE',  ( -2.009930929872525418, 1.574803149606302854, -0.8055662819784117357 ) ) ;
#22984=ORIENTED_EDGE ( 'NONE', *, *, #20311, .F. ) ;
#22986=ORIENTED_EDGE ( 'NONE', *, *, #29954, .F. ) ;
#22988=AXIS2_PLACEMENT_3D ( 'NONE', #44118, #5662, #28888 ) ;
#22989=CARTESIAN_POINT ( 'NONE',  ( -1.628069513120385503, 0.001843152681973240061, -0.6423508795876955446 ) ) ;
#22990=DIRECTION ( 'NONE',  ( -0.9998717552508122886, -0.01601477604151180928, 0.000000000000000000 ) ) ;
#22993=CARTESIAN_POINT ( 'NONE',  ( 0.08119777152254364916, 1.623385212329073957, 0.000000000000000000 ) ) ;
#22995=EDGE_LOOP ( 'NONE', ( #228, #12223, #8418, #42027 ) ) ;
#22997=CARTESIAN_POINT ( 'NONE',  ( -0.8783128861146038968, 0.01385187720497466773, 1.565997986929510644 ) ) ;
#22998=CARTESIAN_POINT ( 'NONE',  ( 0.000000000000000000, 6.692913385826772199, 0.000000000000000000 ) ) ;
#23000=AXIS2_PLACEMENT_3D ( 'NONE', #9133, #36255, #19968 ) ;
#23004=CARTESIAN_POINT ( 'NONE',  ( 2.889674983507178219, 2.755905511811027164, -0.6090712660037607140 ) ) ;
#23005=ORIENTED_EDGE ( 'NONE', *, *, #32989, .T. ) ;
#23015=CIRCLE ( 'NONE', #26337, 2.246510896728926010 ) ;
#23023=CARTESIAN_POINT ( 'NONE',  ( 1.695772546416036919, 1.205361022782829114E-17, -2.417756147381349141 ) ) ;
#23024=VECTOR ( 'NONE', #34705, 39.37007874015748143 ) ;
#23028=CARTESIAN_POINT ( 'NONE',  ( 0.000000000000000000, 0.000000000000000000, 0.000000000000000000 ) ) ;
#23031=DIRECTION ( 'NONE',  ( -0.01601477604151182663, 0.9998717552508123996, -0.000000000000000000 ) ) ;
#23032=VECTOR ( 'NONE', #1064, 39.37007874015748143 ) ;
#23034=CARTESIAN_POINT ( 'NONE',  ( 0.000000000000000000, 1.574803149606302854, 0.000000000000000000 ) ) ;
#23035=CARTESIAN_POINT ( 'NONE',  ( -1.688048600224982154, 0.000000000000000000, -0.4357642695449713277 ) ) ;
#23038=B_SPLINE_CURVE_WITH_KNOTS ( 'NONE', 3,
 ( #45577, #6873, #49435, #18239 ),
 .UNSPECIFIED., .F., .F.,
 ( 4, 4 ),
 ( 0.0005868951926194780231, 0.04882122509610800631 ),
 .UNSPECIFIED. ) ;
#23042=EDGE_LOOP ( 'NONE', ( #14208, #12577, #16000 ) ) ;
#23046=EDGE_CURVE ( 'NONE', #29367, #17250, #37462, .T. ) ;
#23048=DIRECTION ( 'NONE',  ( 0.8090169943749507819, -1.160734090543304660E-16, -0.5877852522924685852 ) ) ;
#23049=DIRECTION ( 'NONE',  ( -0.000000000000000000, -1.000000000000000000, -0.000000000000000000 ) ) ;
#23059=DIRECTION ( 'NONE',  ( -0.9998717552508121775, -0.01601477604151182316, 0.000000000000000000 ) ) ;
#23061=CARTESIAN_POINT ( 'NONE',  ( 2.505971853429350471, 0.9863260818638780458, 0.7624944251838070564 ) ) ;
#23064=B_SPLINE_CURVE_WITH_KNOTS ( 'NONE', 3,
 ( #8688, #24444, #35803, #48147 ),
 .UNSPECIFIED., .F., .F.,
 ( 4, 4 ),
 ( 0.001375932973688854437, 0.003876164346139760603 ),
 .UNSPECIFIED. ) ;
#23071=CARTESIAN_POINT ( 'NONE',  ( -1.478474649365228100, 1.688261849119575997, -1.951220303998286054 ) ) ;
#23075=CARTESIAN_POINT ( 'NONE',  ( -1.083598637574820334, 1.538470290252458739, 2.747180975113330259 ) ) ;
#23077=EDGE_LOOP ( 'NONE', ( #14534, #25307, #17872, #50565 ) ) ;
#23078=AXIS2_PLACEMENT_3D ( 'NONE', #22237, #2607, #26849 ) ;
#23079=CARTESIAN_POINT ( 'NONE',  ( 0.5110594979943910987, 0.000000000000000000, -1.666798357583575418 ) ) ;
#23080=FACE_OUTER_BOUND ( 'NONE', #40841, .T. ) ;
#23081=CARTESIAN_POINT ( 'NONE',  ( 0.000000000000000000, 1.574803149606302854, 0.000000000000000000 ) ) ;
#23082=CARTESIAN_POINT ( 'NONE',  ( -1.083598637574820112, 0.000000000000000000, 2.747180975113330259 ) ) ;
#23083=LINE ( 'NONE', #10957, #50174 ) ;
#23085=VERTEX_POINT ( 'NONE', #17070 ) ;
#23093=CONICAL_SURFACE ( 'NONE', #50245, 1.850107469027523210, 0.6386652850508578450 ) ;
#23100=DIRECTION ( 'NONE',  ( -0.01601477604151182663, 0.9998717552508123996, -0.000000000000000000 ) ) ;
#23103=ADVANCED_FACE ( 'NONE', ( #48255 ), #12941, .F. ) ;
#23106=AXIS2_PLACEMENT_3D ( 'NONE', #20115, #11614, #8513 ) ;
#23109=EDGE_CURVE ( 'NONE', #3300, #18896, #32832, .T. ) ;
#23112=EDGE_CURVE ( 'NONE', #33027, #11117, #2904, .T. ) ;
#23116=CARTESIAN_POINT ( 'NONE',  ( 1.018961996185594021, 0.04424020667788951949, 1.609505285524495344 ) ) ;
#23117=CARTESIAN_POINT ( 'NONE',  ( 0.9914495361338625523, 1.636256239573039117, 2.781765111341823360 ) ) ;
#23120=CARTESIAN_POINT ( 'NONE',  ( 2.623503965249848857, 5.905511811023623991, 1.355882097269874187 ) ) ;
#23128=CARTESIAN_POINT ( 'NONE',  ( -0.5286458662987738588, 5.905511811023623991, 2.100489422084708124 ) ) ;
#23132=B_SPLINE_CURVE_WITH_KNOTS ( 'NONE', 3,
 ( #50207, #30900, #11277, #49960 ),
 .UNSPECIFIED., .F., .F.,
 ( 4, 4 ),
 ( 0.001826648268129119979, 0.004326648414133393156 ),
 .UNSPECIFIED. ) ;
#23133=ADVANCED_FACE ( 'NONE', ( #6468 ), #3092, .F. ) ;
#23134=EDGE_LOOP ( 'NONE', ( #40777, #14961, #20082, #31966 ) ) ;
#23138=CARTESIAN_POINT ( 'NONE',  ( 2.240374965981713817, 0.5220472870780150654, -0.4608727740821708108 ) ) ;
#23139=EDGE_CURVE ( 'NONE', #2113, #34134, #46113, .T. ) ;
#23141=CARTESIAN_POINT ( 'NONE',  ( 2.122871581070786995, 0.000000000000000000, 0.2710165112059633730 ) ) ;
#23145=ORIENTED_EDGE ( 'NONE', *, *, #41835, .F. ) ;
#23149=CARTESIAN_POINT ( 'NONE',  ( 1.838947341486932396, 0.05737377265108637575, 0.6492553997849701553 ) ) ;
#23150=B_SPLINE_CURVE_WITH_KNOTS ( 'NONE', 3,
 ( #36471, #28195, #4718, #1088 ),
 .UNSPECIFIED., .F., .F.,
 ( 4, 4 ),
 ( 0.01072160763121544902, 0.03070979195761600056 ),
 .UNSPECIFIED. ) ;
#23154=EDGE_LOOP ( 'NONE', ( #28056, #10004, #6811, #316 ) ) ;
#23157=CARTESIAN_POINT ( 'NONE',  ( 2.164658444855302122, 5.905511811023623991, -0.04795272066889885720 ) ) ;
#23158=ORIENTED_EDGE ( 'NONE', *, *, #13159, .F. ) ;
#23159=CARTESIAN_POINT ( 'NONE',  ( -1.001904449526793695, 1.691854617476330036, -1.967052558704270426 ) ) ;
#23160=EDGE_CURVE ( 'NONE', #16446, #40209, #49525, .T. ) ;
#23161=CYLINDRICAL_SURFACE ( 'NONE', #7727, 2.165354330708661568 ) ;
#23164=CARTESIAN_POINT ( 'NONE',  ( -0.6235241006192322466, 1.205361022782829114E-17, 2.074304693190349269 ) ) ;
#23168=EDGE_CURVE ( 'NONE', #26808, #24752, #50031, .T. ) ;
#23170=VERTEX_POINT ( 'NONE', #19081 ) ;
#23175=PLANE ( 'NONE',  #30192 ) ;
#23176=VERTEX_POINT ( 'NONE', #41831 ) ;
#23182=ORIENTED_EDGE ( 'NONE', *, *, #8048, .T. ) ;
#23184=EDGE_LOOP ( 'NONE', ( #14198, #39230, #937, #11664 ) ) ;
#23186=ADVANCED_FACE ( 'NONE', ( #50276 ), #49779, .T. ) ;
#23190=DIRECTION ( 'NONE',  ( -1.105928667600727183E-16, 1.000000000000000000, 6.607616187506045307E-17 ) ) ;
#23197=FACE_OUTER_BOUND ( 'NONE', #34953, .T. ) ;
#23199=ADVANCED_FACE ( 'NONE', ( #42580 ), #31758, .T. ) ;
#23203=CIRCLE ( 'NONE', #48745, 1.743387098533651480 ) ;
#23205=PLANE ( 'NONE',  #31226 ) ;
#23206=CARTESIAN_POINT ( 'NONE',  ( -1.675814739737315540, 1.582635513994296250, 1.399362935606387470 ) ) ;
#23208=AXIS2_PLACEMENT_3D ( 'NONE', #22381, #6119, #25996 ) ;
#23210=EDGE_CURVE ( 'NONE', #9920, #3300, #39371, .T. ) ;
#23214=CARTESIAN_POINT ( 'NONE',  ( -2.159905143290285601, 5.905511811023623991, 0.1535224723189611284 ) ) ;
#23215=B_SPLINE_CURVE_WITH_KNOTS ( 'NONE', 3,
 ( #46332, #10994, #7126, #38866 ),
 .UNSPECIFIED., .F., .F.,
 ( 4, 4 ),
 ( 0.1211873102087489551, 0.1625992483279400380 ),
 .UNSPECIFIED. ) ;
#23217=LINE ( 'NONE', #227, #39106 ) ;
#23222=LINE ( 'NONE', #45681, #3926 ) ;
#23223=ORIENTED_EDGE ( 'NONE', *, *, #47263, .T. ) ;
#23225=EDGE_CURVE ( 'NONE', #13914, #49472, #6211, .T. ) ;
#23226=DIRECTION ( 'NONE',  ( 0.01601477604151182663, -0.9998717552508123996, 0.000000000000000000 ) ) ;
#23228=CARTESIAN_POINT ( 'NONE',  ( -0.9149808212874269708, 1.594821661612501940, -2.013400720915880626 ) ) ;
#23231=CARTESIAN_POINT ( 'NONE',  ( 1.325491792074624087, 1.739919523179865202, -2.638988599164732385 ) ) ;
#23232=DIRECTION ( 'NONE',  ( -3.986037398843765983E-20, -1.000000000000000000, -1.160734090543304660E-16 ) ) ;
#23233=AXIS2_PLACEMENT_3D ( 'NONE', #31325, #31577, #47279 ) ;
#23234=ORIENTED_EDGE ( 'NONE', *, *, #3357, .T. ) ;
#23246=EDGE_CURVE ( 'NONE', #38330, #33353, #38961, .T. ) ;
#23247=VERTEX_POINT ( 'NONE', #36113 ) ;
#23249=ORIENTED_EDGE ( 'NONE', *, *, #35135, .T. ) ;
#23250=ORIENTED_EDGE ( 'NONE', *, *, #30629, .F. ) ;
#23254=FACE_OUTER_BOUND ( 'NONE', #3955, .T. ) ;
#23257=ADVANCED_FACE ( 'NONE', ( #23457 ), #3595, .F. ) ;
#23260=VERTEX_POINT ( 'NONE', #43070 ) ;
#23261=ORIENTED_EDGE ( 'NONE', *, *, #21192, .T. ) ;
#23268=EDGE_CURVE ( 'NONE', #42285, #4915, #19580, .T. ) ;
#23278=VECTOR ( 'NONE', #18263, 39.37007874015748143 ) ;
#23279=ORIENTED_EDGE ( 'NONE', *, *, #40295, .T. ) ;
#23285=EDGE_CURVE ( 'NONE', #1516, #38821, #18445, .T. ) ;
#23287=VERTEX_POINT ( 'NONE', #11841 ) ;
#23288=DIRECTION ( 'NONE',  ( -3.986037398843765983E-20, -1.000000000000000000, -1.160734090543304660E-16 ) ) ;
#23290=DIRECTION ( 'NONE',  ( -0.000000000000000000, 1.000000000000000000, -0.000000000000000000 ) ) ;
#23291=VERTEX_POINT ( 'NONE', #20357 ) ;
#23292=LINE ( 'NONE', #42409, #49890 ) ;
#23293=CARTESIAN_POINT ( 'NONE',  ( 0.6156999374152626325, 1.721443042822825120, -2.415922764597543626 ) ) ;
#23294=CARTESIAN_POINT ( 'NONE',  ( 0.08139965876239094178, 1.610780518492231694, 0.000000000000000000 ) ) ;
#23296=VERTEX_POINT ( 'NONE', #7717 ) ;
#23299=CARTESIAN_POINT ( 'NONE',  ( 0.07982360342473591996, 1.709180471932028711, 0.000000000000000000 ) ) ;
#23305=ORIENTED_EDGE ( 'NONE', *, *, #49650, .T. ) ;
#23306=ORIENTED_EDGE ( 'NONE', *, *, #41150, .F. ) ;
#23308=DIRECTION ( 'NONE',  ( -0.9195277725514544587, 0.000000000000000000, 0.3930250316539147803 ) ) ;
#23309=CARTESIAN_POINT ( 'NONE',  ( 2.151809081513405886, 1.574803149606302854, 0.2418202932658659043 ) ) ;
#23312=CIRCLE ( 'NONE', #6035, 1.850107469027523432 ) ;
#23315=DIRECTION ( 'NONE',  ( -0.01601477604151182663, 0.9998717552508123996, -0.000000000000000000 ) ) ;
#23316=VERTEX_POINT ( 'NONE', #32245 ) ;
#23317=ORIENTED_EDGE ( 'NONE', *, *, #45713, .F. ) ;
#23319=LINE ( 'NONE', #19440, #3600 ) ;
#23328=ADVANCED_FACE ( 'NONE', ( #12105 ), #35854, .T. ) ;
#23335=ORIENTED_EDGE ( 'NONE', *, *, #4075, .T. ) ;
#23336=CARTESIAN_POINT ( 'NONE',  ( -0.04921259842519767197, 6.692913385826772199, 2.164795024401847456 ) ) ;
#23339=ORIENTED_EDGE ( 'NONE', *, *, #9929, .T. ) ;
#23345=CARTESIAN_POINT ( 'NONE',  ( 2.867773316779195447, 1.763947033723992641, -0.7050287376752004675 ) ) ;
#23348=ADVANCED_FACE ( 'NONE', ( #47169 ), #43585, .T. ) ;
#23362=CARTESIAN_POINT ( 'NONE',  ( 2.012225602506017452, 1.648623513513363559, -1.855798130189954875 ) ) ;
#23364=DIRECTION ( 'NONE',  ( -5.695547044540863592E-17, 1.000000000000000000, 1.156482317317871725E-16 ) ) ;
#23371=CARTESIAN_POINT ( 'NONE',  ( -1.410501566226149750, -1.929059041884500851E-16, 1.689247093817288992 ) ) ;
#23372=ORIENTED_EDGE ( 'NONE', *, *, #30289, .F. ) ;
#23373=LINE ( 'NONE', #23128, #36451 ) ;
#23377=ORIENTED_EDGE ( 'NONE', *, *, #50402, .T. ) ;
#23378=ORIENTED_EDGE ( 'NONE', *, *, #25319, .F. ) ;
#23381=AXIS2_PLACEMENT_3D ( 'NONE', #43754, #48628, #8410 ) ;
#23382=EDGE_CURVE ( 'NONE', #25003, #3200, #6729, .T. ) ;
#23385=CARTESIAN_POINT ( 'NONE',  ( -0.8329809839909438907, 1.607838722253305486, -2.833254665166566877 ) ) ;
#23391=ADVANCED_FACE ( 'NONE', ( #32505 ), #16131, .T. ) ;
#23392=CARTESIAN_POINT ( 'NONE',  ( 0.000000000000000000, 1.574803149606302854, 0.000000000000000000 ) ) ;
#23398=CARTESIAN_POINT ( 'NONE',  ( 1.722315188406978059, 1.746093451223542869, -2.398471789169309254 ) ) ;
#23399=CARTESIAN_POINT ( 'NONE',  ( 1.887300604142603921, 1.205361022782829114E-17, 0.9597141752041703500 ) ) ;
#23403=DIRECTION ( 'NONE',  ( -0.08963930890344089242, 0.000000000000000000, 0.9959742939952384022 ) ) ;
#23404=ORIENTED_EDGE ( 'NONE', *, *, #9244, .F. ) ;
#23407=EDGE_CURVE ( 'NONE', #44687, #39932, #5635, .T. ) ;
#23412=FACE_OUTER_BOUND ( 'NONE', #49622, .T. ) ;
#23416=ORIENTED_EDGE ( 'NONE', *, *, #18118, .F. ) ;
#23417=ORIENTED_EDGE ( 'NONE', *, *, #15690, .T. ) ;
#23421=CARTESIAN_POINT ( 'NONE',  ( -0.9052394800409759856, 1.701262340642498039, 2.552059238346994441 ) ) ;
#23424=ORIENTED_EDGE ( 'NONE', *, *, #4177, .T. ) ;
#23426=AXIS2_PLACEMENT_3D ( 'NONE', #12883, #8494, #17516 ) ;
#23437=VERTEX_POINT ( 'NONE', #9509 ) ;
#23442=DIRECTION ( 'NONE',  ( -0.01601477604151182663, 0.9998717552508123996, -0.000000000000000000 ) ) ;
#23444=CARTESIAN_POINT ( 'NONE',  ( 2.145564543721536044, 1.465965819140030213, -2.028691429575976812 ) ) ;
#23455=DIRECTION ( 'NONE',  ( 0.000000000000000000, 0.000000000000000000, -1.000000000000000000 ) ) ;
#23456=AXIS2_PLACEMENT_3D ( 'NONE', #46728, #27135, #35150 ) ;
#23457=FACE_OUTER_BOUND ( 'NONE', #42575, .T. ) ;
#23458=VECTOR ( 'NONE', #8447, 39.37007874015748143 ) ;
#23462=EDGE_CURVE ( 'NONE', #24015, #43876, #18888, .T. ) ;
#23467=DIRECTION ( 'NONE',  ( 0.000000000000000000, 1.000000000000000000, -0.000000000000000000 ) ) ;
#23469=ORIENTED_EDGE ( 'NONE', *, *, #48322, .F. ) ;
#23472=CARTESIAN_POINT ( 'NONE',  ( -2.100190309385016274, 5.905511811023623991, 0.5298329251847222476 ) ) ;
#23475=B_SPLINE_CURVE_WITH_KNOTS ( 'NONE', 3,
 ( #12059, #27283, #3291, #31947 ),
 .UNSPECIFIED., .F., .F.,
 ( 4, 4 ),
 ( 0.001544765274254495443, 0.004044898643818962448 ),
 .UNSPECIFIED. ) ;
#23478=CARTESIAN_POINT ( 'NONE',  ( 0.000000000000000000, 1.574803149606302854, 0.000000000000000000 ) ) ;
#23483=EDGE_LOOP ( 'NONE', ( #10863, #2757, #33310, #42841 ) ) ;
#23484=LINE ( 'NONE', #15740, #44491 ) ;
#23486=VERTEX_POINT ( 'NONE', #9001 ) ;
#23487=ORIENTED_EDGE ( 'NONE', *, *, #35226, .F. ) ;
#23488=AXIS2_PLACEMENT_3D ( 'NONE', #12825, #39419, #20303 ) ;
#23490=CONICAL_SURFACE ( 'NONE', #1249, 1.850107469027523210, 0.6386652850508578450 ) ;
#23492=DIRECTION ( 'NONE',  ( -3.986037398843765983E-20, -1.000000000000000000, -1.160734090543304660E-16 ) ) ;
#23498=DIRECTION ( 'NONE',  ( 0.000000000000000000, -0.000000000000000000, 1.000000000000000000 ) ) ;
#23500=CARTESIAN_POINT ( 'NONE',  ( 0.1067246931122726866, 0.02962905676920215767, 0.000000000000000000 ) ) ;
#23504=VERTEX_POINT ( 'NONE', #7163 ) ;
#23511=ORIENTED_EDGE ( 'NONE', *, *, #37444, .F. ) ;
#23513=CARTESIAN_POINT ( 'NONE',  ( -2.122091976112999490, 5.905511811023623991, 0.4338754535132827161 ) ) ;
#23514=CARTESIAN_POINT ( 'NONE',  ( -2.689601439366095192, 1.673243075243657563, -0.07152793773621130002 ) ) ;
#23518=CARTESIAN_POINT ( 'NONE',  ( 0.08139965876239094178, 1.610780518492231694, 0.000000000000000000 ) ) ;
#23520=DIRECTION ( 'NONE',  ( 0.000000000000000000, 0.000000000000000000, 1.000000000000000000 ) ) ;
#23524=CARTESIAN_POINT ( 'NONE',  ( -0.9836083787002329881, 5.905511811023623991, -1.929060376159713375 ) ) ;
#23528=ORIENTED_EDGE ( 'NONE', *, *, #2616, .T. ) ;
#23531=CARTESIAN_POINT ( 'NONE',  ( 0.5114069481605333367, 0.000000000000000000, -1.915028406767218749 ) ) ;
#23535=VECTOR ( 'NONE', #19411, 39.37007874015748143 ) ;
#23537=DIRECTION ( 'NONE',  ( -3.986037398843765983E-20, -1.000000000000000000, -1.160734090543304660E-16 ) ) ;
#23542=DIRECTION ( 'NONE',  ( -3.986037398843765983E-20, -1.000000000000000000, -1.160734090543304660E-16 ) ) ;
#23543=CARTESIAN_POINT ( 'NONE',  ( -1.662320194739477452, 1.205361022782829114E-17, -1.388601395075575784 ) ) ;
#23544=CARTESIAN_POINT ( 'NONE',  ( 1.598711713508005117, 1.574803149606302854, -1.460438370699377986 ) ) ;
#23545=EDGE_CURVE ( 'NONE', #31120, #30710, #11025, .T. ) ;
#23549=ORIENTED_EDGE ( 'NONE', *, *, #3298, .T. ) ;
#23559=CARTESIAN_POINT ( 'NONE',  ( -2.491402175429631605, 1.567214198537667302, -1.585592796919542025 ) ) ;
#23561=DIRECTION ( 'NONE',  ( -0.000000000000000000, -1.000000000000000000, -0.000000000000000000 ) ) ;
#23562=ORIENTED_EDGE ( 'NONE', *, *, #11258, .T. ) ;
#23571=CARTESIAN_POINT ( 'NONE',  ( -1.971247363764855098, 6.692913385826772199, -0.8960709840011926719 ) ) ;
#23575=CARTESIAN_POINT ( 'NONE',  ( -0.5324620714980967673, 1.707112762236906667, 2.658494868336626737 ) ) ;
#23576=CONICAL_SURFACE ( 'NONE', #8732, 2.246510896728926010, 0.01601546068027819014 ) ;
#23577=FACE_OUTER_BOUND ( 'NONE', #32467, .T. ) ;
#23578=EDGE_CURVE ( 'NONE', #23486, #27371, #17794, .T. ) ;
#23581=B_SPLINE_CURVE_WITH_KNOTS ( 'NONE', 3,
 ( #36000, #39864, #1388, #4756 ),
 .UNSPECIFIED., .F., .F.,
 ( 4, 4 ),
 ( 2.559257443457554172E-07, 0.002500529213542272873 ),
 .UNSPECIFIED. ) ;
#23587=CARTESIAN_POINT ( 'NONE',  ( 2.951990591674675368, 1.765258879000601855, -0.08331184815398361143 ) ) ;
#23589=ADVANCED_FACE ( 'NONE', ( #46117 ), #8690, .T. ) ;
#23591=CARTESIAN_POINT ( 'NONE',  ( -2.121469926805683137, 1.574803149606302854, -0.4337334748181708721 ) ) ;
#23592=VERTEX_POINT ( 'NONE', #25759 ) ;
#23595=ORIENTED_EDGE ( 'NONE', *, *, #38774, .F. ) ;
#23602=DIRECTION ( 'NONE',  ( -0.000000000000000000, -1.000000000000000000, -0.000000000000000000 ) ) ;
#23605=VERTEX_POINT ( 'NONE', #37651 ) ;
#23607=ORIENTED_EDGE ( 'NONE', *, *, #5836, .T. ) ;
#23611=CARTESIAN_POINT ( 'NONE',  ( 0.000000000000000000, 0.000000000000000000, -0.3937007874015748254 ) ) ;
#23612=EDGE_CURVE ( 'NONE', #4851, #28481, #29641, .T. ) ;
#23613=VECTOR ( 'NONE', #27766, 39.37007874015748143 ) ;
#23614=B_SPLINE_CURVE_WITH_KNOTS ( 'NONE', 3,
 ( #44802, #9455, #25197, #38103 ),
 .UNSPECIFIED., .F., .F.,
 ( 4, 4 ),
 ( 0.01452380394872818808, 0.03074912581988934607 ),
 .UNSPECIFIED. ) ;
#23617=CONICAL_SURFACE ( 'NONE', #7959, 3.033577403570480779, 1.554780866114618743 ) ;
#23620=DIRECTION ( 'NONE',  ( -4.561975526775602830E-17, -1.000000000000000000, -1.067327232801823148E-16 ) ) ;
#23622=VERTEX_POINT ( 'NONE', #46365 ) ;
#23624=CARTESIAN_POINT ( 'NONE',  ( 1.772877181557974025, 1.670681026536232405, 1.476767650018351752 ) ) ;
#23625=CARTESIAN_POINT ( 'NONE',  ( -1.405664884363581502, 1.586962458333645021, 1.683711065981816857 ) ) ;
#23626=EDGE_CURVE ( 'NONE', #19859, #16076, #19598, .T. ) ;
#23631=CARTESIAN_POINT ( 'NONE',  ( -1.775400203342670347, 1.691590761327236958, -2.359903268218729089 ) ) ;
#23632=ORIENTED_EDGE ( 'NONE', *, *, #14138, .F. ) ;
#23633=CARTESIAN_POINT ( 'NONE',  ( -1.901641471869979894, -1.240704811463216626E-16, 1.079202499698820095 ) ) ;
#23634=VERTEX_POINT ( 'NONE', #22150 ) ;
#23636=EDGE_CURVE ( 'NONE', #35692, #18948, #23658, .T. ) ;
#23637=CARTESIAN_POINT ( 'NONE',  ( 0.000000000000000000, 6.692913385826772199, -2.165354330708661568 ) ) ;
#23638=EDGE_CURVE ( 'NONE', #25781, #43935, #6090, .T. ) ;
#23639=AXIS2_PLACEMENT_3D ( 'NONE', #15418, #23403, #19781 ) ;
#23640=ORIENTED_EDGE ( 'NONE', *, *, #50678, .T. ) ;
#23642=CARTESIAN_POINT ( 'NONE',  ( -1.591447364397243103, 0.002429723416550041374, -0.7337366736851151927 ) ) ;
#23644=ORIENTED_EDGE ( 'NONE', *, *, #3076, .T. ) ;
#23650=LINE ( 'NONE', #3782, #20096 ) ;
#23653=AXIS2_PLACEMENT_3D ( 'NONE', #22998, #3372, #15746 ) ;
#23655=CARTESIAN_POINT ( 'NONE',  ( 1.956192433058983493, 0.05925166736471587647, -0.03859050128386512513 ) ) ;
#23658=LINE ( 'NONE', #419, #36744 ) ;
#23660=VERTEX_POINT ( 'NONE', #15414 ) ;
#23663=ORIENTED_EDGE ( 'NONE', *, *, #30595, .F. ) ;
#23667=PLANE ( 'NONE',  #24101 ) ;
#23671=B_SPLINE_CURVE_WITH_KNOTS ( 'NONE', 3,
 ( #37896, #10258, #11274, #7401 ),
 .UNSPECIFIED., .F., .F.,
 ( 4, 4 ),
 ( 0.1211873102087489551, 0.1625992483279400380 ),
 .UNSPECIFIED. ) ;
#23672=DIRECTION ( 'NONE',  ( 0.2225209339563184452, 0.000000000000000000, -0.9749279121818227312 ) ) ;
#23673=CARTESIAN_POINT ( 'NONE',  ( 0.2430652128771964016, 5.905511811023623991, -2.151668812760858085 ) ) ;
#23679=ORIENTED_EDGE ( 'NONE', *, *, #11485, .T. ) ;
#23681=EDGE_CURVE ( 'NONE', #27359, #50172, #43523, .T. ) ;
#23685=LINE ( 'NONE', #35061, #16187 ) ;
#23686=ORIENTED_EDGE ( 'NONE', *, *, #43956, .F. ) ;
#23687=EDGE_CURVE ( 'NONE', #2040, #35748, #22731, .T. ) ;
#23688=CARTESIAN_POINT ( 'NONE',  ( 1.905671854841463952, 1.472358791367697650, 2.256015092822682089 ) ) ;
#23690=CARTESIAN_POINT ( 'NONE',  ( 0.8329809839909855240, 5.905511811023623991, -2.833254665166554442 ) ) ;
#23699=ORIENTED_EDGE ( 'NONE', *, *, #22437, .T. ) ;
#23702=EDGE_CURVE ( 'NONE', #17198, #18215, #32623, .T. ) ;
#23707=ORIENTED_EDGE ( 'NONE', *, *, #24265, .T. ) ;
#23712=CARTESIAN_POINT ( 'NONE',  ( -2.464291103507775915, 0.000000000000000000, -1.626664315311338260 ) ) ;
#23719=CARTESIAN_POINT ( 'NONE',  ( 2.165460538733997353, 0.000000000000000000, 0.04798874274655835076 ) ) ;
#23723=DIRECTION ( 'NONE',  ( 0.7227948638273880011, 0.000000000000000000, 0.6910626489868685329 ) ) ;
#23725=ORIENTED_EDGE ( 'NONE', *, *, #45996, .F. ) ;
#23726=CARTESIAN_POINT ( 'NONE',  ( 1.661821349926414726, 1.574803149606302854, 1.388203579611976268 ) ) ;
#23729=DIRECTION ( 'NONE',  ( 0.2225209339563041788, 0.000000000000000000, 0.9749279121818259508 ) ) ;
#23739=PRODUCT_DEFINITION ( 'UNKNOWN', '', #35814, #24727 ) ;
#23741=CARTESIAN_POINT ( 'NONE',  ( 0.002207914879453961535, -5.712274067634378313E-18, 0.04916304461325374242 ) ) ;
#23743=AXIS2_PLACEMENT_3D ( 'NONE', #11673, #23290, #31817 ) ;
#23747=CARTESIAN_POINT ( 'NONE',  ( -0.8069532150559458605, 0.000000000000000000, -2.010061882867143268 ) ) ;
#23749=ORIENTED_EDGE ( 'NONE', *, *, #42491, .T. ) ;
#23750=CARTESIAN_POINT ( 'NONE',  ( 1.979793062125284830, 1.470624965921384364, 2.191257344206569257 ) ) ;
#23753=VECTOR ( 'NONE', #5229, 39.37007874015748143 ) ;
#23764=EDGE_LOOP ( 'NONE', ( #46898, #27931, #2052, #8926 ) ) ;
#23773=ORIENTED_EDGE ( 'NONE', *, *, #18697, .T. ) ;
#23784=FACE_OUTER_BOUND ( 'NONE', #9997, .T. ) ;
#23791=CIRCLE ( 'NONE', #1546, 2.165354330708661568 ) ;
#23793=FACE_OUTER_BOUND ( 'NONE', #41997, .T. ) ;
#23794=CARTESIAN_POINT ( 'NONE',  ( 2.576863348864710801, 0.000000000000000000, 1.442554885838449819 ) ) ;
#23796=VECTOR ( 'NONE', #6962, 39.37007874015748143 ) ;
#23797=ORIENTED_EDGE ( 'NONE', *, *, #35713, .F. ) ;
#23799=ORIENTED_EDGE ( 'NONE', *, *, #37248, .T. ) ;
#23801=DIRECTION ( 'NONE',  ( -3.986037398843765983E-20, -1.000000000000000000, -1.160734090543304660E-16 ) ) ;
#23805=CARTESIAN_POINT ( 'NONE',  ( 0.5544985201248122664, 1.716783259433079856, -2.194164409418295048 ) ) ;
#23807=ADVANCED_FACE ( 'NONE', ( #17895 ), #40185, .T. ) ;
#23810=VERTEX_POINT ( 'NONE', #28292 ) ;
#23820=DIRECTION ( 'NONE',  ( -0.8345732537213079727, -6.391122427287080193E-17, 0.5508969814520945363 ) ) ;
#23822=CIRCLE ( 'NONE', #27944, 1.743387098533651480 ) ;
#23824=ORIENTED_EDGE ( 'NONE', *, *, #29200, .T. ) ;
#23827=EDGE_LOOP ( 'NONE', ( #46956, #38738, #48243, #12828 ) ) ;
#23828=CARTESIAN_POINT ( 'NONE',  ( -1.236813753895212642, 1.541669022091038732, -2.681693691597581974 ) ) ;
#23832=CARTESIAN_POINT ( 'NONE',  ( -0.9106291036520693938, 1.598827635308956108, 2.286305300140973440 ) ) ;
#23834=AXIS2_PLACEMENT_3D ( 'NONE', #2201, #18454, #49644 ) ;
#23837=CARTESIAN_POINT ( 'NONE',  ( -1.930378847043046964, 1.689166098830295892, 2.234429243796722808 ) ) ;
#23838=CARTESIAN_POINT ( 'NONE',  ( 1.461363083917469829, 1.574803149606302854, 1.597866488315584865 ) ) ;
#23840=ORIENTED_EDGE ( 'NONE', *, *, #33162, .T. ) ;
#23841=VERTEX_POINT ( 'NONE', #13769 ) ;
#23842=VECTOR ( 'NONE', #11230, 39.37007874015748143 ) ;
#23843=ORIENTED_EDGE ( 'NONE', *, *, #8020, .T. ) ;
#23845=EDGE_CURVE ( 'NONE', #32006, #49770, #14271, .T. ) ;
#23846=CARTESIAN_POINT ( 'NONE',  ( -1.252056778656947422, 1.687847970117562602, -1.807033786809818077 ) ) ;
#23849=DIRECTION ( 'NONE',  ( 1.160734090543304660E-16, -1.000000000000000000, -0.000000000000000000 ) ) ;
#23851=DIRECTION ( 'NONE',  ( 0.9998717552508121775, 0.01601477604151182663, 0.000000000000000000 ) ) ;
#23853=PLANE ( 'NONE',  #50388 ) ;
#23855=EDGE_LOOP ( 'NONE', ( #3438, #24132, #27847, #16159 ) ) ;
#23856=CARTESIAN_POINT ( 'NONE',  ( 2.932638728931774352, 1.764957438482779528, 0.3475908556738225297 ) ) ;
#23857=CARTESIAN_POINT ( 'NONE',  ( -1.229551338856769371, 1.049866565067838264, -1.608606759830606858 ) ) ;
#23858=( BOUNDED_CURVE ( )  B_SPLINE_CURVE ( 3, ( #17778, #25269, #41027, #25521 ),
 .UNSPECIFIED., .F., .F. ) 
 B_SPLINE_CURVE_WITH_KNOTS ( ( 4, 4 ),
 ( 2.000194674521101224, 2.051115727886003270 ),
 .UNSPECIFIED. ) 
 CURVE ( )  GEOMETRIC_REPRESENTATION_ITEM ( )  RATIONAL_B_SPLINE_CURVE ( ( 1.000000000000000000, 0.9997839321993498007, 0.9997839321993498007, 1.000000000000000000 ) ) 
 REPRESENTATION_ITEM ( '' )  );
#23860=VECTOR ( 'NONE', #16147, 39.37007874015748143 ) ;
#23862=CARTESIAN_POINT ( 'NONE',  ( -1.735432873265435161, 1.581680620477750931, 1.321016258651915409 ) ) ;
#23864=CARTESIAN_POINT ( 'NONE',  ( 2.623503965249849301, 1.455362298632098428, 1.355882097269874187 ) ) ;
#23865=ORIENTED_EDGE ( 'NONE', *, *, #26200, .T. ) ;
#23867=DIRECTION ( 'NONE',  ( -0.000000000000000000, -1.000000000000000000, -0.000000000000000000 ) ) ;
#23869=DIRECTION ( 'NONE',  ( 1.042246309067994810E-16, 1.000000000000000000, 7.572362681945316160E-17 ) ) ;
#23871=AXIS2_PLACEMENT_3D ( 'NONE', #4665, #40298, #20407 ) ;
#23872=CARTESIAN_POINT ( 'NONE',  ( -1.145994540540797635, 0.003253507172150460220, 1.386494442623789070 ) ) ;
#23876=MANIFOLD_SOLID_BREP ( 'Cut-Revolve2', #11415 ) ;
#23878=VERTEX_POINT ( 'NONE', #49842 ) ;
#23879=DIRECTION ( 'NONE',  ( -0.000000000000000000, -1.000000000000000000, -0.000000000000000000 ) ) ;
#23881=ORIENTED_EDGE ( 'NONE', *, *, #26822, .T. ) ;
#23888=ORIENTED_EDGE ( 'NONE', *, *, #5928, .T. ) ;
#23897=VERTEX_POINT ( 'NONE', #37780 ) ;
#23898=DIRECTION ( 'NONE',  ( -3.986037398843765983E-20, -1.000000000000000000, -1.160734090543304660E-16 ) ) ;
#23904=VERTEX_POINT ( 'NONE', #3155 ) ;
#23907=DIRECTION ( 'NONE',  ( 0.01601477604151182663, -0.9998717552508123996, 0.000000000000000000 ) ) ;
#23909=AXIS2_PLACEMENT_3D ( 'NONE', #23081, #38829, #17118 ) ;
#23913=EDGE_CURVE ( 'NONE', #12429, #17233, #27691, .T. ) ;
#23917=FACE_OUTER_BOUND ( 'NONE', #38452, .T. ) ;
#23919=CARTESIAN_POINT ( 'NONE',  ( -3.073077335812187894, 5.118110236220475784, 0.6509316561051814443 ) ) ;
#23922=CARTESIAN_POINT ( 'NONE',  ( -0.4350747367504783636, 0.000000000000000000, -2.121846421795421378 ) ) ;
#23925=CARTESIAN_POINT ( 'NONE',  ( 1.747029694980739345, 6.692913385826772199, 1.330264415365525421 ) ) ;
#23926=CARTESIAN_POINT ( 'NONE',  ( 2.875072944275708586, 1.448522234753447657, -0.6730469799666056741 ) ) ;
#23928=CARTESIAN_POINT ( 'NONE',  ( 2.017818867441111497, 0.03950160972893088096, -0.04135814764324683562 ) ) ;
#23930=ORIENTED_EDGE ( 'NONE', *, *, #40432, .T. ) ;
#23932=DIRECTION ( 'NONE',  ( -0.9998717552508122886, -0.01601477604151182316, 0.000000000000000000 ) ) ;
#23933=EDGE_CURVE ( 'NONE', #49753, #34884, #3786, .T. ) ;
#23937=EDGE_CURVE ( 'NONE', #27371, #48222, #11156, .T. ) ;
#23941=EDGE_CURVE ( 'NONE', #45425, #49792, #2652, .T. ) ;
#23943=DIRECTION ( 'NONE',  ( -0.000000000000000000, -1.000000000000000000, -0.000000000000000000 ) ) ;
#23952=VERTEX_POINT ( 'NONE', #42887 ) ;
#23965=PLANE ( 'NONE',  #43129 ) ;
#23966=ADVANCED_FACE ( 'NONE', ( #50587 ), #46610, .T. ) ;
#23968=ORIENTED_EDGE ( 'NONE', *, *, #2265, .T. ) ;
#23972=DIRECTION ( 'NONE',  ( -8.021399753802077430E-17, -1.000000000000000000, -8.389726389140663754E-17 ) ) ;
#23974=CARTESIAN_POINT ( 'NONE',  ( 1.836043989102772445, 1.744310788554293890, 2.026723291277686467 ) ) ;
#23976=EDGE_CURVE ( 'NONE', #34134, #16416, #50704, .T. ) ;
#23977=CARTESIAN_POINT ( 'NONE',  ( -1.779568955232875060, 1.574803149606302854, -1.233650562797313555 ) ) ;
#23979=CONICAL_SURFACE ( 'NONE', #9131, 2.244934639244524632, 1.554780866114618743 ) ;
#23988=CARTESIAN_POINT ( 'NONE',  ( -0.5286458662987743029, 0.000000000000000000, 2.100489422084707680 ) ) ;
#23993=CARTESIAN_POINT ( 'NONE',  ( 0.8454231601665999074, 1.623017753118757067, 2.112564685048140323 ) ) ;
#23998=CARTESIAN_POINT ( 'NONE',  ( 2.755905511811024056, 4.960629921259846142, 1.023622047244094446 ) ) ;
#23999=DIRECTION ( 'NONE',  ( -7.460697193978162709E-14, 0.000000000000000000, 1.000000000000000000 ) ) ;
#24001=VERTEX_POINT ( 'NONE', #47750 ) ;
#24003=CARTESIAN_POINT ( 'NONE',  ( 0.000000000000000000, 1.574803149606302854, 0.000000000000000000 ) ) ;
#24008=ORIENTED_EDGE ( 'NONE', *, *, #18560, .T. ) ;
#24013=CARTESIAN_POINT ( 'NONE',  ( 2.164971648505046975, 6.332733149760729319, -0.04070796836118365652 ) ) ;
#24015=VERTEX_POINT ( 'NONE', #288 ) ;
#24022=DIRECTION ( 'NONE',  ( -0.01601477604151182663, 0.9998717552508123996, -0.000000000000000000 ) ) ;
#24027=EDGE_CURVE ( 'NONE', #22069, #47632, #12167, .T. ) ;
#24028=CARTESIAN_POINT ( 'NONE',  ( -1.525880051666119286, 0.002351180378572883568, 0.8769966569942660994 ) ) ;
#24039=CARTESIAN_POINT ( 'NONE',  ( 2.339241080213585899, 1.657243480315735873, 1.802537235681917815 ) ) ;
#24041=ORIENTED_EDGE ( 'NONE', *, *, #40733, .F. ) ;
#24051=ORIENTED_EDGE ( 'NONE', *, *, #14138, .T. ) ;
#24052=AXIS2_PLACEMENT_3D ( 'NONE', #17667, #21796, #41169 ) ;
#24056=CONICAL_SURFACE ( 'NONE', #44648, 2.244934639244524632, 1.554780866114618743 ) ;
#24057=ORIENTED_EDGE ( 'NONE', *, *, #15804, .F. ) ;
#24059=EDGE_LOOP ( 'NONE', ( #7385, #9340, #754, #19599, #5613, #12133, #816, #46255, #1898, #35892, #19040 ) ) ;
#24061=CARTESIAN_POINT ( 'NONE',  ( 0.6507993007407579800, 1.619900495825837838, -2.173134161263437392 ) ) ;
#24063=CARTESIAN_POINT ( 'NONE',  ( -1.159317824364283211, 0.5241370646666094757, 1.844421372722656161 ) ) ;
#24067=DIRECTION ( 'NONE',  ( -0.000000000000000000, 1.000000000000000000, -0.000000000000000000 ) ) ;
#24069=ORIENTED_EDGE ( 'NONE', *, *, #16779, .F. ) ;
#24075=ORIENTED_EDGE ( 'NONE', *, *, #25968, .T. ) ;
#24078=CARTESIAN_POINT ( 'NONE',  ( -0.6584127755596833609, 0.000000000000000000, 1.614277297217976859 ) ) ;
#24084=CARTESIAN_POINT ( 'NONE',  ( -2.947574761915765063, 5.905511811023623991, -0.1816379373805338815 ) ) ;
#24086=VERTEX_POINT ( 'NONE', #23524 ) ;
#24095=CIRCLE ( 'NONE', #36447, 2.165354330708661568 ) ;
#24096=EDGE_CURVE ( 'NONE', #16446, #45550, #19646, .T. ) ;
#24101=AXIS2_PLACEMENT_3D ( 'NONE', #4569, #19787, #20308 ) ;
#24102=ADVANCED_FACE ( 'NONE', ( #37471 ), #18646, .T. ) ;
#24104=CARTESIAN_POINT ( 'NONE',  ( -1.936609506549060722, 1.676883605369557051, 0.9862484270667263297 ) ) ;
#24105=CARTESIAN_POINT ( 'NONE',  ( -2.152441353505195387, 0.000000000000000000, -0.2419059403265113872 ) ) ;
#24108=CARTESIAN_POINT ( 'NONE',  ( 0.000000000000000000, 6.692913385826772199, 0.000000000000000000 ) ) ;
#24111=FACE_OUTER_BOUND ( 'NONE', #17790, .T. ) ;
#24115=ORIENTED_EDGE ( 'NONE', *, *, #8624, .T. ) ;
#24116=FACE_OUTER_BOUND ( 'NONE', #49235, .T. ) ;
#24123=VERTEX_POINT ( 'NONE', #28933 ) ;
#24124=PLANE ( 'NONE',  #31165 ) ;
#24132=ORIENTED_EDGE ( 'NONE', *, *, #12810, .T. ) ;
#24134=DIRECTION ( 'NONE',  ( -0.000000000000000000, -1.000000000000000000, -0.000000000000000000 ) ) ;
#24138=LINE ( 'NONE', #28770, #27698 ) ;
#24142=DIRECTION ( 'NONE',  ( 3.586865599282426309E-17, -1.000000000000000000, -1.103923720497134591E-16 ) ) ;
#24144=VERTEX_POINT ( 'NONE', #2345 ) ;
#24151=CIRCLE ( 'NONE', #15089, 2.165354330708661568 ) ;
#24153=ADVANCED_FACE ( 'NONE', ( #49025 ), #13455, .T. ) ;
#24154=CARTESIAN_POINT ( 'NONE',  ( 1.940248144014060205, 1.742434946120271055, 1.610241538648720105 ) ) ;
#24163=VERTEX_POINT ( 'NONE', #5709 ) ;
#24164=DIRECTION ( 'NONE',  ( 0.6910626489868580968, 0.000000000000000000, 0.7227948638273978821 ) ) ;
#24166=CARTESIAN_POINT ( 'NONE',  ( 2.339241080213585899, 1.462148010760873307, 1.802537235681917815 ) ) ;
#24168=( BOUNDED_CURVE ( )  B_SPLINE_CURVE ( 3, ( #35732, #47567, #27979, #8371 ),
 .UNSPECIFIED., .F., .F. ) 
 B_SPLINE_CURVE_WITH_KNOTS ( ( 4, 4 ),
 ( 4.318880402357613946, 4.369812334041601964 ),
 .UNSPECIFIED. ) 
 CURVE ( )  GEOMETRIC_REPRESENTATION_ITEM ( )  RATIONAL_B_SPLINE_CURVE ( ( 1.000000000000000000, 0.9997838398768879031, 0.9997838398768879031, 1.000000000000000000 ) ) 
 REPRESENTATION_ITEM ( '' )  );
#24169=DIRECTION ( 'NONE',  ( 0.5128992774059071280, 0.000000000000000000, -0.8584487936018655452 ) ) ;
#24173=LINE ( 'NONE', #12037, #22037 ) ;
#24174=CARTESIAN_POINT ( 'NONE',  ( -1.723188456408593527, 1.574803149606302854, 1.311251662046200694 ) ) ;
#24181=ORIENTED_EDGE ( 'NONE', *, *, #23626, .T. ) ;
#24183=DIRECTION ( 'NONE',  ( -0.8584487936018728726, -1.160734090543304907E-16, 0.5128992774058949156 ) ) ;
#24187=DIRECTION ( 'NONE',  ( 0.9998717552508121775, 0.01601477604151182663, 0.000000000000000000 ) ) ;
#24192=CARTESIAN_POINT ( 'NONE',  ( 0.1155636338427008941, -0.5222242541845523167, 0.000000000000000000 ) ) ;
#24194=CARTESIAN_POINT ( 'NONE',  ( 1.531154912952772396, 1.205361022782829114E-17, 1.532020527533857646 ) ) ;
#24199=EDGE_LOOP ( 'NONE', ( #37413, #21918, #21742, #28035, #12726, #41771, #5788, #44231, #16275, #1121, #42162 ) ) ;
#24200=DIRECTION ( 'NONE',  ( 0.000000000000000000, 0.000000000000000000, 1.000000000000000000 ) ) ;
#24202=EDGE_CURVE ( 'NONE', #33287, #34811, #40089, .T. ) ;
#24204=ADVANCED_FACE ( 'NONE', ( #41585 ), #25576, .T. ) ;
#24207=EDGE_CURVE ( 'NONE', #40266, #29332, #46648, .T. ) ;
#24211=B_SPLINE_CURVE_WITH_KNOTS ( 'NONE', 3,
 ( #31339, #36232, #4474, #43444 ),
 .UNSPECIFIED., .F., .F.,
 ( 4, 4 ),
 ( 0.0007442978046650536566, 0.04837702953537185296 ),
 .UNSPECIFIED. ) ;
#24220=EDGE_CURVE ( 'NONE', #36796, #18547, #17330, .T. ) ;
#24221=FACE_OUTER_BOUND ( 'NONE', #46172, .T. ) ;
#24223=DIRECTION ( 'NONE',  ( -1.206139481778036182E-16, 1.000000000000000000, -4.526717189434842013E-17 ) ) ;
#24225=CARTESIAN_POINT ( 'NONE',  ( 1.780101451746606722, 1.205361022782829114E-17, 1.234002060668519585 ) ) ;
#24233=ORIENTED_EDGE ( 'NONE', *, *, #32860, .T. ) ;
#24235=DIRECTION ( 'NONE',  ( 0.000000000000000000, 0.000000000000000000, -1.000000000000000000 ) ) ;
#24236=CARTESIAN_POINT ( 'NONE',  ( -2.168245791271168343, 1.587034731952809752, -2.004968704497279930 ) ) ;
#24239=CARTESIAN_POINT ( 'NONE',  ( 2.875073879017507217, 1.665576751341341089, -0.6730428845952017847 ) ) ;
#24242=ORIENTED_EDGE ( 'NONE', *, *, #5150, .F. ) ;
#24247=CIRCLE ( 'NONE', #12706, 2.164630168518208109 ) ;
#24249=ORIENTED_EDGE ( 'NONE', *, *, #1016, .T. ) ;
#24251=FACE_OUTER_BOUND ( 'NONE', #2787, .T. ) ;
#24255=ORIENTED_EDGE ( 'NONE', *, *, #6212, .F. ) ;
#24265=EDGE_CURVE ( 'NONE', #27692, #5918, #34600, .T. ) ;
#24266=CARTESIAN_POINT ( 'NONE',  ( 0.1067246931122726866, 0.02962905676920215767, 0.000000000000000000 ) ) ;
#24267=ORIENTED_EDGE ( 'NONE', *, *, #35951, .T. ) ;
#24272=EDGE_CURVE ( 'NONE', #31774, #41036, #38167, .T. ) ;
#24273=DIRECTION ( 'NONE',  ( -0.01601477604151182663, 0.9998717552508123996, -0.000000000000000000 ) ) ;
#24276=DIRECTION ( 'NONE',  ( -8.881784197001252323E-16, 0.000000000000000000, 1.000000000000000000 ) ) ;
#24279=ORIENTED_EDGE ( 'NONE', *, *, #29537, .T. ) ;
#24284=CARTESIAN_POINT ( 'NONE',  ( 2.755905511811024056, 4.960629921259846142, 1.023622047244094446 ) ) ;
#24285=CIRCLE ( 'NONE', #30037, 2.164630168518208109 ) ;
#24294=DIRECTION ( 'NONE',  ( 0.000000000000000000, 0.000000000000000000, 1.000000000000000000 ) ) ;
#24295=DIRECTION ( 'NONE',  ( 0.9749279121818227312, 0.000000000000000000, 0.2225209339563184452 ) ) ;
#24296=EDGE_CURVE ( 'NONE', #6941, #17122, #36876, .T. ) ;
#24299=CARTESIAN_POINT ( 'NONE',  ( -0.8429824507881226170, 1.205361022782829114E-17, -1.637047627937372241 ) ) ;
#24302=CARTESIAN_POINT ( 'NONE',  ( -1.905671854841497481, 5.905511811023623991, 2.256015092822653667 ) ) ;
#24306=ORIENTED_EDGE ( 'NONE', *, *, #17306, .T. ) ;
#24308=CARTESIAN_POINT ( 'NONE',  ( -0.4462886659516242527, 1.602328624241157851, 2.183640264916793861 ) ) ;
#24310=CARTESIAN_POINT ( 'NONE',  ( 1.709950266952970921, 0.000000000000000000, -0.3398067978735070382 ) ) ;
#24312=AXIS2_PLACEMENT_3D ( 'NONE', #31281, #3911, #35657 ) ;
#24316=ORIENTED_EDGE ( 'NONE', *, *, #17111, .F. ) ;
#24320=DIRECTION ( 'NONE',  ( 0.000000000000000000, 0.000000000000000000, 1.000000000000000000 ) ) ;
#24323=ORIENTED_EDGE ( 'NONE', *, *, #37346, .F. ) ;
#24326=ORIENTED_EDGE ( 'NONE', *, *, #33271, .T. ) ;
#24330=ORIENTED_EDGE ( 'NONE', *, *, #19155, .T. ) ;
#24334=CARTESIAN_POINT ( 'NONE',  ( 1.773598097765477277, 1.637884173412089250, 1.477342561509449759 ) ) ;
#24335=EDGE_CURVE ( 'NONE', #41856, #29553, #28544, .T. ) ;
#24337=CYLINDRICAL_SURFACE ( 'NONE', #32932, 2.164630168518208109 ) ;
#24341=CARTESIAN_POINT ( 'NONE',  ( -1.088998432874329403, -2.184998798188223135E-16, 1.918626195649137278 ) ) ;
#24342=CARTESIAN_POINT ( 'NONE',  ( -0.04921259842519706829, 1.707113721008201024, 2.241222193722145484 ) ) ;
#24346=ORIENTED_EDGE ( 'NONE', *, *, #24991, .T. ) ;
#24348=CARTESIAN_POINT ( 'NONE',  ( 0.000000000000000000, 5.905511811023623991, 0.000000000000000000 ) ) ;
#24354=AXIS2_PLACEMENT_3D ( 'NONE', #26610, #7501, #27111 ) ;
#24358=CARTESIAN_POINT ( 'NONE',  ( 0.000000000000000000, 1.574803149606302854, 0.000000000000000000 ) ) ;
#24359=CARTESIAN_POINT ( 'NONE',  ( -2.437180031585919782, 5.905511811023623991, -1.667735833703135162 ) ) ;
#24360=AXIS2_PLACEMENT_3D ( 'NONE', #15795, #40334, #32331 ) ;
#24361=B_SPLINE_CURVE_WITH_KNOTS ( 'NONE', 3,
 ( #11347, #3854, #46925, #50773 ),
 .UNSPECIFIED., .F., .F.,
 ( 4, 4 ),
 ( 2.008334170439436058E-07, 0.002500502013016788969 ),
 .UNSPECIFIED. ) ;
#24369=FACE_OUTER_BOUND ( 'NONE', #48843, .T. ) ;
#24370=ORIENTED_EDGE ( 'NONE', *, *, #25550, .F. ) ;
#24372=CARTESIAN_POINT ( 'NONE',  ( -0.8013547812368906342, 1.706765689785105788, -2.841982942531803502 ) ) ;
#24385=CARTESIAN_POINT ( 'NONE',  ( -0.8987785766980536106, 1.205361022782829114E-17, 1.600251783270283390 ) ) ;
#24390=CARTESIAN_POINT ( 'NONE',  ( -2.932023289724621673, 1.575122962489508449, 0.3475074887687388259 ) ) ;
#24396=DIRECTION ( 'NONE',  ( 0.000000000000000000, -1.000000000000000000, 0.000000000000000000 ) ) ;
#24400=VERTEX_POINT ( 'NONE', #34013 ) ;
#24412=ORIENTED_EDGE ( 'NONE', *, *, #45810, .F. ) ;
#24414=DIRECTION ( 'NONE',  ( -3.986037398843765983E-20, -1.000000000000000000, -1.160734090543304660E-16 ) ) ;
#24419=ORIENTED_EDGE ( 'NONE', *, *, #38179, .T. ) ;
#24420=EDGE_CURVE ( 'NONE', #29695, #17626, #3822, .T. ) ;
#24424=B_SPLINE_CURVE_WITH_KNOTS ( 'NONE', 3,
 ( #34337, #19069, #34582, #38952 ),
 .UNSPECIFIED., .F., .F.,
 ( 4, 4 ),
 ( 2.766470520694630865E-07, 0.002500519372013545929 ),
 .UNSPECIFIED. ) ;
#24425=B_SPLINE_CURVE_WITH_KNOTS ( 'NONE', 3,
 ( #38344, #42198, #39272, #19639 ),
 .UNSPECIFIED., .F., .F.,
 ( 4, 4 ),
 ( 2.330000271410587266E-07, 0.002500456604366177622 ),
 .UNSPECIFIED. ) ;
#24427=AXIS2_PLACEMENT_3D ( 'NONE', #18145, #4681, #23520 ) ;
#24428=DIRECTION ( 'NONE',  ( -1.000000000000000000, 0.000000000000000000, -0.000000000000000000 ) ) ;
#24429=DIRECTION ( 'NONE',  ( -0.01601477604151182663, 0.9998717552508123996, -0.000000000000000000 ) ) ;
#24436=EDGE_CURVE ( 'NONE', #34370, #36292, #29876, .T. ) ;
#24444=CARTESIAN_POINT ( 'NONE',  ( 1.215401739843891216, 1.661752038239891593, 1.938290036035023034 ) ) ;
#24449=DIRECTION ( 'NONE',  ( -0.000000000000000000, -1.000000000000000000, -0.000000000000000000 ) ) ;
#24450=ORIENTED_EDGE ( 'NONE', *, *, #3198, .T. ) ;
#24451=DIRECTION ( 'NONE',  ( -0.01601477604151182663, 0.9998717552508123996, -0.000000000000000000 ) ) ;
#24452=DIRECTION ( 'NONE',  ( 0.01601477604151182663, -0.9998717552508123996, 0.000000000000000000 ) ) ;
#24453=B_SPLINE_CURVE_WITH_KNOTS ( 'NONE', 3,
 ( #24078, #47785, #3953, #35699 ),
 .UNSPECIFIED., .F., .F.,
 ( 4, 4 ),
 ( 0.1211873102087489551, 0.1625992483279400380 ),
 .UNSPECIFIED. ) ;
#24459=ORIENTED_EDGE ( 'NONE', *, *, #41088, .T. ) ;
#24460=CARTESIAN_POINT ( 'NONE',  ( -2.074049943651441019, 6.692913385826772199, 0.6221544894623932676 ) ) ;
#24470=ORIENTED_EDGE ( 'NONE', *, *, #7393, .T. ) ;
#24471=AXIS2_PLACEMENT_3D ( 'NONE', #24358, #31597, #27708 ) ;
#24473=ORIENTED_EDGE ( 'NONE', *, *, #21321, .T. ) ;
#24478=FACE_OUTER_BOUND ( 'NONE', #36658, .T. ) ;
#24480=ORIENTED_EDGE ( 'NONE', *, *, #43477, .F. ) ;
#24482=EDGE_LOOP ( 'NONE', ( #20133, #30623, #36714, #6978 ) ) ;
#24483=CARTESIAN_POINT ( 'NONE',  ( 0.04921259842519669359, 1.610264983814881479, 2.246280244424690320 ) ) ;
#24486=DIRECTION ( 'NONE',  ( -0.9998717552508122886, -0.01601477604151181275, 0.000000000000000000 ) ) ;
#24488=B_SPLINE_CURVE_WITH_KNOTS ( 'NONE', 3,
 ( #29394, #20882, #33543, #40513 ),
 .UNSPECIFIED., .F., .F.,
 ( 4, 4 ),
 ( 2.655981437406432628E-07, 0.002500437702427189216 ),
 .UNSPECIFIED. ) ;
#24489=CARTESIAN_POINT ( 'NONE',  ( -1.477903774005060233, 1.618613820676564341, 1.616798831468284625 ) ) ;
#24490=LINE ( 'NONE', #8996, #2257 ) ;
#24495=CARTESIAN_POINT ( 'NONE',  ( -2.932023289724621673, 1.575122962489508449, 0.3475074887687388259 ) ) ;
#24496=ADVANCED_FACE ( 'NONE', ( #1739 ), #27727, .F. ) ;
#24497=LINE ( 'NONE', #20872, #12796 ) ;
#24499=EDGE_CURVE ( 'NONE', #48342, #26667, #10989, .T. ) ;
#24504=EDGE_CURVE ( 'NONE', #34423, #4372, #25710, .T. ) ;
#24509=DIRECTION ( 'NONE',  ( -0.000000000000000000, -1.000000000000000000, -0.000000000000000000 ) ) ;
#24510=CARTESIAN_POINT ( 'NONE',  ( -1.971247363764854876, 5.905511811023623991, -0.8960709840011923388 ) ) ;
#24513=CARTESIAN_POINT ( 'NONE',  ( -2.104388748321702529, 0.5252928353968839836, -0.4298348072943085629 ) ) ;
#24529=DIRECTION ( 'NONE',  ( -0.4738686624730094055, -1.021948367985145802E-16, 0.8805955318567321166 ) ) ;
#24532=VERTEX_POINT ( 'NONE', #38141 ) ;
#24533=DIRECTION ( 'NONE',  ( 0.000000000000000000, 0.000000000000000000, -1.000000000000000000 ) ) ;
#24535=VERTEX_POINT ( 'NONE', #42245 ) ;
#24537=CARTESIAN_POINT ( 'NONE',  ( 2.002746723317192057, 1.743427769888226786, 1.534191940547938060 ) ) ;
#24542=EDGE_LOOP ( 'NONE', ( #48450, #42117, #12049, #49929 ) ) ;
#24543=CARTESIAN_POINT ( 'NONE',  ( -1.030301126714985971, 0.000000000000000000, -1.501813316714599500 ) ) ;
#24545=DIRECTION ( 'NONE',  ( 0.5877852522924685852, 0.000000000000000000, 0.8090169943749507819 ) ) ;
#24552=B_SPLINE_CURVE_WITH_KNOTS ( 'NONE', 3,
 ( #38550, #2925, #38797, #18673 ),
 .UNSPECIFIED., .F., .F.,
 ( 4, 4 ),
 ( 0.01248276987548075333, 0.03073907100476382798 ),
 .UNSPECIFIED. ) ;
#24559=ORIENTED_EDGE ( 'NONE', *, *, #43600, .F. ) ;
#24562=CARTESIAN_POINT ( 'NONE',  ( 1.879299076413774250, 0.5249316475426859530, -0.1336616210247123793 ) ) ;
#24563=AXIS2_PLACEMENT_3D ( 'NONE', #12769, #40896, #8634 ) ;
#24569=ADVANCED_FACE ( 'NONE', ( #39140 ), #30895, .T. ) ;
#24570=ORIENTED_EDGE ( 'NONE', *, *, #45117, .F. ) ;
#24572=ORIENTED_EDGE ( 'NONE', *, *, #12812, .F. ) ;
#24578=ADVANCED_FACE ( 'NONE', ( #6884 ), #50955, .F. ) ;
#24582=ORIENTED_EDGE ( 'NONE', *, *, #13224, .T. ) ;
#24587=VERTEX_POINT ( 'NONE', #11520 ) ;
#24596=VERTEX_POINT ( 'NONE', #26500 ) ;
#24598=CARTESIAN_POINT ( 'NONE',  ( -0.7582255214199161708, 0.000000000000000000, -1.687894986714875811 ) ) ;
#24599=VERTEX_POINT ( 'NONE', #18764 ) ;
#24602=ORIENTED_EDGE ( 'NONE', *, *, #12623, .F. ) ;
#24606=AXIS2_PLACEMENT_3D ( 'NONE', #35939, #568, #16315 ) ;
#24611=LINE ( 'NONE', #37005, #32515 ) ;
#24612=AXIS2_PLACEMENT_3D ( 'NONE', #42184, #26438, #22570 ) ;
#24615=CARTESIAN_POINT ( 'NONE',  ( 0.5284761224300885685, 1.574803149606302854, -2.099874368989729234 ) ) ;
#24618=CARTESIAN_POINT ( 'NONE',  ( 2.535292374475893951, 1.653425583089147111, -0.06459790964117027856 ) ) ;
#24619=EDGE_CURVE ( 'NONE', #47691, #22113, #50446, .T. ) ;
#24621=CARTESIAN_POINT ( 'NONE',  ( 1.556712866041120247, 5.905511811023623991, 2.509548638715870084 ) ) ;
#24624=DIRECTION ( 'NONE',  ( 0.000000000000000000, -1.000000000000000000, -1.156482317317871478E-16 ) ) ;
#24626=CARTESIAN_POINT ( 'NONE',  ( 1.472219874544873131, 1.482402307789154161, 2.560030851058970214 ) ) ;
#24635=CARTESIAN_POINT ( 'NONE',  ( -1.355031041518317325, 0.004193974497218569755, 1.143546472689453530 ) ) ;
#24636=CARTESIAN_POINT ( 'NONE',  ( 2.308203157375244152E-16, 0.07874015748031502893, -1.682967650661292502 ) ) ;
#24639=B_SPLINE_CURVE_WITH_KNOTS ( 'NONE', 3,
 ( #6897, #31406, #34526, #27517 ),
 .UNSPECIFIED., .F., .F.,
 ( 4, 4 ),
 ( 0.1211775127643062860, 0.1625894504277921315 ),
 .UNSPECIFIED. ) ;
#24653=VERTEX_POINT ( 'NONE', #31469 ) ;
#24654=CARTESIAN_POINT ( 'NONE',  ( 2.951990591674675368, 0.000000000000000000, -0.08331184815398383348 ) ) ;
#24655=PLANE ( 'NONE',  #40051 ) ;
#24657=CARTESIAN_POINT ( 'NONE',  ( -1.712067434724807269, 0.0003367829894146713294, -0.3402900276016438963 ) ) ;
#24660=VERTEX_POINT ( 'NONE', #27074 ) ;
#24667=DIRECTION ( 'NONE',  ( -1.729310098865080642E-17, 1.000000000000000000, 1.276627980444840260E-16 ) ) ;
#24670=CARTESIAN_POINT ( 'NONE',  ( 0.1828395243478885546, 1.016784016014155245, -2.580520392578918187 ) ) ;
#24679=ORIENTED_EDGE ( 'NONE', *, *, #12405, .T. ) ;
#24682=CARTESIAN_POINT ( 'NONE',  ( -2.949782676795219771, 0.000000000000000000, -0.1324748927672794452 ) ) ;
#24685=B_SPLINE_CURVE_WITH_KNOTS ( 'NONE', 3,
 ( #18058, #14174, #38445, #29678 ),
 .UNSPECIFIED., .F., .F.,
 ( 4, 4 ),
 ( 0.0009431515978678377396, 0.003443434775124777723 ),
 .UNSPECIFIED. ) ;
#24689=ORIENTED_EDGE ( 'NONE', *, *, #35570, .F. ) ;
#24693=EDGE_CURVE ( 'NONE', #22293, #15466, #33773, .T. ) ;
#24696=VERTEX_POINT ( 'NONE', #15468 ) ;
#24702=CARTESIAN_POINT ( 'NONE',  ( 2.738124037479889417, 1.758476085681704326, -0.1722314944998213082 ) ) ;
#24710=LINE ( 'NONE', #33228, #26746 ) ;
#24721=FACE_OUTER_BOUND ( 'NONE', #25015, .T. ) ;
#24727=PRODUCT_DEFINITION_CONTEXT ( 'detailed design', #18712, 'design' ) ;
#24729=ORIENTED_EDGE ( 'NONE', *, *, #38457, .F. ) ;
#24732=ORIENTED_EDGE ( 'NONE', *, *, #18900, .F. ) ;
#24734=CARTESIAN_POINT ( 'NONE',  ( -1.428275480578807599, 1.594612651218729749, 2.294580664572506645 ) ) ;
#24737=LINE ( 'NONE', #32756, #41099 ) ;
#24738=ORIENTED_EDGE ( 'NONE', *, *, #36865, .T. ) ;
#24740=FACE_OUTER_BOUND ( 'NONE', #15995, .T. ) ;
#24742=VERTEX_POINT ( 'NONE', #22962 ) ;
#24751=EDGE_CURVE ( 'NONE', #38194, #36441, #11837, .T. ) ;
#24752=VERTEX_POINT ( 'NONE', #3089 ) ;
#24755=CARTESIAN_POINT ( 'NONE',  ( 2.061875708210571201, 1.740926663775191674, 1.053657044629532802 ) ) ;
#24756=ORIENTED_EDGE ( 'NONE', *, *, #17354, .T. ) ;
#24757=DIRECTION ( 'NONE',  ( -0.6234898018587318180, 9.077469801274542449E-17, -0.7818314824680309139 ) ) ;
#24758=B_SPLINE_CURVE_WITH_KNOTS ( 'NONE', 3,
 ( #10458, #38091, #10712, #42450 ),
 .UNSPECIFIED., .F., .F.,
 ( 4, 4 ),
 ( 2.558210376252241617E-07, 0.002500373932690979316 ),
 .UNSPECIFIED. ) ;
#24759=ORIENTED_EDGE ( 'NONE', *, *, #26447, .F. ) ;
#24764=VECTOR ( 'NONE', #17247, 39.37007874015748143 ) ;
#24769=CYLINDRICAL_SURFACE ( 'NONE', #34466, 2.165354330708661568 ) ;
#24773=ORIENTED_EDGE ( 'NONE', *, *, #21156, .F. ) ;
#24775=CARTESIAN_POINT ( 'NONE',  ( 2.164658444855302122, 5.905511811023623991, -0.04795272066889885720 ) ) ;
#24777=B_SPLINE_CURVE_WITH_KNOTS ( 'NONE', 3,
 ( #42129, #6002, #15021, #21758 ),
 .UNSPECIFIED., .F., .F.,
 ( 4, 4 ),
 ( 2.074911753762320913E-07, 0.01858314050568160916 ),
 .UNSPECIFIED. ) ;
#24778=CARTESIAN_POINT ( 'NONE',  ( -2.150611651783668865, 1.640647882934381574, -0.2522489660909295051 ) ) ;
#24779=ORIENTED_EDGE ( 'NONE', *, *, #40092, .T. ) ;
#24783=CARTESIAN_POINT ( 'NONE',  ( 3.937007874015748143, 5.118110236220475784, 1.181102362204724310 ) ) ;
#24785=FACE_OUTER_BOUND ( 'NONE', #34869, .T. ) ;
#24787=ORIENTED_EDGE ( 'NONE', *, *, #31750, .T. ) ;
#24792=VERTEX_POINT ( 'NONE', #10832 ) ;
#24794=CARTESIAN_POINT ( 'NONE',  ( 2.390031926231672710, 1.654552468068580806, 1.342016610150888134 ) ) ;
#24796=CARTESIAN_POINT ( 'NONE',  ( 0.2212097921902143327, 0.01045795994330635768, -1.908835200420839984 ) ) ;
#24802=CYLINDRICAL_SURFACE ( 'NONE', #3505, 2.165354330708661568 ) ;
#24805=VECTOR ( 'NONE', #7938, 39.37007874015748143 ) ;
#24806=B_SPLINE_CURVE_WITH_KNOTS ( 'NONE', 3,
 ( #40125, #8116, #20751, #23862 ),
 .UNSPECIFIED., .F., .F.,
 ( 4, 4 ),
 ( 0.001651792006055582919, 0.004151899744057469845 ),
 .UNSPECIFIED. ) ;
#24808=LINE ( 'NONE', #47489, #3342 ) ;
#24809=EDGE_CURVE ( 'NONE', #24660, #16416, #30644, .T. ) ;
#24814=ORIENTED_EDGE ( 'NONE', *, *, #30774, .F. ) ;
#24817=CARTESIAN_POINT ( 'NONE',  ( 0.002207914879453961535, -5.712274067634378313E-18, 0.04916304461325374242 ) ) ;
#24819=ORIENTED_EDGE ( 'NONE', *, *, #13449, .F. ) ;
#24820=CARTESIAN_POINT ( 'NONE',  ( 2.684779361005118048, 1.757638757588847911, -0.5623051772365603718 ) ) ;
#24825=VERTEX_POINT ( 'NONE', #5117 ) ;
#24826=B_SPLINE_CURVE_WITH_KNOTS ( 'NONE', 3,
 ( #51012, #205, #15956, #43819 ),
 .UNSPECIFIED., .F., .F.,
 ( 4, 4 ),
 ( 0.1211873102087489551, 0.1625992483279400380 ),
 .UNSPECIFIED. ) ;
#24827=ORIENTED_EDGE ( 'NONE', *, *, #38094, .F. ) ;
#24829=CARTESIAN_POINT ( 'NONE',  ( 0.5756566573088583993, 1.502670515430445386, 2.896516654582643291 ) ) ;
#24836=ORIENTED_EDGE ( 'NONE', *, *, #9550, .T. ) ;
#24840=CARTESIAN_POINT ( 'NONE',  ( -0.9225641150147850800, 1.049866565067838264, -1.802300656478875052 ) ) ;
#24841=CARTESIAN_POINT ( 'NONE',  ( 0.4350747367505088947, 1.205361022782829114E-17, -2.121846421795415161 ) ) ;
#24846=EDGE_CURVE ( 'NONE', #29348, #18296, #9717, .T. ) ;
#24851=VERTEX_POINT ( 'NONE', #40747 ) ;
#24857=DIRECTION ( 'NONE',  ( -3.986037398843765983E-20, -1.000000000000000000, -1.160734090543304660E-16 ) ) ;
#24859=CARTESIAN_POINT ( 'NONE',  ( -1.979793062125317471, 1.556934451446513545, 2.191257344206539504 ) ) ;
#24864=DIRECTION ( 'NONE',  ( 1.347303628949392478E-32, -1.160734090543304660E-16, 1.000000000000000000 ) ) ;
#24865=EDGE_CURVE ( 'NONE', #33261, #17939, #27768, .T. ) ;
#24871=EDGE_CURVE ( 'NONE', #30098, #42285, #32240, .T. ) ;
#24872=B_SPLINE_CURVE_WITH_KNOTS ( 'NONE', 3,
 ( #13666, #36913, #16778, #48474 ),
 .UNSPECIFIED., .F., .F.,
 ( 4, 4 ),
 ( 2.396516866961895415E-07, 0.002500331606968418403 ),
 .UNSPECIFIED. ) ;
#24873=CARTESIAN_POINT ( 'NONE',  ( 2.743641484424565569, 1.660104339391717643, -0.07395487895817318136 ) ) ;
#24876=DIRECTION ( 'NONE',  ( 0.6579387259397138088, 0.000000000000000000, -0.7530714660036099684 ) ) ;
#24879=EDGE_CURVE ( 'NONE', #37287, #43799, #42969, .T. ) ;
#24885=FACE_OUTER_BOUND ( 'NONE', #28806, .T. ) ;
#24887=EDGE_LOOP ( 'NONE', ( #23888, #5993, #24249, #47036 ) ) ;
#24891=CARTESIAN_POINT ( 'NONE',  ( -0.9914495361339011881, 1.536537968533926657, 2.781765111341808705 ) ) ;
#24893=ORIENTED_EDGE ( 'NONE', *, *, #35762, .F. ) ;
#24895=CARTESIAN_POINT ( 'NONE',  ( -1.891551709140807169, 1.611988491233848908, 1.073772966847271526 ) ) ;
#24897=DIRECTION ( 'NONE',  ( -0.000000000000000000, -1.000000000000000000, -0.000000000000000000 ) ) ;
#24903=VERTEX_POINT ( 'NONE', #28345 ) ;
#24906=CARTESIAN_POINT ( 'NONE',  ( -1.252433315296644256, 1.589416742343778610, -1.807552045033091082 ) ) ;
#24907=CARTESIAN_POINT ( 'NONE',  ( 0.08119777152254364916, 1.623385212329073957, 0.000000000000000000 ) ) ;
#24910=VERTEX_POINT ( 'NONE', #20611 ) ;
#24912=CARTESIAN_POINT ( 'NONE',  ( -1.472219874544909768, 1.597879704547665369, 2.560030851058948898 ) ) ;
#24919=EDGE_LOOP ( 'NONE', ( #11814, #9044, #47218, #27380 ) ) ;
#24923=ORIENTED_EDGE ( 'NONE', *, *, #23225, .T. ) ;
#24924=CARTESIAN_POINT ( 'NONE',  ( -2.612312576780101647, 1.576028912971601192, -0.6467214908075719082 ) ) ;
#24926=VERTEX_POINT ( 'NONE', #48441 ) ;
#24927=CARTESIAN_POINT ( 'NONE',  ( 1.971247363764867977, 1.574803149606302854, -0.8960709840011636951 ) ) ;
#24939=CYLINDRICAL_SURFACE ( 'NONE', #10993, 2.164630168518208109 ) ;
#24947=PLANE ( 'NONE',  #34515 ) ;
#24950=VECTOR ( 'NONE', #46646, 39.37007874015748143 ) ;
#24956=DIRECTION ( 'NONE',  ( 0.01601477604151182663, -0.9998717552508123996, 0.000000000000000000 ) ) ;
#24958=CONICAL_SURFACE ( 'NONE', #5158, 3.483074324928249421, 1.244861948955335196 ) ;
#24962=ORIENTED_EDGE ( 'NONE', *, *, #48491, .T. ) ;
#24966=ORIENTED_EDGE ( 'NONE', *, *, #27877, .T. ) ;
#24968=ORIENTED_EDGE ( 'NONE', *, *, #11098, .F. ) ;
#24969=CARTESIAN_POINT ( 'NONE',  ( -1.942732458483407365, 0.000000000000000000, 2.223636218514596585 ) ) ;
#24971=EDGE_CURVE ( 'NONE', #47888, #7882, #34388, .T. ) ;
#24972=ORIENTED_EDGE ( 'NONE', *, *, #41510, .T. ) ;
#24975=ORIENTED_EDGE ( 'NONE', *, *, #15879, .F. ) ;
#24978=ADVANCED_FACE ( 'NONE', ( #37390 ), #31921, .T. ) ;
#24979=ORIENTED_EDGE ( 'NONE', *, *, #33050, .F. ) ;
#24983=AXIS2_PLACEMENT_3D ( 'NONE', #12014, #20781, #29288 ) ;
#24988=VECTOR ( 'NONE', #19629, 39.37007874015748143 ) ;
#24989=B_SPLINE_CURVE_WITH_KNOTS ( 'NONE', 3,
 ( #25545, #33313, #2058, #36666 ),
 .UNSPECIFIED., .F., .F.,
 ( 4, 4 ),
 ( 0.1211775127643062860, 0.1625894504277921315 ),
 .UNSPECIFIED. ) ;
#24991=EDGE_CURVE ( 'NONE', #45444, #46840, #50876, .T. ) ;
#24994=CARTESIAN_POINT ( 'NONE',  ( 1.497019771146616662, 1.049866565877818347, -1.363210918505332714 ) ) ;
#24998=CARTESIAN_POINT ( 'NONE',  ( 1.548545842648739956, 1.732704746525083772, 1.697655184951773810 ) ) ;
#25002=FACE_OUTER_BOUND ( 'NONE', #10188, .T. ) ;
#25003=VERTEX_POINT ( 'NONE', #14133 ) ;
#25004=CARTESIAN_POINT ( 'NONE',  ( -1.236813753895212642, 5.905511811023623991, -2.681693691597581974 ) ) ;
#25005=CARTESIAN_POINT ( 'NONE',  ( 0.002207914879453961969, 6.692913385826772199, 0.04916304461325451958 ) ) ;
#25006=VERTEX_POINT ( 'NONE', #44849 ) ;
#25009=EDGE_CURVE ( 'NONE', #41613, #19132, #30005, .T. ) ;
#25015=EDGE_LOOP ( 'NONE', ( #45872, #10097, #463, #50664 ) ) ;
#25020=DIRECTION ( 'NONE',  ( -0.9998717552508121775, -0.01601477604151182316, 0.000000000000000000 ) ) ;
#25021=VECTOR ( 'NONE', #14727, 39.37007874015748143 ) ;
#25028=CONICAL_SURFACE ( 'NONE', #17628, 3.483074324928249421, 1.244861948955335196 ) ;
#25030=VERTEX_POINT ( 'NONE', #48693 ) ;
#25031=EDGE_CURVE ( 'NONE', #21218, #25699, #39226, .T. ) ;
#25033=DIRECTION ( 'NONE',  ( -0.9998717552508122886, -0.01601477604151181275, 0.000000000000000000 ) ) ;
#25034=DIRECTION ( 'NONE',  ( -0.01601477604151182663, 0.9998717552508123996, -0.000000000000000000 ) ) ;
#25036=ORIENTED_EDGE ( 'NONE', *, *, #34610, .T. ) ;
#25038=CARTESIAN_POINT ( 'NONE',  ( -2.277873973731453283, 1.205361022782829114E-17, 1.879489153247635214 ) ) ;
#25041=EDGE_CURVE ( 'NONE', #8712, #7499, #45099, .T. ) ;
#25044=CARTESIAN_POINT ( 'NONE',  ( 0.002207914879453961969, 5.905511811023623991, 0.04916304461325442243 ) ) ;
#25047=EDGE_LOOP ( 'NONE', ( #39184, #20111, #46372, #24572 ) ) ;
#25052=DIRECTION ( 'NONE',  ( 0.9998717552508121775, 0.01601477604151182663, 0.000000000000000000 ) ) ;
#25054=ORIENTED_EDGE ( 'NONE', *, *, #49650, .F. ) ;
#25055=CONICAL_SURFACE ( 'NONE', #38259, 3.033577403570480779, 1.554780866114618743 ) ;
#25060=ADVANCED_FACE ( 'NONE', ( #17755 ), #7182, .T. ) ;
#25063=VECTOR ( 'NONE', #29776, 39.37007874015748143 ) ;
#25066=DIRECTION ( 'NONE',  ( 0.9510565162951500895, 0.000000000000000000, 0.3090169943749582204 ) ) ;
#25067=ADVANCED_FACE ( 'NONE', ( #22643 ), #50778, .T. ) ;
#25069=AXIS2_PLACEMENT_3D ( 'NONE', #21710, #37470, #49024 ) ;
#25070=EDGE_LOOP ( 'NONE', ( #6882, #49394, #17557, #30506 ) ) ;
#25071=DIRECTION ( 'NONE',  ( -0.9998717552508121775, -0.01601477604151182316, 0.000000000000000000 ) ) ;
#25074=ADVANCED_FACE ( 'NONE', ( #3026 ), #13747, .F. ) ;
#25076=DIRECTION ( 'NONE',  ( -0.7530714660036196273, 0.000000000000000000, 0.6579387259397027066 ) ) ;
#25078=( BOUNDED_CURVE ( )  B_SPLINE_CURVE ( 3, ( #41216, #37344, #45309, #13335 ),
 .UNSPECIFIED., .F., .F. ) 
 B_SPLINE_CURVE_WITH_KNOTS ( ( 4, 4 ),
 ( 5.813044721214517985, 5.863817393281590462 ),
 .UNSPECIFIED. ) 
 CURVE ( )  GEOMETRIC_REPRESENTATION_ITEM ( )  RATIONAL_B_SPLINE_CURVE ( ( 1.000000000000000000, 0.9997851895178078152, 0.9997851895178078152, 1.000000000000000000 ) ) 
 REPRESENTATION_ITEM ( '' )  );
#25080=EDGE_CURVE ( 'NONE', #34410, #20385, #29442, .T. ) ;
#25082=CARTESIAN_POINT ( 'NONE',  ( 2.168245791271198097, 5.905511811023623991, -2.004968704497247955 ) ) ;
#25084=EDGE_CURVE ( 'NONE', #24599, #25849, #48411, .T. ) ;
#25087=ORIENTED_EDGE ( 'NONE', *, *, #12907, .T. ) ;
#25092=VERTEX_POINT ( 'NONE', #34772 ) ;
#25094=CONICAL_SURFACE ( 'NONE', #48126, 2.246510896728926010, 0.01601546068027819014 ) ;
#25098=B_SPLINE_CURVE_WITH_KNOTS ( 'NONE', 3,
 ( #40770, #5395, #13399, #17279 ),
 .UNSPECIFIED., .F., .F.,
 ( 4, 4 ),
 ( 2.008072039916852648E-07, 0.006151689351068225821 ),
 .UNSPECIFIED. ) ;
#25100=EDGE_CURVE ( 'NONE', #34448, #44880, #15397, .T. ) ;
#25102=ORIENTED_EDGE ( 'NONE', *, *, #41574, .T. ) ;
#25104=DIRECTION ( 'NONE',  ( 0.9998717552508121775, 0.01601477604151182663, 0.000000000000000000 ) ) ;
#25106=ADVANCED_FACE ( 'NONE', ( #19264 ), #19511, .F. ) ;
#25112=VERTEX_POINT ( 'NONE', #18522 ) ;
#25115=CARTESIAN_POINT ( 'NONE',  ( 1.325491792074623643, 0.000000000000000000, -2.638988599164732385 ) ) ;
#25119=DIRECTION ( 'NONE',  ( 0.000000000000000000, 0.000000000000000000, 1.000000000000000000 ) ) ;
#25121=DIRECTION ( 'NONE',  ( -0.9998717552508121775, -0.01601477604151182316, 0.000000000000000000 ) ) ;
#25124=CARTESIAN_POINT ( 'NONE',  ( -2.138597145901436125, 6.692913385826772199, 0.3393547186366932533 ) ) ;
#25126=CARTESIAN_POINT ( 'NONE',  ( 0.002207914879453961969, 5.905511811023623991, 0.04916304461325442243 ) ) ;
#25128=AXIS2_PLACEMENT_3D ( 'NONE', #10961, #30838, #19204 ) ;
#25134=ORIENTED_EDGE ( 'NONE', *, *, #11105, .F. ) ;
#25135=DIRECTION ( 'NONE',  ( 0.000000000000000000, -1.000000000000000000, -0.000000000000000000 ) ) ;
#25137=DIRECTION ( 'NONE',  ( 0.01601477604151182663, -0.9998717552508123996, 0.000000000000000000 ) ) ;
#25138=DIRECTION ( 'NONE',  ( -0.01601477604151182663, 0.9998717552508123996, -0.000000000000000000 ) ) ;
#25141=LINE ( 'NONE', #9389, #49701 ) ;
#25143=VECTOR ( 'NONE', #39770, 39.37007874015748143 ) ;
#25146=CARTESIAN_POINT ( 'NONE',  ( 1.769879628650530723, 0.05626752682809384870, -0.8100022834900426627 ) ) ;
#25153=DIRECTION ( 'NONE',  ( 0.9989930665413151445, 5.167793568183051143E-18, -0.04486483035050446017 ) ) ;
#25155=ORIENTED_EDGE ( 'NONE', *, *, #29460, .F. ) ;
#25156=CARTESIAN_POINT ( 'NONE',  ( -1.420868632364155282, 0.000000000000000000, 1.070159647439151707 ) ) ;
#25159=CARTESIAN_POINT ( 'NONE',  ( -2.734482843737247038, 1.578211097029592169, -1.115254632218712016 ) ) ;
#25161=CARTESIAN_POINT ( 'NONE',  ( -1.252307872741886374, 1.622227152372770487, -1.807379388168664613 ) ) ;
#25168=CARTESIAN_POINT ( 'NONE',  ( 0.04921259842519669359, 1.621581020286960051, 2.952755905511811108 ) ) ;
#25170=VERTEX_POINT ( 'NONE', #7652 ) ;
#25173=VECTOR ( 'NONE', #13194, 39.37007874015748143 ) ;
#25177=VECTOR ( 'NONE', #12880, 39.37007874015748143 ) ;
#25180=CARTESIAN_POINT ( 'NONE',  ( 0.08119777152254364916, 1.623385212329073957, 0.000000000000000000 ) ) ;
#25181=AXIS2_PLACEMENT_3D ( 'NONE', #3175, #23048, #30546 ) ;
#25185=CARTESIAN_POINT ( 'NONE',  ( -2.164823134740035737, 6.692913385826772199, -0.04796011690018289753 ) ) ;
#25186=ORIENTED_EDGE ( 'NONE', *, *, #46450, .T. ) ;
#25187=AXIS2_PLACEMENT_3D ( 'NONE', #2492, #25464, #37869 ) ;
#25197=CARTESIAN_POINT ( 'NONE',  ( 2.313772584725266146, 1.653356997568332210, -1.468340530687288981 ) ) ;
#25203=CARTESIAN_POINT ( 'NONE',  ( 0.000000000000000000, 1.574803149606302854, 0.000000000000000000 ) ) ;
#25204=EDGE_CURVE ( 'NONE', #9920, #13689, #3088, .T. ) ;
#25205=DIRECTION ( 'NONE',  ( -0.000000000000000000, -1.000000000000000000, 0.000000000000000000 ) ) ;
#25206=AXIS2_PLACEMENT_3D ( 'NONE', #15473, #31223, #11591 ) ;
#25207=AXIS2_PLACEMENT_3D ( 'NONE', #19569, #35085, #15205 ) ;
#25213=CARTESIAN_POINT ( 'NONE',  ( 0.08139965876239094178, 1.610780518492231694, 0.000000000000000000 ) ) ;
#25214=CARTESIAN_POINT ( 'NONE',  ( 0.08139965876239094178, 1.610780518492231694, 0.000000000000000000 ) ) ;
#25215=FACE_OUTER_BOUND ( 'NONE', #1228, .T. ) ;
#25218=VERTEX_POINT ( 'NONE', #40441 ) ;
#25219=CARTESIAN_POINT ( 'NONE',  ( 1.022166022721139322, 1.636725766563431606, 2.770237021105635300 ) ) ;
#25220=VERTEX_POINT ( 'NONE', #4291 ) ;
#25221=ADVANCED_FACE ( 'NONE', ( #28803 ), #12967, .F. ) ;
#25233=ORIENTED_EDGE ( 'NONE', *, *, #30590, .F. ) ;
#25240=CIRCLE ( 'NONE', #2173, 2.246510896728926010 ) ;
#25252=B_SPLINE_CURVE_WITH_KNOTS ( 'NONE', 3,
 ( #25168, #13048, #1161, #6052 ),
 .UNSPECIFIED., .F., .F.,
 ( 4, 4 ),
 ( 0.0008137531722819554792, 0.003314056422229540947 ),
 .UNSPECIFIED. ) ;
#25256=CARTESIAN_POINT ( 'NONE',  ( -0.3498457532482182053, 1.702298530840201662, 2.203421978946157989 ) ) ;
#25257=DIRECTION ( 'NONE',  ( -0.9998717552508121775, -0.01601477604151182316, 0.000000000000000000 ) ) ;
#25262=VERTEX_POINT ( 'NONE', #28033 ) ;
#25263=DIRECTION ( 'NONE',  ( -0.5128992774059071280, 0.000000000000000000, 0.8584487936018655452 ) ) ;
#25269=CARTESIAN_POINT ( 'NONE',  ( -0.6393972184786450574, 0.000000000000000000, 1.750134138416205687 ) ) ;
#25270=B_SPLINE_CURVE_WITH_KNOTS ( 'NONE', 3,
 ( #9790, #49237, #37418, #41285 ),
 .UNSPECIFIED., .F., .F.,
 ( 4, 4 ),
 ( 2.271194419226085044E-07, 0.01976584882222652551 ),
 .UNSPECIFIED. ) ;
#25275=CARTESIAN_POINT ( 'NONE',  ( 1.748857742710046237, 1.648042031076149883, -2.379187494666238134 ) ) ;
#25278=VECTOR ( 'NONE', #4737, 39.37007874015748143 ) ;
#25285=DIRECTION ( 'NONE',  ( 0.9009688679024154823, -1.160734090543304660E-16, 0.4338837391175656699 ) ) ;
#25287=DIRECTION ( 'NONE',  ( -0.01601477604151182663, 0.9998717552508123996, -0.000000000000000000 ) ) ;
#25290=EDGE_CURVE ( 'NONE', #2346, #13212, #24173, .T. ) ;
#25291=CARTESIAN_POINT ( 'NONE',  ( -2.159905143290285601, 6.332733149760729319, 0.1535224723189610174 ) ) ;
#25292=DIRECTION ( 'NONE',  ( -0.4338837391175526803, 1.045958227173635857E-16, -0.9009688679024218105 ) ) ;
#25295=LINE ( 'NONE', #25038, #3929 ) ;
#25299=DIRECTION ( 'NONE',  ( -3.986037398843765983E-20, -1.000000000000000000, -1.160734090543304660E-16 ) ) ;
#25300=VERTEX_POINT ( 'NONE', #415 ) ;
#25302=VERTEX_POINT ( 'NONE', #44540 ) ;
#25305=LINE ( 'NONE', #21439, #39909 ) ;
#25306=CARTESIAN_POINT ( 'NONE',  ( 2.278027606577265107, 1.645963535160160696, -0.4694667435916627385 ) ) ;
#25307=ORIENTED_EDGE ( 'NONE', *, *, #28012, .T. ) ;
#25309=CARTESIAN_POINT ( 'NONE',  ( 1.162932091021788183, 1.205361022782829114E-17, -1.684364178081092067 ) ) ;
#25314=FACE_OUTER_BOUND ( 'NONE', #26456, .T. ) ;
#25316=B_SPLINE_CURVE_WITH_KNOTS ( 'NONE', 3,
 ( #13110, #28324, #1229, #5356 ),
 .UNSPECIFIED., .F., .F.,
 ( 4, 4 ),
 ( 2.175066537435804214E-07, 0.002500264305833190676 ),
 .UNSPECIFIED. ) ;
#25317=CARTESIAN_POINT ( 'NONE',  ( 1.720314620805546646, 0.000000000000000000, 0.2826945007888405637 ) ) ;
#25318=B_SPLINE_CURVE_WITH_KNOTS ( 'NONE', 3,
 ( #4559, #16440, #31938, #35800 ),
 .UNSPECIFIED., .F., .F.,
 ( 4, 4 ),
 ( 9.107130028278628622E-06, 2.039057899801572380E-05 ),
 .UNSPECIFIED. ) ;
#25319=EDGE_CURVE ( 'NONE', #16395, #37228, #39917, .T. ) ;
#25320=ORIENTED_EDGE ( 'NONE', *, *, #48344, .F. ) ;
#25327=DIRECTION ( 'NONE',  ( 0.6579387259397027066, 0.000000000000000000, 0.7530714660036195163 ) ) ;
#25338=VECTOR ( 'NONE', #40349, 39.37007874015748143 ) ;
#25341=VERTEX_POINT ( 'NONE', #45293 ) ;
#25342=ORIENTED_EDGE ( 'NONE', *, *, #9993, .T. ) ;
#25345=ORIENTED_EDGE ( 'NONE', *, *, #49799, .T. ) ;
#25353=DIRECTION ( 'NONE',  ( 0.01601477604151182663, -0.9998717552508123996, 0.000000000000000000 ) ) ;
#25355=DIRECTION ( 'NONE',  ( -0.7818314824680309139, 0.000000000000000000, 0.6234898018587318180 ) ) ;
#25362=( CONVERSION_BASED_UNIT ( 'INCH', #36995 ) LENGTH_UNIT ( ) NAMED_UNIT ( #28796 ) );
#25364=EDGE_CURVE ( 'NONE', #9169, #17362, #21576, .T. ) ;
#25366=CARTESIAN_POINT ( 'NONE',  ( 1.550261229843175492, 1.634307024739966696, 1.699618603577774945 ) ) ;
#25367=DIRECTION ( 'NONE',  ( 0.9959742939952397345, 0.000000000000000000, -0.08963930890342654279 ) ) ;
#25370=DIRECTION ( 'NONE',  ( -0.9510565162951544194, 0.000000000000000000, 0.3090169943749447312 ) ) ;
#25373=CARTESIAN_POINT ( 'NONE',  ( -1.690941099774203815, 0.0008361491594236539725, -0.4364244636917575804 ) ) ;
#25374=CIRCLE ( 'NONE', #24563, 2.244934639244525076 ) ;
#25380=VECTOR ( 'NONE', #22498, 39.37007874015748143 ) ;
#25385=CARTESIAN_POINT ( 'NONE',  ( 0.002207914879453961969, 6.692913385826772199, 0.04916304461325451958 ) ) ;
#25387=ORIENTED_EDGE ( 'NONE', *, *, #49316, .F. ) ;
#25388=CARTESIAN_POINT ( 'NONE',  ( 2.277873973731426194, 0.000000000000000000, 1.879489153247667854 ) ) ;
#25394=CARTESIAN_POINT ( 'NONE',  ( 0.04921259842519689481, 0.000000000000000000, 1.742692369722729895 ) ) ;
#25401=CARTESIAN_POINT ( 'NONE',  ( -2.161044708975090156, 5.905511811023623991, 0.1463148319730357971 ) ) ;
#25407=DIRECTION ( 'NONE',  ( -0.9909497617679352555, -1.554141314384320336E-17, 0.1342332658176522420 ) ) ;
#25416=ORIENTED_EDGE ( 'NONE', *, *, #6195, .F. ) ;
#25421=VECTOR ( 'NONE', #16215, 39.37007874015748143 ) ;
#25426=VECTOR ( 'NONE', #26100, 39.37007874015748143 ) ;
#25427=EDGE_CURVE ( 'NONE', #15952, #8046, #31106, .T. ) ;
#25429=PLANE ( 'NONE',  #7954 ) ;
#25440=DIRECTION ( 'NONE',  ( 0.000000000000000000, 0.000000000000000000, 1.000000000000000000 ) ) ;
#25441=CARTESIAN_POINT ( 'NONE',  ( 0.08139965876239094178, 1.610780518492231694, 0.000000000000000000 ) ) ;
#25443=DIRECTION ( 'NONE',  ( -0.9998717552508121775, -0.01601477604151182316, 0.000000000000000000 ) ) ;
#25445=EDGE_CURVE ( 'NONE', #49614, #7280, #6073, .T. ) ;
#25446=ORIENTED_EDGE ( 'NONE', *, *, #22840, .T. ) ;
#25448=CARTESIAN_POINT ( 'NONE',  ( -0.3500732549360408563, 1.603869690133923331, 2.204675616574417685 ) ) ;
#25452=B_SPLINE_CURVE_WITH_KNOTS ( 'NONE', 3,
 ( #6018, #25640, #5769, #40384 ),
 .UNSPECIFIED., .F., .F.,
 ( 4, 4 ),
 ( 0.01233407828749484916, 0.03073846733299314196 ),
 .UNSPECIFIED. ) ;
#25462=CONICAL_SURFACE ( 'NONE', #21345, 1.850107469027523210, 0.6386652850508578450 ) ;
#25464=DIRECTION ( 'NONE',  ( -0.8090169943749507819, 1.288287287306305530E-16, 0.5877852522924685852 ) ) ;
#25465=VECTOR ( 'NONE', #32563, 39.37007874015748143 ) ;
#25469=ORIENTED_EDGE ( 'NONE', *, *, #28855, .T. ) ;
#25476=EDGE_CURVE ( 'NONE', #344, #33287, #2827, .T. ) ;
#25477=CARTESIAN_POINT ( 'NONE',  ( -0.7855418668307150298, 5.905511811023623991, -2.846347029613745416 ) ) ;
#25481=EDGE_LOOP ( 'NONE', ( #29201, #32576, #46662, #27498, #40854, #1295, #32337, #37554, #5070, #24559, #3284 ) ) ;
#25484=AXIS2_PLACEMENT_3D ( 'NONE', #6303, #18174, #33930 ) ;
#25486=ORIENTED_EDGE ( 'NONE', *, *, #21494, .F. ) ;
#25496=ORIENTED_EDGE ( 'NONE', *, *, #32989, .F. ) ;
#25497=DIRECTION ( 'NONE',  ( 0.000000000000000000, 0.000000000000000000, 1.000000000000000000 ) ) ;
#25504=DIRECTION ( 'NONE',  ( -0.01601477604151182663, 0.9998717552508123996, -0.000000000000000000 ) ) ;
#25505=CARTESIAN_POINT ( 'NONE',  ( -1.930190994932097004, 6.692913385826772199, -0.9827944786818715306 ) ) ;
#25506=B_SPLINE_CURVE_WITH_KNOTS ( 'NONE', 3,
 ( #13628, #41001, #37130, #1492 ),
 .UNSPECIFIED., .F., .F.,
 ( 4, 4 ),
 ( 0.01079281432884818606, 0.03073583335247125417 ),
 .UNSPECIFIED. ) ;
#25510=ORIENTED_EDGE ( 'NONE', *, *, #38839, .F. ) ;
#25512=DIRECTION ( 'NONE',  ( 2.866708903754326305E-17, 1.000000000000000000, 1.255987235303924321E-16 ) ) ;
#25514=ORIENTED_EDGE ( 'NONE', *, *, #38170, .T. ) ;
#25517=ADVANCED_FACE ( 'NONE', ( #15346 ), #39343, .T. ) ;
#25518=ORIENTED_EDGE ( 'NONE', *, *, #23687, .T. ) ;
#25520=CARTESIAN_POINT ( 'NONE',  ( -0.7331725592709618100, 1.597733653658881758, 2.093588567519426569 ) ) ;
#25521=CARTESIAN_POINT ( 'NONE',  ( -0.6982598466389058345, 0.000000000000000000, 1.720449438420079691 ) ) ;
#25524=AXIS2_PLACEMENT_3D ( 'NONE', #23747, #38987, #3622 ) ;
#25532=ORIENTED_EDGE ( 'NONE', *, *, #28940, .T. ) ;
#25535=LINE ( 'NONE', #17537, #47935 ) ;
#25539=DIRECTION ( 'NONE',  ( -0.9989930665413151445, 0.000000000000000000, 0.04486483035050446017 ) ) ;
#25541=ORIENTED_EDGE ( 'NONE', *, *, #47475, .F. ) ;
#25543=B_SPLINE_CURVE_WITH_KNOTS ( 'NONE', 3,
 ( #7354, #19459, #3476, #46310 ),
 .UNSPECIFIED., .F., .F.,
 ( 4, 4 ),
 ( 2.002015897020957629E-07, 0.02001440658365299941 ),
 .UNSPECIFIED. ) ;
#25545=CARTESIAN_POINT ( 'NONE',  ( 0.5284761224300885685, 1.574803149606302854, -2.099874368989729234 ) ) ;
#25546=ADVANCED_FACE ( 'NONE', ( #26704 ), #45923, .T. ) ;
#25547=ORIENTED_EDGE ( 'NONE', *, *, #45074, .T. ) ;
#25550=EDGE_CURVE ( 'NONE', #40703, #6865, #49903, .T. ) ;
#25551=EDGE_CURVE ( 'NONE', #43566, #46444, #15598, .T. ) ;
#25553=VERTEX_POINT ( 'NONE', #15093 ) ;
#25559=DIRECTION ( 'NONE',  ( 0.000000000000000000, 0.000000000000000000, -1.000000000000000000 ) ) ;
#25560=DIRECTION ( 'NONE',  ( 1.160706738777443955E-16, 1.000000000000000000, -5.589669052740684758E-17 ) ) ;
#25561=EDGE_LOOP ( 'NONE', ( #21288, #16697, #46067, #9835 ) ) ;
#25566=ADVANCED_FACE ( 'NONE', ( #26954 ), #31952, .T. ) ;
#25567=DIRECTION ( 'NONE',  ( -0.9909497617679352555, 0.000000000000000000, 0.1342332658176522697 ) ) ;
#25568=CARTESIAN_POINT ( 'NONE',  ( -0.8239235538337883469, 1.661896910481805767, 2.055279188836330206 ) ) ;
#25569=VECTOR ( 'NONE', #29111, 39.37007874015748854 ) ;
#25575=CARTESIAN_POINT ( 'NONE',  ( 1.550261229843175492, 1.634307024739966696, 1.699618603577774945 ) ) ;
#25576=CYLINDRICAL_SURFACE ( 'NONE', #17831, 2.165354330708661568 ) ;
#25577=ADVANCED_FACE ( 'NONE', ( #46057 ), #29474, .T. ) ;
#25581=EDGE_LOOP ( 'NONE', ( #42050, #49564, #12325, #13977, #505, #25416, #39099, #36652, #24323, #31756, #3096, #13259, #35571 ) ) ;
#25585=B_SPLINE_CURVE_WITH_KNOTS ( 'NONE', 3,
 ( #22653, #3542, #161, #38408 ),
 .UNSPECIFIED., .F., .F.,
 ( 4, 4 ),
 ( 2.396442746870937374E-07, 0.01967631564410392969 ),
 .UNSPECIFIED. ) ;
#25587=CARTESIAN_POINT ( 'NONE',  ( -0.1450362469327505233, 5.905511811023623991, -2.160491579385213523 ) ) ;
#25592=ORIENTED_EDGE ( 'NONE', *, *, #7475, .T. ) ;
#25593=B_SPLINE_CURVE_WITH_KNOTS ( 'NONE', 3,
 ( #28894, #36915, #44629, #1539 ),
 .UNSPECIFIED., .F., .F.,
 ( 4, 4 ),
 ( 0.01084969948538288577, 0.03073585646796594267 ),
 .UNSPECIFIED. ) ;
#25595=ORIENTED_EDGE ( 'NONE', *, *, #31717, .F. ) ;
#25598=CYLINDRICAL_SURFACE ( 'NONE', #26812, 2.165354330708661568 ) ;
#25600=B_SPLINE_CURVE_WITH_KNOTS ( 'NONE', 3,
 ( #5328, #40701, #48649, #2226 ),
 .UNSPECIFIED., .F., .F.,
 ( 4, 4 ),
 ( 0.001741610281575217993, 0.004241651184184463616 ),
 .UNSPECIFIED. ) ;
#25601=VECTOR ( 'NONE', #31791, 39.37007874015748143 ) ;
#25602=ORIENTED_EDGE ( 'NONE', *, *, #48491, .F. ) ;
#25607=ORIENTED_EDGE ( 'NONE', *, *, #21965, .T. ) ;
#25609=CARTESIAN_POINT ( 'NONE',  ( -1.979793062125318803, 5.905511811023623991, 2.191257344206540392 ) ) ;
#25611=EDGE_CURVE ( 'NONE', #46032, #33703, #19450, .T. ) ;
#25613=ORIENTED_EDGE ( 'NONE', *, *, #17299, .T. ) ;
#25615=AXIS2_PLACEMENT_3D ( 'NONE', #5856, #18495, #49936 ) ;
#25619=CARTESIAN_POINT ( 'NONE',  ( -1.883550378546958060, 1.205361022782829114E-17, -1.069467267250448161 ) ) ;
#25621=CARTESIAN_POINT ( 'NONE',  ( -0.2646829987305902021, 0.000000000000000000, -2.940868978332400463 ) ) ;
#25627=CARTESIAN_POINT ( 'NONE',  ( -1.461782879395278734, 6.692913385826772199, -1.598346982901828861 ) ) ;
#25628=B_SPLINE_CURVE_WITH_KNOTS ( 'NONE', 3,
 ( #5288, #21042, #5545, #33693 ),
 .UNSPECIFIED., .F., .F.,
 ( 4, 4 ),
 ( 2.032896354352839205E-07, 0.002500497150405497481 ),
 .UNSPECIFIED. ) ;
#25633=ORIENTED_EDGE ( 'NONE', *, *, #21992, .T. ) ;
#25636=EDGE_CURVE ( 'NONE', #18328, #37024, #7849, .T. ) ;
#25640=CARTESIAN_POINT ( 'NONE',  ( -0.4894113334356742229, 1.605499969913384728, 2.421265748518004468 ) ) ;
#25646=CARTESIAN_POINT ( 'NONE',  ( -1.467375622110394184, 1.037978273280383279, -2.103394750075909148 ) ) ;
#25648=CARTESIAN_POINT ( 'NONE',  ( -1.083598637574820334, 1.538470290252458739, 2.747180975113330259 ) ) ;
#25650=LINE ( 'NONE', #41402, #29076 ) ;
#25652=FACE_OUTER_BOUND ( 'NONE', #36464, .T. ) ;
#25662=LINE ( 'NONE', #41170, #44418 ) ;
#25666=CARTESIAN_POINT ( 'NONE',  ( 2.318785432985194905, 1.656916041303249987, 1.828187805987539827 ) ) ;
#25667=ORIENTED_EDGE ( 'NONE', *, *, #41807, .F. ) ;
#25670=CARTESIAN_POINT ( 'NONE',  ( -2.532674450597738769, 1.050099741429788791, 0.2934120129488018702 ) ) ;
#25672=ORIENTED_EDGE ( 'NONE', *, *, #21913, .T. ) ;
#25674=DIRECTION ( 'NONE',  ( 0.01601477604151182663, -0.9998717552508123996, 0.000000000000000000 ) ) ;
#25677=CARTESIAN_POINT ( 'NONE',  ( 0.9836083787002611878, 1.574803149606302854, -1.929060376159698720 ) ) ;
#25679=ORIENTED_EDGE ( 'NONE', *, *, #36863, .T. ) ;
#25695=EDGE_CURVE ( 'NONE', #5907, #36731, #49109, .T. ) ;
#25696=CARTESIAN_POINT ( 'NONE',  ( 2.179222933086670366, 2.755905511811027164, 2.848360286204475234 ) ) ;
#25698=CARTESIAN_POINT ( 'NONE',  ( -2.100227814008681637, 1.588094595312779855, -2.076109931251943763 ) ) ;
#25699=VERTEX_POINT ( 'NONE', #11974 ) ;
#25705=LINE ( 'NONE', #21842, #22801 ) ;
#25707=CARTESIAN_POINT ( 'NONE',  ( -0.6924561055946872878, 0.005671908246031987996, 1.704985425709532043 ) ) ;
#25708=ADVANCED_FACE ( 'NONE', ( #867 ), #27456, .T. ) ;
#25710=B_SPLINE_CURVE_WITH_KNOTS ( 'NONE', 3,
 ( #6128, #26999, #46598, #42503 ),
 .UNSPECIFIED., .F., .F.,
 ( 4, 4 ),
 ( 0.001106910458727990501, 0.003607175275882030987 ),
 .UNSPECIFIED. ) ;
#25715=CARTESIAN_POINT ( 'NONE',  ( -1.472219874544909768, 1.696317054561777171, 2.560030851058948898 ) ) ;
#25716=ADVANCED_FACE ( 'NONE', ( #12232 ), #8359, .T. ) ;
#25717=FACE_OUTER_BOUND ( 'NONE', #31596, .T. ) ;
#25719=AXIS2_PLACEMENT_3D ( 'NONE', #34947, #26934, #46777 ) ;
#25723=ORIENTED_EDGE ( 'NONE', *, *, #5644, .F. ) ;
#25724=ORIENTED_EDGE ( 'NONE', *, *, #10303, .F. ) ;
#25730=ORIENTED_EDGE ( 'NONE', *, *, #26702, .F. ) ;
#25733=AXIS2_PLACEMENT_3D ( 'NONE', #28679, #17083, #9326 ) ;
#25736=DIRECTION ( 'NONE',  ( 0.9998717552508121775, 0.01601477604151182663, 0.000000000000000000 ) ) ;
#25738=CARTESIAN_POINT ( 'NONE',  ( -0.3136974817027969320, 1.205361022782829114E-17, -2.936457595020224520 ) ) ;
#25741=EDGE_CURVE ( 'NONE', #8210, #40819, #44728, .T. ) ;
#25742=ORIENTED_EDGE ( 'NONE', *, *, #41438, .T. ) ;
#25743=VERTEX_POINT ( 'NONE', #2143 ) ;
#25744=CARTESIAN_POINT ( 'NONE',  ( -0.2493161376872249368, 1.671100300131709737, -2.221122275763622866 ) ) ;
#25745=EDGE_CURVE ( 'NONE', #27359, #21474, #22023, .T. ) ;
#25747=CARTESIAN_POINT ( 'NONE',  ( 1.387332044438934986, 1.697314215445209218, -1.825773270393029168 ) ) ;
#25749=AXIS2_PLACEMENT_3D ( 'NONE', #2061, #25808, #49506 ) ;
#25751=ORIENTED_EDGE ( 'NONE', *, *, #41818, .F. ) ;
#25755=VERTEX_POINT ( 'NONE', #33402 ) ;
#25756=CARTESIAN_POINT ( 'NONE',  ( 0.04921259842519603439, 6.692913385826772199, 2.164795024401847456 ) ) ;
#25758=CIRCLE ( 'NONE', #29038, 2.165354330708661568 ) ;
#25759=CARTESIAN_POINT ( 'NONE',  ( -0.04921259842519758176, 5.905511811023623991, 2.213182383082911375 ) ) ;
#25760=DIRECTION ( 'NONE',  ( -3.986037398843765983E-20, -1.000000000000000000, -1.160734090543304660E-16 ) ) ;
#25771=CARTESIAN_POINT ( 'NONE',  ( -2.277873973731453727, 1.585326468414270495, 1.879489153247635214 ) ) ;
#25775=EDGE_CURVE ( 'NONE', #43424, #782, #41591, .T. ) ;
#25781=VERTEX_POINT ( 'NONE', #48827 ) ;
#25783=CARTESIAN_POINT ( 'NONE',  ( -0.3381173457103602287, 1.574803149606302854, 2.138793126519845877 ) ) ;
#25784=EDGE_LOOP ( 'NONE', ( #21942, #9475, #14228, #38924 ) ) ;
#25791=CIRCLE ( 'NONE', #24983, 2.165354330708661568 ) ;
#25792=CARTESIAN_POINT ( 'NONE',  ( -1.743516651958532115, 0.0004834999639498430428, -4.958524412099369637E-19 ) ) ;
#25794=VERTEX_POINT ( 'NONE', #28986 ) ;
#25795=AXIS2_PLACEMENT_3D ( 'NONE', #8593, #40858, #40602 ) ;
#25801=VECTOR ( 'NONE', #11090, 39.37007874015748854 ) ;
#25802=CARTESIAN_POINT ( 'NONE',  ( 0.9436074722315215269, 1.690207154491363273, -2.072844574113425153 ) ) ;
#25803=CARTESIAN_POINT ( 'NONE',  ( -2.623503965249869729, 1.569838463031876685, 1.355882097269834885 ) ) ;
#25805=ORIENTED_EDGE ( 'NONE', *, *, #40017, .F. ) ;
#25808=DIRECTION ( 'NONE',  ( -0.000000000000000000, -1.000000000000000000, -0.000000000000000000 ) ) ;
#25810=CARTESIAN_POINT ( 'NONE',  ( -2.076715649576790224, 1.576214352228098470, 0.6230206298219045369 ) ) ;
#25812=EDGE_LOOP ( 'NONE', ( #5926, #14638, #1415, #15663 ) ) ;
#25813=ORIENTED_EDGE ( 'NONE', *, *, #31572, .T. ) ;
#25818=ORIENTED_EDGE ( 'NONE', *, *, #35135, .F. ) ;
#25819=EDGE_LOOP ( 'NONE', ( #21372, #6741, #49026, #1782 ) ) ;
#25820=CARTESIAN_POINT ( 'NONE',  ( -2.047277537895663801, 1.675111054312220515, 0.7169459839182066307 ) ) ;
#25826=( BOUNDED_CURVE ( )  B_SPLINE_CURVE ( 3, ( #6608, #37343, #22352, #38107 ),
 .UNSPECIFIED., .F., .F. ) 
 B_SPLINE_CURVE_WITH_KNOTS ( ( 4, 4 ),
 ( 2.995205087924649234, 3.045949865762518360 ),
 .UNSPECIFIED. ) 
 CURVE ( )  GEOMETRIC_REPRESENTATION_ITEM ( )  RATIONAL_B_SPLINE_CURVE ( ( 1.000000000000000000, 0.9997854254717271072, 0.9997854254717271072, 1.000000000000000000 ) ) 
 REPRESENTATION_ITEM ( '' )  );
#25830=DIRECTION ( 'NONE',  ( -0.000000000000000000, -1.000000000000000000, -0.000000000000000000 ) ) ;
#25831=DIRECTION ( 'NONE',  ( -0.9998717552508122886, -0.01601477604151182316, 0.000000000000000000 ) ) ;
#25833=ORIENTED_EDGE ( 'NONE', *, *, #6165, .T. ) ;
#25838=EDGE_CURVE ( 'NONE', #21355, #24653, #31013, .T. ) ;
#25842=ORIENTED_EDGE ( 'NONE', *, *, #3876, .F. ) ;
#25844=VERTEX_POINT ( 'NONE', #37266 ) ;
#25848=EDGE_LOOP ( 'NONE', ( #37579, #25155, #6523, #44175 ) ) ;
#25849=VERTEX_POINT ( 'NONE', #3404 ) ;
#25850=DIRECTION ( 'NONE',  ( 0.000000000000000000, 0.000000000000000000, 1.000000000000000000 ) ) ;
#25857=ORIENTED_EDGE ( 'NONE', *, *, #22581, .T. ) ;
#25858=EDGE_CURVE ( 'NONE', #17250, #35873, #26083, .T. ) ;
#25861=CARTESIAN_POINT ( 'NONE',  ( -1.461363083917493810, 6.692913385826772199, 1.597866488315562439 ) ) ;
#25863=B_SPLINE_CURVE_WITH_KNOTS ( 'NONE', 3,
 ( #37823, #33449, #2451, #2193 ),
 .UNSPECIFIED., .F., .F.,
 ( 4, 4 ),
 ( 2.032912791916312219E-07, 0.002500496826745732259 ),
 .UNSPECIFIED. ) ;
#25865=DIRECTION ( 'NONE',  ( 0.3930250316539278810, 0.000000000000000000, -0.9195277725514489076 ) ) ;
#25867=CARTESIAN_POINT ( 'NONE',  ( 0.08139965876239094178, 1.610780518492231694, 0.000000000000000000 ) ) ;
#25872=ORIENTED_EDGE ( 'NONE', *, *, #48014, .F. ) ;
#25874=AXIS2_PLACEMENT_3D ( 'NONE', #42572, #19071, #38954 ) ;
#25877=CARTESIAN_POINT ( 'NONE',  ( -2.695799277629577162, 1.571269479597534824, -1.205759334241492731 ) ) ;
#25878=CARTESIAN_POINT ( 'NONE',  ( 0.7513820654849657776, 1.719936709731724189, 2.142107623314860376 ) ) ;
#25879=ORIENTED_EDGE ( 'NONE', *, *, #15489, .F. ) ;
#25888=CARTESIAN_POINT ( 'NONE',  ( 2.793030215715258446, 0.000000000000000000, 0.9592557174602679426 ) ) ;
#25896=DIRECTION ( 'NONE',  ( 0.000000000000000000, 0.000000000000000000, 1.000000000000000000 ) ) ;
#25897=ORIENTED_EDGE ( 'NONE', *, *, #12225, .T. ) ;
#25898=CARTESIAN_POINT ( 'NONE',  ( -2.437180031585919782, 1.582844051365913662, -1.667735833703134718 ) ) ;
#25907=ORIENTED_EDGE ( 'NONE', *, *, #25445, .F. ) ;
#25908=CARTESIAN_POINT ( 'NONE',  ( -1.531154912952794378, 5.905511811023623991, 1.532020527533836329 ) ) ;
#25924=CARTESIAN_POINT ( 'NONE',  ( 0.08119777152254364916, 1.623385212329073957, 0.000000000000000000 ) ) ;
#25927=EDGE_CURVE ( 'NONE', #29864, #23897, #11411, .T. ) ;
#25936=EDGE_CURVE ( 'NONE', #15315, #38140, #49948, .T. ) ;
#25939=ORIENTED_EDGE ( 'NONE', *, *, #28685, .T. ) ;
#25943=EDGE_LOOP ( 'NONE', ( #27954, #24051, #7543, #21095 ) ) ;
#25945=LINE ( 'NONE', #50148, #29629 ) ;
#25953=AXIS2_PLACEMENT_3D ( 'NONE', #45375, #17524, #33284 ) ;
#25955=DIRECTION ( 'NONE',  ( 0.000000000000000000, -0.000000000000000000, 1.000000000000000000 ) ) ;
#25959=CARTESIAN_POINT ( 'NONE',  ( 2.734482843737263025, 1.452693199995327644, -1.115254632218672270 ) ) ;
#25963=CARTESIAN_POINT ( 'NONE',  ( -0.3498457532482182053, 1.702298530840201662, 2.203421978946157989 ) ) ;
#25968=EDGE_CURVE ( 'NONE', #45742, #19132, #36019, .T. ) ;
#25977=ADVANCED_FACE ( 'NONE', ( #7028 ), #1349, .T. ) ;
#25979=ORIENTED_EDGE ( 'NONE', *, *, #21092, .F. ) ;
#25994=ORIENTED_EDGE ( 'NONE', *, *, #37602, .F. ) ;
#25995=EDGE_CURVE ( 'NONE', #35300, #41147, #37315, .T. ) ;
#25996=DIRECTION ( 'NONE',  ( 1.160734090543304660E-16, -1.000000000000000000, 0.000000000000000000 ) ) ;
#25998=VERTEX_POINT ( 'NONE', #35661 ) ;
#26000=ORIENTED_EDGE ( 'NONE', *, *, #13871, .F. ) ;
#26001=ORIENTED_EDGE ( 'NONE', *, *, #35077, .T. ) ;
#26005=EDGE_CURVE ( 'NONE', #19370, #34440, #14550, .T. ) ;
#26007=DIRECTION ( 'NONE',  ( -0.01601477604151182663, 0.9998717552508123996, -0.000000000000000000 ) ) ;
#26008=CARTESIAN_POINT ( 'NONE',  ( -1.325491792074585451, 1.600165750963108646, -2.638988599164751481 ) ) ;
#26009=DIRECTION ( 'NONE',  ( -0.7227948638273878901, 0.000000000000000000, -0.6910626489868684219 ) ) ;
#26014=CONICAL_SURFACE ( 'NONE', #32584, 3.483074324928249421, 1.244861948955335196 ) ;
#26016=VECTOR ( 'NONE', #50796, 39.37007874015748143 ) ;
#26022=CARTESIAN_POINT ( 'NONE',  ( -0.2783729501556720387, 0.02346101323895649626, 1.809574371873096110 ) ) ;
#26023=AXIS2_PLACEMENT_3D ( 'NONE', #38252, #2874, #18627 ) ;
#26024=LINE ( 'NONE', #2022, #19333 ) ;
#26029=ADVANCED_FACE ( 'NONE', ( #47233 ), #8034, .F. ) ;
#26030=LINE ( 'NONE', #42031, #44832 ) ;
#26031=CARTESIAN_POINT ( 'NONE',  ( -1.472219874544909768, 1.597879704547665369, 2.560030851058948898 ) ) ;
#26032=DIRECTION ( 'NONE',  ( 0.9989930665413151445, 0.000000000000000000, -0.04486483035050446017 ) ) ;
#26036=DIRECTION ( 'NONE',  ( 0.000000000000000000, 0.000000000000000000, -1.000000000000000000 ) ) ;
#26037=ORIENTED_EDGE ( 'NONE', *, *, #16332, .F. ) ;
#26042=DIRECTION ( 'NONE',  ( 5.500355109725658086E-17, -1.000000000000000000, 1.022137253806229789E-16 ) ) ;
#26049=EDGE_LOOP ( 'NONE', ( #397, #39642, #41710, #5610 ) ) ;
#26051=CARTESIAN_POINT ( 'NONE',  ( -2.926032761125793247, 0.000000000000000000, 0.3963580683592094478 ) ) ;
#26056=DIRECTION ( 'NONE',  ( 0.000000000000000000, 0.000000000000000000, -1.000000000000000000 ) ) ;
#26057=AXIS2_PLACEMENT_3D ( 'NONE', #42179, #25674, #6819 ) ;
#26059=ORIENTED_EDGE ( 'NONE', *, *, #17766, .F. ) ;
#26061=DIRECTION ( 'NONE',  ( -9.701723960855857903E-17, 1.000000000000000000, 8.476140964546263859E-17 ) ) ;
#26071=EDGE_CURVE ( 'NONE', #30219, #38377, #3914, .T. ) ;
#26072=CARTESIAN_POINT ( 'NONE',  ( -2.151809081513409438, 1.673437530708463017, 0.2418202932658340965 ) ) ;
#26076=CARTESIAN_POINT ( 'NONE',  ( -0.9914495361339011881, 1.605369965488712136, 2.781765111341808705 ) ) ;
#26079=DIRECTION ( 'NONE',  ( 0.000000000000000000, -1.000000000000000000, 0.000000000000000000 ) ) ;
#26080=ADVANCED_FACE ( 'NONE', ( #43900 ), #40044, .F. ) ;
#26081=CARTESIAN_POINT ( 'NONE',  ( -0.1181847168586561830, 0.01737573915606907896, -1.862146645277666934 ) ) ;
#26083=CIRCLE ( 'NONE', #44201, 2.164630168518208109 ) ;
#26085=ORIENTED_EDGE ( 'NONE', *, *, #41257, .T. ) ;
#26088=CARTESIAN_POINT ( 'NONE',  ( 1.927369588301418135, 0.5223483550995119407, -1.213278145923846862 ) ) ;
#26089=VERTEX_POINT ( 'NONE', #27904 ) ;
#26091=ORIENTED_EDGE ( 'NONE', *, *, #7903, .T. ) ;
#26093=PLANE ( 'NONE',  #7217 ) ;
#26098=EDGE_CURVE ( 'NONE', #42847, #31120, #40315, .T. ) ;
#26099=ORIENTED_EDGE ( 'NONE', *, *, #20604, .T. ) ;
#26100=DIRECTION ( 'NONE',  ( -0.000000000000000000, -1.000000000000000000, 0.000000000000000000 ) ) ;
#26105=ORIENTED_EDGE ( 'NONE', *, *, #44017, .F. ) ;
#26107=DIRECTION ( 'NONE',  ( 1.086719731106949452E-16, -1.000000000000000000, -4.078527368698568598E-17 ) ) ;
#26108=ORIENTED_EDGE ( 'NONE', *, *, #14702, .F. ) ;
#26109=VERTEX_POINT ( 'NONE', #2529 ) ;
#26111=LINE ( 'NONE', #26856, #46581 ) ;
#26112=CARTESIAN_POINT ( 'NONE',  ( -1.402715216960007005, 0.000000000000000000, 1.097573363406495472 ) ) ;
#26113=DIRECTION ( 'NONE',  ( -0.8805955318567322276, 0.000000000000000000, -0.4738686624730094610 ) ) ;
#26119=ORIENTED_EDGE ( 'NONE', *, *, #15940, .F. ) ;
#26120=FACE_OUTER_BOUND ( 'NONE', #18376, .T. ) ;
#26122=AXIS2_PLACEMENT_3D ( 'NONE', #14899, #35282, #31152 ) ;
#26128=EDGE_CURVE ( 'NONE', #43511, #2179, #17865, .T. ) ;
#26129=( BOUNDED_CURVE ( )  B_SPLINE_CURVE ( 3, ( #15921, #946, #35806, #31677 ),
 .UNSPECIFIED., .F., .F. ) 
 B_SPLINE_CURVE_WITH_KNOTS ( ( 4, 4 ),
 ( 1.648115238091181434, 1.699061793389599950 ),
 .UNSPECIFIED. ) 
 CURVE ( )  GEOMETRIC_REPRESENTATION_ITEM ( )  RATIONAL_B_SPLINE_CURVE ( ( 1.000000000000000000, 0.9997837157376677775, 0.9997837157376677775, 1.000000000000000000 ) ) 
 REPRESENTATION_ITEM ( '' )  );
#26132=CARTESIAN_POINT ( 'NONE',  ( -1.591447364397243103, 0.002429723416550041374, -0.7337366736851151927 ) ) ;
#26133=CARTESIAN_POINT ( 'NONE',  ( 0.000000000000000000, 1.574803149606302854, 0.000000000000000000 ) ) ;
#26137=AXIS2_PLACEMENT_3D ( 'NONE', #30559, #50868, #47013 ) ;
#26138=CARTESIAN_POINT ( 'NONE',  ( 2.739172746247211965, 1.660034045467230657, -0.1722785920648685354 ) ) ;
#26140=CARTESIAN_POINT ( 'NONE',  ( 0.4435105686220205401, -2.456726483784180385E-16, 2.168331686854577001 ) ) ;
#26144=CARTESIAN_POINT ( 'NONE',  ( -1.556712866041156662, 1.548291375251236834, 2.509548638715847435 ) ) ;
#26145=ORIENTED_EDGE ( 'NONE', *, *, #5851, .T. ) ;
#26150=ORIENTED_EDGE ( 'NONE', *, *, #43827, .F. ) ;
#26165=ORIENTED_EDGE ( 'NONE', *, *, #36454, .F. ) ;
#26167=PLANE ( 'NONE',  #50680 ) ;
#26168=FACE_OUTER_BOUND ( 'NONE', #48358, .T. ) ;
#26170=ORIENTED_EDGE ( 'NONE', *, *, #43547, .F. ) ;
#26172=CARTESIAN_POINT ( 'NONE',  ( -1.929629134066536134, 1.574803149606302854, 0.9824921284572128988 ) ) ;
#26173=CARTESIAN_POINT ( 'NONE',  ( -2.277873973731453727, 1.562946399538843290, 1.879489153247635214 ) ) ;
#26175=CARTESIAN_POINT ( 'NONE',  ( -1.110003343315104862, 1.595669590305086816, -2.191522224601501367 ) ) ;
#26177=DIRECTION ( 'NONE',  ( 0.9998717552508121775, 0.01601477604151182663, 0.000000000000000000 ) ) ;
#26178=ORIENTED_EDGE ( 'NONE', *, *, #27076, .F. ) ;
#26182=CARTESIAN_POINT ( 'NONE',  ( 0.3467207527347885843, -2.578434962089329135E-16, 2.186201806782070545 ) ) ;
#26183=ORIENTED_EDGE ( 'NONE', *, *, #7267, .F. ) ;
#26193=AXIS2_PLACEMENT_3D ( 'NONE', #11175, #50601, #35679 ) ;
#26194=AXIS2_PLACEMENT_3D ( 'NONE', #11108, #50046, #50291 ) ;
#26195=ORIENTED_EDGE ( 'NONE', *, *, #37358, .F. ) ;
#26197=FACE_OUTER_BOUND ( 'NONE', #10509, .T. ) ;
#26200=EDGE_CURVE ( 'NONE', #27482, #26900, #27395, .T. ) ;
#26203=CARTESIAN_POINT ( 'NONE',  ( 0.7381027496705270252, 1.499047760149736952, -2.859439394060913298 ) ) ;
#26205=PLANE ( 'NONE',  #25128 ) ;
#26209=CARTESIAN_POINT ( 'NONE',  ( -2.168245791271168343, 1.587034731952809752, -2.004968704497279930 ) ) ;
#26212=AXIS2_PLACEMENT_3D ( 'NONE', #25441, #33207, #48890 ) ;
#26221=CARTESIAN_POINT ( 'NONE',  ( 0.7697133566244497294, 1.497596064125990667, -2.850715420863024985 ) ) ;
#26229=PLANE ( 'NONE',  #25187 ) ;
#26231=AXIS2_PLACEMENT_3D ( 'NONE', #2541, #34547, #26531 ) ;
#26234=CARTESIAN_POINT ( 'NONE',  ( -1.010509689441836390, 0.01173450346422093109, -1.474572740271697047 ) ) ;
#26238=FACE_BOUND ( 'NONE', #29646, .T. ) ;
#26244=DIRECTION ( 'NONE',  ( -0.01601477604151182663, 0.9998717552508123996, -0.000000000000000000 ) ) ;
#26252=CARTESIAN_POINT ( 'NONE',  ( -0.7148041136150262709, 1.205361022782829114E-17, -2.044646019095620826 ) ) ;
#26253=EDGE_CURVE ( 'NONE', #34410, #42971, #13895, .T. ) ;
#26256=LINE ( 'NONE', #37128, #27071 ) ;
#26260=ADVANCED_FACE ( 'NONE', ( #4055 ), #34784, .F. ) ;
#26262=DIRECTION ( 'NONE',  ( -0.01601477604151182663, 0.9998717552508123996, -0.000000000000000000 ) ) ;
#26265=CARTESIAN_POINT ( 'NONE',  ( 0.000000000000000000, 0.000000000000000000, 0.000000000000000000 ) ) ;
#26281=EDGE_CURVE ( 'NONE', #17189, #1621, #25585, .T. ) ;
#26284=B_SPLINE_CURVE_WITH_KNOTS ( 'NONE', 3,
 ( #28627, #29396, #47956, #40515 ),
 .UNSPECIFIED., .F., .F.,
 ( 4, 4 ),
 ( 2.007575928058895981E-07, 0.002500799887775291813 ),
 .UNSPECIFIED. ) ;
#26285=CARTESIAN_POINT ( 'NONE',  ( 0.7855418668307558860, 0.000000000000000000, -2.846347029613733870 ) ) ;
#26288=CARTESIAN_POINT ( 'NONE',  ( -1.088097428176262760, 1.690474079180120492, 1.917118167796188821 ) ) ;
#26290=VERTEX_POINT ( 'NONE', #26519 ) ;
#26292=VERTEX_POINT ( 'NONE', #3795 ) ;
#26296=CARTESIAN_POINT ( 'NONE',  ( 1.387661672111480948, 5.905511811023623991, -1.663104731517921930 ) ) ;
#26299=ORIENTED_EDGE ( 'NONE', *, *, #38149, .F. ) ;
#26300=CARTESIAN_POINT ( 'NONE',  ( -2.139229417893219853, 1.205361022782829114E-17, -0.3394403656973710159 ) ) ;
#26305=ORIENTED_EDGE ( 'NONE', *, *, #49291, .T. ) ;
#26306=CARTESIAN_POINT ( 'NONE',  ( 0.8069532150559736161, 1.205361022782829114E-17, -2.010061882867131278 ) ) ;
#26321=DIRECTION ( 'NONE',  ( 0.000000000000000000, 1.000000000000000000, 0.000000000000000000 ) ) ;
#26324=EDGE_CURVE ( 'NONE', #16783, #972, #7167, .T. ) ;
#26327=EDGE_LOOP ( 'NONE', ( #46868, #31827, #42541, #11153, #37212, #10576, #11385, #17417, #22436, #41105, #39333 ) ) ;
#26330=DIRECTION ( 'NONE',  ( 0.1785568947986229116, 0.000000000000000000, 0.9839295885986321100 ) ) ;
#26331=DIRECTION ( 'NONE',  ( -0.9998717552508122886, -0.01601477604151185785, 0.000000000000000000 ) ) ;
#26337=AXIS2_PLACEMENT_3D ( 'NONE', #14045, #10168, #22807 ) ;
#26343=ORIENTED_EDGE ( 'NONE', *, *, #39082, .T. ) ;
#26350=CONICAL_SURFACE ( 'NONE', #17298, 2.244934639244524632, 1.554780866114618743 ) ;
#26353=LINE ( 'NONE', #26600, #11161 ) ;
#26355=ORIENTED_EDGE ( 'NONE', *, *, #41851, .T. ) ;
#26356=CARTESIAN_POINT ( 'NONE',  ( -2.122513613727505799, 1.575480814016643638, -0.4339716895473832436 ) ) ;
#26358=ORIENTED_EDGE ( 'NONE', *, *, #36863, .F. ) ;
#26360=CARTESIAN_POINT ( 'NONE',  ( 2.603169958878716717, 0.9849481997864895089, 0.3029612783779465635 ) ) ;
#26363=CARTESIAN_POINT ( 'NONE',  ( 0.8329809839909848579, 0.000000000000000000, -2.833254665166554442 ) ) ;
#26364=EDGE_CURVE ( 'NONE', #22920, #44681, #29449, .T. ) ;
#26368=AXIS2_PLACEMENT_3D ( 'NONE', #22993, #38745, #3367 ) ;
#26375=EDGE_CURVE ( 'NONE', #47793, #20337, #27017, .T. ) ;
#26383=ORIENTED_EDGE ( 'NONE', *, *, #31717, .T. ) ;
#26386=CIRCLE ( 'NONE', #50256, 2.244934639244525076 ) ;
#26391=CARTESIAN_POINT ( 'NONE',  ( -2.339241080213612545, 1.682800407567106360, 1.802537235681883843 ) ) ;
#26392=CARTESIAN_POINT ( 'NONE',  ( 1.681836973804981428, 0.5249316475426862860, 0.8491494810026807283 ) ) ;
#26399=DIRECTION ( 'NONE',  ( 0.000000000000000000, 0.000000000000000000, 1.000000000000000000 ) ) ;
#26400=DIRECTION ( 'NONE',  ( 8.881784197001252323E-16, 0.000000000000000000, 1.000000000000000000 ) ) ;
#26404=CARTESIAN_POINT ( 'NONE',  ( -2.455258355620455024, 1.565786800488158770, -1.640348343447587398 ) ) ;
#26405=VERTEX_POINT ( 'NONE', #21074 ) ;
#26407=EDGE_LOOP ( 'NONE', ( #46545, #1197, #19856, #28578 ) ) ;
#26413=CARTESIAN_POINT ( 'NONE',  ( 1.481515513156649977, 0.000000000000000000, -0.9189724476880527515 ) ) ;
#26414=CIRCLE ( 'NONE', #45337, 2.244934639244525076 ) ;
#26417=ORIENTED_EDGE ( 'NONE', *, *, #224, .F. ) ;
#26424=VECTOR ( 'NONE', #34056, 39.37007874015748143 ) ;
#26425=DIRECTION ( 'NONE',  ( -0.01601477604151182663, 0.9998717552508123996, -0.000000000000000000 ) ) ;
#26428=CARTESIAN_POINT ( 'NONE',  ( 1.464430631143598172, 0.03384846671821301750, -1.332052510296074965 ) ) ;
#26429=DIRECTION ( 'NONE',  ( 0.000000000000000000, -1.000000000000000000, 0.000000000000000000 ) ) ;
#26432=LINE ( 'NONE', #9936, #5885 ) ;
#26436=VERTEX_POINT ( 'NONE', #44302 ) ;
#26437=ORIENTED_EDGE ( 'NONE', *, *, #35226, .T. ) ;
#26438=DIRECTION ( 'NONE',  ( 0.01601477604151182663, -0.9998717552508123996, 0.000000000000000000 ) ) ;
#26440=ADVANCED_FACE ( 'NONE', ( #28812 ), #20031, .T. ) ;
#26441=CARTESIAN_POINT ( 'NONE',  ( -1.775400203342670347, 1.552775173289138166, -2.359903268218729089 ) ) ;
#26444=EDGE_CURVE ( 'NONE', #16487, #9349, #25318, .T. ) ;
#26447=EDGE_CURVE ( 'NONE', #15782, #16783, #36389, .T. ) ;
#26453=FACE_OUTER_BOUND ( 'NONE', #1331, .T. ) ;
#26454=CARTESIAN_POINT ( 'NONE',  ( 0.07982360342473591996, 1.709180471932028711, 0.000000000000000000 ) ) ;
#26455=CARTESIAN_POINT ( 'NONE',  ( 1.485598995959307889, 5.905511811023623991, 1.625606721701626567 ) ) ;
#26456=EDGE_LOOP ( 'NONE', ( #43261, #51022, #38976, #27266 ) ) ;
#26457=DIRECTION ( 'NONE',  ( -0.9998717552508122886, -0.01601477604151181275, 0.000000000000000000 ) ) ;
#26458=VECTOR ( 'NONE', #29861, 39.37007874015748143 ) ;
#26460=ORIENTED_EDGE ( 'NONE', *, *, #38094, .T. ) ;
#26461=CARTESIAN_POINT ( 'NONE',  ( -1.833791099076586217, 1.574803149606302854, -1.151507526013721083 ) ) ;
#26462=CARTESIAN_POINT ( 'NONE',  ( 1.519644562253804621, 0.03439821511908755514, 1.274821374926282669 ) ) ;
#26467=VERTEX_POINT ( 'NONE', #44550 ) ;
#26474=ADVANCED_FACE ( 'NONE', ( #32193 ), #12048, .T. ) ;
#26479=CARTESIAN_POINT ( 'NONE',  ( 2.793030215715258446, 1.451280567205322836, 0.9592557174602683867 ) ) ;
#26483=LINE ( 'NONE', #22118, #19046 ) ;
#26484=AXIS2_PLACEMENT_3D ( 'NONE', #29867, #1988, #25736 ) ;
#26488=DIRECTION ( 'NONE',  ( -0.9998717552508122886, -0.01601477604151181275, 0.000000000000000000 ) ) ;
#26489=B_SPLINE_CURVE_WITH_KNOTS ( 'NONE', 3,
 ( #23625, #12008, #4014, #8136 ),
 .UNSPECIFIED., .F., .F.,
 ( 4, 4 ),
 ( 0.0003090509669333037202, 0.002809230294771062394 ),
 .UNSPECIFIED. ) ;
#26494=ORIENTED_EDGE ( 'NONE', *, *, #37248, .F. ) ;
#26495=EDGE_CURVE ( 'NONE', #48519, #14792, #43416, .T. ) ;
#26498=VERTEX_POINT ( 'NONE', #12557 ) ;
#26500=CARTESIAN_POINT ( 'NONE',  ( 1.319349709118413205, 0.000000000000000000, 1.584915398547334764 ) ) ;
#26503=CARTESIAN_POINT ( 'NONE',  ( -2.813306909032236014, 1.576974190620015648, 0.8968504722502548265 ) ) ;
#26506=CARTESIAN_POINT ( 'NONE',  ( 2.277873973731426194, 1.754757658573260048, 1.879489153247668076 ) ) ;
#26507=CARTESIAN_POINT ( 'NONE',  ( -0.5443978225238782498, 1.600757226547528500, -2.157565353623420723 ) ) ;
#26508=PLANE ( 'NONE',  #17926 ) ;
#26512=B_SPLINE_CURVE_WITH_KNOTS ( 'NONE', 3,
 ( #19933, #23071, #27435, #70 ),
 .UNSPECIFIED., .F., .F.,
 ( 4, 4 ),
 ( 0.01148951601955449514, 0.03073652705649548150 ),
 .UNSPECIFIED. ) ;
#26513=DIRECTION ( 'NONE',  ( 0.9998717552508121775, 0.01601477604151182663, 0.000000000000000000 ) ) ;
#26514=PLANE ( 'NONE',  #48703 ) ;
#26516=VERTEX_POINT ( 'NONE', #33729 ) ;
#26517=CONICAL_SURFACE ( 'NONE', #4263, 3.033577403570480779, 1.554780866114618743 ) ;
#26519=CARTESIAN_POINT ( 'NONE',  ( 0.3467207527347881402, 5.905511811023623991, 2.186201806782071433 ) ) ;
#26520=EDGE_LOOP ( 'NONE', ( #663, #11268, #254, #33539, #31228, #34800, #19665, #9945, #34826, #17855, #44718, #18369 ) ) ;
#26526=CARTESIAN_POINT ( 'NONE',  ( 2.222091332265985208, 1.743492810207595500, 0.6702560524809636489 ) ) ;
#26528=FACE_OUTER_BOUND ( 'NONE', #17938, .T. ) ;
#26530=AXIS2_PLACEMENT_3D ( 'NONE', #27402, #11915, #19396 ) ;
#26531=DIRECTION ( 'NONE',  ( 0.000000000000000000, 0.000000000000000000, -1.000000000000000000 ) ) ;
#26535=B_SPLINE_CURVE_WITH_KNOTS ( 'NONE', 3,
 ( #20949, #33354, #17341, #41093 ),
 .UNSPECIFIED., .F., .F.,
 ( 4, 4 ),
 ( 0.1211775127643062722, 0.1625894504277921315 ),
 .UNSPECIFIED. ) ;
#26541=DIRECTION ( 'NONE',  ( 0.000000000000000000, 1.160734090543304660E-16, -1.000000000000000000 ) ) ;
#26542=ORIENTED_EDGE ( 'NONE', *, *, #41835, .T. ) ;
#26543=CARTESIAN_POINT ( 'NONE',  ( 1.355960331127249452, 0.04963785175798203497, -1.364517356352728861 ) ) ;
#26547=CARTESIAN_POINT ( 'NONE',  ( 1.037524086854322292, 5.905511811023623991, 2.764473043227584803 ) ) ;
#26551=ORIENTED_EDGE ( 'NONE', *, *, #37237, .T. ) ;
#26552=LINE ( 'NONE', #26306, #40543 ) ;
#26554=ORIENTED_EDGE ( 'NONE', *, *, #47745, .T. ) ;
#26557=EDGE_CURVE ( 'NONE', #5044, #8046, #25705, .T. ) ;
#26558=ORIENTED_EDGE ( 'NONE', *, *, #1036, .F. ) ;
#26560=DIRECTION ( 'NONE',  ( -0.000000000000000000, 1.000000000000000000, -0.000000000000000000 ) ) ;
#26561=VECTOR ( 'NONE', #2557, 39.37007874015748143 ) ;
#26563=ADVANCED_FACE ( 'NONE', ( #49413 ), #49149, .T. ) ;
#26565=AXIS2_PLACEMENT_3D ( 'NONE', #29036, #48113, #1166 ) ;
#26569=CIRCLE ( 'NONE', #25733, 2.244934639244525076 ) ;
#26575=LINE ( 'NONE', #41569, #11464 ) ;
#26577=ADVANCED_FACE ( 'NONE', ( #6605 ), #4663, .T. ) ;
#26579=CARTESIAN_POINT ( 'NONE',  ( -2.889674983507169337, 1.575792602931942232, -0.6090712660038034576 ) ) ;
#26582=ORIENTED_EDGE ( 'NONE', *, *, #17468, .F. ) ;
#26588=AXIS2_PLACEMENT_3D ( 'NONE', #13686, #2569, #22199 ) ;
#26600=CARTESIAN_POINT ( 'NONE',  ( 0.04921259842519603439, 6.692913385826772199, 2.164795024401847456 ) ) ;
#26602=ADVANCED_FACE ( 'NONE', ( #1962 ), #14343, .F. ) ;
#26603=EDGE_CURVE ( 'NONE', #16416, #38863, #45590, .T. ) ;
#26606=DIRECTION ( 'NONE',  ( -0.000000000000000000, -1.000000000000000000, -0.000000000000000000 ) ) ;
#26609=CARTESIAN_POINT ( 'NONE',  ( 1.944213194762889119, 0.05905979794000976862, 0.2136995197171435157 ) ) ;
#26610=CARTESIAN_POINT ( 'NONE',  ( 0.9838852166858921278, 0.000000000000000000, 1.929635236160317735 ) ) ;
#26612=CYLINDRICAL_SURFACE ( 'NONE', #39205, 2.165354330708661568 ) ;
#26613=ORIENTED_EDGE ( 'NONE', *, *, #29197, .F. ) ;
#26614=CARTESIAN_POINT ( 'NONE',  ( 0.3595914698493179462, 0.000000000000000000, 1.705899337635486290 ) ) ;
#26615=ADVANCED_FACE ( 'NONE', ( #29586 ), #33583, .T. ) ;
#26616=FACE_OUTER_BOUND ( 'NONE', #36768, .T. ) ;
#26620=EDGE_CURVE ( 'NONE', #46385, #27405, #18217, .T. ) ;
#26622=EDGE_LOOP ( 'NONE', ( #22814, #39368, #21203, #16794 ) ) ;
#26628=DIRECTION ( 'NONE',  ( -0.2225209339563041788, 0.000000000000000000, -0.9749279121818259508 ) ) ;
#26633=LINE ( 'NONE', #22771, #2066 ) ;
#26634=ORIENTED_EDGE ( 'NONE', *, *, #21701, .T. ) ;
#26635=CARTESIAN_POINT ( 'NONE',  ( -1.252056778656947422, 1.687847970117562602, -1.807033786809818077 ) ) ;
#26637=LINE ( 'NONE', #38528, #3670 ) ;
#26643=VERTEX_POINT ( 'NONE', #13838 ) ;
#26647=EDGE_CURVE ( 'NONE', #42204, #7708, #11229, .T. ) ;
#26649=CARTESIAN_POINT ( 'NONE',  ( -2.339241080213612545, 1.564176246289736616, 1.802537235681883843 ) ) ;
#26651=CARTESIAN_POINT ( 'NONE',  ( 1.735586374879371174, 5.905511811023623991, -2.388829707800026014 ) ) ;
#26654=ORIENTED_EDGE ( 'NONE', *, *, #11771, .F. ) ;
#26657=CARTESIAN_POINT ( 'NONE',  ( 0.08139965876239094178, 1.610780518492231694, 0.000000000000000000 ) ) ;
#26659=EDGE_CURVE ( 'NONE', #16076, #29695, #50490, .T. ) ;
#26660=CARTESIAN_POINT ( 'NONE',  ( 0.1067246931122726866, 0.02962905676920215767, 0.000000000000000000 ) ) ;
#26662=CARTESIAN_POINT ( 'NONE',  ( -2.010517631316633747, 5.905511811023623991, 0.8058170502102095512 ) ) ;
#26667=VERTEX_POINT ( 'NONE', #34979 ) ;
#26673=CARTESIAN_POINT ( 'NONE',  ( -2.275362778309363065, 1.679744148766246337, -1.442986439457680126 ) ) ;
#26675=CONICAL_SURFACE ( 'NONE', #6889, 2.244934639244524632, 1.554780866114618743 ) ;
#26678=ORIENTED_EDGE ( 'NONE', *, *, #28280, .F. ) ;
#26679=CARTESIAN_POINT ( 'NONE',  ( 2.153610746787201435, 1.643970771453353130, -0.8669779829368272628 ) ) ;
#26681=PLANE ( 'NONE',  #30503 ) ;
#26683=LINE ( 'NONE', #11951, #37303 ) ;
#26685=VECTOR ( 'NONE', #33903, 39.37007874015748143 ) ;
#26692=CARTESIAN_POINT ( 'NONE',  ( -1.738757879605812073, 7.027592017269983715E-05, -0.1273499085982673085 ) ) ;
#26695=DIRECTION ( 'NONE',  ( -0.000000000000000000, 1.000000000000000000, -0.000000000000000000 ) ) ;
#26702=EDGE_CURVE ( 'NONE', #19788, #13030, #50166, .T. ) ;
#26703=AXIS2_PLACEMENT_3D ( 'NONE', #3203, #35461, #50387 ) ;
#26704=FACE_OUTER_BOUND ( 'NONE', #24542, .T. ) ;
#26708=DIRECTION ( 'NONE',  ( -0.4338837391175656699, 0.000000000000000000, 0.9009688679024154823 ) ) ;
#26714=ORIENTED_EDGE ( 'NONE', *, *, #8366, .T. ) ;
#26717=DIRECTION ( 'NONE',  ( -0.01601477604151182663, 0.9998717552508123996, -0.000000000000000000 ) ) ;
#26718=LINE ( 'NONE', #39104, #35739 ) ;
#26723=ORIENTED_EDGE ( 'NONE', *, *, #47779, .T. ) ;
#26729=ORIENTED_EDGE ( 'NONE', *, *, #7781, .F. ) ;
#26731=CARTESIAN_POINT ( 'NONE',  ( 0.8329809839909849689, 1.496921813388997435, -2.833254665166554442 ) ) ;
#26734=DIRECTION ( 'NONE',  ( 0.000000000000000000, 1.000000000000000000, 0.000000000000000000 ) ) ;
#26735=CARTESIAN_POINT ( 'NONE',  ( -1.744243240276441398, 6.692913385826772199, 1.328042291889479642 ) ) ;
#26738=VERTEX_POINT ( 'NONE', #15100 ) ;
#26741=AXIS2_PLACEMENT_3D ( 'NONE', #20984, #20467, #36229 ) ;
#26744=VERTEX_POINT ( 'NONE', #31105 ) ;
#26746=VECTOR ( 'NONE', #43790, 39.37007874015748854 ) ;
#26749=VECTOR ( 'NONE', #41029, 39.37007874015748143 ) ;
#26753=DIRECTION ( 'NONE',  ( -3.986037398843765983E-20, -1.000000000000000000, -1.160734090543304660E-16 ) ) ;
#26757=EDGE_CURVE ( 'NONE', #50819, #18885, #31445, .T. ) ;
#26759=CARTESIAN_POINT ( 'NONE',  ( 2.318785432993162310, 1.755386055154334990, 1.828187805977548930 ) ) ;
#26764=CARTESIAN_POINT ( 'NONE',  ( 2.164658444855302122, 5.905511811023623991, -0.04795272066889885720 ) ) ;
#26775=AXIS2_PLACEMENT_3D ( 'NONE', #29958, #37971, #18337 ) ;
#26780=CONICAL_SURFACE ( 'NONE', #4537, 2.246510896728926010, 0.01601546068027819014 ) ;
#26781=CARTESIAN_POINT ( 'NONE',  ( -1.546800823997126262, 1.683127104815683728, -1.546979550173933182 ) ) ;
#26785=LINE ( 'NONE', #42537, #8671 ) ;
#26787=ADVANCED_FACE ( 'NONE', ( #24885 ), #22841, .T. ) ;
#26791=ORIENTED_EDGE ( 'NONE', *, *, #26364, .F. ) ;
#26792=DIRECTION ( 'NONE',  ( 0.000000000000000000, 0.000000000000000000, 1.000000000000000000 ) ) ;
#26793=ADVANCED_FACE ( 'NONE', ( #4496 ), #32384, .T. ) ;
#26794=VERTEX_POINT ( 'NONE', #47820 ) ;
#26801=ORIENTED_EDGE ( 'NONE', *, *, #48239, .T. ) ;
#26803=CARTESIAN_POINT ( 'NONE',  ( 0.1946711146504565004, 1.620088713232310518, -2.711980127628132120 ) ) ;
#26806=CARTESIAN_POINT ( 'NONE',  ( 2.164658444855302122, 5.905511811023623991, -0.04795272066889885720 ) ) ;
#26808=VERTEX_POINT ( 'NONE', #1123 ) ;
#26811=CARTESIAN_POINT ( 'NONE',  ( 0.000000000000000000, 0.000000000000000000, 0.000000000000000000 ) ) ;
#26812=AXIS2_PLACEMENT_3D ( 'NONE', #37492, #1342, #17102 ) ;
#26813=CONICAL_SURFACE ( 'NONE', #4567, 2.246510896728926010, 0.01601546068027819014 ) ;
#26822=EDGE_CURVE ( 'NONE', #7819, #25003, #19720, .T. ) ;
#26823=VECTOR ( 'NONE', #30610, 39.37007874015748143 ) ;
#26829=EDGE_CURVE ( 'NONE', #1980, #30932, #12333, .T. ) ;
#26831=CARTESIAN_POINT ( 'NONE',  ( 2.042485253772177156, 1.205361022782829114E-17, 0.6118985000151695441 ) ) ;
#26832=CARTESIAN_POINT ( 'NONE',  ( 0.002207914879453961969, 5.905511811023623991, 0.04916304461325442243 ) ) ;
#26840=EDGE_CURVE ( 'NONE', #24696, #16316, #17093, .T. ) ;
#26849=DIRECTION ( 'NONE',  ( -0.9998717552508122886, -0.01601477604151180928, 0.000000000000000000 ) ) ;
#26850=AXIS2_PLACEMENT_3D ( 'NONE', #9347, #40848, #5475 ) ;
#26852=VECTOR ( 'NONE', #3936, 39.37007874015748143 ) ;
#26853=LINE ( 'NONE', #39752, #20586 ) ;
#26856=CARTESIAN_POINT ( 'NONE',  ( -0.4350747367504789187, 5.905511811023623991, -2.121846421795420490 ) ) ;
#26857=CARTESIAN_POINT ( 'NONE',  ( 0.002207914879453961535, -5.712274067634378313E-18, 0.04916304461325374242 ) ) ;
#26858=CYLINDRICAL_SURFACE ( 'NONE', #23653, 2.165354330708661568 ) ;
#26859=VERTEX_POINT ( 'NONE', #28229 ) ;
#26863=DIRECTION ( 'NONE',  ( -0.01601477604151182663, 0.9998717552508123996, -0.000000000000000000 ) ) ;
#26865=VERTEX_POINT ( 'NONE', #20748 ) ;
#26868=PLANE ( 'NONE',  #48054 ) ;
#26872=VERTEX_POINT ( 'NONE', #31606 ) ;
#26874=EDGE_CURVE ( 'NONE', #1640, #25170, #7398, .T. ) ;
#26876=EDGE_CURVE ( 'NONE', #9734, #27371, #40686, .T. ) ;
#26877=CIRCLE ( 'NONE', #49117, 2.164630168518208109 ) ;
#26883=EDGE_CURVE ( 'NONE', #27703, #45433, #8024, .T. ) ;
#26887=CARTESIAN_POINT ( 'NONE',  ( 2.136190583516914820, 1.205361022782829114E-17, -0.1451986319116555235 ) ) ;
#26891=ORIENTED_EDGE ( 'NONE', *, *, #4971, .T. ) ;
#26897=DIRECTION ( 'NONE',  ( -0.9998717552508121775, -0.01601477604151182316, 0.000000000000000000 ) ) ;
#26899=CARTESIAN_POINT ( 'NONE',  ( 1.556712866041120247, 1.743522182421873401, 2.509548638715870084 ) ) ;
#26900=VERTEX_POINT ( 'NONE', #40386 ) ;
#26905=ORIENTED_EDGE ( 'NONE', *, *, #4226, .T. ) ;
#26907=DIRECTION ( 'NONE',  ( -0.9998717552508122886, -0.01601477604151182316, 0.000000000000000000 ) ) ;
#26908=VERTEX_POINT ( 'NONE', #8875 ) ;
#26913=AXIS2_PLACEMENT_3D ( 'NONE', #37084, #17962, #30093 ) ;
#26915=VERTEX_POINT ( 'NONE', #41395 ) ;
#26917=FACE_OUTER_BOUND ( 'NONE', #31855, .T. ) ;
#26918=AXIS2_PLACEMENT_3D ( 'NONE', #3784, #3273, #3528 ) ;
#26923=FACE_OUTER_BOUND ( 'NONE', #45845, .T. ) ;
#26928=ORIENTED_EDGE ( 'NONE', *, *, #32925, .F. ) ;
#26930=CARTESIAN_POINT ( 'NONE',  ( -2.164823134740036181, 1.673236549936605977, -0.04796011690018290446 ) ) ;
#26934=DIRECTION ( 'NONE',  ( -3.986037398843765983E-20, -1.000000000000000000, -1.160734090543304660E-16 ) ) ;
#26937=EDGE_LOOP ( 'NONE', ( #50815, #31685, #18109, #35821 ) ) ;
#26943=DIRECTION ( 'NONE',  ( 0.01601477604151182663, -0.9998717552508123996, 0.000000000000000000 ) ) ;
#26945=CARTESIAN_POINT ( 'NONE',  ( -1.530693736245497316, 5.905511811023623991, -1.531579597454066688 ) ) ;
#26950=EDGE_CURVE ( 'NONE', #7408, #2174, #10408, .T. ) ;
#26953=ADVANCED_FACE ( 'NONE', ( #1637 ), #46710, .T. ) ;
#26954=FACE_OUTER_BOUND ( 'NONE', #36846, .T. ) ;
#26966=DIRECTION ( 'NONE',  ( -0.9998717552508121775, -0.01601477604151182316, 0.000000000000000000 ) ) ;
#26969=ORIENTED_EDGE ( 'NONE', *, *, #14702, .T. ) ;
#26974=EDGE_CURVE ( 'NONE', #39762, #20325, #42505, .T. ) ;
#26980=CARTESIAN_POINT ( 'NONE',  ( 0.6157060065419059924, 0.5249316497054298258, 1.780600057069692710 ) ) ;
#26983=CARTESIAN_POINT ( 'NONE',  ( 1.617022397669051870, 1.737311993599926607, 1.925629205347350492 ) ) ;
#26985=ORIENTED_EDGE ( 'NONE', *, *, #30774, .T. ) ;
#26986=DIRECTION ( 'NONE',  ( 0.000000000000000000, 0.000000000000000000, 1.000000000000000000 ) ) ;
#26988=ADVANCED_FACE ( 'NONE', ( #21011 ), #12143, .T. ) ;
#26990=DIRECTION ( 'NONE',  ( -0.2660368455666826670, 0.000000000000000000, 0.9639628606958512425 ) ) ;
#26991=ORIENTED_EDGE ( 'NONE', *, *, #38939, .F. ) ;
#26993=DIRECTION ( 'NONE',  ( -0.04486483035051863633, 1.288287287306305283E-16, 0.9989930665413144784 ) ) ;
#26999=CARTESIAN_POINT ( 'NONE',  ( 0.5548376931676505253, 1.651171896322103150, -2.195393375338218878 ) ) ;
#27003=CARTESIAN_POINT ( 'NONE',  ( 2.112319093887386146, 0.000000000000000000, 0.3357951146312926904 ) ) ;
#27009=CARTESIAN_POINT ( 'NONE',  ( -2.695799277629577162, 0.000000000000000000, -1.205759334241492509 ) ) ;
#27017=LINE ( 'NONE', #42771, #18676 ) ;
#27019=CARTESIAN_POINT ( 'NONE',  ( 1.971834065208952769, 1.205361022782829114E-17, 0.8963217522330182430 ) ) ;
#27020=AXIS2_PLACEMENT_3D ( 'NONE', #22294, #6794, #14284 ) ;
#27026=CARTESIAN_POINT ( 'NONE',  ( 0.04921259842519613847, 5.905511811023623991, -2.165433070866141119 ) ) ;
#27027=CARTESIAN_POINT ( 'NONE',  ( 0.1067246931122726866, 0.02962905676920215767, 0.000000000000000000 ) ) ;
#27030=CARTESIAN_POINT ( 'NONE',  ( -2.878724150143177507, 0.000000000000000000, -0.6570500018395228903 ) ) ;
#27034=AXIS2_PLACEMENT_3D ( 'NONE', #29938, #45653, #36670 ) ;
#27035=B_SPLINE_CURVE_WITH_KNOTS ( 'NONE', 3,
 ( #3354, #30222, #42338, #7483 ),
 .UNSPECIFIED., .F., .F.,
 ( 4, 4 ),
 ( 2.136715943794443357E-07, 0.01735814470125059822 ),
 .UNSPECIFIED. ) ;
#27040=CARTESIAN_POINT ( 'NONE',  ( 0.04921259842519675604, 1.019021312707606430, 2.584985224492306610 ) ) ;
#27042=CARTESIAN_POINT ( 'NONE',  ( 0.1067246931122726866, 0.02962905676920215767, 0.000000000000000000 ) ) ;
#27044=EDGE_CURVE ( 'NONE', #19370, #25998, #2412, .T. ) ;
#27046=EDGE_CURVE ( 'NONE', #47061, #22090, #15431, .T. ) ;
#27048=DIRECTION ( 'NONE',  ( -0.000000000000000000, 1.000000000000000000, -0.000000000000000000 ) ) ;
#27049=ADVANCED_FACE ( 'NONE', ( #29521 ), #42614, .T. ) ;
#27052=DIRECTION ( 'NONE',  ( 0.6579387259397138088, 8.738534663690390683E-17, -0.7530714660036099684 ) ) ;
#27056=ORIENTED_EDGE ( 'NONE', *, *, #9263, .F. ) ;
#27058=EDGE_CURVE ( 'NONE', #6407, #33053, #16639, .T. ) ;
#27060=CARTESIAN_POINT ( 'NONE',  ( -1.739002864725096353, 1.589738220721540696, 2.065247083924816263 ) ) ;
#27061=VERTEX_POINT ( 'NONE', #42393 ) ;
#27062=AXIS2_PLACEMENT_3D ( 'NONE', #3708, #19941, #39584 ) ;
#27063=EDGE_CURVE ( 'NONE', #50666, #25092, #9224, .T. ) ;
#27065=ORIENTED_EDGE ( 'NONE', *, *, #40436, .T. ) ;
#27071=VECTOR ( 'NONE', #48687, 39.37007874015748143 ) ;
#27074=CARTESIAN_POINT ( 'NONE',  ( -0.4788131938641533303, 1.613355999311305133, 2.914091152102185944 ) ) ;
#27075=CARTESIAN_POINT ( 'NONE',  ( -2.950518648203841021, 1.673261099661152773, -0.1160872160806489667 ) ) ;
#27076=EDGE_CURVE ( 'NONE', #5201, #41095, #40987, .T. ) ;
#27080=DIRECTION ( 'NONE',  ( -0.9839295885986321100, -1.160734090543304660E-16, 0.1785568947986229116 ) ) ;
#27081=B_SPLINE_CURVE_WITH_KNOTS ( 'NONE', 3,
 ( #3172, #33423, #13788, #45248 ),
 .UNSPECIFIED., .F., .F.,
 ( 4, 4 ),
 ( 3.689117391458506506E-07, 0.04851997785222408183 ),
 .UNSPECIFIED. ) ;
#27087=B_SPLINE_CURVE_WITH_KNOTS ( 'NONE', 3,
 ( #35537, #38397, #15657, #15151 ),
 .UNSPECIFIED., .F., .F.,
 ( 4, 4 ),
 ( 2.895194837543627171E-07, 0.01651717637142990913 ),
 .UNSPECIFIED. ) ;
#27100=CARTESIAN_POINT ( 'NONE',  ( -0.3742159057234073494, 0.02192591290182492950, 1.786486621533327712 ) ) ;
#27101=CARTESIAN_POINT ( 'NONE',  ( -1.387241876633673598, 1.574803149606302854, 1.662624236931676824 ) ) ;
#27103=B_SPLINE_CURVE_WITH_KNOTS ( 'NONE', 3,
 ( #18668, #26404, #22289, #22036 ),
 .UNSPECIFIED., .F., .F.,
 ( 4, 4 ),
 ( 2.396011864035455169E-07, 0.002500390292889080948 ),
 .UNSPECIFIED. ) ;
#27106=EDGE_CURVE ( 'NONE', #25849, #42, #22754, .T. ) ;
#27111=DIRECTION ( 'NONE',  ( -1.045785279492548401E-16, -1.000000000000000000, 5.036236473261409814E-17 ) ) ;
#27113=FACE_OUTER_BOUND ( 'NONE', #5470, .T. ) ;
#27114=VECTOR ( 'NONE', #11663, 39.37007874015748143 ) ;
#27120=B_SPLINE_CURVE_WITH_KNOTS ( 'NONE', 3,
 ( #15381, #15629, #27745, #386 ),
 .UNSPECIFIED., .F., .F.,
 ( 4, 4 ),
 ( 2.008389810339514362E-07, 0.01780505990002694341 ),
 .UNSPECIFIED. ) ;
#27125=PLANE ( 'NONE',  #44913 ) ;
#27126=CARTESIAN_POINT ( 'NONE',  ( -2.152441353505195387, 0.000000000000000000, -0.2419059403265113872 ) ) ;
#27131=B_SPLINE_CURVE_WITH_KNOTS ( 'NONE', 3,
 ( #46344, #2249, #29619, #29870 ),
 .UNSPECIFIED., .F., .F.,
 ( 4, 4 ),
 ( 0.01379717137572002324, 0.03074487227025578251 ),
 .UNSPECIFIED. ) ;
#27132=ORIENTED_EDGE ( 'NONE', *, *, #32751, .F. ) ;
#27135=DIRECTION ( 'NONE',  ( 0.01601477604151182663, -0.9998717552508123996, 0.000000000000000000 ) ) ;
#27136=EDGE_LOOP ( 'NONE', ( #30622, #46171, #20520, #34022 ) ) ;
#27137=EDGE_CURVE ( 'NONE', #12624, #8046, #1174, .T. ) ;
#27138=CARTESIAN_POINT ( 'NONE',  ( 2.592410251782301778, 1.759648616974466950, 1.413663899099648180 ) ) ;
#27140=AXIS2_PLACEMENT_3D ( 'NONE', #602, #32362, #20210 ) ;
#27145=ORIENTED_EDGE ( 'NONE', *, *, #38439, .F. ) ;
#27148=AXIS2_PLACEMENT_3D ( 'NONE', #28166, #40055, #20427 ) ;
#27149=ORIENTED_EDGE ( 'NONE', *, *, #50803, .F. ) ;
#27151=CARTESIAN_POINT ( 'NONE',  ( -0.6089661318347402430, 1.603610328167266230, -2.391523368051897247 ) ) ;
#27152=CARTESIAN_POINT ( 'NONE',  ( 1.472219874544873131, 1.742205712729733014, 2.560030851058970214 ) ) ;
#27155=DIRECTION ( 'NONE',  ( -3.986037398843765983E-20, -1.000000000000000000, -1.160734090543304660E-16 ) ) ;
#27156=ORIENTED_EDGE ( 'NONE', *, *, #42428, .F. ) ;
#27157=B_SPLINE_CURVE_WITH_KNOTS ( 'NONE', 3,
 ( #11302, #20044, #31949, #47644 ),
 .UNSPECIFIED., .F., .F.,
 ( 4, 4 ),
 ( 0.1211775127643062860, 0.1625894504277921315 ),
 .UNSPECIFIED. ) ;
#27163=VECTOR ( 'NONE', #5148, 39.37007874015748143 ) ;
#27166=ORIENTED_EDGE ( 'NONE', *, *, #14264, .T. ) ;
#27168=PLANE ( 'NONE',  #5931 ) ;
#27169=DIRECTION ( 'NONE',  ( -0.01601477604151182663, 0.9998717552508123996, -0.000000000000000000 ) ) ;
#27172=ORIENTED_EDGE ( 'NONE', *, *, #367, .F. ) ;
#27174=LINE ( 'NONE', #42168, #42558 ) ;
#27175=CARTESIAN_POINT ( 'NONE',  ( 0.7308738700548027545, 6.692913385826772199, 2.087463732006447970 ) ) ;
#27178=VECTOR ( 'NONE', #38019, 39.37007874015748143 ) ;
#27181=PLANE ( 'NONE',  #20525 ) ;
#27185=ORIENTED_EDGE ( 'NONE', *, *, #37063, .F. ) ;
#27191=VERTEX_POINT ( 'NONE', #32064 ) ;
#27193=DIRECTION ( 'NONE',  ( 0.000000000000000000, 1.000000000000000000, 0.000000000000000000 ) ) ;
#27194=CARTESIAN_POINT ( 'NONE',  ( 2.013783482383322720, 1.740156378764222245, 1.139548688847630942 ) ) ;
#27205=B_SPLINE_CURVE_WITH_KNOTS ( 'NONE', 3,
 ( #25159, #5538, #35755, #384 ),
 .UNSPECIFIED., .F., .F.,
 ( 4, 4 ),
 ( 2.175031256469753215E-07, 0.01988369477650668918 ),
 .UNSPECIFIED. ) ;
#27206=CARTESIAN_POINT ( 'NONE',  ( -1.723687301221637824, 6.692913385826772199, -1.311649477509824857 ) ) ;
#27208=ORIENTED_EDGE ( 'NONE', *, *, #49799, .F. ) ;
#27209=CARTESIAN_POINT ( 'NONE',  ( -1.721689136163420786, 1.040663155869206546, 1.895833630352641297 ) ) ;
#27210=B_SPLINE_CURVE_WITH_KNOTS ( 'NONE', 3,
 ( #28462, #39078, #47289, #47799 ),
 .UNSPECIFIED., .F., .F.,
 ( 4, 4 ),
 ( 0.1211775127643062860, 0.1625773253007936625 ),
 .UNSPECIFIED. ) ;
#27215=CARTESIAN_POINT ( 'NONE',  ( 0.002207914879453961535, -5.712274067634378313E-18, 0.04916304461325374242 ) ) ;
#27218=CARTESIAN_POINT ( 'NONE',  ( 3.937007874015748143, 2.755905511811027164, 1.181102362204724088 ) ) ;
#27222=ORIENTED_EDGE ( 'NONE', *, *, #188, .T. ) ;
#27223=CARTESIAN_POINT ( 'NONE',  ( -1.236813753895213086, 1.699986652445209634, -2.681693691597581974 ) ) ;
#27239=EDGE_LOOP ( 'NONE', ( #34866, #6536, #10345, #43076 ) ) ;
#27243=ADVANCED_FACE ( 'NONE', ( #23793 ), #47242, .F. ) ;
#27245=ORIENTED_EDGE ( 'NONE', *, *, #47370, .T. ) ;
#27246=CARTESIAN_POINT ( 'NONE',  ( -1.642191404871911731, 0.000000000000000000, 0.5853255206279681655 ) ) ;
#27248=ORIENTED_EDGE ( 'NONE', *, *, #23545, .T. ) ;
#27249=PLANE ( 'NONE',  #31652 ) ;
#27253=ORIENTED_EDGE ( 'NONE', *, *, #2957, .T. ) ;
#27259=CARTESIAN_POINT ( 'NONE',  ( 0.000000000000000000, 0.000000000000000000, 0.000000000000000000 ) ) ;
#27262=EDGE_CURVE ( 'NONE', #13018, #49693, #20161, .T. ) ;
#27264=DIRECTION ( 'NONE',  ( -0.9998717552508122886, -0.01601477604151181275, 0.000000000000000000 ) ) ;
#27266=ORIENTED_EDGE ( 'NONE', *, *, #3598, .F. ) ;
#27273=CARTESIAN_POINT ( 'NONE',  ( 1.871568535323528293, 0.5220372540190395538, -1.294378953913108754 ) ) ;
#27274=CARTESIAN_POINT ( 'NONE',  ( -0.8429824507881226170, 1.205361022782829114E-17, -1.637047627937372241 ) ) ;
#27277=CARTESIAN_POINT ( 'NONE',  ( -1.274276310699785864, 1.035612906144991907, 2.228729129513292495 ) ) ;
#27279=CARTESIAN_POINT ( 'NONE',  ( 2.223067892362281750, 1.710700052957827788, 0.6705733560908055946 ) ) ;
#27283=CARTESIAN_POINT ( 'NONE',  ( 1.629751586730974422, 1.668388608423060138, -1.626288599946028590 ) ) ;
#27286=DIRECTION ( 'NONE',  ( 3.586865599282270385E-17, -1.000000000000000000, 1.103923720497139891E-16 ) ) ;
#27293=CARTESIAN_POINT ( 'NONE',  ( -0.8190294238272288752, 1.698713383322939530, 2.322353365030251915 ) ) ;
#27296=ORIENTED_EDGE ( 'NONE', *, *, #44772, .T. ) ;
#27298=LINE ( 'NONE', #35825, #28073 ) ;
#27303=ORIENTED_EDGE ( 'NONE', *, *, #36592, .F. ) ;
#27304=ORIENTED_EDGE ( 'NONE', *, *, #27757, .T. ) ;
#27307=DIRECTION ( 'NONE',  ( -0.000000000000000000, 1.000000000000000000, 0.000000000000000000 ) ) ;
#27314=ORIENTED_EDGE ( 'NONE', *, *, #43700, .T. ) ;
#27315=CARTESIAN_POINT ( 'NONE',  ( 2.277873973731426638, 1.463603380278871713, 1.879489153247667632 ) ) ;
#27318=CONICAL_SURFACE ( 'NONE', #5080, 2.244934639244524632, 1.554780866114618743 ) ;
#27321=ORIENTED_EDGE ( 'NONE', *, *, #21195, .F. ) ;
#27328=CARTESIAN_POINT ( 'NONE',  ( 2.808237744965994320, 0.000000000000000000, 0.9124517550441679781 ) ) ;
#27330=FACE_OUTER_BOUND ( 'NONE', #39186, .T. ) ;
#27333=DIRECTION ( 'NONE',  ( -0.9998717552508122886, -0.01601477604151182316, 0.000000000000000000 ) ) ;
#27336=DIRECTION ( 'NONE',  ( 0.6910626489868684219, 0.000000000000000000, -0.7227948638273878901 ) ) ;
#27338=CARTESIAN_POINT ( 'NONE',  ( 2.823445274216730638, 1.205361022782829114E-17, 0.8656477926280680135 ) ) ;
#27339=ORIENTED_EDGE ( 'NONE', *, *, #23407, .T. ) ;
#27343=EDGE_LOOP ( 'NONE', ( #41375, #8072, #46724, #31016 ) ) ;
#27345=CARTESIAN_POINT ( 'NONE',  ( -1.880560108260527885, 1.049866565067837598, -0.7502705391232876719 ) ) ;
#27359=VERTEX_POINT ( 'NONE', #5454 ) ;
#27360=CARTESIAN_POINT ( 'NONE',  ( 0.5756566573088583993, 1.728235332270611879, 2.896516654582643291 ) ) ;
#27365=EDGE_LOOP ( 'NONE', ( #32328, #3447, #5266, #38825 ) ) ;
#27371=VERTEX_POINT ( 'NONE', #9072 ) ;
#27372=ORIENTED_EDGE ( 'NONE', *, *, #21310, .T. ) ;
#27373=CARTESIAN_POINT ( 'NONE',  ( 0.002207914879453961535, -5.712274067634378313E-18, 0.04916304461325374242 ) ) ;
#27375=DIRECTION ( 'NONE',  ( -0.000000000000000000, -1.000000000000000000, -0.000000000000000000 ) ) ;
#27377=ORIENTED_EDGE ( 'NONE', *, *, #8108, .T. ) ;
#27379=DIRECTION ( 'NONE',  ( -0.000000000000000000, 1.000000000000000000, -0.000000000000000000 ) ) ;
#27380=ORIENTED_EDGE ( 'NONE', *, *, #29575, .F. ) ;
#27381=DIRECTION ( 'NONE',  ( 0.000000000000000000, 0.000000000000000000, 1.000000000000000000 ) ) ;
#27385=EDGE_CURVE ( 'NONE', #30240, #30125, #20925, .T. ) ;
#27389=CARTESIAN_POINT ( 'NONE',  ( 1.128560816269277955, 1.725977917706353670, 1.984842472008916170 ) ) ;
#27393=CARTESIAN_POINT ( 'NONE',  ( 0.4506430153629077950, 0.03513753811042658048, -1.817852439337431569 ) ) ;
#27395=B_SPLINE_CURVE_WITH_KNOTS ( 'NONE', 3,
 ( #49973, #34033, #49217, #14145 ),
 .UNSPECIFIED., .F., .F.,
 ( 4, 4 ),
 ( 0.0001198035261475026192, 0.0009683180137351917165 ),
 .UNSPECIFIED. ) ;
#27398=AXIS2_PLACEMENT_3D ( 'NONE', #13130, #46977, #27381 ) ;
#27402=CARTESIAN_POINT ( 'NONE',  ( 0.000000000000000000, 1.574803149606302854, 0.000000000000000000 ) ) ;
#27403=CARTESIAN_POINT ( 'NONE',  ( 1.037524086854322514, 0.000000000000000000, 2.764473043227584803 ) ) ;
#27405=VERTEX_POINT ( 'NONE', #33351 ) ;
#27407=LINE ( 'NONE', #35677, #14706 ) ;
#27415=LINE ( 'NONE', #26662, #39209 ) ;
#27416=EDGE_CURVE ( 'NONE', #19878, #47775, #9584, .T. ) ;
#27423=ORIENTED_EDGE ( 'NONE', *, *, #27137, .T. ) ;
#27430=ORIENTED_EDGE ( 'NONE', *, *, #44067, .F. ) ;
#27434=EDGE_LOOP ( 'NONE', ( #47293, #47710, #42896 ) ) ;
#27435=CARTESIAN_POINT ( 'NONE',  ( -1.626937427625217314, 1.689925977444973304, -2.155561787858257361 ) ) ;
#27438=ORIENTED_EDGE ( 'NONE', *, *, #12488, .T. ) ;
#27439=DIRECTION ( 'NONE',  ( -0.9998717552508122886, -0.01601477604151182316, 0.000000000000000000 ) ) ;
#27441=ORIENTED_EDGE ( 'NONE', *, *, #22487, .F. ) ;
#27443=DIRECTION ( 'NONE',  ( 3.586865599282270385E-17, -1.000000000000000000, 1.103923720497139891E-16 ) ) ;
#27445=CONICAL_SURFACE ( 'NONE', #47193, 3.033577403570480779, 1.554780866114618743 ) ;
#27446=B_SPLINE_CURVE_WITH_KNOTS ( 'NONE', 3,
 ( #25317, #47998, #32309, #36953 ),
 .UNSPECIFIED., .F., .F.,
 ( 4, 4 ),
 ( 0.1211873102087489551, 0.1625992483279400380 ),
 .UNSPECIFIED. ) ;
#27447=LINE ( 'NONE', #18953, #37120 ) ;
#27448=CARTESIAN_POINT ( 'NONE',  ( -1.979793062125317693, 1.688404340953838068, 2.191257344206539504 ) ) ;
#27452=CIRCLE ( 'NONE', #11791, 1.850107469027523432 ) ;
#27455=ADVANCED_FACE ( 'NONE', ( #38235 ), #18605, .T. ) ;
#27456=CYLINDRICAL_SURFACE ( 'NONE', #7107, 2.164630168518208109 ) ;
#27458=ORIENTED_EDGE ( 'NONE', *, *, #40456, .T. ) ;
#27460=CARTESIAN_POINT ( 'NONE',  ( 0.5756566573088586214, 1.205361022782829114E-17, 2.896516654582643291 ) ) ;
#27464=DIRECTION ( 'NONE',  ( -0.9510565162951500895, 0.000000000000000000, -0.3090169943749582204 ) ) ;
#27465=CARTESIAN_POINT ( 'NONE',  ( 2.324843851831239760, 1.712330180919884315, -0.05514665559127426842 ) ) ;
#27469=DIRECTION ( 'NONE',  ( -6.394449067488625930E-17, -1.000000000000000000, 9.687176266499597757E-17 ) ) ;
#27472=ORIENTED_EDGE ( 'NONE', *, *, #37933, .F. ) ;
#27482=VERTEX_POINT ( 'NONE', #22476 ) ;
#27489=ORIENTED_EDGE ( 'NONE', *, *, #34769, .F. ) ;
#27490=CARTESIAN_POINT ( 'NONE',  ( 0.000000000000000000, 6.692913385826772199, 0.000000000000000000 ) ) ;
#27494=ORIENTED_EDGE ( 'NONE', *, *, #33792, .T. ) ;
#27496=DIRECTION ( 'NONE',  ( -0.000000000000000000, 1.000000000000000000, -0.000000000000000000 ) ) ;
#27497=DIRECTION ( 'NONE',  ( 3.986037398843765983E-20, 1.000000000000000000, 1.160734090543304660E-16 ) ) ;
#27498=ORIENTED_EDGE ( 'NONE', *, *, #6212, .T. ) ;
#27500=ORIENTED_EDGE ( 'NONE', *, *, #6394, .F. ) ;
#27507=VECTOR ( 'NONE', #1169, 39.37007874015748854 ) ;
#27508=CONICAL_SURFACE ( 'NONE', #18468, 1.850107469027523210, 0.6386652850508578450 ) ;
#27511=CARTESIAN_POINT ( 'NONE',  ( 0.4930719867878015084, 1.719503719051284074, 2.441437611110367278 ) ) ;
#27512=VECTOR ( 'NONE', #21539, 39.37007874015748143 ) ;
#27515=EDGE_CURVE ( 'NONE', #47004, #11192, #27035, .T. ) ;
#27517=CARTESIAN_POINT ( 'NONE',  ( 1.393175312147112432, 0.000000000000000000, 1.048074961516293202 ) ) ;
#27518=CONICAL_SURFACE ( 'NONE', #25069, 3.033577403570480779, 1.554780866114618743 ) ;
#27531=EDGE_CURVE ( 'NONE', #29523, #22090, #23222, .T. ) ;
#27532=CARTESIAN_POINT ( 'NONE',  ( 0.04921259842519669359, 1.610264983814881479, 2.246280244424690320 ) ) ;
#27533=CARTESIAN_POINT ( 'NONE',  ( -2.952069331832154919, 2.755905511811027164, 1.181102362204724088 ) ) ;
#27536=CARTESIAN_POINT ( 'NONE',  ( 0.07982360342473591996, 1.709180471932028711, 0.000000000000000000 ) ) ;
#27538=B_SPLINE_CURVE_WITH_KNOTS ( 'NONE', 3,
 ( #24998, #43836, #23974, #12357 ),
 .UNSPECIFIED., .F., .F.,
 ( 4, 4 ),
 ( 0.01409236801188419770, 0.03074671883294705782 ),
 .UNSPECIFIED. ) ;
#27539=CARTESIAN_POINT ( 'NONE',  ( 2.708693820787337891, 1.761460031494409550, -1.175591050816825023 ) ) ;
#27542=ORIENTED_EDGE ( 'NONE', *, *, #48244, .F. ) ;
#27548=ADVANCED_FACE ( 'NONE', ( #45939 ), #26093, .F. ) ;
#27549=CARTESIAN_POINT ( 'NONE',  ( 0.04921259842519670746, 1.514263714023589502, 2.952755905511811108 ) ) ;
#27550=DIRECTION ( 'NONE',  ( -0.01601477604151182663, 0.9998717552508123996, -0.000000000000000000 ) ) ;
#27557=LINE ( 'NONE', #22935, #3463 ) ;
#27560=ORIENTED_EDGE ( 'NONE', *, *, #45027, .T. ) ;
#27565=CARTESIAN_POINT ( 'NONE',  ( 1.921114995622270172, 0.9943725288147066133, -1.768687470589421995 ) ) ;
#27566=ORIENTED_EDGE ( 'NONE', *, *, #48197, .F. ) ;
#27567=ORIENTED_EDGE ( 'NONE', *, *, #18395, .F. ) ;
#27573=CARTESIAN_POINT ( 'NONE',  ( 1.662320194739497659, 0.000000000000000000, -1.388601395075552025 ) ) ;
#27585=CONICAL_SURFACE ( 'NONE', #8619, 2.246510896728926010, 0.01601546068027819014 ) ;
#27586=DIRECTION ( 'NONE',  ( -0.01601477604151182663, 0.9998717552508123996, -0.000000000000000000 ) ) ;
#27587=EDGE_CURVE ( 'NONE', #37294, #48631, #19343, .T. ) ;
#27588=CARTESIAN_POINT ( 'NONE',  ( 1.083598637574782364, 1.205361022782829114E-17, 2.747180975113346246 ) ) ;
#27589=ORIENTED_EDGE ( 'NONE', *, *, #46916, .T. ) ;
#27590=EDGE_CURVE ( 'NONE', #31865, #5433, #36942, .T. ) ;
#27591=DIRECTION ( 'NONE',  ( -0.01601477604151182663, 0.9998717552508123996, -0.000000000000000000 ) ) ;
#27596=DIRECTION ( 'NONE',  ( -0.9639628606958550172, 1.288287287306305283E-16, 0.2660368455666688448 ) ) ;
#27597=DIRECTION ( 'NONE',  ( -0.3513748240813434620, 0.000000000000000000, 0.9362348706397368714 ) ) ;
#27598=ORIENTED_EDGE ( 'NONE', *, *, #4523, .F. ) ;
#27605=ADVANCED_FACE ( 'NONE', ( #3863 ), #39383, .T. ) ;
#27606=ORIENTED_EDGE ( 'NONE', *, *, #23702, .T. ) ;
#27607=CARTESIAN_POINT ( 'NONE',  ( -1.083598637574821222, 5.905511811023623103, 2.747180975113331147 ) ) ;
#27613=CARTESIAN_POINT ( 'NONE',  ( -2.145573069066419425, 1.685811222653325059, -2.028682512764306445 ) ) ;
#27614=LINE ( 'NONE', #15502, #19875 ) ;
#27622=DIRECTION ( 'NONE',  ( 0.000000000000000000, 0.000000000000000000, 1.000000000000000000 ) ) ;
#27624=EDGE_CURVE ( 'NONE', #23841, #18859, #28107, .T. ) ;
#27628=ORIENTED_EDGE ( 'NONE', *, *, #5746, .T. ) ;
#27634=ORIENTED_EDGE ( 'NONE', *, *, #5465, .T. ) ;
#27637=ORIENTED_EDGE ( 'NONE', *, *, #36248, .F. ) ;
#27644=CARTESIAN_POINT ( 'NONE',  ( 0.8339530007628703778, 0.5232038923981141565, 2.082002554611946721 ) ) ;
#27652=AXIS2_PLACEMENT_3D ( 'NONE', #26660, #18921, #34675 ) ;
#27660=ORIENTED_EDGE ( 'NONE', *, *, #40943, .F. ) ;
#27662=ORIENTED_EDGE ( 'NONE', *, *, #42287, .F. ) ;
#27663=DIRECTION ( 'NONE',  ( -1.045785279492548401E-16, -1.000000000000000000, 5.036236473261409814E-17 ) ) ;
#27667=FACE_OUTER_BOUND ( 'NONE', #12394, .T. ) ;
#27668=EDGE_CURVE ( 'NONE', #35509, #45901, #19594, .T. ) ;
#27669=B_SPLINE_CURVE_WITH_KNOTS ( 'NONE', 3,
 ( #20273, #47858, #21305, #658 ),
 .UNSPECIFIED., .F., .F.,
 ( 4, 4 ),
 ( 1.741267681540161096E-05, 0.002517424578720645068 ),
 .UNSPECIFIED. ) ;
#27679=DIRECTION ( 'NONE',  ( -0.9998717552508122886, -0.01601477604151181275, 0.000000000000000000 ) ) ;
#27680=ORIENTED_EDGE ( 'NONE', *, *, #6282, .T. ) ;
#27683=CARTESIAN_POINT ( 'NONE',  ( -0.9526633209967887428, 0.000000000000000000, 1.562355641993038669 ) ) ;
#27690=CARTESIAN_POINT ( 'NONE',  ( 2.755905511811024056, 2.913385826771657250, 1.023622047244094446 ) ) ;
#27691=CIRCLE ( 'NONE', #42512, 1.850107469027523432 ) ;
#27692=VERTEX_POINT ( 'NONE', #36128 ) ;
#27693=VECTOR ( 'NONE', #16161, 39.37007874015748143 ) ;
#27695=ORIENTED_EDGE ( 'NONE', *, *, #32273, .F. ) ;
#27696=VERTEX_POINT ( 'NONE', #32258 ) ;
#27697=CARTESIAN_POINT ( 'NONE',  ( 0.07982360342473591996, 1.709180471932028711, 0.000000000000000000 ) ) ;
#27698=VECTOR ( 'NONE', #4257, 39.37007874015748143 ) ;
#27699=CARTESIAN_POINT ( 'NONE',  ( -0.5756566573089004768, 1.710292258889409833, 2.896516654582634853 ) ) ;
#27700=VECTOR ( 'NONE', #37158, 39.37007874015748143 ) ;
#27703=VERTEX_POINT ( 'NONE', #32004 ) ;
#27704=VERTEX_POINT ( 'NONE', #230 ) ;
#27705=AXIS2_PLACEMENT_3D ( 'NONE', #29611, #14622, #33751 ) ;
#27706=EDGE_CURVE ( 'NONE', #29934, #32006, #12118, .T. ) ;
#27707=ORIENTED_EDGE ( 'NONE', *, *, #41818, .T. ) ;
#27708=DIRECTION ( 'NONE',  ( 0.000000000000000000, 0.000000000000000000, 1.000000000000000000 ) ) ;
#27715=CARTESIAN_POINT ( 'NONE',  ( -2.152441353505195387, 5.905511811023623991, -0.2419059403265106933 ) ) ;
#27717=DIRECTION ( 'NONE',  ( -0.9998717552508122886, -0.01601477604151180928, 0.000000000000000000 ) ) ;
#27719=DIRECTION ( 'NONE',  ( 0.000000000000000000, 0.000000000000000000, 1.000000000000000000 ) ) ;
#27720=DIRECTION ( 'NONE',  ( 0.000000000000000000, 0.000000000000000000, 1.000000000000000000 ) ) ;
#27724=CARTESIAN_POINT ( 'NONE',  ( -1.503187667631459279, 0.5249316497054297148, 1.135806887463298942 ) ) ;
#27726=CARTESIAN_POINT ( 'NONE',  ( 0.000000000000000000, 0.000000000000000000, 0.000000000000000000 ) ) ;
#27727=CONICAL_SURFACE ( 'NONE', #15361, 3.033577403570480779, 1.554780866114618743 ) ;
#27731=ORIENTED_EDGE ( 'NONE', *, *, #33665, .T. ) ;
#27732=DIRECTION ( 'NONE',  ( -0.8090169943749422332, 1.288287287306305283E-16, -0.5877852522924802425 ) ) ;
#27735=FACE_OUTER_BOUND ( 'NONE', #6541, .T. ) ;
#27738=ORIENTED_EDGE ( 'NONE', *, *, #1824, .T. ) ;
#27743=CARTESIAN_POINT ( 'NONE',  ( 0.000000000000000000, 1.574803149606302854, 0.000000000000000000 ) ) ;
#27745=CARTESIAN_POINT ( 'NONE',  ( 0.2718136966839837521, 1.715997676552674323, -2.471090629072964173 ) ) ;
#27747=ORIENTED_EDGE ( 'NONE', *, *, #22724, .F. ) ;
#27756=ORIENTED_EDGE ( 'NONE', *, *, #21384, .F. ) ;
#27757=EDGE_CURVE ( 'NONE', #30054, #25781, #33283, .T. ) ;
#27758=LINE ( 'NONE', #23633, #46333 ) ;
#27759=EDGE_LOOP ( 'NONE', ( #23223, #29690, #39775, #33726 ) ) ;
#27761=DIRECTION ( 'NONE',  ( -3.981026654148627524E-17, 1.000000000000000000, 1.225234019452863932E-16 ) ) ;
#27766=DIRECTION ( 'NONE',  ( -0.9989930665413144784, 5.247434042673083099E-18, -0.04486483035051863633 ) ) ;
#27767=ORIENTED_EDGE ( 'NONE', *, *, #40026, .T. ) ;
#27768=CIRCLE ( 'NONE', #12113, 0.3937007874015748254 ) ;
#27769=EDGE_CURVE ( 'NONE', #17176, #11883, #24488, .T. ) ;
#27775=CARTESIAN_POINT ( 'NONE',  ( -1.514466370293032993, 0.000000000000000000, 2.534789744887398388 ) ) ;
#27777=CARTESIAN_POINT ( 'NONE',  ( 0.3820226255272446414, 0.03403845698394380309, 1.829505193364920679 ) ) ;
#27779=CARTESIAN_POINT ( 'NONE',  ( 0.1067246931122726866, 0.02962905676920215767, 0.000000000000000000 ) ) ;
#27785=DIRECTION ( 'NONE',  ( 0.000000000000000000, 0.000000000000000000, 1.000000000000000000 ) ) ;
#27787=DIRECTION ( 'NONE',  ( -0.9998717552508122886, -0.01601477604151185785, 0.000000000000000000 ) ) ;
#27788=CARTESIAN_POINT ( 'NONE',  ( 1.951523201471517588, 0.05917688107560774985, -0.1369052102211298083 ) ) ;
#27789=DIRECTION ( 'NONE',  ( 0.9989930665413151445, 0.000000000000000000, -0.04486483035050446017 ) ) ;
#27790=LINE ( 'NONE', #5075, #6785 ) ;
#27794=CARTESIAN_POINT ( 'NONE',  ( -2.734482843737247038, 1.205361022782829114E-17, -1.115254632218711794 ) ) ;
#27802=DIRECTION ( 'NONE',  ( 0.000000000000000000, 1.000000000000000000, 0.000000000000000000 ) ) ;
#27807=DIRECTION ( 'NONE',  ( -0.3930250316539147803, 0.000000000000000000, -0.9195277725514544587 ) ) ;
#27811=EDGE_CURVE ( 'NONE', #11675, #29343, #29427, .T. ) ;
#27817=EDGE_CURVE ( 'NONE', #50859, #5041, #40768, .T. ) ;
#27825=B_SPLINE_CURVE_WITH_KNOTS ( 'NONE', 3,
 ( #29044, #48879, #13565, #7705 ),
 .UNSPECIFIED., .F., .F.,
 ( 4, 4 ),
 ( 0.01334467773481458862, 0.03074214098855171384 ),
 .UNSPECIFIED. ) ;
#27842=FACE_OUTER_BOUND ( 'NONE', #4539, .T. ) ;
#27844=VERTEX_POINT ( 'NONE', #36902 ) ;
#27847=ORIENTED_EDGE ( 'NONE', *, *, #26324, .T. ) ;
#27850=ORIENTED_EDGE ( 'NONE', *, *, #1471, .T. ) ;
#27851=EDGE_CURVE ( 'NONE', #21208, #50444, #32522, .T. ) ;
#27852=CARTESIAN_POINT ( 'NONE',  ( 2.878724150143186833, 0.000000000000000000, -0.6570500018394808128 ) ) ;
#27855=ORIENTED_EDGE ( 'NONE', *, *, #25968, .F. ) ;
#27864=B_SPLINE_CURVE_WITH_KNOTS ( 'NONE', 3,
 ( #22417, #49727, #33542, #6159 ),
 .UNSPECIFIED., .F., .F.,
 ( 4, 4 ),
 ( 0.1211873102087489551, 0.1625992483279400380 ),
 .UNSPECIFIED. ) ;
#27866=EDGE_LOOP ( 'NONE', ( #2581, #4127, #18525, #27598 ) ) ;
#27868=CARTESIAN_POINT ( 'NONE',  ( 1.300279662861326013, 0.04874602395362847423, 1.413491677621213860 ) ) ;
#27871=CONICAL_SURFACE ( 'NONE', #11413, 2.244934639244524632, 1.554780866114618743 ) ;
#27874=ORIENTED_EDGE ( 'NONE', *, *, #28828, .F. ) ;
#27877=EDGE_CURVE ( 'NONE', #33984, #18859, #23858, .T. ) ;
#27888=CARTESIAN_POINT ( 'NONE',  ( 0.08139965876239094178, 1.610780518492231694, 0.000000000000000000 ) ) ;
#27890=CARTESIAN_POINT ( 'NONE',  ( 0.2178414669595446496, 0.5249316497054297148, -1.871410041920607004 ) ) ;
#27895=CARTESIAN_POINT ( 'NONE',  ( -0.7381027496704858359, 0.000000000000000000, -2.859439394060923512 ) ) ;
#27896=EDGE_CURVE ( 'NONE', #4293, #17674, #49258, .T. ) ;
#27901=CONICAL_SURFACE ( 'NONE', #10604, 1.850107469027523210, 0.6386652850508578450 ) ;
#27904=CARTESIAN_POINT ( 'NONE',  ( 0.3543214468173200293, 1.713577057256821190, 2.228085083314873316 ) ) ;
#27909=EDGE_CURVE ( 'NONE', #196, #23904, #32545, .T. ) ;
#27911=AXIS2_PLACEMENT_3D ( 'NONE', #42426, #66, #47275 ) ;
#27921=ORIENTED_EDGE ( 'NONE', *, *, #40616, .T. ) ;
#27926=CARTESIAN_POINT ( 'NONE',  ( 0.7521025634872258170, 1.621523052975431867, 2.144027383376515328 ) ) ;
#27931=ORIENTED_EDGE ( 'NONE', *, *, #27769, .T. ) ;
#27932=DIRECTION ( 'NONE',  ( -1.206139481778036182E-16, 1.000000000000000000, -4.526717189434842013E-17 ) ) ;
#27939=ADVANCED_FACE ( 'NONE', ( #14413 ), #31166, .F. ) ;
#27940=ORIENTED_EDGE ( 'NONE', *, *, #45530, .T. ) ;
#27943=CARTESIAN_POINT ( 'NONE',  ( -0.8987785766980536106, 1.205361022782829114E-17, 1.600251783270283390 ) ) ;
#27944=AXIS2_PLACEMENT_3D ( 'NONE', #14229, #26606, #10617 ) ;
#27946=ADVANCED_FACE ( 'NONE', ( #37667 ), #10285, .T. ) ;
#27947=EDGE_CURVE ( 'NONE', #45649, #34423, #15496, .T. ) ;
#27949=DIRECTION ( 'NONE',  ( -0.000000000000000000, -1.000000000000000000, -0.000000000000000000 ) ) ;
#27953=ORIENTED_EDGE ( 'NONE', *, *, #38939, .T. ) ;
#27954=ORIENTED_EDGE ( 'NONE', *, *, #20009, .T. ) ;
#27958=CARTESIAN_POINT ( 'NONE',  ( 0.000000000000000000, 6.692913385826772199, 0.000000000000000000 ) ) ;
#27959=CARTESIAN_POINT ( 'NONE',  ( 0.3545323396393251780, 1.647963639598186036, 2.229247198548944375 ) ) ;
#27961=VECTOR ( 'NONE', #48592, 39.37007874015748143 ) ;
#27962=ORIENTED_EDGE ( 'NONE', *, *, #184, .F. ) ;
#27964=CONICAL_SURFACE ( 'NONE', #36197, 2.089297179032357121, 0.2617993877991570129 ) ;
#27966=CARTESIAN_POINT ( 'NONE',  ( -0.5756566573089003658, 0.000000000000000000, 2.896516654582634853 ) ) ;
#27970=CARTESIAN_POINT ( 'NONE',  ( -0.8949303405208608453, 1.574803149606302854, -1.971765468592543202 ) ) ;
#27973=CARTESIAN_POINT ( 'NONE',  ( 2.555365368299595323E-16, 1.585169487999011917, 2.086614173228346303 ) ) ;
#27978=DIRECTION ( 'NONE',  ( -0.01601477604151182663, 0.9998717552508123996, -0.000000000000000000 ) ) ;
#27979=CARTESIAN_POINT ( 'NONE',  ( -0.4842960162298967641, 0.000000000000000000, -1.816169684210588331 ) ) ;
#27983=DIRECTION ( 'NONE',  ( 2.842176228468331432E-14, 0.000000000000000000, 1.000000000000000000 ) ) ;
#27987=CARTESIAN_POINT ( 'NONE',  ( 0.000000000000000000, 6.692913385826772199, 0.000000000000000000 ) ) ;
#27991=CARTESIAN_POINT ( 'NONE',  ( 0.8515791614234311524, 0.000000000000000000, 1.521253268579216167 ) ) ;
#27993=DIRECTION ( 'NONE',  ( -0.9998717552508122886, -0.01601477604151182316, 0.000000000000000000 ) ) ;
#27995=ORIENTED_EDGE ( 'NONE', *, *, #20568, .F. ) ;
#27996=ORIENTED_EDGE ( 'NONE', *, *, #39939, .T. ) ;
#27998=CARTESIAN_POINT ( 'NONE',  ( 1.856205413694107520, 1.642665920110450317, -1.706627555837983090 ) ) ;
#27999=EDGE_LOOP ( 'NONE', ( #43856, #27500, #44074, #7870 ) ) ;
#28001=DIRECTION ( 'NONE',  ( -3.981026654148627524E-17, 1.000000000000000000, 1.225234019452863932E-16 ) ) ;
#28003=CARTESIAN_POINT ( 'NONE',  ( 1.472219874544873131, 1.643743200001983151, 2.560030851058970214 ) ) ;
#28008=DIRECTION ( 'NONE',  ( -3.986037398843765983E-20, -1.000000000000000000, -1.160734090543304660E-16 ) ) ;
#28012=EDGE_CURVE ( 'NONE', #24400, #3300, #523, .T. ) ;
#28013=CARTESIAN_POINT ( 'NONE',  ( -2.793030215715272213, 1.675725205278408403, 0.9592557174602281966 ) ) ;
#28018=CARTESIAN_POINT ( 'NONE',  ( 0.9914495361338625523, 1.734714548371065312, 2.781765111341823360 ) ) ;
#28031=VECTOR ( 'NONE', #39838, 39.37007874015748143 ) ;
#28032=DIRECTION ( 'NONE',  ( -0.000000000000000000, 1.000000000000000000, -0.000000000000000000 ) ) ;
#28033=CARTESIAN_POINT ( 'NONE',  ( -0.2134117707794043750, 0.02450148541315291459, -1.822192086320855164 ) ) ;
#28035=ORIENTED_EDGE ( 'NONE', *, *, #47626, .T. ) ;
#28039=CARTESIAN_POINT ( 'NONE',  ( 1.083598637574781920, 5.905511811023623991, 2.747180975113346246 ) ) ;
#28045=DIRECTION ( 'NONE',  ( -0.9510565162951500895, 0.000000000000000000, -0.3090169943749582204 ) ) ;
#28048=DIRECTION ( 'NONE',  ( 0.000000000000000000, -1.000000000000000000, 0.000000000000000000 ) ) ;
#28054=DIRECTION ( 'NONE',  ( 8.902872254220023478E-17, 1.000000000000000000, -9.311674343991161395E-17 ) ) ;
#28056=ORIENTED_EDGE ( 'NONE', *, *, #15996, .F. ) ;
#28058=ORIENTED_EDGE ( 'NONE', *, *, #37602, .T. ) ;
#28059=ADVANCED_FACE ( 'NONE', ( #48341 ), #38584, .T. ) ;
#28060=DIRECTION ( 'NONE',  ( -3.981026654148627524E-17, 1.000000000000000000, 1.225234019452863932E-16 ) ) ;
#28062=CIRCLE ( 'NONE', #15720, 2.165354330708661568 ) ;
#28063=DIRECTION ( 'NONE',  ( 0.000000000000000000, 0.000000000000000000, 1.000000000000000000 ) ) ;
#28064=EDGE_CURVE ( 'NONE', #22637, #39017, #3113, .T. ) ;
#28067=EDGE_CURVE ( 'NONE', #27692, #29609, #20832, .T. ) ;
#28068=DIRECTION ( 'NONE',  ( 0.000000000000000000, 1.000000000000000000, 0.000000000000000000 ) ) ;
#28073=VECTOR ( 'NONE', #189, 39.37007874015748143 ) ;
#28076=ORIENTED_EDGE ( 'NONE', *, *, #8915, .T. ) ;
#28078=DIRECTION ( 'NONE',  ( 0.04486483035050446017, -1.160734090543304660E-16, 0.9989930665413151445 ) ) ;
#28079=DIRECTION ( 'NONE',  ( -0.000000000000000000, 1.000000000000000000, -0.000000000000000000 ) ) ;
#28081=CARTESIAN_POINT ( 'NONE',  ( -0.3498457532482182053, 1.702298530840201662, 2.203421978946157989 ) ) ;
#28084=CYLINDRICAL_SURFACE ( 'NONE', #21750, 2.164630168518208109 ) ;
#28089=CARTESIAN_POINT ( 'NONE',  ( 1.129748414438405124, 1.627571742414081202, 1.986830176535870907 ) ) ;
#28091=CARTESIAN_POINT ( 'NONE',  ( 1.064963178929838161, 0.01474687883001544499, 1.686498296765969407 ) ) ;
#28094=CARTESIAN_POINT ( 'NONE',  ( -0.9360721529196992519, 0.000000000000000000, 1.470771056236103158 ) ) ;
#28097=EDGE_CURVE ( 'NONE', #30125, #24532, #18360, .T. ) ;
#28103=ORIENTED_EDGE ( 'NONE', *, *, #32930, .T. ) ;
#28105=CARTESIAN_POINT ( 'NONE',  ( 0.5286458662987441048, 1.205361022782829114E-17, 2.100489422084715230 ) ) ;
#28106=AXIS2_PLACEMENT_3D ( 'NONE', #17961, #49160, #48390 ) ;
#28107=LINE ( 'NONE', #19847, #46748 ) ;
#28108=DIRECTION ( 'NONE',  ( 1.000000000000000000, -0.000000000000000000, -0.000000000000000000 ) ) ;
#28109=VERTEX_POINT ( 'NONE', #36770 ) ;
#28117=ADVANCED_FACE ( 'NONE', ( #13277 ), #8121, .T. ) ;
#28118=DIRECTION ( 'NONE',  ( -0.01601477604151182663, 0.9998717552508123996, -0.000000000000000000 ) ) ;
#28120=ORIENTED_EDGE ( 'NONE', *, *, #43600, .T. ) ;
#28121=EDGE_CURVE ( 'NONE', #344, #37003, #46047, .T. ) ;
#28122=PRODUCT ( 'Front Cover', 'Front Cover', '', ( #47726 ) ) ;
#28134=ORIENTED_EDGE ( 'NONE', *, *, #7190, .T. ) ;
#28139=VERTEX_POINT ( 'NONE', #5525 ) ;
#28140=LINE ( 'NONE', #32553, #7008 ) ;
#28147=CARTESIAN_POINT ( 'NONE',  ( 0.1155636338427008941, -0.5222242541845523167, 0.000000000000000000 ) ) ;
#28150=ORIENTED_EDGE ( 'NONE', *, *, #30294, .T. ) ;
#28153=DIRECTION ( 'NONE',  ( -0.000000000000000000, 1.000000000000000000, -0.000000000000000000 ) ) ;
#28159=ORIENTED_EDGE ( 'NONE', *, *, #42498, .F. ) ;
#28162=ORIENTED_EDGE ( 'NONE', *, *, #38439, .T. ) ;
#28166=CARTESIAN_POINT ( 'NONE',  ( 0.000000000000000000, 1.574803149606302854, 0.000000000000000000 ) ) ;
#28167=EDGE_CURVE ( 'NONE', #49749, #23247, #37794, .T. ) ;
#28168=EDGE_LOOP ( 'NONE', ( #3904, #19061, #12994, #35798 ) ) ;
#28169=EDGE_CURVE ( 'NONE', #30932, #22707, #25650, .T. ) ;
#28172=DIRECTION ( 'NONE',  ( 0.000000000000000000, 0.000000000000000000, 1.000000000000000000 ) ) ;
#28174=ORIENTED_EDGE ( 'NONE', *, *, #6454, .T. ) ;
#28176=ORIENTED_EDGE ( 'NONE', *, *, #15173, .T. ) ;
#28179=CARTESIAN_POINT ( 'NONE',  ( 1.686111637834603938, 0.05492582915004715072, 0.9632209503012270080 ) ) ;
#28189=CARTESIAN_POINT ( 'NONE',  ( -2.159071745913425655, 1.046027471231291139, -1.366223401065049581 ) ) ;
#28190=CARTESIAN_POINT ( 'NONE',  ( 0.07982360342473591996, 1.709180471932028711, 0.000000000000000000 ) ) ;
#28192=B_SPLINE_CURVE_WITH_KNOTS ( 'NONE', 3,
 ( #13230, #36725, #17103, #32865 ),
 .UNSPECIFIED., .F., .F.,
 ( 4, 4 ),
 ( 0.01468254673471047073, 0.03075083447507073742 ),
 .UNSPECIFIED. ) ;
#28195=CARTESIAN_POINT ( 'NONE',  ( -2.422455304366706752, 1.574882862795218275, -0.1580547953490660518 ) ) ;
#28196=EDGE_CURVE ( 'NONE', #14792, #39458, #6292, .T. ) ;
#28199=CARTESIAN_POINT ( 'NONE',  ( 0.8291286199751974895, 1.205361022782829114E-17, -1.835126787948130556 ) ) ;
#28202=CARTESIAN_POINT ( 'NONE',  ( -0.9914495361339012991, 1.703811331058339373, 2.781765111341808705 ) ) ;
#28203=ORIENTED_EDGE ( 'NONE', *, *, #16629, .T. ) ;
#28204=EDGE_LOOP ( 'NONE', ( #29896, #13501, #24979, #38616, #41194, #41197, #16678, #24759, #37366, #21972, #20232 ) ) ;
#28208=CIRCLE ( 'NONE', #47147, 2.165354330708661568 ) ;
#28209=CARTESIAN_POINT ( 'NONE',  ( -1.905671854841497481, 1.689559879305088996, 2.256015092822653223 ) ) ;
#28214=EDGE_CURVE ( 'NONE', #7202, #47691, #22040, .T. ) ;
#28215=CIRCLE ( 'NONE', #5965, 2.086614173228346303 ) ;
#28217=LINE ( 'NONE', #43958, #25278 ) ;
#28218=CARTESIAN_POINT ( 'NONE',  ( 0.000000000000000000, 6.692913385826772199, 0.000000000000000000 ) ) ;
#28219=VECTOR ( 'NONE', #12686, 39.37007874015748143 ) ;
#28229=CARTESIAN_POINT ( 'NONE',  ( 0.2156685157584260770, 1.722625337188476546, -2.945280361644574185 ) ) ;
#28231=EDGE_LOOP ( 'NONE', ( #28942, #7299, #22172, #31361 ) ) ;
#28232=CARTESIAN_POINT ( 'NONE',  ( -1.393175312147127531, 0.000000000000000000, 1.048074961516273218 ) ) ;
#28234=EDGE_CURVE ( 'NONE', #21109, #38547, #41139, .T. ) ;
#28238=DIRECTION ( 'NONE',  ( -0.000000000000000000, 1.000000000000000000, -0.000000000000000000 ) ) ;
#28243=CARTESIAN_POINT ( 'NONE',  ( 0.07982360342473591996, 1.709180471932028711, 0.000000000000000000 ) ) ;
#28244=CARTESIAN_POINT ( 'NONE',  ( 0.6150616064519864867, 0.03777100275179151589, 1.778883059170359493 ) ) ;
#28251=VECTOR ( 'NONE', #21746, 39.37007874015748854 ) ;
#28254=CARTESIAN_POINT ( 'NONE',  ( -1.405314191946755997, 1.685393272164901646, 1.683309666213049560 ) ) ;
#28257=VECTOR ( 'NONE', #24294, 39.37007874015748143 ) ;
#28262=EDGE_CURVE ( 'NONE', #19788, #7819, #50300, .T. ) ;
#28263=DIRECTION ( 'NONE',  ( 0.000000000000000000, 0.000000000000000000, 1.000000000000000000 ) ) ;
#28266=CONICAL_SURFACE ( 'NONE', #34074, 2.244934639244524632, 1.554780866114618743 ) ;
#28267=VERTEX_POINT ( 'NONE', #41158 ) ;
#28268=CARTESIAN_POINT ( 'NONE',  ( 0.000000000000000000, 6.692913385826772199, 0.000000000000000000 ) ) ;
#28271=CARTESIAN_POINT ( 'NONE',  ( -2.867773316779185677, 1.576133919414932638, -0.7050287376752426560 ) ) ;
#28274=EDGE_CURVE ( 'NONE', #30462, #42563, #427, .T. ) ;
#28280=EDGE_CURVE ( 'NONE', #25218, #47368, #35908, .T. ) ;
#28282=DIRECTION ( 'NONE',  ( -0.000000000000000000, 1.000000000000000000, -0.000000000000000000 ) ) ;
#28284=EDGE_CURVE ( 'NONE', #30522, #41853, #12789, .T. ) ;
#28289=VERTEX_POINT ( 'NONE', #39777 ) ;
#28292=CARTESIAN_POINT ( 'NONE',  ( -1.905671854841497481, 1.555429617898292705, 2.256015092822653667 ) ) ;
#28293=CARTESIAN_POINT ( 'NONE',  ( 1.950008968278537091, 5.905511811023623991, 0.9934589848971188131 ) ) ;
#28295=ADVANCED_FACE ( 'NONE', ( #16803 ), #24802, .T. ) ;
#28299=ORIENTED_EDGE ( 'NONE', *, *, #17299, .F. ) ;
#28300=LINE ( 'NONE', #32195, #10624 ) ;
#28303=DIRECTION ( 'NONE',  ( -0.000000000000000000, -1.000000000000000000, -0.000000000000000000 ) ) ;
#28305=ORIENTED_EDGE ( 'NONE', *, *, #37514, .F. ) ;
#28306=DIRECTION ( 'NONE',  ( -0.9989930665413151445, -0.000000000000000000, 0.04486483035050446017 ) ) ;
#28307=VERTEX_POINT ( 'NONE', #4409 ) ;
#28312=VERTEX_POINT ( 'NONE', #21189 ) ;
#28315=EDGE_LOOP ( 'NONE', ( #8572, #17411, #21747, #13471, #806, #7113, #2946, #11992, #21179, #19795, #2256 ) ) ;
#28316=CARTESIAN_POINT ( 'NONE',  ( 0.3136974817028395091, 1.508467219206862664, -2.936457595020219635 ) ) ;
#28321=CONICAL_SURFACE ( 'NONE', #9356, 2.165354330708661568, 0.2617993877991570129 ) ;
#28324=CARTESIAN_POINT ( 'NONE',  ( 2.708693820785017525, 1.662986522273777412, -1.175591050822254457 ) ) ;
#28330=EDGE_CURVE ( 'NONE', #15665, #35860, #36425, .T. ) ;
#28331=ADVANCED_FACE ( 'NONE', ( #32302 ), #28667, .T. ) ;
#28334=CARTESIAN_POINT ( 'NONE',  ( 2.715141060683428531, 0.000000000000000000, -1.160506983230063405 ) ) ;
#28336=CIRCLE ( 'NONE', #14349, 2.246510896728926010 ) ;
#28337=ORIENTED_EDGE ( 'NONE', *, *, #11979, .F. ) ;
#28342=CARTESIAN_POINT ( 'NONE',  ( -1.735586374879336757, 5.905511811023623991, -2.388829707800050883 ) ) ;
#28344=EDGE_LOOP ( 'NONE', ( #16087, #18465, #15929, #7334 ) ) ;
#28345=CARTESIAN_POINT ( 'NONE',  ( -1.661821349926434932, 1.574803149606302854, 1.388203579611951843 ) ) ;
#28346=CARTESIAN_POINT ( 'NONE',  ( 2.309000164489917406, 1.744884814208895296, 0.2631132722234555410 ) ) ;
#28347=FACE_OUTER_BOUND ( 'NONE', #35457, .T. ) ;
#28349=ADVANCED_FACE ( 'NONE', ( #13191 ), #24958, .T. ) ;
#28351=CARTESIAN_POINT ( 'NONE',  ( 2.793030215715258446, 1.451280567205322836, 0.9592557174602683867 ) ) ;
#28356=EDGE_CURVE ( 'NONE', #23316, #38999, #20410, .T. ) ;
#28357=CIRCLE ( 'NONE', #10206, 2.165354330708661568 ) ;
#28361=EDGE_CURVE ( 'NONE', #41060, #38999, #34727, .T. ) ;
#28362=VECTOR ( 'NONE', #25370, 39.37007874015748143 ) ;
#28364=AXIS2_PLACEMENT_3D ( 'NONE', #27726, #23602, #8118 ) ;
#28372=CONICAL_SURFACE ( 'NONE', #20979, 1.850107469027523210, 0.6386652850508578450 ) ;
#28373=CARTESIAN_POINT ( 'NONE',  ( 1.979793062125284608, 1.750113821271474857, 2.191257344206569257 ) ) ;
#28376=VERTEX_POINT ( 'NONE', #40301 ) ;
#28380=ORIENTED_EDGE ( 'NONE', *, *, #34603, .T. ) ;
#28388=CARTESIAN_POINT ( 'NONE',  ( -1.695772546416001836, 5.905511811023623991, -2.417756147381374010 ) ) ;
#28390=VECTOR ( 'NONE', #18143, 39.37007874015748143 ) ;
#28394=ORIENTED_EDGE ( 'NONE', *, *, #31857, .F. ) ;
#28398=CARTESIAN_POINT ( 'NONE',  ( 2.339241080213585899, 1.755713673067765379, 1.802537235681918037 ) ) ;
#28401=DIRECTION ( 'NONE',  ( -0.9998717552508122886, -0.01601477604151182316, 0.000000000000000000 ) ) ;
#28403=EDGE_LOOP ( 'NONE', ( #34194, #15845, #28058, #23279 ) ) ;
#28405=CIRCLE ( 'NONE', #39989, 1.743387098533651480 ) ;
#28418=ORIENTED_EDGE ( 'NONE', *, *, #27590, .F. ) ;
#28424=AXIS2_PLACEMENT_3D ( 'NONE', #18334, #10335, #37966 ) ;
#28425=VERTEX_POINT ( 'NONE', #17822 ) ;
#28427=CARTESIAN_POINT ( 'NONE',  ( 2.164658444855302122, 5.905511811023623991, -0.04795272066889885720 ) ) ;
#28431=ORIENTED_EDGE ( 'NONE', *, *, #50619, .F. ) ;
#28436=ORIENTED_EDGE ( 'NONE', *, *, #25100, .F. ) ;
#28438=VECTOR ( 'NONE', #36269, 39.37007874015748854 ) ;
#28444=CARTESIAN_POINT ( 'NONE',  ( 2.312113436335841321, 1.646509482104762334, 0.2635349935491774209 ) ) ;
#28445=ORIENTED_EDGE ( 'NONE', *, *, #27624, .F. ) ;
#28447=CARTESIAN_POINT ( 'NONE',  ( -0.9788642269881570046, 0.000000000000000000, 1.542392924267547594 ) ) ;
#28449=ORIENTED_EDGE ( 'NONE', *, *, #28884, .T. ) ;
#28454=EDGE_CURVE ( 'NONE', #32849, #31431, #4732, .T. ) ;
#28457=ORIENTED_EDGE ( 'NONE', *, *, #40399, .T. ) ;
#28462=CARTESIAN_POINT ( 'NONE',  ( -2.164823134740035737, 1.574803149606302854, -0.04796011690018223833 ) ) ;
#28464=CARTESIAN_POINT ( 'NONE',  ( 2.793030215715258446, 1.664308485742666877, 0.9592557174602684977 ) ) ;
#28465=VERTEX_POINT ( 'NONE', #21957 ) ;
#28468=AXIS2_PLACEMENT_3D ( 'NONE', #24003, #16261, #12388 ) ;
#28470=B_SPLINE_CURVE_WITH_KNOTS ( 'NONE', 3,
 ( #28081, #32232, #36872, #28598 ),
 .UNSPECIFIED., .F., .F.,
 ( 4, 4 ),
 ( 0.01239106743709809423, 0.03073847721854806869 ),
 .UNSPECIFIED. ) ;
#28473=CARTESIAN_POINT ( 'NONE',  ( 0.5286458662987441048, 1.205361022782829114E-17, 2.100489422084715230 ) ) ;
#28474=CIRCLE ( 'NONE', #30144, 2.165354330708661568 ) ;
#28475=EDGE_CURVE ( 'NONE', #4194, #11914, #11754, .T. ) ;
#28481=VERTEX_POINT ( 'NONE', #25309 ) ;
#28483=ADVANCED_FACE ( 'NONE', ( #1817 ), #40622, .T. ) ;
#28484=DIRECTION ( 'NONE',  ( -0.6234898018587431423, 0.000000000000000000, 0.7818314824680221431 ) ) ;
#28485=ORIENTED_EDGE ( 'NONE', *, *, #5990, .T. ) ;
#28488=LINE ( 'NONE', #47821, #45232 ) ;
#28491=CARTESIAN_POINT ( 'NONE',  ( -0.9788642269881570046, 0.000000000000000000, 1.542392924267547594 ) ) ;
#28493=CARTESIAN_POINT ( 'NONE',  ( 0.9914495361338626633, 5.905511811023623103, 2.781765111341825136 ) ) ;
#28494=ORIENTED_EDGE ( 'NONE', *, *, #5465, .F. ) ;
#28502=CARTESIAN_POINT ( 'NONE',  ( -2.076715649576790224, 1.576214352228098470, 0.6230206298219045369 ) ) ;
#28503=ORIENTED_EDGE ( 'NONE', *, *, #27817, .F. ) ;
#28506=AXIS2_PLACEMENT_3D ( 'NONE', #7289, #23031, #38781 ) ;
#28508=VECTOR ( 'NONE', #43059, 39.37007874015748143 ) ;
#28509=EDGE_LOOP ( 'NONE', ( #33836, #9561, #44202, #39176 ) ) ;
#28510=CARTESIAN_POINT ( 'NONE',  ( 0.08139965876239094178, 1.610780518492231694, 0.000000000000000000 ) ) ;
#28512=PLANE ( 'NONE',  #30225 ) ;
#28513=CONICAL_SURFACE ( 'NONE', #6269, 2.246510896728926010, 0.01601546068027819014 ) ;
#28516=ORIENTED_EDGE ( 'NONE', *, *, #44539, .F. ) ;
#28519=AXIS2_PLACEMENT_3D ( 'NONE', #8080, #43436, #3448 ) ;
#28525=ORIENTED_EDGE ( 'NONE', *, *, #38026, .F. ) ;
#28527=VERTEX_POINT ( 'NONE', #25820 ) ;
#28528=VERTEX_POINT ( 'NONE', #41072 ) ;
#28530=EDGE_CURVE ( 'NONE', #35466, #28267, #41322, .T. ) ;
#28541=DIRECTION ( 'NONE',  ( 0.000000000000000000, 0.000000000000000000, 1.000000000000000000 ) ) ;
#28542=DIRECTION ( 'NONE',  ( -0.9998717552508121775, -0.01601477604151182663, 0.000000000000000000 ) ) ;
#28544=CIRCLE ( 'NONE', #36820, 1.850107469027523432 ) ;
#28545=ORIENTED_EDGE ( 'NONE', *, *, #8147, .T. ) ;
#28550=CARTESIAN_POINT ( 'NONE',  ( 2.715141060683428531, 5.905511811023623991, -1.160506983230062739 ) ) ;
#28558=CARTESIAN_POINT ( 'NONE',  ( 2.528673309384623646, 1.751762191246605260, -0.1628250514548083838 ) ) ;
#28568=PLANE ( 'NONE',  #7811 ) ;
#28569=ORIENTED_EDGE ( 'NONE', *, *, #18761, .F. ) ;
#28571=CARTESIAN_POINT ( 'NONE',  ( 1.052882392200863215, 1.637204117213755250, 2.758708974820646809 ) ) ;
#28578=ORIENTED_EDGE ( 'NONE', *, *, #36577, .T. ) ;
#28582=AXIS2_PLACEMENT_3D ( 'NONE', #22895, #38893, #42252 ) ;
#28583=ORIENTED_EDGE ( 'NONE', *, *, #14442, .T. ) ;
#28585=CARTESIAN_POINT ( 'NONE',  ( 1.223349603905365068, 0.04751384826852676074, 1.475034436811822669 ) ) ;
#28586=ORIENTED_EDGE ( 'NONE', *, *, #27416, .T. ) ;
#28594=CARTESIAN_POINT ( 'NONE',  ( 2.813305137472101425, 1.450017550732547456, 0.8968559245517169209 ) ) ;
#28595=CONICAL_SURFACE ( 'NONE', #31076, 3.483074324928249421, 1.244861948955335196 ) ;
#28598=CARTESIAN_POINT ( 'NONE',  ( -0.4788131938641533303, 1.711801685632677428, 2.914091152102185944 ) ) ;
#28599=ORIENTED_EDGE ( 'NONE', *, *, #45349, .T. ) ;
#28602=CARTESIAN_POINT ( 'NONE',  ( 0.07982360342473591996, 1.709180471932028711, 0.000000000000000000 ) ) ;
#28603=EDGE_CURVE ( 'NONE', #23841, #16862, #35671, .T. ) ;
#28607=CARTESIAN_POINT ( 'NONE',  ( 2.623503965249849301, 1.760141956857387724, 1.355882097269874187 ) ) ;
#28608=DIRECTION ( 'NONE',  ( -0.000000000000000000, 1.000000000000000000, -0.000000000000000000 ) ) ;
#28611=DIRECTION ( 'NONE',  ( 0.7227948638273878901, -8.024280841161103757E-17, 0.6910626489868684219 ) ) ;
#28616=DIRECTION ( 'NONE',  ( 0.000000000000000000, 0.000000000000000000, 1.000000000000000000 ) ) ;
#28620=ORIENTED_EDGE ( 'NONE', *, *, #28972, .F. ) ;
#28626=LINE ( 'NONE', #44372, #17700 ) ;
#28627=CARTESIAN_POINT ( 'NONE',  ( 0.3136974817028395091, 1.508467219206862664, -2.936457595020219635 ) ) ;
#28630=CARTESIAN_POINT ( 'NONE',  ( 1.722315188380549422, 1.647628733693584868, -2.398471789188510783 ) ) ;
#28631=CARTESIAN_POINT ( 'NONE',  ( -2.889674983507169337, 1.575089141731351505, -0.6090712660038034576 ) ) ;
#28633=CARTESIAN_POINT ( 'NONE',  ( -0.04921259842519689481, 6.692913385826772199, 2.213182383082911375 ) ) ;
#28634=VECTOR ( 'NONE', #22644, 39.37007874015748143 ) ;
#28637=PLANE ( 'NONE',  #14049 ) ;
#28639=CARTESIAN_POINT ( 'NONE',  ( -1.446240454009885879, 0.003210851617283033092, -1.013622345577424699 ) ) ;
#28640=ORIENTED_EDGE ( 'NONE', *, *, #23382, .F. ) ;
#28645=ADVANCED_FACE ( 'NONE', ( #47738 ), #13443, .F. ) ;
#28653=LINE ( 'NONE', #24013, #19140 ) ;
#28655=ADVANCED_FACE ( 'NONE', ( #20412 ), #15111, .F. ) ;
#28660=CARTESIAN_POINT ( 'NONE',  ( 1.834499544866850851, 1.737284818394516206, 1.400019292979238772 ) ) ;
#28666=ORIENTED_EDGE ( 'NONE', *, *, #24871, .T. ) ;
#28667=PLANE ( 'NONE',  #32372 ) ;
#28668=CARTESIAN_POINT ( 'NONE',  ( 2.009930929872536964, 6.692913385826772199, -0.8055662819783819817 ) ) ;
#28672=CARTESIAN_POINT ( 'NONE',  ( 0.7506868623604561197, 1.205361022782829114E-17, 1.860140722251951484 ) ) ;
#28675=CARTESIAN_POINT ( 'NONE',  ( 0.08139965876239094178, 1.610780518492231694, 0.000000000000000000 ) ) ;
#28676=DIRECTION ( 'NONE',  ( -0.9998717552508122886, -0.01601477604151181275, 0.000000000000000000 ) ) ;
#28677=ORIENTED_EDGE ( 'NONE', *, *, #1917, .F. ) ;
#28679=CARTESIAN_POINT ( 'NONE',  ( 0.07982360342473591996, 1.709180471932028711, 0.000000000000000000 ) ) ;
#28685=EDGE_CURVE ( 'NONE', #49753, #7280, #10083, .T. ) ;
#28686=B_SPLINE_CURVE_WITH_KNOTS ( 'NONE', 3,
 ( #27152, #50348, #39287, #26899 ),
 .UNSPECIFIED., .F., .F.,
 ( 4, 4 ),
 ( 2.329983654547761784E-07, 0.002500456612749824697 ),
 .UNSPECIFIED. ) ;
#28692=VECTOR ( 'NONE', #37732, 39.37007874015748143 ) ;
#28693=CARTESIAN_POINT ( 'NONE',  ( 0.4465877632310379930, 0.5234978637819114322, 2.185288426772703296 ) ) ;
#28695=AXIS2_PLACEMENT_3D ( 'NONE', #26811, #42309, #3324 ) ;
#28698=ORIENTED_EDGE ( 'NONE', *, *, #4163, .F. ) ;
#28708=B_SPLINE_CURVE_WITH_KNOTS ( 'NONE', 3,
 ( #26506, #11020, #26759, #19263 ),
 .UNSPECIFIED., .F., .F.,
 ( 4, 4 ),
 ( 2.558209911251601479E-07, 0.002500373748775632822 ),
 .UNSPECIFIED. ) ;
#28710=CARTESIAN_POINT ( 'NONE',  ( 0.000000000000000000, 1.574803149606302854, 0.000000000000000000 ) ) ;
#28714=CARTESIAN_POINT ( 'NONE',  ( 1.695772546416037363, 1.477242674555747426, -2.417756147381349141 ) ) ;
#28715=EDGE_CURVE ( 'NONE', #6874, #16346, #42320, .T. ) ;
#28718=ORIENTED_EDGE ( 'NONE', *, *, #29274, .T. ) ;
#28721=DIRECTION ( 'NONE',  ( -0.01601477604151182663, 0.9998717552508123996, -0.000000000000000000 ) ) ;
#28723=DIRECTION ( 'NONE',  ( 0.8805955318567321166, 0.000000000000000000, 0.4738686624730094055 ) ) ;
#28724=FACE_OUTER_BOUND ( 'NONE', #15280, .T. ) ;
#28727=CARTESIAN_POINT ( 'NONE',  ( 0.08119777152254364916, 1.623385212329073957, 0.000000000000000000 ) ) ;
#28729=ORIENTED_EDGE ( 'NONE', *, *, #48524, .T. ) ;
#28730=DIRECTION ( 'NONE',  ( 1.558091277195270436E-17, -1.000000000000000000, -1.150229170499806500E-16 ) ) ;
#28736=CARTESIAN_POINT ( 'NONE',  ( 2.867773316779195447, 1.205361022782829114E-17, -0.7050287376752006896 ) ) ;
#28740=CONICAL_SURFACE ( 'NONE', #21353, 3.033577403570480779, 1.554780866114618743 ) ;
#28752=VERTEX_POINT ( 'NONE', #6209 ) ;
#28755=ORIENTED_EDGE ( 'NONE', *, *, #32672, .F. ) ;
#28763=CARTESIAN_POINT ( 'NONE',  ( -1.312442655063644770, 0.006898494447474761912, -1.186737126055851022 ) ) ;
#28765=ORIENTED_EDGE ( 'NONE', *, *, #24871, .F. ) ;
#28770=CARTESIAN_POINT ( 'NONE',  ( 2.122091976112993272, 5.905511811023623991, 0.4338754535133124146 ) ) ;
#28772=PLANE ( 'NONE',  #31437 ) ;
#28775=EDGE_LOOP ( 'NONE', ( #20570, #48153, #40262, #16048 ) ) ;
#28780=DIRECTION ( 'NONE',  ( 0.9989930665413151445, 0.000000000000000000, -0.04486483035050446017 ) ) ;
#28783=AXIS2_PLACEMENT_3D ( 'NONE', #13316, #50086, #29048 ) ;
#28786=ORIENTED_EDGE ( 'NONE', *, *, #7381, .T. ) ;
#28790=ORIENTED_EDGE ( 'NONE', *, *, #10551, .T. ) ;
#28793=EDGE_LOOP ( 'NONE', ( #23607, #2452, #17281, #31099 ) ) ;
#28796=DIMENSIONAL_EXPONENTS ( 1.000000000000000000, 0.000000000000000000, 0.000000000000000000, 0.000000000000000000, 0.000000000000000000, 0.000000000000000000, 0.000000000000000000 ) ;
#28802=CARTESIAN_POINT ( 'NONE',  ( -1.037524086854360483, 0.000000000000000000, 2.764473043227569260 ) ) ;
#28803=FACE_OUTER_BOUND ( 'NONE', #36439, .T. ) ;
#28805=B_SPLINE_CURVE_WITH_KNOTS ( 'NONE', 3,
 ( #39945, #31433, #35312, #39688 ),
 .UNSPECIFIED., .F., .F.,
 ( 4, 4 ),
 ( 0.0009642369134306138503, 0.004861909058386497222 ),
 .UNSPECIFIED. ) ;
#28806=EDGE_LOOP ( 'NONE', ( #22945, #51052, #38494, #46408 ) ) ;
#28807=FACE_OUTER_BOUND ( 'NONE', #35562, .T. ) ;
#28812=FACE_OUTER_BOUND ( 'NONE', #7015, .T. ) ;
#28816=CIRCLE ( 'NONE', #3240, 2.244934639244525076 ) ;
#28826=CARTESIAN_POINT ( 'NONE',  ( 1.930249146414562578, 0.05883613814988478824, 0.3111320644955062886 ) ) ;
#28828=EDGE_CURVE ( 'NONE', #2040, #47582, #42306, .T. ) ;
#28830=ORIENTED_EDGE ( 'NONE', *, *, #13039, .T. ) ;
#28831=ORIENTED_EDGE ( 'NONE', *, *, #25476, .F. ) ;
#28840=CARTESIAN_POINT ( 'NONE',  ( 0.000000000000000000, 1.574803149606302854, 0.000000000000000000 ) ) ;
#28841=DIRECTION ( 'NONE',  ( 0.9639628606958549062, 3.084137967884539202E-17, -0.2660368455666687892 ) ) ;
#28847=CONICAL_SURFACE ( 'NONE', #49443, 2.244934639244524632, 1.554780866114618743 ) ;
#28849=ORIENTED_EDGE ( 'NONE', *, *, #30997, .F. ) ;
#28851=CARTESIAN_POINT ( 'NONE',  ( -1.483604961240789555, 5.905511811023623991, 1.623324365321667129 ) ) ;
#28855=EDGE_CURVE ( 'NONE', #16985, #8210, #7206, .T. ) ;
#28856=EDGE_LOOP ( 'NONE', ( #21941, #30298, #3363, #32102 ) ) ;
#28858=CARTESIAN_POINT ( 'NONE',  ( 1.090138530625468061, 5.905511811023623991, 1.920534397867777798 ) ) ;
#28864=EDGE_CURVE ( 'NONE', #41853, #48369, #48055, .T. ) ;
#28873=CARTESIAN_POINT ( 'NONE',  ( 1.556712866041120247, 1.480457248723645591, 2.509548638715870084 ) ) ;
#28874=ORIENTED_EDGE ( 'NONE', *, *, #14205, .F. ) ;
#28877=CARTESIAN_POINT ( 'NONE',  ( 0.000000000000000000, 1.574803149606302854, 0.000000000000000000 ) ) ;
#28884=EDGE_CURVE ( 'NONE', #27061, #47061, #34590, .T. ) ;
#28887=EDGE_LOOP ( 'NONE', ( #16733, #18427, #47538, #41464 ) ) ;
#28888=DIRECTION ( 'NONE',  ( 0.000000000000000000, 0.000000000000000000, -1.000000000000000000 ) ) ;
#28893=DIRECTION ( 'NONE',  ( 0.000000000000000000, 0.000000000000000000, 1.000000000000000000 ) ) ;
#28894=CARTESIAN_POINT ( 'NONE',  ( -2.014567149787738654, 1.675634971041569443, -0.8075478974698888646 ) ) ;
#28899=CARTESIAN_POINT ( 'NONE',  ( 2.100227814008711391, 1.205361022782829114E-17, -2.076109931251913565 ) ) ;
#28903=EDGE_CURVE ( 'NONE', #46686, #26290, #33259, .T. ) ;
#28906=PLANE ( 'NONE',  #8059 ) ;
#28908=VERTEX_POINT ( 'NONE', #23206 ) ;
#28921=ORIENTED_EDGE ( 'NONE', *, *, #11103, .T. ) ;
#28922=CARTESIAN_POINT ( 'NONE',  ( 1.474379988472116487, 1.633091647787944911, 1.762361831087230213 ) ) ;
#28926=AXIS2_PLACEMENT_3D ( 'NONE', #46337, #3250, #46586 ) ;
#28928=CARTESIAN_POINT ( 'NONE',  ( 2.112319093887386146, 0.000000000000000000, 0.3357951146312926904 ) ) ;
#28929=LINE ( 'NONE', #9061, #22662 ) ;
#28932=CARTESIAN_POINT ( 'NONE',  ( 2.491402175429655141, 5.905511811023623991, -1.585592796919505387 ) ) ;
#28933=CARTESIAN_POINT ( 'NONE',  ( 2.947574761915768171, 1.447536563168191126, -0.1816379373804911657 ) ) ;
#28939=ORIENTED_EDGE ( 'NONE', *, *, #45428, .F. ) ;
#28940=EDGE_CURVE ( 'NONE', #36553, #49693, #3091, .T. ) ;
#28941=EDGE_CURVE ( 'NONE', #19249, #38642, #14581, .T. ) ;
#28942=ORIENTED_EDGE ( 'NONE', *, *, #31040, .T. ) ;
#28944=ORIENTED_EDGE ( 'NONE', *, *, #1324, .T. ) ;
#28952=DIRECTION ( 'NONE',  ( 0.000000000000000000, 0.000000000000000000, -1.000000000000000000 ) ) ;
#28954=ORIENTED_EDGE ( 'NONE', *, *, #6590, .T. ) ;
#28957=AXIS2_PLACEMENT_3D ( 'NONE', #45956, #22747, #42609 ) ;
#28962=FACE_OUTER_BOUND ( 'NONE', #20948, .T. ) ;
#28964=ORIENTED_EDGE ( 'NONE', *, *, #9062, .F. ) ;
#28966=CARTESIAN_POINT ( 'NONE',  ( -2.491402175429632493, 5.905511811023623991, -1.585592796919543579 ) ) ;
#28968=ORIENTED_EDGE ( 'NONE', *, *, #14836, .F. ) ;
#28969=ORIENTED_EDGE ( 'NONE', *, *, #41028, .F. ) ;
#28972=EDGE_CURVE ( 'NONE', #28465, #1977, #27538, .T. ) ;
#28973=EDGE_CURVE ( 'NONE', #16862, #26872, #1248, .T. ) ;
#28976=VERTEX_POINT ( 'NONE', #482 ) ;
#28983=VECTOR ( 'NONE', #15157, 39.37007874015748143 ) ;
#28986=CARTESIAN_POINT ( 'NONE',  ( -1.547114303032252502, 1.584696887024839906, -1.547279266820049237 ) ) ;
#28989=ORIENTED_EDGE ( 'NONE', *, *, #42091, .T. ) ;
#28991=VECTOR ( 'NONE', #27052, 39.37007874015748854 ) ;
#28993=B_SPLINE_CURVE_WITH_KNOTS ( 'NONE', 3,
 ( #28660, #24537, #12658, #28398 ),
 .UNSPECIFIED., .F., .F.,
 ( 4, 4 ),
 ( 0.01434375831065246368, 0.03074838983875128814 ),
 .UNSPECIFIED. ) ;
#28996=AXIS2_PLACEMENT_3D ( 'NONE', #23034, #22283, #26399 ) ;
#29001=ORIENTED_EDGE ( 'NONE', *, *, #13617, .F. ) ;
#29008=CARTESIAN_POINT ( 'NONE',  ( 0.04921259842519675604, 1.049866565067837820, 2.024102349885854135 ) ) ;
#29014=LINE ( 'NONE', #43991, #46591 ) ;
#29017=ORIENTED_EDGE ( 'NONE', *, *, #26557, .F. ) ;
#29020=ORIENTED_EDGE ( 'NONE', *, *, #29830, .T. ) ;
#29024=CARTESIAN_POINT ( 'NONE',  ( 1.387661672111481836, 0.000000000000000000, -1.663104731517921930 ) ) ;
#29026=AXIS2_PLACEMENT_3D ( 'NONE', #1862, #38008, #22255 ) ;
#29031=EDGE_LOOP ( 'NONE', ( #40654, #7451, #28786, #40071 ) ) ;
#29032=FACE_OUTER_BOUND ( 'NONE', #33830, .T. ) ;
#29035=ORIENTED_EDGE ( 'NONE', *, *, #15053, .F. ) ;
#29036=CARTESIAN_POINT ( 'NONE',  ( 0.07982360342473591996, 1.709180471932028711, 0.000000000000000000 ) ) ;
#29038=AXIS2_PLACEMENT_3D ( 'NONE', #30065, #17937, #38329 ) ;
#29039=EDGE_LOOP ( 'NONE', ( #15614, #50378, #21555, #14711 ) ) ;
#29040=CARTESIAN_POINT ( 'NONE',  ( -1.258178306623050746, 0.002647435328324944988, -1.271028168397900338 ) ) ;
#29043=CARTESIAN_POINT ( 'NONE',  ( -0.3382312733057311060, 1.205361022782829114E-17, -2.139420919314970693 ) ) ;
#29044=CARTESIAN_POINT ( 'NONE',  ( 0.6507993007407579800, 1.619900495825837838, -2.173134161263437392 ) ) ;
#29048=DIRECTION ( 'NONE',  ( -0.9998717552508121775, -0.01601477604151182663, 0.000000000000000000 ) ) ;
#29051=CARTESIAN_POINT ( 'NONE',  ( -1.317187389162816080, 0.004599037771469988850, -1.191273556348049434 ) ) ;
#29053=CARTESIAN_POINT ( 'NONE',  ( -0.04921259842519706829, 1.516406576848131849, 2.952755905511811108 ) ) ;
#29054=DIRECTION ( 'NONE',  ( -0.9998717552508121775, -0.01601477604151182316, 0.000000000000000000 ) ) ;
#29055=ORIENTED_EDGE ( 'NONE', *, *, #13614, .T. ) ;
#29056=CARTESIAN_POINT ( 'NONE',  ( -1.325491792074585451, 1.543512378121542961, -2.638988599164751925 ) ) ;
#29057=FACE_OUTER_BOUND ( 'NONE', #28793, .T. ) ;
#29061=EDGE_CURVE ( 'NONE', #22430, #22117, #31990, .T. ) ;
#29062=CARTESIAN_POINT ( 'NONE',  ( -0.3499216181689347449, 1.669488919521048276, 2.203840029116182375 ) ) ;
#29069=ORIENTED_EDGE ( 'NONE', *, *, #31338, .F. ) ;
#29075=AXIS2_PLACEMENT_3D ( 'NONE', #2643, #14521, #3400 ) ;
#29076=VECTOR ( 'NONE', #13786, 39.37007874015748143 ) ;
#29079=ORIENTED_EDGE ( 'NONE', *, *, #28067, .T. ) ;
#29080=ORIENTED_EDGE ( 'NONE', *, *, #41203, .F. ) ;
#29086=ORIENTED_EDGE ( 'NONE', *, *, #17996, .F. ) ;
#29093=B_SPLINE_CURVE_WITH_KNOTS ( 'NONE', 3,
 ( #433, #16188, #47638, #12313 ),
 .UNSPECIFIED., .F., .F.,
 ( 4, 4 ),
 ( 6.016737642395432559E-07, 0.0003054758831321558767 ),
 .UNSPECIFIED. ) ;
#29097=AXIS2_PLACEMENT_3D ( 'NONE', #651, #32160, #47850 ) ;
#29098=ADVANCED_FACE ( 'NONE', ( #16232 ), #27445, .F. ) ;
#29104=EDGE_CURVE ( 'NONE', #35146, #2592, #31213, .T. ) ;
#29109=EDGE_CURVE ( 'NONE', #43424, #3538, #8511, .T. ) ;
#29111=DIRECTION ( 'NONE',  ( 0.5128992774058948045, -9.966352232896248990E-17, 0.8584487936018727616 ) ) ;
#29113=CARTESIAN_POINT ( 'NONE',  ( -1.266372989542556393, 1.601078161548953771, -2.667458713958470895 ) ) ;
#29114=CARTESIAN_POINT ( 'NONE',  ( -1.613340714851948965, 1.583636149837539975, -1.474425128113891814 ) ) ;
#29116=ORIENTED_EDGE ( 'NONE', *, *, #19604, .F. ) ;
#29117=CYLINDRICAL_SURFACE ( 'NONE', #6007, 0.3937007874015748254 ) ;
#29124=DIRECTION ( 'NONE',  ( -0.01601477604151182663, 0.9998717552508123996, -0.000000000000000000 ) ) ;
#29132=DIRECTION ( 'NONE',  ( -0.000000000000000000, 1.000000000000000000, 0.000000000000000000 ) ) ;
#29133=( BOUNDED_CURVE ( )  B_SPLINE_CURVE ( 3, ( #43194, #19956, #40373, #16617 ),
 .UNSPECIFIED., .F., .F. ) 
 B_SPLINE_CURVE_WITH_KNOTS ( ( 4, 4 ),
 ( 1.095572580490222991, 1.146464844878060996 ),
 .UNSPECIFIED. ) 
 CURVE ( )  GEOMETRIC_REPRESENTATION_ITEM ( )  RATIONAL_B_SPLINE_CURVE ( ( 1.000000000000000000, 0.9997841764314150392, 0.9997841764314150392, 1.000000000000000000 ) ) 
 REPRESENTATION_ITEM ( '' )  );
#29137=CARTESIAN_POINT ( 'NONE',  ( 1.041764289084840645, 1.629758184783876240, -2.276669304528769366 ) ) ;
#29138=AXIS2_PLACEMENT_3D ( 'NONE', #34878, #3377, #46709 ) ;
#29139=CARTESIAN_POINT ( 'NONE',  ( -1.711605288297850969, 0.0005051743623580321960, -0.3401845456954783464 ) ) ;
#29140=B_SPLINE_CURVE_WITH_KNOTS ( 'NONE', 3,
 ( #24927, #14070, #1432, #33955 ),
 .UNSPECIFIED., .F., .F.,
 ( 4, 4 ),
 ( 0.1211775127643062860, 0.1625894504277921315 ),
 .UNSPECIFIED. ) ;
#29143=CIRCLE ( 'NONE', #15946, 2.165354330708661568 ) ;
#29144=ADVANCED_FACE ( 'NONE', ( #2524 ), #49967, .T. ) ;
#29149=DIRECTION ( 'NONE',  ( -3.986037398843765983E-20, -1.000000000000000000, -1.160734090543304660E-16 ) ) ;
#29150=FACE_OUTER_BOUND ( 'NONE', #29417, .T. ) ;
#29153=ORIENTED_EDGE ( 'NONE', *, *, #34610, .F. ) ;
#29155=CARTESIAN_POINT ( 'NONE',  ( -2.168245791271169676, 5.905511811023623991, -2.004968704497281262 ) ) ;
#29164=ORIENTED_EDGE ( 'NONE', *, *, #13737, .F. ) ;
#29165=ORIENTED_EDGE ( 'NONE', *, *, #28214, .F. ) ;
#29167=CARTESIAN_POINT ( 'NONE',  ( 0.08139965876239094178, 1.610780518492231694, 0.000000000000000000 ) ) ;
#29173=DIRECTION ( 'NONE',  ( -0.9998717552508121775, -0.01601477604151182316, 0.000000000000000000 ) ) ;
#29176=CIRCLE ( 'NONE', #21778, 2.164630168518208109 ) ;
#29180=CARTESIAN_POINT ( 'NONE',  ( 0.000000000000000000, 0.000000000000000000, 0.000000000000000000 ) ) ;
#29184=CARTESIAN_POINT ( 'NONE',  ( 2.878724150143186833, 5.905511811023623991, -0.6570500018394801467 ) ) ;
#29186=CARTESIAN_POINT ( 'NONE',  ( 2.996777194923521126, 5.118110236220475784, 0.9139393566314087947 ) ) ;
#29188=CONICAL_SURFACE ( 'NONE', #36613, 3.483074324928249421, 1.244861948955335196 ) ;
#29197=EDGE_CURVE ( 'NONE', #18948, #24587, #9507, .T. ) ;
#29200=EDGE_CURVE ( 'NONE', #3200, #9387, #5971, .T. ) ;
#29201=ORIENTED_EDGE ( 'NONE', *, *, #19658, .T. ) ;
#29202=PLANE ( 'NONE',  #33455 ) ;
#29205=ORIENTED_EDGE ( 'NONE', *, *, #15436, .T. ) ;
#29218=B_SPLINE_CURVE_WITH_KNOTS ( 'NONE', 3,
 ( #35797, #47111, #157, #11781 ),
 .UNSPECIFIED., .F., .F.,
 ( 4, 4 ),
 ( 0.05979284115972890307, 0.06207050146966483495 ),
 .UNSPECIFIED. ) ;
#29224=FACE_OUTER_BOUND ( 'NONE', #37783, .T. ) ;
#29228=CARTESIAN_POINT ( 'NONE',  ( -0.7380211471543357549, 0.01609890615456165824, -1.645940171248041928 ) ) ;
#29230=CARTESIAN_POINT ( 'NONE',  ( 2.086662150992999010, 0.000000000000000000, -0.4594568716432768096 ) ) ;
#29240=EDGE_CURVE ( 'NONE', #1553, #29362, #2766, .T. ) ;
#29241=FACE_OUTER_BOUND ( 'NONE', #44528, .T. ) ;
#29242=ORIENTED_EDGE ( 'NONE', *, *, #27909, .F. ) ;
#29243=DIRECTION ( 'NONE',  ( 7.237058681235204266E-17, -1.000000000000000000, 9.074984547606538936E-17 ) ) ;
#29244=DIRECTION ( 'NONE',  ( -6.394449067488487880E-17, -1.000000000000000000, -9.687176266499690201E-17 ) ) ;
#29247=DIRECTION ( 'NONE',  ( -0.000000000000000000, -1.000000000000000000, -0.000000000000000000 ) ) ;
#29254=B_SPLINE_CURVE_WITH_KNOTS ( 'NONE', 3,
 ( #12808, #36557, #39912, #12032 ),
 .UNSPECIFIED., .F., .F.,
 ( 4, 4 ),
 ( 2.074994163403008576E-07, 0.002500489216568123514 ),
 .UNSPECIFIED. ) ;
#29255=ORIENTED_EDGE ( 'NONE', *, *, #27896, .T. ) ;
#29257=DIRECTION ( 'NONE',  ( 0.9998717552508121775, 0.01601477604151182663, 0.000000000000000000 ) ) ;
#29261=CARTESIAN_POINT ( 'NONE',  ( -2.006326915404077038, 1.581476153537414220, -1.383332181782276127 ) ) ;
#29264=ORIENTED_EDGE ( 'NONE', *, *, #35242, .F. ) ;
#29273=EDGE_CURVE ( 'NONE', #15190, #32538, #1620, .T. ) ;
#29274=EDGE_CURVE ( 'NONE', #5605, #36136, #1100, .T. ) ;
#29275=EDGE_CURVE ( 'NONE', #37703, #43876, #14903, .T. ) ;
#29276=CARTESIAN_POINT ( 'NONE',  ( 2.734482843737263025, 5.118110236220475784, -1.115254632218672270 ) ) ;
#29277=EDGE_LOOP ( 'NONE', ( #389, #44091, #34611, #26714 ) ) ;
#29280=CARTESIAN_POINT ( 'NONE',  ( -0.4369915662458470074, 0.02092044581182531462, -1.768387524372482034 ) ) ;
#29283=CARTESIAN_POINT ( 'NONE',  ( -0.9914495361339011881, 1.605369965488712136, 2.781765111341808705 ) ) ;
#29288=DIRECTION ( 'NONE',  ( 7.105427357601001859E-15, 0.000000000000000000, -1.000000000000000000 ) ) ;
#29293=AXIS2_PLACEMENT_3D ( 'NONE', #30651, #14394, #26513 ) ;
#29294=ORIENTED_EDGE ( 'NONE', *, *, #38984, .F. ) ;
#29299=ORIENTED_EDGE ( 'NONE', *, *, #41798, .T. ) ;
#29301=DIRECTION ( 'NONE',  ( 0.000000000000000000, 0.000000000000000000, -1.000000000000000000 ) ) ;
#29306=UNCERTAINTY_MEASURE_WITH_UNIT (LENGTH_MEASURE( 1.000000000000000082E-05 ), #10660, 'distance_accuracy_value', 'NONE');
#29312=CARTESIAN_POINT ( 'NONE',  ( -0.8515791614234526907, 0.000000000000000000, 1.521253268579204398 ) ) ;
#29317=CARTESIAN_POINT ( 'NONE',  ( -0.2468853591798393365, 0.5233347894274020806, -2.194114114529797988 ) ) ;
#29318=ORIENTED_EDGE ( 'NONE', *, *, #35278, .F. ) ;
#29321=EDGE_LOOP ( 'NONE', ( #46026, #26343, #29080, #29020 ) ) ;
#29329=VECTOR ( 'NONE', #9201, 39.37007874015748143 ) ;
#29332=VERTEX_POINT ( 'NONE', #16621 ) ;
#29343=VERTEX_POINT ( 'NONE', #10771 ) ;
#29344=EDGE_CURVE ( 'NONE', #12327, #23437, #30649, .T. ) ;
#29348=VERTEX_POINT ( 'NONE', #4741 ) ;
#29353=CARTESIAN_POINT ( 'NONE',  ( -1.716372755931022454, 1.049866565067837820, -1.074000356310436555 ) ) ;
#29356=ORIENTED_EDGE ( 'NONE', *, *, #28884, .F. ) ;
#29360=AXIS2_PLACEMENT_3D ( 'NONE', #37520, #29762, #48324 ) ;
#29362=VERTEX_POINT ( 'NONE', #18775 ) ;
#29364=VECTOR ( 'NONE', #45588, 39.37007874015748143 ) ;
#29366=ADVANCED_FACE ( 'NONE', ( #34529 ), #34776, .T. ) ;
#29367=VERTEX_POINT ( 'NONE', #47808 ) ;
#29368=CARTESIAN_POINT ( 'NONE',  ( 0.000000000000000000, 5.905511811023623991, 0.000000000000000000 ) ) ;
#29375=AXIS2_PLACEMENT_3D ( 'NONE', #19293, #11807, #24200 ) ;
#29376=CARTESIAN_POINT ( 'NONE',  ( 1.223349603905365068, 0.04751384826852676074, 1.475034436811822669 ) ) ;
#29377=FACE_OUTER_BOUND ( 'NONE', #37137, .T. ) ;
#29379=DIRECTION ( 'NONE',  ( -0.000000000000000000, -1.000000000000000000, -0.000000000000000000 ) ) ;
#29381=B_SPLINE_CURVE_WITH_KNOTS ( 'NONE', 3,
 ( #43210, #877, #20498, #16889 ),
 .UNSPECIFIED., .F., .F.,
 ( 4, 4 ),
 ( 0.1211873102087489551, 0.1625992483279400380 ),
 .UNSPECIFIED. ) ;
#29384=DIRECTION ( 'NONE',  ( -0.6234898018587318180, 0.000000000000000000, -0.7818314824680309139 ) ) ;
#29387=DIRECTION ( 'NONE',  ( 0.000000000000000000, 0.000000000000000000, -1.000000000000000000 ) ) ;
#29391=EDGE_LOOP ( 'NONE', ( #37551, #48283, #7454, #24480 ) ) ;
#29394=CARTESIAN_POINT ( 'NONE',  ( -1.905671854841497481, 1.591126119768930147, 2.256015092822653223 ) ) ;
#29396=CARTESIAN_POINT ( 'NONE',  ( 0.2810050591710572809, 1.508447189148403922, -2.939399966304093503 ) ) ;
#29400=EDGE_CURVE ( 'NONE', #21767, #36721, #31794, .T. ) ;
#29401=VECTOR ( 'NONE', #26753, 39.37007874015748143 ) ;
#29402=DIRECTION ( 'NONE',  ( -0.000000000000000000, -1.000000000000000000, -0.000000000000000000 ) ) ;
#29407=CARTESIAN_POINT ( 'NONE',  ( -1.395323331152583002, 0.5249316475426865081, -1.265979166134213241 ) ) ;
#29409=EDGE_LOOP ( 'NONE', ( #34096, #44926, #9010, #18823, #38389, #13824, #28831, #41168, #9342, #41518, #31500, #14440, #17490 ) ) ;
#29416=DIRECTION ( 'NONE',  ( 1.558091277195270436E-17, -1.000000000000000000, -1.150229170499806500E-16 ) ) ;
#29417=EDGE_LOOP ( 'NONE', ( #894, #35664, #22196, #27662, #38328, #30977, #43418, #30936, #14700, #27756, #43489, #30814, #32031, #17927, #45322, #5839, #24787 ) ) ;
#29418=ORIENTED_EDGE ( 'NONE', *, *, #26444, .F. ) ;
#29425=EDGE_LOOP ( 'NONE', ( #28666, #786, #23377, #304 ) ) ;
#29427=B_SPLINE_CURVE_WITH_KNOTS ( 'NONE', 3,
 ( #21652, #44371, #29655, #45121 ),
 .UNSPECIFIED., .F., .F.,
 ( 4, 4 ),
 ( 0.002197616311132118659, 0.003926668439082322930 ),
 .UNSPECIFIED. ) ;
#29429=CARTESIAN_POINT ( 'NONE',  ( -2.076676417810221942, 1.641831778720078017, 0.6230078826482280396 ) ) ;
#29436=AXIS2_PLACEMENT_3D ( 'NONE', #45237, #11165, #26897 ) ;
#29438=LINE ( 'NONE', #37197, #49410 ) ;
#29442=CIRCLE ( 'NONE', #26918, 2.165354330708661568 ) ;
#29447=DIRECTION ( 'NONE',  ( 0.000000000000000000, 0.000000000000000000, 1.000000000000000000 ) ) ;
#29448=CARTESIAN_POINT ( 'NONE',  ( -2.160407304981126320, 6.692913385826772199, -0.1462862061266902158 ) ) ;
#29449=( BOUNDED_CURVE ( )  B_SPLINE_CURVE ( 3, ( #27274, #47371, #11786, #31413 ),
 .UNSPECIFIED., .F., .F. ) 
 B_SPLINE_CURVE_WITH_KNOTS ( ( 4, 4 ),
 ( 4.146021982105191128, 4.196929668049186546 ),
 .UNSPECIFIED. ) 
 CURVE ( )  GEOMETRIC_REPRESENTATION_ITEM ( )  RATIONAL_B_SPLINE_CURVE ( ( 1.000000000000000000, 0.9997840456193998193, 0.9997840456193998193, 1.000000000000000000 ) ) 
 REPRESENTATION_ITEM ( '' )  );
#29453=DIRECTION ( 'NONE',  ( 0.000000000000000000, 0.000000000000000000, 1.000000000000000000 ) ) ;
#29454=DIRECTION ( 'NONE',  ( -3.986037398843765983E-20, -1.000000000000000000, -1.160734090543304660E-16 ) ) ;
#29455=VERTEX_POINT ( 'NONE', #33401 ) ;
#29457=CARTESIAN_POINT ( 'NONE',  ( 1.930190994932110771, 5.905511811023623991, -0.9827944786818444411 ) ) ;
#29460=EDGE_CURVE ( 'NONE', #28307, #29367, #37265, .T. ) ;
#29461=ORIENTED_EDGE ( 'NONE', *, *, #4226, .F. ) ;
#29466=B_SPLINE_CURVE_WITH_KNOTS ( 'NONE', 3,
 ( #26679, #11692, #30815, #38818 ),
 .UNSPECIFIED., .F., .F.,
 ( 4, 4 ),
 ( 0.01469741895130448860, 0.03075036094151098465 ),
 .UNSPECIFIED. ) ;
#29471=EDGE_CURVE ( 'NONE', #29695, #39301, #47806, .T. ) ;
#29472=VERTEX_POINT ( 'NONE', #36497 ) ;
#29474=CONICAL_SURFACE ( 'NONE', #7222, 2.244934639244524632, 1.554780866114618743 ) ;
#29475=CARTESIAN_POINT ( 'NONE',  ( 0.8952071785065199849, 1.205361022782829114E-17, 1.972340328593147785 ) ) ;
#29478=DIRECTION ( 'NONE',  ( 1.142080616180678453E-16, -1.000000000000000000, 2.072570748943325363E-17 ) ) ;
#29481=ORIENTED_EDGE ( 'NONE', *, *, #42754, .F. ) ;
#29482=CARTESIAN_POINT ( 'NONE',  ( 0.2156685157584260770, 1.510622172706404864, -2.945280361644574185 ) ) ;
#29483=ADVANCED_FACE ( 'NONE', ( #5759 ), #41539, .T. ) ;
#29487=CARTESIAN_POINT ( 'NONE',  ( 0.000000000000000000, 6.692913385826772199, 0.000000000000000000 ) ) ;
#29488=DIRECTION ( 'NONE',  ( 0.8090169943749422332, -1.160734090543304660E-16, 0.5877852522924802425 ) ) ;
#29490=EDGE_CURVE ( 'NONE', #30462, #36192, #11642, .T. ) ;
#29492=ORIENTED_EDGE ( 'NONE', *, *, #26098, .F. ) ;
#29494=AXIS2_PLACEMENT_3D ( 'NONE', #6599, #38097, #29054 ) ;
#29497=CARTESIAN_POINT ( 'NONE',  ( -1.905671854841497481, 1.555429617898292705, 2.256015092822653667 ) ) ;
#29498=B_SPLINE_CURVE_WITH_KNOTS ( 'NONE', 3,
 ( #35494, #23872, #8382, #31622 ),
 .UNSPECIFIED., .F., .F.,
 ( 4, 4 ),
 ( 6.057676006406350327E-07, 0.0007515069461672322206 ),
 .UNSPECIFIED. ) ;
#29499=CARTESIAN_POINT ( 'NONE',  ( -2.491402175429631605, 1.680428061220146096, -1.585592796919542025 ) ) ;
#29500=ORIENTED_EDGE ( 'NONE', *, *, #35026, .F. ) ;
#29506=CARTESIAN_POINT ( 'NONE',  ( -2.083222340934659300, 0.5254407309824460359, -0.5259600971123018498 ) ) ;
#29515=EDGE_CURVE ( 'NONE', #40104, #42907, #12740, .T. ) ;
#29517=CARTESIAN_POINT ( 'NONE',  ( 0.8329809839909850799, 1.633788288308783976, -2.833254665166554442 ) ) ;
#29521=FACE_OUTER_BOUND ( 'NONE', #28403, .T. ) ;
#29522=FACE_OUTER_BOUND ( 'NONE', #7635, .T. ) ;
#29523=VERTEX_POINT ( 'NONE', #33649 ) ;
#29524=CARTESIAN_POINT ( 'NONE',  ( -2.221753473495927445, 1.582160102031600735, -1.525534007743318377 ) ) ;
#29525=VECTOR ( 'NONE', #50510, 39.37007874015748143 ) ;
#29527=ORIENTED_EDGE ( 'NONE', *, *, #43378, .F. ) ;
#29530=ORIENTED_EDGE ( 'NONE', *, *, #23225, .F. ) ;
#29531=AXIS2_PLACEMENT_3D ( 'NONE', #23028, #15029, #46488 ) ;
#29533=ADVANCED_FACE ( 'NONE', ( #38284 ), #10140, .T. ) ;
#29536=DIRECTION ( 'NONE',  ( 0.000000000000000000, 0.000000000000000000, -1.000000000000000000 ) ) ;
#29537=EDGE_CURVE ( 'NONE', #35582, #970, #46486, .T. ) ;
#29543=ORIENTED_EDGE ( 'NONE', *, *, #23941, .T. ) ;
#29548=ORIENTED_EDGE ( 'NONE', *, *, #21056, .F. ) ;
#29551=AXIS2_PLACEMENT_3D ( 'NONE', #11053, #41790, #26792 ) ;
#29552=DIRECTION ( 'NONE',  ( -0.000000000000000000, -1.000000000000000000, -0.000000000000000000 ) ) ;
#29553=VERTEX_POINT ( 'NONE', #49340 ) ;
#29554=CARTESIAN_POINT ( 'NONE',  ( -2.139032205770588835, 1.608024637552048164, 0.3394136515002111887 ) ) ;
#29559=CIRCLE ( 'NONE', #3972, 2.165354330708661568 ) ;
#29571=CARTESIAN_POINT ( 'NONE',  ( 0.9248149864487152927, 1.627908877233774421, 2.324103449680534172 ) ) ;
#29572=EDGE_CURVE ( 'NONE', #25302, #13127, #22518, .T. ) ;
#29573=CARTESIAN_POINT ( 'NONE',  ( -1.859752235501543227, 0.5249316475426858419, 0.3015826090669521120 ) ) ;
#29575=EDGE_CURVE ( 'NONE', #11672, #45506, #45252, .T. ) ;
#29577=CARTESIAN_POINT ( 'NONE',  ( -2.951990591674674480, 1.205361022782829114E-17, -0.08331184815402571664 ) ) ;
#29579=CARTESIAN_POINT ( 'NONE',  ( -0.2802969821979833243, 1.022684513435495157, -2.565347650952780612 ) ) ;
#29580=ORIENTED_EDGE ( 'NONE', *, *, #20066, .F. ) ;
#29582=B_SPLINE_CURVE_WITH_KNOTS ( 'NONE', 3,
 ( #5118, #20354, #40240, #12611 ),
 .UNSPECIFIED., .F., .F.,
 ( 4, 4 ),
 ( 0.0001573404397883737223, 0.004927678653679096535 ),
 .UNSPECIFIED. ) ;
#29583=DIRECTION ( 'NONE',  ( 0.01601477604151182663, -0.9998717552508123996, 0.000000000000000000 ) ) ;
#29586=FACE_OUTER_BOUND ( 'NONE', #34774, .T. ) ;
#29594=CARTESIAN_POINT ( 'NONE',  ( 2.932638728931774352, 1.205361022782829114E-17, 0.3475908556738223631 ) ) ;
#29597=CARTESIAN_POINT ( 'NONE',  ( 0.7759887336347247588, 0.04034854520891290042, -1.724780676950718794 ) ) ;
#29601=DIRECTION ( 'NONE',  ( -0.01601477604151182663, 0.9998717552508123996, -0.000000000000000000 ) ) ;
#29603=EDGE_CURVE ( 'NONE', #38735, #20325, #8991, .T. ) ;
#29605=CIRCLE ( 'NONE', #5682, 1.743387098533651480 ) ;
#29609=VERTEX_POINT ( 'NONE', #2399 ) ;
#29611=CARTESIAN_POINT ( 'NONE',  ( 3.937007874015748143, 0.000000000000000000, 0.000000000000000000 ) ) ;
#29614=ORIENTED_EDGE ( 'NONE', *, *, #39086, .T. ) ;
#29616=CARTESIAN_POINT ( 'NONE',  ( 2.013783482383322720, 1.740156378764222245, 1.139548688847630942 ) ) ;
#29617=B_SPLINE_CURVE_WITH_KNOTS ( 'NONE', 3,
 ( #17405, #41407, #9916, #6033 ),
 .UNSPECIFIED., .F., .F.,
 ( 4, 4 ),
 ( 0.001422306547608694852, 0.003922515224842213107 ),
 .UNSPECIFIED. ) ;
#29619=CARTESIAN_POINT ( 'NONE',  ( 1.442672029790674104, 1.738133376546725506, 2.318676429272163109 ) ) ;
#29628=CARTESIAN_POINT ( 'NONE',  ( 1.306513359544259956, 1.663211357094787957, -1.881986840193734967 ) ) ;
#29629=VECTOR ( 'NONE', #49396, 39.37007874015748143 ) ;
#29634=ADVANCED_FACE ( 'NONE', ( #30775 ), #34939, .T. ) ;
#29638=CARTESIAN_POINT ( 'NONE',  ( 0.000000000000000000, 10.31496062992126284, 0.000000000000000000 ) ) ;
#29641=LINE ( 'NONE', #37906, #2945 ) ;
#29642=DIRECTION ( 'NONE',  ( 0.000000000000000000, 1.160734090543304660E-16, -1.000000000000000000 ) ) ;
#29643=EDGE_CURVE ( 'NONE', #29652, #19240, #30577, .T. ) ;
#29644=DIRECTION ( 'NONE',  ( 0.01601477604151182663, -0.9998717552508123996, 0.000000000000000000 ) ) ;
#29646=EDGE_LOOP ( 'NONE', ( #18679, #37973, #7521, #24773 ) ) ;
#29652=VERTEX_POINT ( 'NONE', #15026 ) ;
#29655=CARTESIAN_POINT ( 'NONE',  ( -0.3818873615803586308, 0.007309285104348540660, 1.828759827582272068 ) ) ;
#29672=DIRECTION ( 'NONE',  ( 0.7227948638273880011, 0.000000000000000000, 0.6910626489868685329 ) ) ;
#29673=B_SPLINE_CURVE_WITH_KNOTS ( 'NONE', 3,
 ( #23993, #15992, #34856, #50540 ),
 .UNSPECIFIED., .F., .F.,
 ( 4, 4 ),
 ( 0.001225133028562884257, 0.003725407075890712141 ),
 .UNSPECIFIED. ) ;
#29677=ORIENTED_EDGE ( 'NONE', *, *, #13706, .F. ) ;
#29678=CARTESIAN_POINT ( 'NONE',  ( 0.1525302393087137887, 1.710345001767278994, -2.243756654240526505 ) ) ;
#29681=VECTOR ( 'NONE', #47254, 39.37007874015748143 ) ;
#29690=ORIENTED_EDGE ( 'NONE', *, *, #45117, .T. ) ;
#29691=CARTESIAN_POINT ( 'NONE',  ( 0.000000000000000000, 0.07874015748031502893, 0.000000000000000000 ) ) ;
#29693=CARTESIAN_POINT ( 'NONE',  ( -0.2134117707794043750, 0.02450148541315291459, -1.822192086320855164 ) ) ;
#29695=VERTEX_POINT ( 'NONE', #8033 ) ;
#29700=EDGE_CURVE ( 'NONE', #42296, #33123, #11651, .T. ) ;
#29706=AXIS2_PLACEMENT_3D ( 'NONE', #44214, #28721, #20985 ) ;
#29711=CARTESIAN_POINT ( 'NONE',  ( 0.000000000000000000, 2.755905511811027164, 0.000000000000000000 ) ) ;
#29712=CONICAL_SURFACE ( 'NONE', #23106, 3.033577403570480779, 1.554780866114618743 ) ;
#29713=ORIENTED_EDGE ( 'NONE', *, *, #7676, .F. ) ;
#29725=VERTEX_POINT ( 'NONE', #24302 ) ;
#29726=CARTESIAN_POINT ( 'NONE',  ( -1.477691947303356290, 1.684234009953186728, 1.616556376299586706 ) ) ;
#29728=ORIENTED_EDGE ( 'NONE', *, *, #28097, .T. ) ;
#29729=CARTESIAN_POINT ( 'NONE',  ( -0.8368120681608454126, 0.004905009409801163595, -1.624234696386792631 ) ) ;
#29741=CARTESIAN_POINT ( 'NONE',  ( -2.623503965249869729, 1.678368413758691391, 1.355882097269835107 ) ) ;
#29742=CARTESIAN_POINT ( 'NONE',  ( -1.281152772984899491, 0.000000000000000000, -2.660341145381166506 ) ) ;
#29743=ORIENTED_EDGE ( 'NONE', *, *, #6815, .T. ) ;
#29747=( BOUNDED_CURVE ( )  B_SPLINE_CURVE ( 3, ( #42914, #7815, #11942, #22551 ),
 .UNSPECIFIED., .F., .F. ) 
 B_SPLINE_CURVE_WITH_KNOTS ( ( 4, 4 ),
 ( 1.467165271168491936, 1.518105237349054670 ),
 .UNSPECIFIED. ) 
 CURVE ( )  GEOMETRIC_REPRESENTATION_ITEM ( )  RATIONAL_B_SPLINE_CURVE ( ( 1.000000000000000000, 0.9997837716768099847, 0.9997837716768099847, 1.000000000000000000 ) ) 
 REPRESENTATION_ITEM ( '' )  );
#29748=B_SPLINE_CURVE_WITH_KNOTS ( 'NONE', 3,
 ( #6786, #6542, #50102, #10909 ),
 .UNSPECIFIED., .F., .F.,
 ( 4, 4 ),
 ( 2.008297436534455258E-07, 0.01816780577132326782 ),
 .UNSPECIFIED. ) ;
#29749=LINE ( 'NONE', #25619, #19515 ) ;
#29755=EDGE_LOOP ( 'NONE', ( #45176, #34430, #7068, #8362 ) ) ;
#29762=DIRECTION ( 'NONE',  ( -0.000000000000000000, 1.000000000000000000, -0.000000000000000000 ) ) ;
#29768=CIRCLE ( 'NONE', #33907, 2.244934639244525076 ) ;
#29769=ORIENTED_EDGE ( 'NONE', *, *, #26281, .F. ) ;
#29776=DIRECTION ( 'NONE',  ( 0.000000000000000000, 1.000000000000000000, -0.000000000000000000 ) ) ;
#29778=ORIENTED_EDGE ( 'NONE', *, *, #49695, .F. ) ;
#29782=VERTEX_POINT ( 'NONE', #35411 ) ;
#29789=CARTESIAN_POINT ( 'NONE',  ( 1.109524193798303804, 0.000000000000000000, 1.344750771968474590 ) ) ;
#29790=ORIENTED_EDGE ( 'NONE', *, *, #16295, .T. ) ;
#29791=ORIENTED_EDGE ( 'NONE', *, *, #43956, .T. ) ;
#29794=ORIENTED_EDGE ( 'NONE', *, *, #25695, .T. ) ;
#29802=DIRECTION ( 'NONE',  ( 5.500355109725808462E-17, -1.000000000000000000, -1.022137253806221654E-16 ) ) ;
#29805=DIRECTION ( 'NONE',  ( 0.000000000000000000, -1.000000000000000000, 0.000000000000000000 ) ) ;
#29811=EDGE_LOOP ( 'NONE', ( #16242, #3684, #21805, #42813 ) ) ;
#29820=B_SPLINE_CURVE_WITH_KNOTS ( 'NONE', 3,
 ( #40782, #20383, #44121, #36138 ),
 .UNSPECIFIED., .F., .F.,
 ( 4, 4 ),
 ( 2.102946038521954085E-07, 0.002500239258116422787 ),
 .UNSPECIFIED. ) ;
#29822=VECTOR ( 'NONE', #36272, 39.37007874015748143 ) ;
#29824=ORIENTED_EDGE ( 'NONE', *, *, #8413, .F. ) ;
#29829=CARTESIAN_POINT ( 'NONE',  ( 2.424495731808704591, 1.651670313967669390, 0.7360212284965905738 ) ) ;
#29830=EDGE_CURVE ( 'NONE', #23878, #8216, #27446, .T. ) ;
#29832=PLANE ( 'NONE',  #20413 ) ;
#29838=CARTESIAN_POINT ( 'NONE',  ( 0.000000000000000000, 1.574803149606302854, 0.000000000000000000 ) ) ;
#29847=DIRECTION ( 'NONE',  ( -0.9749279121818259508, 0.000000000000000000, 0.2225209339563041788 ) ) ;
#29849=AXIS2_PLACEMENT_3D ( 'NONE', #29487, #41871, #5739 ) ;
#29853=AXIS2_PLACEMENT_3D ( 'NONE', #45762, #22303, #46762 ) ;
#29855=ORIENTED_EDGE ( 'NONE', *, *, #37798, .F. ) ;
#29857=CONICAL_SURFACE ( 'NONE', #14190, 2.244934639244524632, 1.554780866114618743 ) ;
#29858=CARTESIAN_POINT ( 'NONE',  ( -2.120667608396066051, 0.5253322431346389987, 0.3369259977602169220 ) ) ;
#29859=VERTEX_POINT ( 'NONE', #33086 ) ;
#29861=DIRECTION ( 'NONE',  ( 5.500355109725658086E-17, -1.000000000000000000, 1.022137253806229789E-16 ) ) ;
#29864=VERTEX_POINT ( 'NONE', #20938 ) ;
#29867=CARTESIAN_POINT ( 'NONE',  ( 0.1155636338427008941, -0.5222242541845523167, 0.000000000000000000 ) ) ;
#29870=CARTESIAN_POINT ( 'NONE',  ( 1.556712866041120247, 1.743522182421873401, 2.509548638715870084 ) ) ;
#29872=ORIENTED_EDGE ( 'NONE', *, *, #9062, .T. ) ;
#29873=EDGE_CURVE ( 'NONE', #46587, #8462, #2809, .T. ) ;
#29876=LINE ( 'NONE', #21620, #29364 ) ;
#29878=CARTESIAN_POINT ( 'NONE',  ( 1.386843392441768241, 1.730114785850798587, -1.825100698618727257 ) ) ;
#29880=EDGE_CURVE ( 'NONE', #7588, #17434, #32835, .T. ) ;
#29881=VECTOR ( 'NONE', #3577, 39.37007874015748854 ) ;
#29882=CARTESIAN_POINT ( 'NONE',  ( 1.481515513156649977, 0.000000000000000000, -0.9189724476880527515 ) ) ;
#29884=VECTOR ( 'NONE', #19748, 39.37007874015748143 ) ;
#29885=CARTESIAN_POINT ( 'NONE',  ( -1.236813753895213086, 1.601547340627394567, -2.681693691597581974 ) ) ;
#29893=CARTESIAN_POINT ( 'NONE',  ( 0.000000000000000000, 1.574803149606302854, 0.000000000000000000 ) ) ;
#29894=AXIS2_PLACEMENT_3D ( 'NONE', #15023, #6770, #6267 ) ;
#29895=VECTOR ( 'NONE', #1046, 39.37007874015748143 ) ;
#29896=ORIENTED_EDGE ( 'NONE', *, *, #38424, .F. ) ;
#29904=LINE ( 'NONE', #27026, #2542 ) ;
#29907=CARTESIAN_POINT ( 'NONE',  ( -2.659291275338656391, 1.673716702457430650, 0.4098875308770844605 ) ) ;
#29908=CARTESIAN_POINT ( 'NONE',  ( 1.971247363764867977, 5.905511811023623991, -0.8960709840011632510 ) ) ;
#29911=ORIENTED_EDGE ( 'NONE', *, *, #44479, .T. ) ;
#29918=CARTESIAN_POINT ( 'NONE',  ( -2.793030215715272213, 1.205361022782829114E-17, 0.9592557174602285297 ) ) ;
#29920=DIRECTION ( 'NONE',  ( -0.01601477604151182663, 0.9998717552508123996, -0.000000000000000000 ) ) ;
#29924=DIRECTION ( 'NONE',  ( -0.08963930890342654279, 0.000000000000000000, -0.9959742939952397345 ) ) ;
#29931=VECTOR ( 'NONE', #6466, 39.37007874015748143 ) ;
#29933=DIRECTION ( 'NONE',  ( -3.986037398843765983E-20, -1.000000000000000000, -1.160734090543304660E-16 ) ) ;
#29934=VERTEX_POINT ( 'NONE', #17576 ) ;
#29938=CARTESIAN_POINT ( 'NONE',  ( 0.000000000000000000, 1.574803149606302854, 0.000000000000000000 ) ) ;
#29954=EDGE_CURVE ( 'NONE', #47540, #1516, #22718, .T. ) ;
#29957=LINE ( 'NONE', #45166, #16577 ) ;
#29958=CARTESIAN_POINT ( 'NONE',  ( 0.002207914879453961535, -5.712274067634378313E-18, 0.04916304461325374242 ) ) ;
#29974=LINE ( 'NONE', #6989, #26016 ) ;
#29978=VERTEX_POINT ( 'NONE', #38475 ) ;
#29980=EDGE_CURVE ( 'NONE', #45076, #47505, #21788, .T. ) ;
#29985=CARTESIAN_POINT ( 'NONE',  ( 2.919426793319799707, 1.764751637901927905, 0.4451252810446822417 ) ) ;
#29990=CARTESIAN_POINT ( 'NONE',  ( 1.955086072707955314, 1.749719979519482882, 2.212843190799998805 ) ) ;
#29993=CYLINDRICAL_SURFACE ( 'NONE', #29849, 2.165354330708661568 ) ;
#29997=EDGE_LOOP ( 'NONE', ( #21648, #7270, #25342, #15947 ) ) ;
#29998=VECTOR ( 'NONE', #7731, 39.37007874015748143 ) ;
#29999=ORIENTED_EDGE ( 'NONE', *, *, #21569, .F. ) ;
#30005=B_SPLINE_CURVE_WITH_KNOTS ( 'NONE', 3,
 ( #33524, #42011, #45858, #6648 ),
 .UNSPECIFIED., .F., .F.,
 ( 4, 4 ),
 ( 0.01377987572523645989, 0.03074485555701141071 ),
 .UNSPECIFIED. ) ;
#30006=LINE ( 'NONE', #41881, #12338 ) ;
#30012=VERTEX_POINT ( 'NONE', #18848 ) ;
#30014=DIRECTION ( 'NONE',  ( 0.5128992774058948045, 0.000000000000000000, 0.8584487936018727616 ) ) ;
#30017=CARTESIAN_POINT ( 'NONE',  ( -1.500395101971645273, 1.546412888404644637, 2.543196936333195435 ) ) ;
#30021=CARTESIAN_POINT ( 'NONE',  ( -2.318790890269176064, 1.563058755309824299, 1.828180962769875739 ) ) ;
#30033=CARTESIAN_POINT ( 'NONE',  ( -2.164823134740035737, 6.692913385826772199, -0.04796011690018289753 ) ) ;
#30035=CARTESIAN_POINT ( 'NONE',  ( 2.734482843737263025, 1.663397001319319113, -1.115254632218672493 ) ) ;
#30037=AXIS2_PLACEMENT_3D ( 'NONE', #25005, #12620, #32251 ) ;
#30038=CARTESIAN_POINT ( 'NONE',  ( 2.069752515245542046, 1.205361022782829114E-17, -0.5228856972975560735 ) ) ;
#30043=VERTEX_POINT ( 'NONE', #33846 ) ;
#30054=VERTEX_POINT ( 'NONE', #22465 ) ;
#30057=( BOUNDED_CURVE ( )  B_SPLINE_CURVE ( 3, ( #31690, #47132, #36078, #11804 ),
 .UNSPECIFIED., .F., .F. ) 
 B_SPLINE_CURVE_WITH_KNOTS ( ( 4, 4 ),
 ( 0.5174987408647891973, 0.5682857577414799355 ),
 .UNSPECIFIED. ) 
 CURVE ( )  GEOMETRIC_REPRESENTATION_ITEM ( )  RATIONAL_B_SPLINE_CURVE ( ( 1.000000000000000000, 0.9997850681263177330, 0.9997850681263177330, 1.000000000000000000 ) ) 
 REPRESENTATION_ITEM ( '' )  );
#30060=EDGE_CURVE ( 'NONE', #28528, #22720, #38224, .T. ) ;
#30061=ORIENTED_EDGE ( 'NONE', *, *, #20243, .T. ) ;
#30062=FACE_OUTER_BOUND ( 'NONE', #30749, .T. ) ;
#30065=CARTESIAN_POINT ( 'NONE',  ( 0.000000000000000000, 1.574803149606302854, 0.000000000000000000 ) ) ;
#30066=EDGE_LOOP ( 'NONE', ( #35239, #45432, #37500, #36334 ) ) ;
#30069=DIRECTION ( 'NONE',  ( -0.01601477604151182663, 0.9998717552508123996, -0.000000000000000000 ) ) ;
#30071=EDGE_CURVE ( 'NONE', #33703, #49472, #45674, .T. ) ;
#30073=CARTESIAN_POINT ( 'NONE',  ( -1.325491792074585451, 1.698604322780517650, -2.638988599164751481 ) ) ;
#30075=ORIENTED_EDGE ( 'NONE', *, *, #36093, .F. ) ;
#30076=VECTOR ( 'NONE', #29244, 39.37007874015748143 ) ;
#30080=CARTESIAN_POINT ( 'NONE',  ( -1.720314620805551087, 0.000000000000000000, 0.2826945007888154726 ) ) ;
#30083=CARTESIAN_POINT ( 'NONE',  ( -1.472219874544909768, 1.546549606962118517, 2.560030851058948898 ) ) ;
#30092=CARTESIAN_POINT ( 'NONE',  ( -0.1516866087075746383, 1.607047215343822222, -2.234383150555500297 ) ) ;
#30093=DIRECTION ( 'NONE',  ( 0.000000000000000000, 0.000000000000000000, 1.000000000000000000 ) ) ;
#30095=CARTESIAN_POINT ( 'NONE',  ( -0.6808484915247774438, 0.01701463086705359146, 1.674057048625058552 ) ) ;
#30097=CARTESIAN_POINT ( 'NONE',  ( 0.1067246931122726866, 0.02962905676920215767, 0.000000000000000000 ) ) ;
#30098=VERTEX_POINT ( 'NONE', #50526 ) ;
#30100=ORIENTED_EDGE ( 'NONE', *, *, #11858, .F. ) ;
#30105=ORIENTED_EDGE ( 'NONE', *, *, #39939, .F. ) ;
#30107=VECTOR ( 'NONE', #25567, 39.37007874015747433 ) ;
#30114=CONICAL_SURFACE ( 'NONE', #16931, 1.850107469027523210, 0.6386652850508578450 ) ;
#30116=CARTESIAN_POINT ( 'NONE',  ( -1.171042467547485311, 1.689145562575557369, 1.864045119995098698 ) ) ;
#30117=ADVANCED_FACE ( 'NONE', ( #4116 ), #8237, .F. ) ;
#30119=CARTESIAN_POINT ( 'NONE',  ( 0.08119777152254364916, 1.623385212329073957, 0.000000000000000000 ) ) ;
#30120=EDGE_CURVE ( 'NONE', #40985, #43780, #13534, .T. ) ;
#30124=FACE_OUTER_BOUND ( 'NONE', #19549, .T. ) ;
#30125=VERTEX_POINT ( 'NONE', #7476 ) ;
#30127=ORIENTED_EDGE ( 'NONE', *, *, #31422, .T. ) ;
#30129=DIRECTION ( 'NONE',  ( -0.9839295885986295565, 0.000000000000000000, -0.1785568947986370392 ) ) ;
#30131=DIRECTION ( 'NONE',  ( 0.000000000000000000, 0.000000000000000000, -1.000000000000000000 ) ) ;
#30134=CARTESIAN_POINT ( 'NONE',  ( -2.339241080213612101, 1.584370211609867685, 1.802537235681884065 ) ) ;
#30142=DIRECTION ( 'NONE',  ( 0.5877852522924802425, 0.000000000000000000, -0.8090169943749422332 ) ) ;
#30144=AXIS2_PLACEMENT_3D ( 'NONE', #16317, #8567, #24320 ) ;
#30147=LINE ( 'NONE', #10776, #9999 ) ;
#30155=EDGE_CURVE ( 'NONE', #45550, #9734, #42584, .T. ) ;
#30156=VERTEX_POINT ( 'NONE', #39733 ) ;
#30164=FACE_OUTER_BOUND ( 'NONE', #47164, .T. ) ;
#30165=VERTEX_POINT ( 'NONE', #23214 ) ;
#30169=CARTESIAN_POINT ( 'NONE',  ( 2.147141360900377105, -3.961648633104548749E-17, 0.3405121111982924997 ) ) ;
#30171=ORIENTED_EDGE ( 'NONE', *, *, #31210, .F. ) ;
#30172=EDGE_CURVE ( 'NONE', #48863, #15175, #8582, .T. ) ;
#30173=PLANE ( 'NONE',  #19811 ) ;
#30174=CARTESIAN_POINT ( 'NONE',  ( 0.000000000000000000, 1.585169487999011917, -2.086614173228346303 ) ) ;
#30185=AXIS2_PLACEMENT_3D ( 'NONE', #48727, #32534, #44120 ) ;
#30189=ORIENTED_EDGE ( 'NONE', *, *, #3290, .F. ) ;
#30192=AXIS2_PLACEMENT_3D ( 'NONE', #12326, #43805, #7685 ) ;
#30194=ORIENTED_EDGE ( 'NONE', *, *, #20034, .F. ) ;
#30205=CARTESIAN_POINT ( 'NONE',  ( 1.022151107061777253, 1.491913292174420480, 2.770242619046225485 ) ) ;
#30206=DIRECTION ( 'NONE',  ( 0.9998717552508121775, 0.01601477604151182663, 0.000000000000000000 ) ) ;
#30208=CARTESIAN_POINT ( 'NONE',  ( -1.487662594350689371, 0.000000000000000000, -0.9622808653958315750 ) ) ;
#30210=DIRECTION ( 'NONE',  ( 0.04486483035050446017, 0.000000000000000000, 0.9989930665413151445 ) ) ;
#30213=CARTESIAN_POINT ( 'NONE',  ( 2.867773316779195447, 1.205361022782829114E-17, -0.7050287376752006896 ) ) ;
#30216=DIRECTION ( 'NONE',  ( -0.000000000000000000, 1.000000000000000000, -0.000000000000000000 ) ) ;
#30218=CIRCLE ( 'NONE', #37679, 1.743387098533651480 ) ;
#30219=VERTEX_POINT ( 'NONE', #40504 ) ;
#30222=CARTESIAN_POINT ( 'NONE',  ( 0.9114270535481910906, 1.729787598242565005, 2.568545968997903994 ) ) ;
#30223=AXIS2_PLACEMENT_3D ( 'NONE', #38585, #50637, #42694 ) ;
#30224=VERTEX_POINT ( 'NONE', #24755 ) ;
#30225=AXIS2_PLACEMENT_3D ( 'NONE', #44001, #43741, #32155 ) ;
#30227=DIRECTION ( 'NONE',  ( 0.000000000000000000, -1.000000000000000000, 0.000000000000000000 ) ) ;
#30228=EDGE_CURVE ( 'NONE', #4915, #16314, #24285, .T. ) ;
#30229=ORIENTED_EDGE ( 'NONE', *, *, #50311, .T. ) ;
#30233=EDGE_CURVE ( 'NONE', #15669, #47219, #42408, .T. ) ;
#30236=ORIENTED_EDGE ( 'NONE', *, *, #40489, .T. ) ;
#30237=CARTESIAN_POINT ( 'NONE',  ( -1.979793062125317693, 1.688404340953838068, 2.191257344206539504 ) ) ;
#30238=ADVANCED_FACE ( 'NONE', ( #43843 ), #20620, .T. ) ;
#30240=VERTEX_POINT ( 'NONE', #9260 ) ;
#30241=ORIENTED_EDGE ( 'NONE', *, *, #40943, .T. ) ;
#30242=CARTESIAN_POINT ( 'NONE',  ( -1.574237088929739459, 0.000000000000000000, 0.7912475138866331692 ) ) ;
#30256=ORIENTED_EDGE ( 'NONE', *, *, #2957, .F. ) ;
#30258=CARTESIAN_POINT ( 'NONE',  ( 0.000000000000000000, 1.574803149606302854, 0.000000000000000000 ) ) ;
#30259=AXIS2_PLACEMENT_3D ( 'NONE', #46226, #10885, #33891 ) ;
#30264=AXIS2_PLACEMENT_3D ( 'NONE', #10372, #26113, #41860 ) ;
#30266=CARTESIAN_POINT ( 'NONE',  ( 2.501748315610153206, 1.656306346848011035, -1.122817972635221428 ) ) ;
#30268=DIRECTION ( 'NONE',  ( 3.986037398843765983E-20, 1.000000000000000000, 1.160734090543304660E-16 ) ) ;
#30270=EDGE_CURVE ( 'NONE', #24599, #23486, #36642, .T. ) ;
#30277=( NAMED_UNIT ( * ) SI_UNIT ( $, .STERADIAN. ) SOLID_ANGLE_UNIT ( ) );
#30280=DIRECTION ( 'NONE',  ( -0.01601477604151182663, 0.9998717552508123996, -0.000000000000000000 ) ) ;
#30281=CARTESIAN_POINT ( 'NONE',  ( -1.679154924913551783, 0.000000000000000000, 0.4938453199301923724 ) ) ;
#30283=AXIS2_PLACEMENT_3D ( 'NONE', #35700, #35196, #43433 ) ;
#30284=ORIENTED_EDGE ( 'NONE', *, *, #48495, .T. ) ;
#30289=EDGE_CURVE ( 'NONE', #4909, #21208, #39702, .T. ) ;
#30290=ORIENTED_EDGE ( 'NONE', *, *, #30294, .F. ) ;
#30291=B_SPLINE_CURVE_WITH_KNOTS ( 'NONE', 3,
 ( #1259, #48456, #13142, #28873 ),
 .UNSPECIFIED., .F., .F.,
 ( 4, 4 ),
 ( 2.331295889524321270E-07, 0.002500721242867300076 ),
 .UNSPECIFIED. ) ;
#30293=FACE_OUTER_BOUND ( 'NONE', #32386, .T. ) ;
#30294=EDGE_CURVE ( 'NONE', #33109, #49287, #35824, .T. ) ;
#30298=ORIENTED_EDGE ( 'NONE', *, *, #10013, .F. ) ;
#30300=DIRECTION ( 'NONE',  ( -1.000000000000000000, 3.986037398843765983E-20, 0.000000000000000000 ) ) ;
#30306=CARTESIAN_POINT ( 'NONE',  ( -1.068075307999487578, 1.574803149606302854, 1.883606783264637485 ) ) ;
#30310=B_SPLINE_CURVE_WITH_KNOTS ( 'NONE', 3,
 ( #5809, #14579, #14064, #22070 ),
 .UNSPECIFIED., .F., .F.,
 ( 4, 4 ),
 ( 0.0001266523219680714730, 0.002626713048324111777 ),
 .UNSPECIFIED. ) ;
#30311=CARTESIAN_POINT ( 'NONE',  ( 0.07982360342473591996, 1.709180471932028711, 0.000000000000000000 ) ) ;
#30319=ORIENTED_EDGE ( 'NONE', *, *, #28274, .F. ) ;
#30320=ORIENTED_EDGE ( 'NONE', *, *, #12605, .F. ) ;
#30323=CARTESIAN_POINT ( 'NONE',  ( 0.000000000000000000, 1.595182601976580683, 2.089297179032357121 ) ) ;
#30326=DIRECTION ( 'NONE',  ( 0.000000000000000000, 0.000000000000000000, 1.000000000000000000 ) ) ;
#30332=CARTESIAN_POINT ( 'NONE',  ( -0.1553040931457698726, 0.000000000000000000, -1.907653760764371986 ) ) ;
#30333=CARTESIAN_POINT ( 'NONE',  ( 1.905671854841463730, 1.650492703781866632, 2.256015092822682089 ) ) ;
#30334=CARTESIAN_POINT ( 'NONE',  ( -1.661821349926434932, 1.574803149606302854, 1.388203579611951843 ) ) ;
#30335=CIRCLE ( 'NONE', #15510, 1.743387098533651480 ) ;
#30337=DIRECTION ( 'NONE',  ( 0.9998717552508121775, 0.01601477604151182663, 0.000000000000000000 ) ) ;
#30342=B_SPLINE_CURVE_WITH_KNOTS ( 'NONE', 3,
 ( #1618, #37255, #5749, #29497 ),
 .UNSPECIFIED., .F., .F.,
 ( 4, 4 ),
 ( 0.0003115223527231955440, 0.04960045202335521680 ),
 .UNSPECIFIED. ) ;
#30345=ADVANCED_FACE ( 'NONE', ( #20363 ), #15220, .T. ) ;
#30348=CARTESIAN_POINT ( 'NONE',  ( 1.602753508900452317, 0.000000000000000000, 1.341098548255033496 ) ) ;
#30349=ORIENTED_EDGE ( 'NONE', *, *, #12069, .T. ) ;
#30358=ADVANCED_FACE ( 'NONE', ( #34289 ), #6149, .T. ) ;
#30360=( BOUNDED_CURVE ( )  B_SPLINE_CURVE ( 3, ( #38591, #49900, #30332, #18958 ),
 .UNSPECIFIED., .F., .F. ) 
 B_SPLINE_CURVE_WITH_KNOTS ( ( 4, 4 ),
 ( 4.494890529461359030, 4.545835423895593586 ),
 .UNSPECIFIED. ) 
 CURVE ( )  GEOMETRIC_REPRESENTATION_ITEM ( )  RATIONAL_B_SPLINE_CURVE ( ( 1.000000000000000000, 0.9997837298384644189, 0.9997837298384644189, 1.000000000000000000 ) ) 
 REPRESENTATION_ITEM ( '' )  );
#30363=B_SPLINE_CURVE_WITH_KNOTS ( 'NONE', 3,
 ( #15986, #39740, #35362, #8500 ),
 .UNSPECIFIED., .F., .F.,
 ( 4, 4 ),
 ( 0.001110332479353618330, 0.04732555827936550663 ),
 .UNSPECIFIED. ) ;
#30367=CARTESIAN_POINT ( 'NONE',  ( -2.441132277248549087, 1.049488665752825067, 0.7414267697872314322 ) ) ;
#30371=DIRECTION ( 'NONE',  ( 0.000000000000000000, 1.000000000000000000, 0.000000000000000000 ) ) ;
#30373=AXIS2_PLACEMENT_3D ( 'NONE', #43659, #36195, #28172 ) ;
#30376=DIRECTION ( 'NONE',  ( -0.9998717552508121775, -0.01601477604151182316, 0.000000000000000000 ) ) ;
#30377=AXIS2_PLACEMENT_3D ( 'NONE', #40484, #5365, #16223 ) ;
#30379=ORIENTED_EDGE ( 'NONE', *, *, #6356, .T. ) ;
#30380=LINE ( 'NONE', #41487, #41390 ) ;
#30381=ORIENTED_EDGE ( 'NONE', *, *, #32170, .F. ) ;
#30382=EDGE_LOOP ( 'NONE', ( #14321, #21987, #42659, #38679 ) ) ;
#30389=CARTESIAN_POINT ( 'NONE',  ( 1.033984067356529257, 1.658846302404568318, -2.033666571521502764 ) ) ;
#30392=DIRECTION ( 'NONE',  ( -0.9998717552508122886, -0.01601477604151185785, 0.000000000000000000 ) ) ;
#30393=DIRECTION ( 'NONE',  ( 0.9009688679024218105, 5.032645177658756258E-17, -0.4338837391175526803 ) ) ;
#30398=AXIS2_PLACEMENT_3D ( 'NONE', #32009, #23226, #50792 ) ;
#30402=AXIS2_PLACEMENT_3D ( 'NONE', #1014, #5143, #45129 ) ;
#30403=VERTEX_POINT ( 'NONE', #6411 ) ;
#30407=ORIENTED_EDGE ( 'NONE', *, *, #36534, .T. ) ;
#30419=DIRECTION ( 'NONE',  ( 0.000000000000000000, -1.000000000000000000, -1.156482317317871478E-16 ) ) ;
#30422=ORIENTED_EDGE ( 'NONE', *, *, #33342, .T. ) ;
#30423=LINE ( 'NONE', #45883, #38878 ) ;
#30425=ORIENTED_EDGE ( 'NONE', *, *, #32335, .T. ) ;
#30435=CARTESIAN_POINT ( 'NONE',  ( 2.298430379965446857, 1.646290322915411997, 0.3610056012771685197 ) ) ;
#30437=EDGE_LOOP ( 'NONE', ( #41565, #20838, #34226, #29911 ) ) ;
#30438=ORIENTED_EDGE ( 'NONE', *, *, #19604, .T. ) ;
#30442=ORIENTED_EDGE ( 'NONE', *, *, #42731, .F. ) ;
#30444=VECTOR ( 'NONE', #23820, 39.37007874015748143 ) ;
#30447=CARTESIAN_POINT ( 'NONE',  ( 0.000000000000000000, 5.905511811023623991, 0.000000000000000000 ) ) ;
#30456=ORIENTED_EDGE ( 'NONE', *, *, #19647, .F. ) ;
#30458=CARTESIAN_POINT ( 'NONE',  ( 1.698878324176545718, 1.702304198788448186, -1.556207456470257267 ) ) ;
#30459=CARTESIAN_POINT ( 'NONE',  ( -1.940243258964476247, 1.049866565877818347, 0.5786780621199733021 ) ) ;
#30460=CARTESIAN_POINT ( 'NONE',  ( -2.623503965249869729, 1.579940539283962053, 1.355882097269835107 ) ) ;
#30462=VERTEX_POINT ( 'NONE', #37403 ) ;
#30463=DIRECTION ( 'NONE',  ( 0.000000000000000000, 0.000000000000000000, 1.000000000000000000 ) ) ;
#30469=CARTESIAN_POINT ( 'NONE',  ( -2.878724150143177507, 5.905511811023623991, -0.6570500018395222241 ) ) ;
#30470=AXIS2_PLACEMENT_3D ( 'NONE', #32418, #6940, #28263 ) ;
#30471=EDGE_CURVE ( 'NONE', #33027, #31047, #26024, .T. ) ;
#30473=ORIENTED_EDGE ( 'NONE', *, *, #30489, .F. ) ;
#30480=B_SPLINE_CURVE_WITH_KNOTS ( 'NONE', 3,
 ( #47635, #16957, #12310, #43782 ),
 .UNSPECIFIED., .F., .F.,
 ( 4, 4 ),
 ( 0.0001946104268145259239, 0.004916092170850017672 ),
 .UNSPECIFIED. ) ;
#30482=ORIENTED_EDGE ( 'NONE', *, *, #5584, .F. ) ;
#30487=CARTESIAN_POINT ( 'NONE',  ( -2.122091976112999490, 1.205361022782829114E-17, 0.4338754535132819390 ) ) ;
#30489=EDGE_CURVE ( 'NONE', #49749, #20873, #44626, .T. ) ;
#30495=DIRECTION ( 'NONE',  ( -0.01601477604151182663, 0.9998717552508123996, -0.000000000000000000 ) ) ;
#30499=ORIENTED_EDGE ( 'NONE', *, *, #47110, .T. ) ;
#30500=EDGE_CURVE ( 'NONE', #39563, #36975, #46439, .T. ) ;
#30503=AXIS2_PLACEMENT_3D ( 'NONE', #42429, #7072, #22818 ) ;
#30505=EDGE_CURVE ( 'NONE', #209, #29472, #34139, .T. ) ;
#30506=ORIENTED_EDGE ( 'NONE', *, *, #22437, .F. ) ;
#30507=CYLINDRICAL_SURFACE ( 'NONE', #42248, 2.165354330708661568 ) ;
#30508=EDGE_CURVE ( 'NONE', #14034, #13750, #13197, .T. ) ;
#30509=ORIENTED_EDGE ( 'NONE', *, *, #22784, .F. ) ;
#30510=ORIENTED_EDGE ( 'NONE', *, *, #35858, .F. ) ;
#30515=CARTESIAN_POINT ( 'NONE',  ( -1.977278193622379332, 1.577807025067274882, -0.8986486843887250275 ) ) ;
#30519=CARTESIAN_POINT ( 'NONE',  ( 1.747029694980739345, 5.905511811023623991, 1.330264415365525421 ) ) ;
#30520=CARTESIAN_POINT ( 'NONE',  ( -0.7331725592709618100, 1.597733653658881758, 2.093588567519426569 ) ) ;
#30522=VERTEX_POINT ( 'NONE', #50470 ) ;
#30524=CARTESIAN_POINT ( 'NONE',  ( -2.889674983507169337, 1.575089141731351505, -0.6090712660038034576 ) ) ;
#30527=CARTESIAN_POINT ( 'NONE',  ( -1.936544984245357481, 1.681005499398536829, 1.481397815340367963 ) ) ;
#30531=EDGE_CURVE ( 'NONE', #12924, #24123, #43340, .T. ) ;
#30536=CARTESIAN_POINT ( 'NONE',  ( 0.002207914879453961969, 5.905511811023623991, 0.04916304461325442243 ) ) ;
#30537=CARTESIAN_POINT ( 'NONE',  ( -1.678197894094463738, 0.0003569711654407151991, 0.4935343617671685834 ) ) ;
#30542=DIRECTION ( 'NONE',  ( -0.9998717552508122886, -0.01601477604151185785, 0.000000000000000000 ) ) ;
#30545=AXIS2_PLACEMENT_3D ( 'NONE', #2768, #4042, #24428 ) ;
#30546=DIRECTION ( 'NONE',  ( -9.390536051998861478E-17, -1.000000000000000000, 6.822623802544654332E-17 ) ) ;
#30550=ORIENTED_EDGE ( 'NONE', *, *, #20051, .F. ) ;
#30553=LINE ( 'NONE', #18173, #38912 ) ;
#30557=CARTESIAN_POINT ( 'NONE',  ( 1.956098637639549720, 1.739232450405700847, -1.232242025355393844 ) ) ;
#30559=CARTESIAN_POINT ( 'NONE',  ( 0.000000000000000000, 1.574803149606302854, 0.000000000000000000 ) ) ;
#30561=ORIENTED_EDGE ( 'NONE', *, *, #20604, .F. ) ;
#30565=DIRECTION ( 'NONE',  ( 0.5128992774059071280, 0.000000000000000000, -0.8584487936018655452 ) ) ;
#30566=EDGE_CURVE ( 'NONE', #46130, #38271, #47063, .T. ) ;
#30572=CARTESIAN_POINT ( 'NONE',  ( -0.8152639642640674422, 0.5238118319854313532, 2.032205794941940535 ) ) ;
#30576=DIRECTION ( 'NONE',  ( -0.01601477604151182663, 0.9998717552508123996, -0.000000000000000000 ) ) ;
#30577=B_SPLINE_CURVE_WITH_KNOTS ( 'NONE', 3,
 ( #26391, #50093, #30527, #3150 ),
 .UNSPECIFIED., .F., .F.,
 ( 4, 4 ),
 ( 2.558111556691897706E-07, 0.01962445202192432056 ),
 .UNSPECIFIED. ) ;
#30581=VERTEX_POINT ( 'NONE', #11542 ) ;
#30585=DIRECTION ( 'NONE',  ( -0.9195277725514489076, 4.565640798866420661E-17, -0.3930250316539278810 ) ) ;
#30586=AXIS2_PLACEMENT_3D ( 'NONE', #41832, #33337, #29447 ) ;
#30588=CIRCLE ( 'NONE', #918, 2.165354330708661568 ) ;
#30590=EDGE_CURVE ( 'NONE', #20664, #47540, #43988, .T. ) ;
#30595=EDGE_CURVE ( 'NONE', #7931, #11610, #40359, .T. ) ;
#30601=DIRECTION ( 'NONE',  ( 0.000000000000000000, 0.000000000000000000, -1.000000000000000000 ) ) ;
#30604=CARTESIAN_POINT ( 'NONE',  ( 0.4435105686220198740, 6.692913385826772199, 2.168331686854578333 ) ) ;
#30606=LINE ( 'NONE', #49920, #39496 ) ;
#30609=DIRECTION ( 'NONE',  ( -0.9998717552508121775, -0.01601477604151182316, 0.000000000000000000 ) ) ;
#30610=DIRECTION ( 'NONE',  ( -8.032339854997460071E-17, 1.000000000000000000, 1.007223559679395367E-16 ) ) ;
#30612=ORIENTED_EDGE ( 'NONE', *, *, #32631, .F. ) ;
#30617=PLANE ( 'NONE',  #11246 ) ;
#30622=ORIENTED_EDGE ( 'NONE', *, *, #8296, .F. ) ;
#30623=ORIENTED_EDGE ( 'NONE', *, *, #38559, .T. ) ;
#30624=DIRECTION ( 'NONE',  ( 0.000000000000000000, 0.000000000000000000, -1.000000000000000000 ) ) ;
#30628=VERTEX_POINT ( 'NONE', #12561 ) ;
#30629=EDGE_CURVE ( 'NONE', #31910, #9471, #2767, .T. ) ;
#30633=ORIENTED_EDGE ( 'NONE', *, *, #11771, .T. ) ;
#30634=ADVANCED_FACE ( 'NONE', ( #12824 ), #689, .F. ) ;
#30639=B_SPLINE_CURVE_WITH_KNOTS ( 'NONE', 3,
 ( #42973, #27998, #23362, #3751 ),
 .UNSPECIFIED., .F., .F.,
 ( 4, 4 ),
 ( 0.01429305550857794260, 0.03074760744400447526 ),
 .UNSPECIFIED. ) ;
#30641=CARTESIAN_POINT ( 'NONE',  ( 0.6235241006192022706, 0.000000000000000000, 2.074304693190358151 ) ) ;
#30644=B_SPLINE_CURVE_WITH_KNOTS ( 'NONE', 3,
 ( #480, #32763, #47681, #21128 ),
 .UNSPECIFIED., .F., .F.,
 ( 4, 4 ),
 ( 2.032841712500688428E-07, 0.01831524776319553433 ),
 .UNSPECIFIED. ) ;
#30646=DIRECTION ( 'NONE',  ( -4.561975526775755056E-17, -1.000000000000000000, 1.067327232801816862E-16 ) ) ;
#30649=LINE ( 'NONE', #8609, #22555 ) ;
#30650=EDGE_CURVE ( 'NONE', #9488, #19294, #30480, .T. ) ;
#30651=CARTESIAN_POINT ( 'NONE',  ( 0.1155636338427008941, -0.5222242541845523167, 0.000000000000000000 ) ) ;
#30653=CARTESIAN_POINT ( 'NONE',  ( -1.690941099774203815, 0.0008361491594236539725, -0.4364244636917575804 ) ) ;
#30660=CARTESIAN_POINT ( 'NONE',  ( -1.742423195192579266, 0.000000000000000000, 0.06108742340491801065 ) ) ;
#30663=CARTESIAN_POINT ( 'NONE',  ( 1.723188456408574210, 6.692913385826772199, 1.311251662046226452 ) ) ;
#30664=EDGE_LOOP ( 'NONE', ( #18448, #22859, #23528, #50877 ) ) ;
#30666=CARTESIAN_POINT ( 'NONE',  ( -0.9602959360900468200, 0.01253876862113688373, 1.511314840084332145 ) ) ;
#30667=VECTOR ( 'NONE', #50345, 39.37007874015748143 ) ;
#30672=FACE_OUTER_BOUND ( 'NONE', #46658, .T. ) ;
#30675=CARTESIAN_POINT ( 'NONE',  ( 2.734482843737263025, 5.905511811023623991, -1.115254632218672048 ) ) ;
#30676=ORIENTED_EDGE ( 'NONE', *, *, #32867, .T. ) ;
#30684=EDGE_LOOP ( 'NONE', ( #1105, #12707, #25813, #37940 ) ) ;
#30685=EDGE_CURVE ( 'NONE', #31188, #47699, #45672, .T. ) ;
#30693=CARTESIAN_POINT ( 'NONE',  ( 1.067222945471691053, 0.5249316475426858419, -1.552631840522197493 ) ) ;
#30697=EDGE_LOOP ( 'NONE', ( #29418, #25054, #15633, #32255, #46010, #13757 ) ) ;
#30699=CONICAL_SURFACE ( 'NONE', #5116, 2.165354330708661568, 0.2617993877991570129 ) ;
#30702=VECTOR ( 'NONE', #22323, 39.37007874015748143 ) ;
#30709=CARTESIAN_POINT ( 'NONE',  ( -1.936750629140493007, 1.578456148182591168, 0.9863243683714766341 ) ) ;
#30710=VERTEX_POINT ( 'NONE', #40700 ) ;
#30716=DIRECTION ( 'NONE',  ( -7.105427357601001859E-15, 0.000000000000000000, 1.000000000000000000 ) ) ;
#30722=LINE ( 'NONE', #14467, #48097 ) ;
#30723=CARTESIAN_POINT ( 'NONE',  ( 0.1067246931122726866, 0.02962905676920215767, 0.000000000000000000 ) ) ;
#30725=EDGE_CURVE ( 'NONE', #38443, #23660, #23064, .T. ) ;
#30728=CIRCLE ( 'NONE', #19980, 2.165354330708661568 ) ;
#30731=AXIS2_PLACEMENT_3D ( 'NONE', #30119, #49437, #21868 ) ;
#30741=CONICAL_SURFACE ( 'NONE', #37361, 1.850107469027523210, 0.6386652850508578450 ) ;
#30742=CARTESIAN_POINT ( 'NONE',  ( 0.04921259842519667277, 1.716250793712470912, 2.716745896894408929 ) ) ;
#30743=ORIENTED_EDGE ( 'NONE', *, *, #3978, .T. ) ;
#30745=PLANE ( 'NONE',  #24354 ) ;
#30746=FACE_OUTER_BOUND ( 'NONE', #21333, .T. ) ;
#30747=CARTESIAN_POINT ( 'NONE',  ( 2.793030215715258446, 2.755905511811027164, 0.9592557174602682757 ) ) ;
#30749=EDGE_LOOP ( 'NONE', ( #34161, #31561, #28162, #34882 ) ) ;
#30751=CARTESIAN_POINT ( 'NONE',  ( -2.623503965249869729, 1.579940539283962053, 1.355882097269835107 ) ) ;
#30758=B_SPLINE_CURVE_WITH_KNOTS ( 'NONE', 3,
 ( #13580, #29317, #29579, #45046 ),
 .UNSPECIFIED., .F., .F.,
 ( 4, 4 ),
 ( 0.0007776637210865601979, 0.04825954388179014287 ),
 .UNSPECIFIED. ) ;
#30761=DIRECTION ( 'NONE',  ( -3.986037398843765983E-20, -1.000000000000000000, -1.160734090543304660E-16 ) ) ;
#30762=FACE_OUTER_BOUND ( 'NONE', #40371, .T. ) ;
#30764=ORIENTED_EDGE ( 'NONE', *, *, #12507, .F. ) ;
#30774=EDGE_CURVE ( 'NONE', #35146, #9349, #25826, .T. ) ;
#30775=FACE_OUTER_BOUND ( 'NONE', #22924, .T. ) ;
#30776=CARTESIAN_POINT ( 'NONE',  ( 1.500384305836228060, 1.644172902614663867, 2.543203386723825066 ) ) ;
#30778=EDGE_LOOP ( 'NONE', ( #5888, #31267, #940, #27208, #11926, #19291, #11451, #27321, #10123, #24729, #13486, #14677, #21009 ) ) ;
#30786=LINE ( 'NONE', #31039, #49347 ) ;
#30788=EDGE_CURVE ( 'NONE', #42563, #28312, #19927, .T. ) ;
#30791=ORIENTED_EDGE ( 'NONE', *, *, #47626, .F. ) ;
#30800=ORIENTED_EDGE ( 'NONE', *, *, #50002, .F. ) ;
#30804=LINE ( 'NONE', #11937, #49588 ) ;
#30806=ORIENTED_EDGE ( 'NONE', *, *, #34267, .T. ) ;
#30807=AXIS2_PLACEMENT_3D ( 'NONE', #35235, #50414, #10977 ) ;
#30810=AXIS2_PLACEMENT_3D ( 'NONE', #27490, #26734, #15121 ) ;
#30812=VECTOR ( 'NONE', #17890, 39.37007874015748143 ) ;
#30814=ORIENTED_EDGE ( 'NONE', *, *, #7152, .T. ) ;
#30815=CARTESIAN_POINT ( 'NONE',  ( 2.540858811888025759, 1.656921574833092992, -1.032495749324521706 ) ) ;
#30817=FACE_OUTER_BOUND ( 'NONE', #38545, .T. ) ;
#30818=ADVANCED_FACE ( 'NONE', ( #10477 ), #36677, .T. ) ;
#30821=CARTESIAN_POINT ( 'NONE',  ( -2.721588301569279444, 1.676830576168054865, -1.145422913327642567 ) ) ;
#30824=ORIENTED_EDGE ( 'NONE', *, *, #8915, .F. ) ;
#30826=CARTESIAN_POINT ( 'NONE',  ( 2.951990591674675368, 1.666783180044518087, -0.08331184815398359755 ) ) ;
#30828=ORIENTED_EDGE ( 'NONE', *, *, #6348, .T. ) ;
#30829=B_SPLINE_CURVE_WITH_KNOTS ( 'NONE', 3,
 ( #22820, #15070, #30821, #12721 ),
 .UNSPECIFIED., .F., .F.,
 ( 4, 4 ),
 ( 2.175073774845426906E-07, 0.002500264446635720034 ),
 .UNSPECIFIED. ) ;
#30830=FACE_OUTER_BOUND ( 'NONE', #49333, .T. ) ;
#30832=CARTESIAN_POINT ( 'NONE',  ( 0.08139965876239094178, 1.610780518492231694, 0.000000000000000000 ) ) ;
#30833=CARTESIAN_POINT ( 'NONE',  ( 2.695799277629594037, 1.205361022782829114E-17, -1.205759334241453651 ) ) ;
#30835=ORIENTED_EDGE ( 'NONE', *, *, #19244, .T. ) ;
#30836=ORIENTED_EDGE ( 'NONE', *, *, #9433, .F. ) ;
#30838=DIRECTION ( 'NONE',  ( 0.04486483035050446017, -1.160734090543304660E-16, 0.9989930665413151445 ) ) ;
#30839=EDGE_CURVE ( 'NONE', #13030, #16254, #29143, .T. ) ;
#30847=CARTESIAN_POINT ( 'NONE',  ( -2.152441353505195387, 6.692913385826772199, -0.2419059403265105823 ) ) ;
#30851=ORIENTED_EDGE ( 'NONE', *, *, #13629, .F. ) ;
#30853=EDGE_CURVE ( 'NONE', #33984, #17233, #35933, .T. ) ;
#30855=CARTESIAN_POINT ( 'NONE',  ( -1.597750071202345135, 0.000000000000000000, -0.7364305798568749895 ) ) ;
#30862=ORIENTED_EDGE ( 'NONE', *, *, #13774, .T. ) ;
#30865=DIRECTION ( 'NONE',  ( 0.6579387259397027066, 0.000000000000000000, 0.7530714660036195163 ) ) ;
#30870=ORIENTED_EDGE ( 'NONE', *, *, #19717, .F. ) ;
#30871=CARTESIAN_POINT ( 'NONE',  ( 1.905671854841463730, 1.650492703781866632, 2.256015092822682089 ) ) ;
#30873=CARTESIAN_POINT ( 'NONE',  ( 0.04921259842519613847, 5.905511811023623991, 2.213282802432569252 ) ) ;
#30880=CARTESIAN_POINT ( 'NONE',  ( 2.949046667275482481, 1.446726060616999154, -0.1488634180638622739 ) ) ;
#30881=LINE ( 'NONE', #38378, #8471 ) ;
#30883=PLANE ( 'NONE',  #21561 ) ;
#30886=EDGE_CURVE ( 'NONE', #14806, #23260, #277, .T. ) ;
#30887=PLANE ( 'NONE',  #34824 ) ;
#30888=AXIS2_PLACEMENT_3D ( 'NONE', #15671, #3804, #19535 ) ;
#30895=PLANE ( 'NONE',  #47483 ) ;
#30897=CARTESIAN_POINT ( 'NONE',  ( 0.4517796511351843680, 1.715138028758778521, 2.213898087213642007 ) ) ;
#30900=CARTESIAN_POINT ( 'NONE',  ( 2.321319991045708075, 1.679465340878977919, -0.1535128031905659829 ) ) ;
#30905=CARTESIAN_POINT ( 'NONE',  ( 0.1067246931122726866, 0.02962905676920215767, 0.000000000000000000 ) ) ;
#30906=CARTESIAN_POINT ( 'NONE',  ( -2.793030215715272213, 1.577298709702483093, 0.9592557174602283077 ) ) ;
#30908=ORIENTED_EDGE ( 'NONE', *, *, #44155, .T. ) ;
#30909=CARTESIAN_POINT ( 'NONE',  ( -0.7380211471543357549, 0.01609890615456165824, -1.645940171248041928 ) ) ;
#30910=EDGE_CURVE ( 'NONE', #28307, #49731, #20062, .T. ) ;
#30914=CARTESIAN_POINT ( 'NONE',  ( 1.900276455977023549, 1.738338356005314722, -1.313328886422038710 ) ) ;
#30917=EDGE_CURVE ( 'NONE', #20275, #4372, #11015, .T. ) ;
#30918=AXIS2_PLACEMENT_3D ( 'NONE', #35916, #546, #16293 ) ;
#30920=ORIENTED_EDGE ( 'NONE', *, *, #26822, .F. ) ;
#30923=CARTESIAN_POINT ( 'NONE',  ( 0.08119777152254364916, 1.623385212329073957, 0.000000000000000000 ) ) ;
#30925=CARTESIAN_POINT ( 'NONE',  ( 0.04921259842519603439, 6.692913385826772199, 2.213282802432569252 ) ) ;
#30927=EDGE_LOOP ( 'NONE', ( #9938, #17166, #1866, #13470, #47468, #50138, #40650, #40064, #45126, #9533, #44275, #36478, #11977 ) ) ;
#30932=VERTEX_POINT ( 'NONE', #23345 ) ;
#30933=CARTESIAN_POINT ( 'NONE',  ( 1.698224779224786429, 1.735102128624146811, -1.555582603516539875 ) ) ;
#30936=ORIENTED_EDGE ( 'NONE', *, *, #35774, .F. ) ;
#30937=LINE ( 'NONE', #7191, #24805 ) ;
#30938=EDGE_CURVE ( 'NONE', #11395, #33586, #26718, .T. ) ;
#30941=VERTEX_POINT ( 'NONE', #46317 ) ;
#30946=EDGE_CURVE ( 'NONE', #20050, #50754, #42957, .T. ) ;
#30950=CARTESIAN_POINT ( 'NONE',  ( -0.5110594979943671179, 0.000000000000000000, -1.666798357583582524 ) ) ;
#30951=FACE_OUTER_BOUND ( 'NONE', #45085, .T. ) ;
#30960=ORIENTED_EDGE ( 'NONE', *, *, #2924, .F. ) ;
#30964=DIRECTION ( 'NONE',  ( 0.000000000000000000, 0.000000000000000000, 1.000000000000000000 ) ) ;
#30965=CARTESIAN_POINT ( 'NONE',  ( -2.141381699469527167, 0.5249902829290868933, -0.1454317651979360748 ) ) ;
#30968=CARTESIAN_POINT ( 'NONE',  ( 0.9218113296639885990, 0.000000000000000000, -1.800737481590852118 ) ) ;
#30977=ORIENTED_EDGE ( 'NONE', *, *, #4004, .F. ) ;
#30987=ORIENTED_EDGE ( 'NONE', *, *, #1344, .F. ) ;
#30997=EDGE_CURVE ( 'NONE', #16032, #19475, #41495, .T. ) ;
#30998=CARTESIAN_POINT ( 'NONE',  ( -2.014631844979636988, 1.610017137301174017, -0.8075755495219558711 ) ) ;
#31002=DIRECTION ( 'NONE',  ( 0.000000000000000000, -1.000000000000000000, -0.000000000000000000 ) ) ;
#31003=DIRECTION ( 'NONE',  ( 0.000000000000000000, 0.000000000000000000, 1.000000000000000000 ) ) ;
#31005=CARTESIAN_POINT ( 'NONE',  ( 0.1067246931122726866, 0.02962905676920215767, 0.000000000000000000 ) ) ;
#31013=CIRCLE ( 'NONE', #29360, 2.165354330708661568 ) ;
#31016=ORIENTED_EDGE ( 'NONE', *, *, #19408, .F. ) ;
#31021=FACE_OUTER_BOUND ( 'NONE', #42143, .T. ) ;
#31025=AXIS2_PLACEMENT_3D ( 'NONE', #28190, #4196, #16329 ) ;
#31029=CARTESIAN_POINT ( 'NONE',  ( -2.950847925457031007, 1.574821451496988933, -0.08326053095501942392 ) ) ;
#31030=CONICAL_SURFACE ( 'NONE', #22781, 3.033577403570480779, 1.554780866114618743 ) ;
#31038=CARTESIAN_POINT ( 'NONE',  ( -1.677240863121680414, 0.0007139418753273822464, 0.4932234035542065742 ) ) ;
#31039=CARTESIAN_POINT ( 'NONE',  ( 0.3381173457103284763, 6.692913385826772199, 2.138793126519850318 ) ) ;
#31040=EDGE_CURVE ( 'NONE', #36016, #27696, #18010, .T. ) ;
#31047=VERTEX_POINT ( 'NONE', #47570 ) ;
#31048=LINE ( 'NONE', #10922, #7037 ) ;
#31049=PLANE ( 'NONE',  #33007 ) ;
#31052=AXIS2_PLACEMENT_3D ( 'NONE', #29838, #9712, #45805 ) ;
#31054=ORIENTED_EDGE ( 'NONE', *, *, #33150, .T. ) ;
#31060=ORIENTED_EDGE ( 'NONE', *, *, #50311, .F. ) ;
#31068=DIRECTION ( 'NONE',  ( -1.206139481778036182E-16, 1.000000000000000000, -4.526717189434842013E-17 ) ) ;
#31071=EDGE_CURVE ( 'NONE', #25341, #17674, #44493, .T. ) ;
#31073=VERTEX_POINT ( 'NONE', #8374 ) ;
#31074=DIRECTION ( 'NONE',  ( -0.01601477604151182663, 0.9998717552508123996, -0.000000000000000000 ) ) ;
#31076=AXIS2_PLACEMENT_3D ( 'NONE', #45767, #10432, #26177 ) ;
#31083=EDGE_CURVE ( 'NONE', #2673, #23176, #37134, .T. ) ;
#31085=DIRECTION ( 'NONE',  ( -0.01601477604151182663, 0.9998717552508123996, -0.000000000000000000 ) ) ;
#31086=DIRECTION ( 'NONE',  ( 0.01601477604151182663, -0.9998717552508123996, 0.000000000000000000 ) ) ;
#31089=EDGE_CURVE ( 'NONE', #13729, #23291, #23581, .T. ) ;
#31094=AXIS2_PLACEMENT_3D ( 'NONE', #44993, #25137, #21264 ) ;
#31097=CARTESIAN_POINT ( 'NONE',  ( 1.743145509346915256, 0.000000000000000000, -0.02902255290747513330 ) ) ;
#31099=ORIENTED_EDGE ( 'NONE', *, *, #28361, .F. ) ;
#31105=CARTESIAN_POINT ( 'NONE',  ( 1.929629134066521701, 6.692913385826772199, 0.9824921284572420976 ) ) ;
#31106=( BOUNDED_CURVE ( )  B_SPLINE_CURVE ( 3, ( #5824, #33967, #17954, #48889 ),
 .UNSPECIFIED., .F., .F. ) 
 B_SPLINE_CURVE_WITH_KNOTS ( ( 4, 4 ),
 ( 2.833434655505596034, 2.884195265334674740 ),
 .UNSPECIFIED. ) 
 CURVE ( )  GEOMETRIC_REPRESENTATION_ITEM ( )  RATIONAL_B_SPLINE_CURVE ( ( 1.000000000000000000, 0.9997852915667326812, 0.9997852915667326812, 1.000000000000000000 ) ) 
 REPRESENTATION_ITEM ( '' )  );
#31107=LINE ( 'NONE', #46811, #32072 ) ;
#31108=CARTESIAN_POINT ( 'NONE',  ( 0.08119777152254364916, 1.623385212329073957, 0.000000000000000000 ) ) ;
#31109=DIRECTION ( 'NONE',  ( -0.000000000000000000, 1.000000000000000000, -0.000000000000000000 ) ) ;
#31117=B_SPLINE_CURVE_WITH_KNOTS ( 'NONE', 3,
 ( #9173, #44529, #24924, #28271 ),
 .UNSPECIFIED., .F., .F.,
 ( 4, 4 ),
 ( 0.01076910417452579295, 0.03073582141358097153 ),
 .UNSPECIFIED. ) ;
#31120=VERTEX_POINT ( 'NONE', #626 ) ;
#31123=CARTESIAN_POINT ( 'NONE',  ( 0.1067246931122726866, 0.02962905676920215767, 0.000000000000000000 ) ) ;
#31126=DIRECTION ( 'NONE',  ( 0.000000000000000000, 0.000000000000000000, 1.000000000000000000 ) ) ;
#31128=EDGE_LOOP ( 'NONE', ( #18354, #22819, #39486, #14118 ) ) ;
#31132=VECTOR ( 'NONE', #42093, 39.37007874015748143 ) ;
#31133=EDGE_CURVE ( 'NONE', #24903, #50014, #20501, .T. ) ;
#31138=ORIENTED_EDGE ( 'NONE', *, *, #21799, .F. ) ;
#31139=EDGE_CURVE ( 'NONE', #39972, #40324, #25141, .T. ) ;
#31140=EDGE_CURVE ( 'NONE', #20851, #20050, #166, .T. ) ;
#31146=AXIS2_PLACEMENT_3D ( 'NONE', #14900, #42761, #46360 ) ;
#31147=CARTESIAN_POINT ( 'NONE',  ( -2.823445274216743073, 1.576824725690453954, 0.8656477926280276014 ) ) ;
#31149=CARTESIAN_POINT ( 'NONE',  ( 2.274988110810610031, 1.744340048923221920, -0.4687729985174870495 ) ) ;
#31152=DIRECTION ( 'NONE',  ( 0.000000000000000000, 0.000000000000000000, 1.000000000000000000 ) ) ;
#31156=CARTESIAN_POINT ( 'NONE',  ( -1.936703619043268043, 1.611265300635113862, 0.9862990711594324944 ) ) ;
#31160=ORIENTED_EDGE ( 'NONE', *, *, #34008, .F. ) ;
#31163=ORIENTED_EDGE ( 'NONE', *, *, #40780, .F. ) ;
#31164=LINE ( 'NONE', #50976, #32037 ) ;
#31165=AXIS2_PLACEMENT_3D ( 'NONE', #112, #27732, #23869 ) ;
#31166=CONICAL_SURFACE ( 'NONE', #37774, 3.033577403570480779, 1.554780866114618743 ) ;
#31167=EDGE_CURVE ( 'NONE', #8328, #24653, #18604, .T. ) ;
#31170=EDGE_CURVE ( 'NONE', #48162, #24696, #5760, .T. ) ;
#31179=ORIENTED_EDGE ( 'NONE', *, *, #9433, .T. ) ;
#31180=VECTOR ( 'NONE', #22697, 39.37007874015748143 ) ;
#31181=EDGE_LOOP ( 'NONE', ( #36941, #32655, #12720, #24470 ) ) ;
#31183=DIRECTION ( 'NONE',  ( 1.000000000000000000, 0.000000000000000000, 0.000000000000000000 ) ) ;
#31185=FACE_OUTER_BOUND ( 'NONE', #7549, .T. ) ;
#31186=CONICAL_SURFACE ( 'NONE', #39436, 1.850107469027523210, 0.6386652850508578450 ) ;
#31188=VERTEX_POINT ( 'NONE', #13523 ) ;
#31190=ORIENTED_EDGE ( 'NONE', *, *, #30508, .T. ) ;
#31194=FACE_OUTER_BOUND ( 'NONE', #22645, .T. ) ;
#31198=AXIS2_PLACEMENT_3D ( 'NONE', #43408, #23801, #39549 ) ;
#31200=VERTEX_POINT ( 'NONE', #38233 ) ;
#31201=ORIENTED_EDGE ( 'NONE', *, *, #47084, .F. ) ;
#31205=ORIENTED_EDGE ( 'NONE', *, *, #28530, .F. ) ;
#31210=EDGE_CURVE ( 'NONE', #50014, #20106, #50530, .T. ) ;
#31213=B_SPLINE_CURVE_WITH_KNOTS ( 'NONE', 3,
 ( #17006, #32766, #32243, #16750 ),
 .UNSPECIFIED., .F., .F.,
 ( 4, 4 ),
 ( 5.967759774831694495E-07, 2.699383640232303923E-05 ),
 .UNSPECIFIED. ) ;
#31214=CARTESIAN_POINT ( 'NONE',  ( 0.7506868623604561197, 1.205361022782829114E-17, 1.860140722251951484 ) ) ;
#31215=AXIS2_PLACEMENT_3D ( 'NONE', #29368, #49702, #30131 ) ;
#31219=CARTESIAN_POINT ( 'NONE',  ( 2.168245791271197209, 0.000000000000000000, -2.004968704497248400 ) ) ;
#31220=DIRECTION ( 'NONE',  ( -0.01601477604151182663, 0.9998717552508123996, -0.000000000000000000 ) ) ;
#31221=EDGE_CURVE ( 'NONE', #14810, #21120, #14980, .T. ) ;
#31223=DIRECTION ( 'NONE',  ( 0.1342332658176522420, 1.288287287306305530E-16, 0.9909497617679352555 ) ) ;
#31226=AXIS2_PLACEMENT_3D ( 'NONE', #51024, #19078, #15469 ) ;
#31228=ORIENTED_EDGE ( 'NONE', *, *, #6864, .F. ) ;
#31229=B_SPLINE_CURVE_WITH_KNOTS ( 'NONE', 3,
 ( #10173, #2176, #40914, #32928 ),
 .UNSPECIFIED., .F., .F.,
 ( 4, 4 ),
 ( 0.1211873102087489551, 0.1625992483279400380 ),
 .UNSPECIFIED. ) ;
#31230=CARTESIAN_POINT ( 'NONE',  ( -2.134236802639925212, 0.000000000000000000, -2.040539317874611847 ) ) ;
#31242=LINE ( 'NONE', #47701, #32889 ) ;
#31244=CARTESIAN_POINT ( 'NONE',  ( -0.9147270545203428638, 1.660442526372950311, -2.012873768794291252 ) ) ;
#31247=AXIS2_PLACEMENT_3D ( 'NONE', #25621, #37765, #25367 ) ;
#31251=ORIENTED_EDGE ( 'NONE', *, *, #38399, .T. ) ;
#31257=LINE ( 'NONE', #7503, #34287 ) ;
#31259=ORIENTED_EDGE ( 'NONE', *, *, #20034, .T. ) ;
#31261=DIRECTION ( 'NONE',  ( -0.000000000000000000, 1.000000000000000000, 0.000000000000000000 ) ) ;
#31262=EDGE_LOOP ( 'NONE', ( #10791, #29165, #49763, #26170, #46052, #1034, #38312, #14562, #9505, #33432, #2372, #44822, #12539 ) ) ;
#31263=DIRECTION ( 'NONE',  ( -0.01601477604151182663, 0.9998717552508123996, -0.000000000000000000 ) ) ;
#31264=EDGE_CURVE ( 'NONE', #49792, #20204, #11357, .T. ) ;
#31265=EDGE_CURVE ( 'NONE', #16316, #14514, #30363, .T. ) ;
#31267=ORIENTED_EDGE ( 'NONE', *, *, #27531, .F. ) ;
#31268=ADVANCED_FACE ( 'NONE', ( #24251 ), #27508, .T. ) ;
#31270=CARTESIAN_POINT ( 'NONE',  ( -0.5905738936209794510, 0.01846054376545745376, 1.713635781666723146 ) ) ;
#31273=CARTESIAN_POINT ( 'NONE',  ( 0.000000000000000000, 10.31496062992126284, 0.000000000000000000 ) ) ;
#31276=EDGE_LOOP ( 'NONE', ( #3895, #43622, #35813, #46286, #21772, #22986, #40330, #45377, #22082, #36270, #23005 ) ) ;
#31277=CARTESIAN_POINT ( 'NONE',  ( -1.105178190331685961, 1.205361022782829114E-17, -1.437421806808603542 ) ) ;
#31279=ORIENTED_EDGE ( 'NONE', *, *, #30120, .F. ) ;
#31281=CARTESIAN_POINT ( 'NONE',  ( 0.08139965876239094178, 1.610780518492231694, 0.000000000000000000 ) ) ;
#31283=ADVANCED_FACE ( 'NONE', ( #47183 ), #8244, .F. ) ;
#31290=EDGE_CURVE ( 'NONE', #1678, #44472, #15229, .T. ) ;
#31297=CARTESIAN_POINT ( 'NONE',  ( 1.695772546416037363, 1.745688802946234297, -2.417756147381349141 ) ) ;
#31298=ORIENTED_EDGE ( 'NONE', *, *, #14401, .T. ) ;
#31300=FACE_OUTER_BOUND ( 'NONE', #29425, .T. ) ;
#31302=FACE_OUTER_BOUND ( 'NONE', #16630, .T. ) ;
#31307=VECTOR ( 'NONE', #29416, 39.37007874015748143 ) ;
#31309=ORIENTED_EDGE ( 'NONE', *, *, #39092, .T. ) ;
#31316=CARTESIAN_POINT ( 'NONE',  ( 1.956903606557731878, 1.706436945410369166, -1.232773380686051690 ) ) ;
#31318=AXIS2_PLACEMENT_3D ( 'NONE', #22209, #44655, #25052 ) ;
#31321=CARTESIAN_POINT ( 'NONE',  ( 0.8338860768354398045, 1.049866565067838264, -1.845005748911692667 ) ) ;
#31325=CARTESIAN_POINT ( 'NONE',  ( -1.780101451746625152, 0.000000000000000000, 1.234002060668493828 ) ) ;
#31329=DIRECTION ( 'NONE',  ( -0.01601477604151182663, 0.9998717552508123996, -0.000000000000000000 ) ) ;
#31335=ADVANCED_FACE ( 'NONE', ( #51041 ), #50785, .T. ) ;
#31338=EDGE_CURVE ( 'NONE', #15353, #35113, #35103, .T. ) ;
#31339=CARTESIAN_POINT ( 'NONE',  ( -0.2783729501556720387, 0.02346101323895649626, 1.809574371873096110 ) ) ;
#31342=ORIENTED_EDGE ( 'NONE', *, *, #17996, .T. ) ;
#31346=CARTESIAN_POINT ( 'NONE',  ( -1.723188456408593527, 6.692913385826772199, 1.311251662046200472 ) ) ;
#31353=CARTESIAN_POINT ( 'NONE',  ( 1.735113842587030497, 0.05571068913886997875, 0.8778189866238004235 ) ) ;
#31354=VECTOR ( 'NONE', #12870, 39.37007874015748143 ) ;
#31359=CARTESIAN_POINT ( 'NONE',  ( 2.878724150143186833, 0.000000000000000000, -0.6570500018394808128 ) ) ;
#31361=ORIENTED_EDGE ( 'NONE', *, *, #46049, .F. ) ;
#31371=DIRECTION ( 'NONE',  ( 0.01601477604151182663, -0.9998717552508123996, 0.000000000000000000 ) ) ;
#31373=VERTEX_POINT ( 'NONE', #1004 ) ;
#31374=ORIENTED_EDGE ( 'NONE', *, *, #10975, .T. ) ;
#31383=B_SPLINE_CURVE_WITH_KNOTS ( 'NONE', 3,
 ( #16516, #17286, #33043, #48725 ),
 .UNSPECIFIED., .F., .F.,
 ( 4, 4 ),
 ( 0.0002445083414965676209, 0.0004292220583399663668 ),
 .UNSPECIFIED. ) ;
#31384=ORIENTED_EDGE ( 'NONE', *, *, #26444, .T. ) ;
#31388=CARTESIAN_POINT ( 'NONE',  ( 2.345377178086121450, 1.748857782376721071, -0.9489428892520402892 ) ) ;
#31394=CONICAL_SURFACE ( 'NONE', #1692, 3.483074324928249421, 1.244861948955335196 ) ;
#31395=ORIENTED_EDGE ( 'NONE', *, *, #9491, .F. ) ;
#31397=FACE_OUTER_BOUND ( 'NONE', #6947, .T. ) ;
#31398=EDGE_CURVE ( 'NONE', #40626, #11395, #35296, .T. ) ;
#31399=ORIENTED_EDGE ( 'NONE', *, *, #25080, .T. ) ;
#31401=CARTESIAN_POINT ( 'NONE',  ( -1.876501151069718265, 1.583532498426239998, 1.559405008154286953 ) ) ;
#31403=( BOUNDED_CURVE ( )  B_SPLINE_CURVE ( 3, ( #10593, #30208, #10337, #44919 ),
 .UNSPECIFIED., .F., .F. ) 
 B_SPLINE_CURVE_WITH_KNOTS ( ( 4, 4 ),
 ( 3.643597954878999623, 3.694401143243455810 ),
 .UNSPECIFIED. ) 
 CURVE ( )  GEOMETRIC_REPRESENTATION_ITEM ( )  RATIONAL_B_SPLINE_CURVE ( ( 1.000000000000000000, 0.9997849312356386076, 0.9997849312356386076, 1.000000000000000000 ) ) 
 REPRESENTATION_ITEM ( '' )  );
#31406=CARTESIAN_POINT ( 'NONE',  ( 1.613190494119344232, 1.049866565067837820, 1.223531214289272695 ) ) ;
#31411=ORIENTED_EDGE ( 'NONE', *, *, #22776, .T. ) ;
#31413=CARTESIAN_POINT ( 'NONE',  ( -0.7582255214199161708, 0.000000000000000000, -1.687894986714875811 ) ) ;
#31418=FACE_OUTER_BOUND ( 'NONE', #49407, .T. ) ;
#31419=CARTESIAN_POINT ( 'NONE',  ( 1.905671854841464175, 0.000000000000000000, 2.256015092822681645 ) ) ;
#31422=EDGE_CURVE ( 'NONE', #16438, #27482, #16806, .T. ) ;
#31426=ADVANCED_FACE ( 'NONE', ( #48213 ), #20625, .T. ) ;
#31428=LINE ( 'NONE', #19537, #17738 ) ;
#31431=VERTEX_POINT ( 'NONE', #25520 ) ;
#31432=ORIENTED_EDGE ( 'NONE', *, *, #29471, .F. ) ;
#31433=CARTESIAN_POINT ( 'NONE',  ( 1.255350140850374441, 0.03167824151409264627, 1.511661998497999537 ) ) ;
#31437=AXIS2_PLACEMENT_3D ( 'NONE', #8647, #43742, #24142 ) ;
#31442=CONICAL_SURFACE ( 'NONE', #39695, 1.850107469027523210, 0.6386652850508578450 ) ;
#31445=B_SPLINE_CURVE_WITH_KNOTS ( 'NONE', 3,
 ( #49911, #26462, #42713, #30348 ),
 .UNSPECIFIED., .F., .F.,
 ( 4, 4 ),
 ( 0.0006330831653206172183, 0.004889894717019593537 ),
 .UNSPECIFIED. ) ;
#31446=DIRECTION ( 'NONE',  ( 0.000000000000000000, -1.000000000000000000, -0.000000000000000000 ) ) ;
#31448=ORIENTED_EDGE ( 'NONE', *, *, #36957, .T. ) ;
#31451=EDGE_CURVE ( 'NONE', #48631, #24742, #10300, .T. ) ;
#31455=ADVANCED_FACE ( 'NONE', ( #21399 ), #15142, .T. ) ;
#31457=CARTESIAN_POINT ( 'NONE',  ( -1.843346842069858216, 1.645568979423359446, -1.157815216737156483 ) ) ;
#31460=ORIENTED_EDGE ( 'NONE', *, *, #17885, .F. ) ;
#31464=CONICAL_SURFACE ( 'NONE', #1797, 3.483074324928249421, 1.244861948955335196 ) ;
#31469=CARTESIAN_POINT ( 'NONE',  ( 1.068075307999460488, 1.574803149606302854, 1.883606783264653028 ) ) ;
#31477=ORIENTED_EDGE ( 'NONE', *, *, #43547, .T. ) ;
#31480=VERTEX_POINT ( 'NONE', #30666 ) ;
#31488=EDGE_CURVE ( 'NONE', #45769, #40209, #27864, .T. ) ;
#31490=ORIENTED_EDGE ( 'NONE', *, *, #6210, .F. ) ;
#31491=CARTESIAN_POINT ( 'NONE',  ( 2.327376634978634673, 0.9888095434482767621, 1.196529185699396036 ) ) ;
#31495=CIRCLE ( 'NONE', #34781, 2.246510896728926010 ) ;
#31497=CONICAL_SURFACE ( 'NONE', #9247, 3.033577403570480779, 1.554780866114618743 ) ;
#31498=CARTESIAN_POINT ( 'NONE',  ( 0.1250607540065018508, 1.205361022782829114E-17, -1.938545675207280272 ) ) ;
#31499=VERTEX_POINT ( 'NONE', #2792 ) ;
#31500=ORIENTED_EDGE ( 'NONE', *, *, #15716, .F. ) ;
#31501=CARTESIAN_POINT ( 'NONE',  ( 1.526813663045976766, 0.5226730630971984093, 1.672780703928434143 ) ) ;
#31509=CARTESIAN_POINT ( 'NONE',  ( 0.07982360342473591996, 1.709180471932028711, 0.000000000000000000 ) ) ;
#31510=CARTESIAN_POINT ( 'NONE',  ( 0.000000000000000000, 0.000000000000000000, 0.000000000000000000 ) ) ;
#31511=VERTEX_POINT ( 'NONE', #37409 ) ;
#31515=B_SPLINE_CURVE_WITH_KNOTS ( 'NONE', 3,
 ( #413, #44535, #8931, #24166 ),
 .UNSPECIFIED., .F., .F.,
 ( 4, 4 ),
 ( 0.001649814413565570993, 0.04583418734355550889 ),
 .UNSPECIFIED. ) ;
#31520=VERTEX_POINT ( 'NONE', #18033 ) ;
#31521=CARTESIAN_POINT ( 'NONE',  ( -2.142805232260985182, 6.692913385826772199, 0.3399247426648309700 ) ) ;
#31531=LINE ( 'NONE', #14589, #872 ) ;
#31536=CARTESIAN_POINT ( 'NONE',  ( 1.083598637574782142, 1.491270273546293046, 2.747180975113346246 ) ) ;
#31537=ORIENTED_EDGE ( 'NONE', *, *, #4126, .T. ) ;
#31541=ORIENTED_EDGE ( 'NONE', *, *, #9700, .T. ) ;
#31545=DIRECTION ( 'NONE',  ( 0.000000000000000000, 0.000000000000000000, 1.000000000000000000 ) ) ;
#31547=CARTESIAN_POINT ( 'NONE',  ( 1.738729679588007171, 0.000000000000000000, -0.1273486421339826147 ) ) ;
#31552=FACE_OUTER_BOUND ( 'NONE', #36569, .T. ) ;
#31555=EDGE_CURVE ( 'NONE', #27703, #49324, #26030, .T. ) ;
#31557=DIRECTION ( 'NONE',  ( -0.9998717552508121775, -0.01601477604151182663, 0.000000000000000000 ) ) ;
#31561=ORIENTED_EDGE ( 'NONE', *, *, #16826, .T. ) ;
#31562=ORIENTED_EDGE ( 'NONE', *, *, #184, .T. ) ;
#31568=CYLINDRICAL_SURFACE ( 'NONE', #12900, 2.165354330708661568 ) ;
#31572=EDGE_CURVE ( 'NONE', #24144, #25794, #48685, .T. ) ;
#31574=CARTESIAN_POINT ( 'NONE',  ( 0.3958187006869922642, 1.717958654416033681, 2.456753799658804915 ) ) ;
#31576=ORIENTED_EDGE ( 'NONE', *, *, #12384, .F. ) ;
#31577=DIRECTION ( 'NONE',  ( 0.5508969814520945363, -1.160734090543304660E-16, 0.8345732537213079727 ) ) ;
#31578=VECTOR ( 'NONE', #29802, 39.37007874015748143 ) ;
#31589=CARTESIAN_POINT ( 'NONE',  ( -0.4460728916448887249, 1.700757277111965449, 2.182451250484750638 ) ) ;
#31590=B_SPLINE_CURVE_WITH_KNOTS ( 'NONE', 3,
 ( #2565, #13174, #25802, #41808 ),
 .UNSPECIFIED., .F., .F.,
 ( 4, 4 ),
 ( 0.001265363855408508167, 0.003765594348430528499 ),
 .UNSPECIFIED. ) ;
#31592=DIRECTION ( 'NONE',  ( -0.01601477604151182663, 0.9998717552508123996, -0.000000000000000000 ) ) ;
#31595=AXIS2_PLACEMENT_3D ( 'NONE', #26265, #42015, #38154 ) ;
#31596=EDGE_LOOP ( 'NONE', ( #48274, #27185, #7794, #27065 ) ) ;
#31597=DIRECTION ( 'NONE',  ( -0.000000000000000000, 1.000000000000000000, -0.000000000000000000 ) ) ;
#31598=DIRECTION ( 'NONE',  ( -0.9998717552508121775, -0.01601477604151182316, 0.000000000000000000 ) ) ;
#31606=CARTESIAN_POINT ( 'NONE',  ( -0.8987785766980536106, 1.205361022782829114E-17, 1.600251783270283390 ) ) ;
#31607=CARTESIAN_POINT ( 'NONE',  ( 0.000000000000000000, 6.692913385826772199, 0.000000000000000000 ) ) ;
#31612=ADVANCED_FACE ( 'NONE', ( #3044 ), #14918, .T. ) ;
#31622=CARTESIAN_POINT ( 'NONE',  ( -1.133754555558240673, 0.009760511380980992774, 1.372484652545675532 ) ) ;
#31625=ORIENTED_EDGE ( 'NONE', *, *, #29275, .T. ) ;
#31627=CARTESIAN_POINT ( 'NONE',  ( -0.5756566573089003658, 1.611847391933241669, 2.896516654582634853 ) ) ;
#31632=CARTESIAN_POINT ( 'NONE',  ( 1.735586374879370952, 0.000000000000000000, -2.388829707800026458 ) ) ;
#31636=ORIENTED_EDGE ( 'NONE', *, *, #21195, .T. ) ;
#31637=ADVANCED_FACE ( 'NONE', ( #7426 ), #23161, .T. ) ;
#31643=EDGE_CURVE ( 'NONE', #1464, #1640, #23475, .T. ) ;
#31648=ORIENTED_EDGE ( 'NONE', *, *, #23845, .F. ) ;
#31652=AXIS2_PLACEMENT_3D ( 'NONE', #7642, #39135, #27761 ) ;
#31656=EDGE_CURVE ( 'NONE', #11744, #643, #7486, .T. ) ;
#31658=DIRECTION ( 'NONE',  ( -0.000000000000000000, -1.000000000000000000, 0.000000000000000000 ) ) ;
#31664=CARTESIAN_POINT ( 'NONE',  ( 0.3820226255272446414, 0.03403845698394380309, 1.829505193364920679 ) ) ;
#31667=FACE_OUTER_BOUND ( 'NONE', #21175, .T. ) ;
#31668=CARTESIAN_POINT ( 'NONE',  ( 0.8660835963268131987, 1.007957364116236709, 2.447728759293120504 ) ) ;
#31674=DIRECTION ( 'NONE',  ( -0.9195277725514489076, 0.000000000000000000, -0.3930250316539278255 ) ) ;
#31677=CARTESIAN_POINT ( 'NONE',  ( -0.04921259842519689481, 2.794703227806734062E-17, 1.924024829198930364 ) ) ;
#31681=FACE_OUTER_BOUND ( 'NONE', #48220, .T. ) ;
#31684=ADVANCED_FACE ( 'NONE', ( #12317 ), #37461, .T. ) ;
#31685=ORIENTED_EDGE ( 'NONE', *, *, #44921, .T. ) ;
#31686=ADVANCED_FACE ( 'NONE', ( #31681 ), #20931, .T. ) ;
#31690=CARTESIAN_POINT ( 'NONE',  ( 1.887300604142603921, 1.205361022782829114E-17, 0.9597141752041703500 ) ) ;
#31692=CARTESIAN_POINT ( 'NONE',  ( 1.621795816027391979, 0.000000000000000000, -0.6396693727619211511 ) ) ;
#31693=VECTOR ( 'NONE', #14100, 39.37007874015748854 ) ;
#31694=DIRECTION ( 'NONE',  ( -0.9998717552508122886, -0.01601477604151182316, 0.000000000000000000 ) ) ;
#31695=ORIENTED_EDGE ( 'NONE', *, *, #31167, .F. ) ;
#31696=AXIS2_PLACEMENT_3D ( 'NONE', #23164, #34797, #15672 ) ;
#31697=AXIS2_PLACEMENT_3D ( 'NONE', #34037, #22657, #25512 ) ;
#31700=ORIENTED_EDGE ( 'NONE', *, *, #5112, .F. ) ;
#31701=CARTESIAN_POINT ( 'NONE',  ( -1.080407128511521764, 1.049866565877817237, 1.712347114401022274 ) ) ;
#31705=ORIENTED_EDGE ( 'NONE', *, *, #4478, .T. ) ;
#31706=DIRECTION ( 'NONE',  ( -0.01601477604151182663, 0.9998717552508123996, -0.000000000000000000 ) ) ;
#31708=CARTESIAN_POINT ( 'NONE',  ( 1.426808618753927282, 0.05077261674489902399, -1.296082183384024811 ) ) ;
#31709=( BOUNDED_CURVE ( )  B_SPLINE_CURVE ( 3, ( #48865, #9676, #37306, #33692 ),
 .UNSPECIFIED., .F., .F. ) 
 B_SPLINE_CURVE_WITH_KNOTS ( ( 4, 4 ),
 ( 3.141592653589793116, 3.207290069758609974 ),
 .UNSPECIFIED. ) 
 CURVE ( )  GEOMETRIC_REPRESENTATION_ITEM ( )  RATIONAL_B_SPLINE_CURVE ( ( 1.000000000000000000, 0.9996403531335149584, 0.9996403531335149584, 1.000000000000000000 ) ) 
 REPRESENTATION_ITEM ( '' )  );
#31710=ADVANCED_FACE ( 'NONE', ( #34794 ), #49739, .F. ) ;
#31715=EDGE_LOOP ( 'NONE', ( #32498, #20060, #26305, #46862 ) ) ;
#31717=EDGE_CURVE ( 'NONE', #25302, #41810, #11850, .T. ) ;
#31718=ORIENTED_EDGE ( 'NONE', *, *, #7267, .T. ) ;
#31720=CARTESIAN_POINT ( 'NONE',  ( 2.168245791271197209, 1.654581109258766558, -2.004968704497248400 ) ) ;
#31722=EDGE_LOOP ( 'NONE', ( #47547, #42650, #20728, #30764, #21887, #27372, #17546, #44040 ) ) ;
#31726=AXIS2_PLACEMENT_3D ( 'NONE', #42321, #45927, #30206 ) ;
#31727=CARTESIAN_POINT ( 'NONE',  ( 0.002207914879453961969, 5.905511811023623991, 0.04916304461325442243 ) ) ;
#31733=DIRECTION ( 'NONE',  ( 0.2660368455666688448, 0.000000000000000000, 0.9639628606958550172 ) ) ;
#31737=B_SPLINE_CURVE_WITH_KNOTS ( 'NONE', 3,
 ( #46263, #7054, #19163, #14548 ),
 .UNSPECIFIED., .F., .F.,
 ( 4, 4 ),
 ( 2.220059671770691363E-07, 0.002500468339801800461 ),
 .UNSPECIFIED. ) ;
#31738=VECTOR ( 'NONE', #46634, 39.37007874015748143 ) ;
#31743=DIRECTION ( 'NONE',  ( -0.9998717552508121775, -0.01601477604151182316, 0.000000000000000000 ) ) ;
#31745=CARTESIAN_POINT ( 'NONE',  ( 1.735586374879370952, 0.000000000000000000, -2.388829707800026458 ) ) ;
#31747=ADVANCED_FACE ( 'NONE', ( #39168 ), #6966, .T. ) ;
#31749=FACE_OUTER_BOUND ( 'NONE', #38615, .T. ) ;
#31750=EDGE_CURVE ( 'NONE', #26744, #26405, #24710, .T. ) ;
#31756=ORIENTED_EDGE ( 'NONE', *, *, #29273, .F. ) ;
#31757=CARTESIAN_POINT ( 'NONE',  ( 0.08139965876239094178, 1.610780518492231694, 0.000000000000000000 ) ) ;
#31758=CONICAL_SURFACE ( 'NONE', #31726, 3.483074324928249421, 1.244861948955335196 ) ;
#31760=ORIENTED_EDGE ( 'NONE', *, *, #7664, .T. ) ;
#31762=AXIS2_PLACEMENT_3D ( 'NONE', #16753, #43331, #8742 ) ;
#31765=CARTESIAN_POINT ( 'NONE',  ( 0.1450362469327832748, 6.692913385826772199, -2.160491579385212191 ) ) ;
#31769=FACE_OUTER_BOUND ( 'NONE', #3216, .T. ) ;
#31772=CARTESIAN_POINT ( 'NONE',  ( -2.607957063749950066, 1.580174266876329670, 1.384773081374161663 ) ) ;
#31774=VERTEX_POINT ( 'NONE', #32463 ) ;
#31779=CARTESIAN_POINT ( 'NONE',  ( 0.3381173457103284763, 6.692913385826772199, 2.138793126519850318 ) ) ;
#31786=ORIENTED_EDGE ( 'NONE', *, *, #49279, .F. ) ;
#31787=CARTESIAN_POINT ( 'NONE',  ( 1.688048600224988149, 0.000000000000000000, -0.4357642695449466252 ) ) ;
#31791=DIRECTION ( 'NONE',  ( -9.701723960855733411E-17, 1.000000000000000000, -8.476140964546406840E-17 ) ) ;
#31792=ADVANCED_FACE ( 'NONE', ( #9208 ), #20965, .T. ) ;
#31794=B_SPLINE_CURVE_WITH_KNOTS ( 'NONE', 3,
 ( #13510, #13003, #8867, #48067 ),
 .UNSPECIFIED., .F., .F.,
 ( 4, 4 ),
 ( 2.018271350767252085E-07, 0.002500207285796618092 ),
 .UNSPECIFIED. ) ;
#31803=EDGE_LOOP ( 'NONE', ( #27634, #7456, #2942, #42029 ) ) ;
#31804=CARTESIAN_POINT ( 'NONE',  ( 0.000000000000000000, 1.574803149606302854, 0.000000000000000000 ) ) ;
#31807=CIRCLE ( 'NONE', #33490, 1.743387098533651480 ) ;
#31810=EDGE_CURVE ( 'NONE', #17939, #33261, #16016, .T. ) ;
#31815=B_SPLINE_CURVE_WITH_KNOTS ( 'NONE', 3,
 ( #36465, #32863, #16072, #36210 ),
 .UNSPECIFIED., .F., .F.,
 ( 4, 4 ),
 ( 6.088918481998526345E-07, 0.0008127897595450017231 ),
 .UNSPECIFIED. ) ;
#31817=DIRECTION ( 'NONE',  ( 0.000000000000000000, 0.000000000000000000, 1.000000000000000000 ) ) ;
#31818=ORIENTED_EDGE ( 'NONE', *, *, #23046, .F. ) ;
#31824=ORIENTED_EDGE ( 'NONE', *, *, #28262, .F. ) ;
#31827=ORIENTED_EDGE ( 'NONE', *, *, #1766, .T. ) ;
#31829=CARTESIAN_POINT ( 'NONE',  ( -1.295944566667802889, 1.542179613706447849, -2.653217792976843015 ) ) ;
#31830=DIRECTION ( 'NONE',  ( 0.000000000000000000, 0.000000000000000000, 1.000000000000000000 ) ) ;
#31836=CARTESIAN_POINT ( 'NONE',  ( -1.236813753895213086, 1.699986652445209634, -2.681693691597581974 ) ) ;
#31839=CARTESIAN_POINT ( 'NONE',  ( 0.000000000000000000, 6.692913385826772199, 0.000000000000000000 ) ) ;
#31842=ORIENTED_EDGE ( 'NONE', *, *, #9479, .F. ) ;
#31847=DIRECTION ( 'NONE',  ( 0.000000000000000000, -1.000000000000000000, 0.000000000000000000 ) ) ;
#31850=CARTESIAN_POINT ( 'NONE',  ( 0.1067246931122726866, 0.02962905676920215767, 0.000000000000000000 ) ) ;
#31851=ADVANCED_FACE ( 'NONE', ( #9465 ), #354, .T. ) ;
#31852=VECTOR ( 'NONE', #35964, 39.37007874015748143 ) ;
#31855=EDGE_LOOP ( 'NONE', ( #33882, #32472, #27921, #45010, #48397, #215 ) ) ;
#31857=EDGE_CURVE ( 'NONE', #39762, #38725, #32753, .T. ) ;
#31859=ORIENTED_EDGE ( 'NONE', *, *, #15139, .F. ) ;
#31862=B_SPLINE_CURVE_WITH_KNOTS ( 'NONE', 3,
 ( #50684, #19496, #42235, #18997 ),
 .UNSPECIFIED., .F., .F.,
 ( 4, 4 ),
 ( 2.175066794692088623E-07, 0.002500264396982808911 ),
 .UNSPECIFIED. ) ;
#31863=DIRECTION ( 'NONE',  ( -0.9989930665413144784, 0.000000000000000000, -0.04486483035051863633 ) ) ;
#31865=VERTEX_POINT ( 'NONE', #12570 ) ;
#31868=CARTESIAN_POINT ( 'NONE',  ( 1.785842763811721357, 0.03714046191358289645, 0.9051173831972618711 ) ) ;
#31870=CARTESIAN_POINT ( 'NONE',  ( -1.915752150681443222, 1.685393533398291233, -1.899733137568783814 ) ) ;
#31874=ORIENTED_EDGE ( 'NONE', *, *, #32751, .T. ) ;
#31877=CARTESIAN_POINT ( 'NONE',  ( 0.002207914879453961969, 6.692913385826772199, 0.04916304461325451958 ) ) ;
#31880=AXIS2_PLACEMENT_3D ( 'NONE', #29711, #36956, #1577 ) ;
#31885=CARTESIAN_POINT ( 'NONE',  ( 2.192594616722325807, 1.677403568648509813, 0.7641623650280537916 ) ) ;
#31907=CARTESIAN_POINT ( 'NONE',  ( -0.8329809839909436686, 1.533199950842965453, -2.833254665166566877 ) ) ;
#31910=VERTEX_POINT ( 'NONE', #33740 ) ;
#31911=CARTESIAN_POINT ( 'NONE',  ( 0.1155636338427008941, -0.5222242541845523167, 0.000000000000000000 ) ) ;
#31917=ORIENTED_EDGE ( 'NONE', *, *, #29700, .T. ) ;
#31918=CARTESIAN_POINT ( 'NONE',  ( -0.04921259842519708216, 1.620047916482694861, 2.952755905511811108 ) ) ;
#31919=ORIENTED_EDGE ( 'NONE', *, *, #17562, .F. ) ;
#31921=CONICAL_SURFACE ( 'NONE', #42587, 1.850107469027523210, 0.6386652850508578450 ) ;
#31925=ADVANCED_FACE ( 'NONE', ( #17721 ), #25094, .T. ) ;
#31926=DIRECTION ( 'NONE',  ( 0.04486483035051863633, 0.000000000000000000, -0.9989930665413144784 ) ) ;
#31931=EDGE_LOOP ( 'NONE', ( #34049, #36935, #12386, #23182 ) ) ;
#31933=CARTESIAN_POINT ( 'NONE',  ( 1.775400203342704986, 1.746929418358725172, -2.359903268218703332 ) ) ;
#31935=ORIENTED_EDGE ( 'NONE', *, *, #4337, .T. ) ;
#31938=CARTESIAN_POINT ( 'NONE',  ( -1.734129965298919718, 4.960977165729326543E-05, 0.1852418127046455421 ) ) ;
#31945=ORIENTED_EDGE ( 'NONE', *, *, #41580, .F. ) ;
#31947=CARTESIAN_POINT ( 'NONE',  ( 1.628466770324754176, 1.733984826446373750, -1.625060189682509870 ) ) ;
#31949=CARTESIAN_POINT ( 'NONE',  ( 1.544727076124027931, 0.5249316475426858419, -1.078632795641746966 ) ) ;
#31952=CONICAL_SURFACE ( 'NONE', #42653, 3.483074324928249421, 1.244861948955335196 ) ;
#31954=ORIENTED_EDGE ( 'NONE', *, *, #36738, .T. ) ;
#31957=CARTESIAN_POINT ( 'NONE',  ( -0.5756566573089004768, 1.527738838675063882, 2.896516654582634853 ) ) ;
#31958=EDGE_CURVE ( 'NONE', #2318, #7103, #18227, .T. ) ;
#31964=VERTEX_POINT ( 'NONE', #6361 ) ;
#31966=ORIENTED_EDGE ( 'NONE', *, *, #31398, .T. ) ;
#31969=VERTEX_POINT ( 'NONE', #29597 ) ;
#31973=ADVANCED_FACE ( 'NONE', ( #13598 ), #48966, .F. ) ;
#31978=CARTESIAN_POINT ( 'NONE',  ( 2.623503965249849301, 1.661669217907264740, 1.355882097269874187 ) ) ;
#31979=ADVANCED_FACE ( 'NONE', ( #41469 ), #11091, .T. ) ;
#31981=ADVANCED_FACE ( 'NONE', ( #25717 ), #6097, .F. ) ;
#31986=VERTEX_POINT ( 'NONE', #49670 ) ;
#31987=ORIENTED_EDGE ( 'NONE', *, *, #32469, .F. ) ;
#31989=CYLINDRICAL_SURFACE ( 'NONE', #8969, 2.165354330708661568 ) ;
#31990=LINE ( 'NONE', #4870, #18394 ) ;
#31992=CARTESIAN_POINT ( 'NONE',  ( 1.087963734054938625, 1.205361022782829114E-17, 1.724994741719410918 ) ) ;
#31995=ADVANCED_FACE ( 'NONE', ( #18484 ), #9723, .T. ) ;
#32004=CARTESIAN_POINT ( 'NONE',  ( -1.312248418042854858, 1.574803149606302854, -1.722429524498108711 ) ) ;
#32006=VERTEX_POINT ( 'NONE', #40369 ) ;
#32009=CARTESIAN_POINT ( 'NONE',  ( 0.08139965876239094178, 1.610780518492231694, 0.000000000000000000 ) ) ;
#32011=CARTESIAN_POINT ( 'NONE',  ( -0.9146000759343694275, 1.693252956796532871, -2.012610095043610769 ) ) ;
#32012=ADVANCED_FACE ( 'NONE', ( #29241 ), #6120, .F. ) ;
#32013=ORIENTED_EDGE ( 'NONE', *, *, #35600, .T. ) ;
#32015=CARTESIAN_POINT ( 'NONE',  ( 2.217727732172433353, 0.5219239147199549178, -0.5566600749325844033 ) ) ;
#32020=ORIENTED_EDGE ( 'NONE', *, *, #14852, .T. ) ;
#32021=EDGE_CURVE ( 'NONE', #36731, #15952, #9631, .T. ) ;
#32022=CARTESIAN_POINT ( 'NONE',  ( -2.168245791271168343, 1.685466330048090322, -2.004968704497279930 ) ) ;
#32027=AXIS2_PLACEMENT_3D ( 'NONE', #30311, #22058, #33439 ) ;
#32028=AXIS2_PLACEMENT_3D ( 'NONE', #28427, #23288, #39038 ) ;
#32031=ORIENTED_EDGE ( 'NONE', *, *, #25551, .T. ) ;
#32035=ORIENTED_EDGE ( 'NONE', *, *, #21898, .T. ) ;
#32037=VECTOR ( 'NONE', #3285, 39.37007874015748143 ) ;
#32040=EDGE_CURVE ( 'NONE', #49693, #30403, #24611, .T. ) ;
#32043=EDGE_CURVE ( 'NONE', #22349, #12025, #9373, .T. ) ;
#32047=DIRECTION ( 'NONE',  ( -0.000000000000000000, -1.000000000000000000, -0.000000000000000000 ) ) ;
#32051=CARTESIAN_POINT ( 'NONE',  ( 0.1067246931122726866, 0.02962905676920215767, 0.000000000000000000 ) ) ;
#32053=CARTESIAN_POINT ( 'NONE',  ( 0.000000000000000000, 1.574803149606302854, 0.000000000000000000 ) ) ;
#32055=CARTESIAN_POINT ( 'NONE',  ( 1.514466370292996578, 5.905511811023623991, 2.534789744887420149 ) ) ;
#32060=ORIENTED_EDGE ( 'NONE', *, *, #30508, .F. ) ;
#32061=ORIENTED_EDGE ( 'NONE', *, *, #35762, .T. ) ;
#32062=CONICAL_SURFACE ( 'NONE', #30402, 3.033577403570480779, 1.554780866114618743 ) ;
#32064=CARTESIAN_POINT ( 'NONE',  ( 2.164971648505046975, 5.905511811023623991, -0.04070796836118371897 ) ) ;
#32067=EDGE_CURVE ( 'NONE', #43799, #11883, #3835, .T. ) ;
#32069=EDGE_LOOP ( 'NONE', ( #28790, #24738, #27377, #11240 ) ) ;
#32070=CARTESIAN_POINT ( 'NONE',  ( 2.755905511811024056, 4.960629921259846142, 1.023622047244094446 ) ) ;
#32072=VECTOR ( 'NONE', #15606, 39.37007874015748143 ) ;
#32073=CARTESIAN_POINT ( 'NONE',  ( 1.769879628650530723, 0.05626752682809384870, -0.8100022834900426627 ) ) ;
#32074=EDGE_CURVE ( 'NONE', #22430, #18703, #39095, .T. ) ;
#32076=CARTESIAN_POINT ( 'NONE',  ( 1.686111637834603938, 0.05492582915004715072, 0.9632209503012270080 ) ) ;
#32085=DIRECTION ( 'NONE',  ( -0.01601477604151182663, 0.9998717552508123996, -0.000000000000000000 ) ) ;
#32086=ORIENTED_EDGE ( 'NONE', *, *, #36243, .F. ) ;
#32090=DIRECTION ( 'NONE',  ( -0.000000000000000000, 1.000000000000000000, -0.000000000000000000 ) ) ;
#32094=LINE ( 'NONE', #20710, #35372 ) ;
#32100=ORIENTED_EDGE ( 'NONE', *, *, #46689, .F. ) ;
#32101=CARTESIAN_POINT ( 'NONE',  ( -2.378234070510009790, 1.575584252498931193, -0.4923382150760590159 ) ) ;
#32102=ORIENTED_EDGE ( 'NONE', *, *, #6917, .T. ) ;
#32106=EDGE_CURVE ( 'NONE', #24532, #40028, #14898, .T. ) ;
#32109=CARTESIAN_POINT ( 'NONE',  ( -2.165460538733998241, 1.205361022782829114E-17, 0.04798874274652762534 ) ) ;
#32110=EDGE_CURVE ( 'NONE', #23592, #21262, #1368, .T. ) ;
#32115=EDGE_CURVE ( 'NONE', #3395, #21117, #14255, .T. ) ;
#32116=CIRCLE ( 'NONE', #27148, 2.165354330708661568 ) ;
#32119=DIRECTION ( 'NONE',  ( -0.000000000000000000, -1.000000000000000000, -0.000000000000000000 ) ) ;
#32121=CARTESIAN_POINT ( 'NONE',  ( 2.923830774217214934, 1.764811239170032131, 0.4126137884981752602 ) ) ;
#32123=ORIENTED_EDGE ( 'NONE', *, *, #16295, .F. ) ;
#32127=LINE ( 'NONE', #16631, #34795 ) ;
#32128=CARTESIAN_POINT ( 'NONE',  ( 0.000000000000000000, 1.574803149606302854, 0.000000000000000000 ) ) ;
#32129=CARTESIAN_POINT ( 'NONE',  ( 2.295325967725798222, 1.744665796922353351, 0.3605850800666594580 ) ) ;
#32130=VECTOR ( 'NONE', #29924, 39.37007874015748143 ) ;
#32131=VERTEX_POINT ( 'NONE', #9882 ) ;
#32132=CARTESIAN_POINT ( 'NONE',  ( -1.546216657190577770, 1.038502057849785887, -2.044459178825514645 ) ) ;
#32140=AXIS2_PLACEMENT_3D ( 'NONE', #13950, #48758, #45660 ) ;
#32145=EDGE_CURVE ( 'NONE', #40985, #42971, #41630, .T. ) ;
#32149=CARTESIAN_POINT ( 'NONE',  ( -2.813308242715026886, 1.572884882776984794, 0.8968463675966862336 ) ) ;
#32155=DIRECTION ( 'NONE',  ( 1.558091277195102803E-17, -1.000000000000000000, 1.150229170499808965E-16 ) ) ;
#32158=EDGE_LOOP ( 'NONE', ( #43717, #50251, #40222, #21044 ) ) ;
#32160=DIRECTION ( 'NONE',  ( -0.01601477604151182663, 0.9998717552508123996, -0.000000000000000000 ) ) ;
#32166=ORIENTED_EDGE ( 'NONE', *, *, #11346, .F. ) ;
#32167=ORIENTED_EDGE ( 'NONE', *, *, #10921, .T. ) ;
#32170=EDGE_CURVE ( 'NONE', #23287, #31073, #45685, .T. ) ;
#32180=CARTESIAN_POINT ( 'NONE',  ( -2.138597145901436125, 1.574803149606302854, 0.3393547186366939750 ) ) ;
#32187=DIRECTION ( 'NONE',  ( 1.509903313490212895E-14, 0.000000000000000000, 1.000000000000000000 ) ) ;
#32190=CARTESIAN_POINT ( 'NONE',  ( 1.672606463373375485, 0.000000000000000000, 0.4917175957957914401 ) ) ;
#32192=DIRECTION ( 'NONE',  ( 0.1785568947986229116, 0.000000000000000000, 0.9839295885986321100 ) ) ;
#32193=FACE_OUTER_BOUND ( 'NONE', #33345, .T. ) ;
#32195=CARTESIAN_POINT ( 'NONE',  ( 2.695799277629594037, 1.205361022782829114E-17, -1.205759334241453651 ) ) ;
#32197=DIRECTION ( 'NONE',  ( 0.000000000000000000, 0.000000000000000000, 1.000000000000000000 ) ) ;
#32202=DIRECTION ( 'NONE',  ( 0.9998717552508121775, 0.01601477604151182663, 0.000000000000000000 ) ) ;
#32205=EDGE_CURVE ( 'NONE', #40819, #21432, #24777, .T. ) ;
#32209=CARTESIAN_POINT ( 'NONE',  ( 0.000000000000000000, 6.692913385826772199, 0.000000000000000000 ) ) ;
#32213=EDGE_CURVE ( 'NONE', #6661, #35582, #34399, .T. ) ;
#32217=ORIENTED_EDGE ( 'NONE', *, *, #36248, .T. ) ;
#32218=CARTESIAN_POINT ( 'NONE',  ( -2.168245791271168343, 1.685466330048090322, -2.004968704497279930 ) ) ;
#32219=FACE_OUTER_BOUND ( 'NONE', #9308, .T. ) ;
#32221=DIRECTION ( 'NONE',  ( 0.000000000000000000, 0.000000000000000000, 1.000000000000000000 ) ) ;
#32223=AXIS2_PLACEMENT_3D ( 'NONE', #3004, #2499, #14623 ) ;
#32224=CARTESIAN_POINT ( 'NONE',  ( -2.813306909019601232, 1.675400517285150270, 0.8968504722891414982 ) ) ;
#32225=EDGE_CURVE ( 'NONE', #31431, #36611, #40144, .T. ) ;
#32230=EDGE_CURVE ( 'NONE', #7280, #13250, #50598, .T. ) ;
#32232=CARTESIAN_POINT ( 'NONE',  ( -0.3928349003157404762, 1.705466165868896988, 2.440311704409034554 ) ) ;
#32233=EDGE_CURVE ( 'NONE', #16438, #9349, #6768, .T. ) ;
#32236=FACE_OUTER_BOUND ( 'NONE', #29997, .T. ) ;
#32237=LINE ( 'NONE', #16227, #31354 ) ;
#32238=ORIENTED_EDGE ( 'NONE', *, *, #25838, .F. ) ;
#32239=ORIENTED_EDGE ( 'NONE', *, *, #26364, .T. ) ;
#32240=LINE ( 'NONE', #47936, #5522 ) ;
#32241=CARTESIAN_POINT ( 'NONE',  ( -1.983277435230861085, 1.585901007090198878, -1.828120848347478455 ) ) ;
#32243=CARTESIAN_POINT ( 'NONE',  ( -1.721723715434402058, 0.0002321930594665579301, 0.2828853756254362528 ) ) ;
#32244=B_SPLINE_CURVE_WITH_KNOTS ( 'NONE', 3,
 ( #13688, #29429, #13942, #25810 ),
 .UNSPECIFIED., .F., .F.,
 ( 4, 4 ),
 ( 0.001790699833465591011, 0.004290724276823231105 ),
 .UNSPECIFIED. ) ;
#32245=CARTESIAN_POINT ( 'NONE',  ( -0.9845150457423005319, 0.000000000000000000, -1.438794182654565601 ) ) ;
#32249=CARTESIAN_POINT ( 'NONE',  ( 1.530693736245519521, 6.692913385826772199, -1.531579597454042707 ) ) ;
#32251=DIRECTION ( 'NONE',  ( 2.753352829315774182E-14, 0.000000000000000000, 1.000000000000000000 ) ) ;
#32255=ORIENTED_EDGE ( 'NONE', *, *, #35114, .T. ) ;
#32258=CARTESIAN_POINT ( 'NONE',  ( -1.350373579275921276, 0.006290961278228680842, 1.139832270491418553 ) ) ;
#32262=DIRECTION ( 'NONE',  ( 0.000000000000000000, 0.000000000000000000, 1.000000000000000000 ) ) ;
#32264=CARTESIAN_POINT ( 'NONE',  ( -2.497042144641281602, 1.050182909770654982, -0.5194553827013835834 ) ) ;
#32265=EDGE_CURVE ( 'NONE', #50554, #17626, #10827, .T. ) ;
#32266=B_SPLINE_CURVE_WITH_KNOTS ( 'NONE', 3,
 ( #10956, #3207, #34704, #3459 ),
 .UNSPECIFIED., .F., .F.,
 ( 4, 4 ),
 ( 3.361685337281771228E-07, 0.04732126538906464980 ),
 .UNSPECIFIED. ) ;
#32273=EDGE_CURVE ( 'NONE', #28312, #23622, #26633, .T. ) ;
#32281=VECTOR ( 'NONE', #27497, 39.37007874015748143 ) ;
#32284=CARTESIAN_POINT ( 'NONE',  ( 1.834323595590318323, 0.000000000000000000, 1.151859023884926891 ) ) ;
#32287=AXIS2_PLACEMENT_3D ( 'NONE', #34304, #38425, #21656 ) ;
#32288=EDGE_CURVE ( 'NONE', #22473, #27704, #34212, .T. ) ;
#32291=AXIS2_PLACEMENT_3D ( 'NONE', #22495, #34120, #1667 ) ;
#32296=CARTESIAN_POINT ( 'NONE',  ( 0.7697289541891751963, 1.731250765710271811, -2.850711116208678675 ) ) ;
#32301=ORIENTED_EDGE ( 'NONE', *, *, #30839, .T. ) ;
#32302=FACE_OUTER_BOUND ( 'NONE', #2545, .T. ) ;
#32304=CARTESIAN_POINT ( 'NONE',  ( -1.735586374879336535, 0.000000000000000000, -2.388829707800051327 ) ) ;
#32309=CARTESIAN_POINT ( 'NONE',  ( 1.999177773822438553, 1.049866565877818125, 0.3204690814889624151 ) ) ;
#32315=CIRCLE ( 'NONE', #10057, 2.164630168518208109 ) ;
#32317=DIRECTION ( 'NONE',  ( -0.6579387259397027066, 0.000000000000000000, -0.7530714660036196273 ) ) ;
#32328=ORIENTED_EDGE ( 'NONE', *, *, #42141, .T. ) ;
#32330=AXIS2_PLACEMENT_3D ( 'NONE', #12566, #24449, #36581 ) ;
#32331=DIRECTION ( 'NONE',  ( 0.000000000000000000, 0.000000000000000000, -1.000000000000000000 ) ) ;
#32335=EDGE_CURVE ( 'NONE', #36271, #40209, #38338, .T. ) ;
#32337=ORIENTED_EDGE ( 'NONE', *, *, #14793, .F. ) ;
#32342=LINE ( 'NONE', #834, #37155 ) ;
#32346=DIRECTION ( 'NONE',  ( -0.000000000000000000, -1.000000000000000000, 0.000000000000000000 ) ) ;
#32348=CARTESIAN_POINT ( 'NONE',  ( 0.1067246931122726866, 0.02962905676920215767, 0.000000000000000000 ) ) ;
#32349=ORIENTED_EDGE ( 'NONE', *, *, #16629, .F. ) ;
#32350=CARTESIAN_POINT ( 'NONE',  ( 0.8912126068892033404, 0.000000000000000000, -1.812984823346281749 ) ) ;
#32356=DIRECTION ( 'NONE',  ( 0.000000000000000000, 0.000000000000000000, -1.000000000000000000 ) ) ;
#32362=DIRECTION ( 'NONE',  ( -0.01601477604151182663, 0.9998717552508123996, -0.000000000000000000 ) ) ;
#32363=VERTEX_POINT ( 'NONE', #43638 ) ;
#32365=AXIS2_PLACEMENT_3D ( 'NONE', #35005, #49940, #30376 ) ;
#32368=ORIENTED_EDGE ( 'NONE', *, *, #4680, .T. ) ;
#32369=CARTESIAN_POINT ( 'NONE',  ( 1.735113842587030497, 0.05571068913886997875, 0.8778189866238004235 ) ) ;
#32372=AXIS2_PLACEMENT_3D ( 'NONE', #5176, #1304, #16285 ) ;
#32374=CARTESIAN_POINT ( 'NONE',  ( -0.2865598533144464444, 0.007820411976265893850, 1.854687926664660758 ) ) ;
#32379=EDGE_CURVE ( 'NONE', #14806, #48863, #10766, .T. ) ;
#32380=CARTESIAN_POINT ( 'NONE',  ( -2.695799277629577162, 1.578813927010291218, -1.205759334241492731 ) ) ;
#32382=ORIENTED_EDGE ( 'NONE', *, *, #31140, .F. ) ;
#32383=DIRECTION ( 'NONE',  ( 0.000000000000000000, -1.000000000000000000, 0.000000000000000000 ) ) ;
#32384=PLANE ( 'NONE',  #36038 ) ;
#32386=EDGE_LOOP ( 'NONE', ( #24115, #44325, #41998, #13144, #16075, #38366, #32799, #46119, #14585, #40845, #23469 ) ) ;
#32389=CARTESIAN_POINT ( 'NONE',  ( -0.1943412135031128696, 1.613985720517193245, -2.708314625670412035 ) ) ;
#32395=EDGE_CURVE ( 'NONE', #42, #16195, #47222, .T. ) ;
#32397=CARTESIAN_POINT ( 'NONE',  ( -2.277873973731453727, 1.683757167080951245, 1.879489153247634992 ) ) ;
#32400=ADVANCED_FACE ( 'NONE', ( #31021 ), #44902, .T. ) ;
#32401=VECTOR ( 'NONE', #38068, 39.37007874015748143 ) ;
#32404=DIRECTION ( 'NONE',  ( -9.390536051998861478E-17, -1.000000000000000000, 6.822623802544654332E-17 ) ) ;
#32406=ORIENTED_EDGE ( 'NONE', *, *, #44627, .F. ) ;
#32408=CARTESIAN_POINT ( 'NONE',  ( 1.435629050127790629, 1.734437112858062235, -2.059699342362053542 ) ) ;
#32410=DIRECTION ( 'NONE',  ( 0.9959742939952397345, -1.160734090543304660E-16, -0.08963930890342654279 ) ) ;
#32418=CARTESIAN_POINT ( 'NONE',  ( 0.000000000000000000, 1.574803149606302854, 0.000000000000000000 ) ) ;
#32423=DIRECTION ( 'NONE',  ( -0.000000000000000000, -1.000000000000000000, -0.000000000000000000 ) ) ;
#32426=CARTESIAN_POINT ( 'NONE',  ( 0.7855418668307559971, 5.905511811023623991, -2.846347029613733870 ) ) ;
#32428=EDGE_CURVE ( 'NONE', #49749, #36594, #1538, .T. ) ;
#32431=ORIENTED_EDGE ( 'NONE', *, *, #34363, .T. ) ;
#32433=DIRECTION ( 'NONE',  ( 4.884978838366539963E-14, 0.000000000000000000, 1.000000000000000000 ) ) ;
#32437=EDGE_CURVE ( 'NONE', #34370, #33474, #39785, .T. ) ;
#32438=PLANE ( 'NONE',  #44536 ) ;
#32446=CARTESIAN_POINT ( 'NONE',  ( 0.1067246931122726866, 0.02962905676920215767, 0.000000000000000000 ) ) ;
#32447=CIRCLE ( 'NONE', #17582, 2.246510896728926010 ) ;
#32449=VERTEX_POINT ( 'NONE', #36176 ) ;
#32450=CARTESIAN_POINT ( 'NONE',  ( -0.7303501086101935602, 5.905511811023623991, 2.086068174627930816 ) ) ;
#32454=EDGE_CURVE ( 'NONE', #2274, #5130, #5182, .T. ) ;
#32463=CARTESIAN_POINT ( 'NONE',  ( -0.2156685157583833057, 1.520013147563287648, -2.945280361644576850 ) ) ;
#32467=EDGE_LOOP ( 'NONE', ( #2986, #13709, #40541, #8630 ) ) ;
#32469=EDGE_CURVE ( 'NONE', #37445, #28425, #44956, .T. ) ;
#32471=EDGE_CURVE ( 'NONE', #13914, #43507, #1218, .T. ) ;
#32472=ORIENTED_EDGE ( 'NONE', *, *, #3298, .F. ) ;
#32473=B_SPLINE_CURVE_WITH_KNOTS ( 'NONE', 3,
 ( #16450, #43789, #15425, #20040 ),
 .UNSPECIFIED., .F., .F.,
 ( 4, 4 ),
 ( 2.008297004145147925E-07, 0.01822228745053504351 ),
 .UNSPECIFIED. ) ;
#32480=CARTESIAN_POINT ( 'NONE',  ( -2.160407304981126320, 1.673304745347873324, -0.1462862061266896330 ) ) ;
#32486=CARTESIAN_POINT ( 'NONE',  ( -2.793030215715272213, 1.675725205278408403, 0.9592557174602281966 ) ) ;
#32488=ORIENTED_EDGE ( 'NONE', *, *, #32170, .T. ) ;
#32494=CARTESIAN_POINT ( 'NONE',  ( 0.1155636338427008941, -0.5222242541845523167, 0.000000000000000000 ) ) ;
#32495=DIRECTION ( 'NONE',  ( -3.986037398843765983E-20, -1.000000000000000000, -1.160734090543304660E-16 ) ) ;
#32496=ADVANCED_FACE ( 'NONE', ( #43644 ), #14406, .T. ) ;
#32497=DIRECTION ( 'NONE',  ( 5.063291518729136385E-17, 1.000000000000000000, -1.184615939703115601E-16 ) ) ;
#32498=ORIENTED_EDGE ( 'NONE', *, *, #18761, .T. ) ;
#32505=FACE_OUTER_BOUND ( 'NONE', #18829, .T. ) ;
#32506=CARTESIAN_POINT ( 'NONE',  ( 1.163887619842433718, 0.04656145577143805392, -1.518228404148327160 ) ) ;
#32507=LINE ( 'NONE', #49216, #47379 ) ;
#32512=ORIENTED_EDGE ( 'NONE', *, *, #1688, .F. ) ;
#32515=VECTOR ( 'NONE', #1624, 39.37007874015748143 ) ;
#32520=CARTESIAN_POINT ( 'NONE',  ( -2.875073865522039807, 1.674437446067899682, -0.6730429437227067879 ) ) ;
#32521=VECTOR ( 'NONE', #7782, 39.37007874015748854 ) ;
#32522=LINE ( 'NONE', #33035, #7248 ) ;
#32532=CARTESIAN_POINT ( 'NONE',  ( 0.1067246931122726866, 0.02962905676920215767, 0.000000000000000000 ) ) ;
#32534=DIRECTION ( 'NONE',  ( -0.000000000000000000, 1.000000000000000000, -0.000000000000000000 ) ) ;
#32538=VERTEX_POINT ( 'NONE', #8802 ) ;
#32539=CARTESIAN_POINT ( 'NONE',  ( 1.064142702668988694, 0.000000000000000000, -1.380941303491905359 ) ) ;
#32544=ORIENTED_EDGE ( 'NONE', *, *, #32454, .T. ) ;
#32545=B_SPLINE_CURVE_WITH_KNOTS ( 'NONE', 3,
 ( #26031, #6161, #45619, #3045 ),
 .UNSPECIFIED., .F., .F.,
 ( 4, 4 ),
 ( 2.329854597834415671E-07, 0.01900427930416172251 ),
 .UNSPECIFIED. ) ;
#32547=VECTOR ( 'NONE', #30585, 39.37007874015748854 ) ;
#32553=CARTESIAN_POINT ( 'NONE',  ( -1.905671854841497259, 1.205361022782829114E-17, 2.256015092822653667 ) ) ;
#32555=DIRECTION ( 'NONE',  ( -0.9998717552508121775, -0.01601477604151182663, 0.000000000000000000 ) ) ;
#32560=EDGE_CURVE ( 'NONE', #21618, #20329, #28929, .T. ) ;
#32562=CARTESIAN_POINT ( 'NONE',  ( 1.472697644137372697, 1.731489898814932316, 1.760436233057293354 ) ) ;
#32563=DIRECTION ( 'NONE',  ( 0.000000000000000000, -1.000000000000000000, 0.000000000000000000 ) ) ;
#32565=DIRECTION ( 'NONE',  ( -0.000000000000000000, -1.000000000000000000, -0.000000000000000000 ) ) ;
#32574=CARTESIAN_POINT ( 'NONE',  ( 1.549689501921142964, 1.667106268065684738, 1.698964208316597446 ) ) ;
#32576=ORIENTED_EDGE ( 'NONE', *, *, #13200, .T. ) ;
#32583=VECTOR ( 'NONE', #26079, 39.37007874015748143 ) ;
#32584=AXIS2_PLACEMENT_3D ( 'NONE', #8945, #16445, #24187 ) ;
#32589=ORIENTED_EDGE ( 'NONE', *, *, #32067, .T. ) ;
#32601=ORIENTED_EDGE ( 'NONE', *, *, #48014, .T. ) ;
#32604=CARTESIAN_POINT ( 'NONE',  ( 2.725796967338451449, 1.659824354563097737, 0.3195722353185223019 ) ) ;
#32605=ADVANCED_FACE ( 'NONE', ( #36952 ), #13958, .T. ) ;
#32609=CARTESIAN_POINT ( 'NONE',  ( -1.672606463373382590, 0.000000000000000000, 0.4917175957957677923 ) ) ;
#32610=ORIENTED_EDGE ( 'NONE', *, *, #7985, .F. ) ;
#32612=CARTESIAN_POINT ( 'NONE',  ( 0.000000000000000000, 1.574803149606302854, 0.000000000000000000 ) ) ;
#32614=ORIENTED_EDGE ( 'NONE', *, *, #40571, .T. ) ;
#32623=B_SPLINE_CURVE_WITH_KNOTS ( 'NONE', 3,
 ( #30906, #7657, #19522, #35286 ),
 .UNSPECIFIED., .F., .F.,
 ( 4, 4 ),
 ( 2.102925093913365354E-07, 0.01991504288061870728 ),
 .UNSPECIFIED. ) ;
#32626=CARTESIAN_POINT ( 'NONE',  ( -0.04921259842519758176, 5.905511811023623991, -2.165433070866141119 ) ) ;
#32627=ORIENTED_EDGE ( 'NONE', *, *, #21494, .T. ) ;
#32628=CARTESIAN_POINT ( 'NONE',  ( 0.4350747367505080065, 5.905511811023623991, -2.121846421795414717 ) ) ;
#32630=AXIS2_PLACEMENT_3D ( 'NONE', #19409, #23542, #39806 ) ;
#32631=EDGE_CURVE ( 'NONE', #31986, #29362, #48768, .T. ) ;
#32635=CARTESIAN_POINT ( 'NONE',  ( -1.531732224425391253, 1.205361022782829114E-17, 0.8801458454442117052 ) ) ;
#32645=EDGE_CURVE ( 'NONE', #1280, #39907, #21824, .T. ) ;
#32649=B_SPLINE_CURVE_WITH_KNOTS ( 'NONE', 3,
 ( #9170, #12795, #24670, #44013 ),
 .UNSPECIFIED., .F., .F.,
 ( 4, 4 ),
 ( 0.0009436092406449438433, 0.04779288783656267248 ),
 .UNSPECIFIED. ) ;
#32650=CARTESIAN_POINT ( 'NONE',  ( 0.08139965876239094178, 1.610780518492231694, 0.000000000000000000 ) ) ;
#32651=EDGE_CURVE ( 'NONE', #21491, #47610, #13448, .T. ) ;
#32652=ORIENTED_EDGE ( 'NONE', *, *, #29104, .T. ) ;
#32655=ORIENTED_EDGE ( 'NONE', *, *, #32672, .T. ) ;
#32658=FACE_OUTER_BOUND ( 'NONE', #9757, .T. ) ;
#32660=ADVANCED_FACE ( 'NONE', ( #25314 ), #45423, .T. ) ;
#32662=ORIENTED_EDGE ( 'NONE', *, *, #46193, .T. ) ;
#32664=CARTESIAN_POINT ( 'NONE',  ( 0.5756566573088583993, 1.629780628454260194, 2.896516654582643291 ) ) ;
#32665=VECTOR ( 'NONE', #33, 39.37007874015748143 ) ;
#32671=CARTESIAN_POINT ( 'NONE',  ( -2.946551303128973842, 1.574890269766889617, -0.1815919737934194866 ) ) ;
#32672=EDGE_CURVE ( 'NONE', #22025, #20718, #17730, .T. ) ;
#32673=AXIS2_PLACEMENT_3D ( 'NONE', #7378, #39119, #4013 ) ;
#32681=ORIENTED_EDGE ( 'NONE', *, *, #5836, .F. ) ;
#32682=DIRECTION ( 'NONE',  ( 0.01601477604151182663, -0.9998717552508123996, 0.000000000000000000 ) ) ;
#32684=VECTOR ( 'NONE', #28060, 39.37007874015748143 ) ;
#32687=CARTESIAN_POINT ( 'NONE',  ( 3.937007874015748143, 2.755905511811027164, 1.181102362204724088 ) ) ;
#32688=VERTEX_POINT ( 'NONE', #41079 ) ;
#32689=ORIENTED_EDGE ( 'NONE', *, *, #29471, .T. ) ;
#32690=DIRECTION ( 'NONE',  ( -0.000000000000000000, -1.000000000000000000, -0.000000000000000000 ) ) ;
#32692=ORIENTED_EDGE ( 'NONE', *, *, #45281, .T. ) ;
#32698=CARTESIAN_POINT ( 'NONE',  ( -1.613153987106138443, 1.649255939716216091, -1.474246598108883699 ) ) ;
#32703=CARTESIAN_POINT ( 'NONE',  ( 0.08119777152254364916, 1.623385212329073957, 0.000000000000000000 ) ) ;
#32706=VERTEX_POINT ( 'NONE', #33595 ) ;
#32708=AXIS2_PLACEMENT_3D ( 'NONE', #39657, #11772, #32433 ) ;
#32717=CARTESIAN_POINT ( 'NONE',  ( -2.808237744966007643, 0.000000000000000000, 0.9124517550441282321 ) ) ;
#32720=ORIENTED_EDGE ( 'NONE', *, *, #24202, .F. ) ;
#32727=EDGE_CURVE ( 'NONE', #38070, #33610, #24361, .T. ) ;
#32728=B_SPLINE_CURVE_WITH_KNOTS ( 'NONE', 3,
 ( #14158, #2543, #29907, #45621 ),
 .UNSPECIFIED., .F., .F.,
 ( 4, 4 ),
 ( 0.01073245408401574987, 0.03073581594907834336 ),
 .UNSPECIFIED. ) ;
#32734=ORIENTED_EDGE ( 'NONE', *, *, #30471, .F. ) ;
#32736=DIRECTION ( 'NONE',  ( -4.561975526775602830E-17, -1.000000000000000000, -1.067327232801823148E-16 ) ) ;
#32737=EDGE_CURVE ( 'NONE', #5208, #46569, #40375, .T. ) ;
#32739=DIRECTION ( 'NONE',  ( 0.6579387259397138088, 0.000000000000000000, -0.7530714660036099684 ) ) ;
#32745=CARTESIAN_POINT ( 'NONE',  ( -0.04921259842519708216, 1.620047916482694861, 2.952755905511811108 ) ) ;
#32748=CONICAL_SURFACE ( 'NONE', #30259, 3.483074324928249421, 1.244861948955335196 ) ;
#32750=ORIENTED_EDGE ( 'NONE', *, *, #49416, .F. ) ;
#32751=EDGE_CURVE ( 'NONE', #35748, #41115, #40830, .T. ) ;
#32752=CARTESIAN_POINT ( 'NONE',  ( -2.695799277629577162, 0.000000000000000000, -1.205759334241492509 ) ) ;
#32753=B_SPLINE_CURVE_WITH_KNOTS ( 'NONE', 3,
 ( #37096, #36327, #47892, #17463 ),
 .UNSPECIFIED., .F., .F.,
 ( 4, 4 ),
 ( 4.200322152323451851E-07, 0.04489399771681849144 ),
 .UNSPECIFIED. ) ;
#32756=CARTESIAN_POINT ( 'NONE',  ( 0.3136974817028392315, 0.000000000000000000, -2.936457595020219635 ) ) ;
#32759=ADVANCED_FACE ( 'NONE', ( #19582 ), #10840, .T. ) ;
#32762=VERTEX_POINT ( 'NONE', #26831 ) ;
#32763=CARTESIAN_POINT ( 'NONE',  ( -0.4358998810510941180, 1.610193826879650514, 2.677619307824346873 ) ) ;
#32766=CARTESIAN_POINT ( 'NONE',  ( -1.722047146480845337, 0.0001160965347763901303, 0.2829291873374986666 ) ) ;
#32769=LINE ( 'NONE', #20089, #13639 ) ;
#32770=ORIENTED_EDGE ( 'NONE', *, *, #31572, .F. ) ;
#32771=DIRECTION ( 'NONE',  ( -0.000000000000000000, 1.000000000000000000, -0.000000000000000000 ) ) ;
#32772=AXIS2_PLACEMENT_3D ( 'NONE', #32348, #48041, #12719 ) ;
#32785=FACE_OUTER_BOUND ( 'NONE', #1656, .T. ) ;
#32786=CARTESIAN_POINT ( 'NONE',  ( 0.7720784846736921114, 1.727602517910236113, -2.612579414938067224 ) ) ;
#32791=CARTESIAN_POINT ( 'NONE',  ( -1.979793062125317471, 1.589971192595758698, 2.191257344206539948 ) ) ;
#32794=PLANE ( 'NONE',  #37312 ) ;
#32797=DIRECTION ( 'NONE',  ( 0.000000000000000000, 0.000000000000000000, 1.000000000000000000 ) ) ;
#32799=ORIENTED_EDGE ( 'NONE', *, *, #25290, .F. ) ;
#32802=DIRECTION ( 'NONE',  ( -0.000000000000000000, 1.000000000000000000, -0.000000000000000000 ) ) ;
#32806=CARTESIAN_POINT ( 'NONE',  ( -2.607960231842429089, 1.568825401333847402, 1.384767194071829577 ) ) ;
#32809=ORIENTED_EDGE ( 'NONE', *, *, #41727, .F. ) ;
#32815=EDGE_CURVE ( 'NONE', #33586, #18815, #38721, .T. ) ;
#32816=ORIENTED_EDGE ( 'NONE', *, *, #28262, .T. ) ;
#32819=ADVANCED_FACE ( 'NONE', ( #15476 ), #23490, .T. ) ;
#32820=CARTESIAN_POINT ( 'NONE',  ( 0.002207914879453961969, 5.905511811023623991, 0.04916304461325442243 ) ) ;
#32821=DIRECTION ( 'NONE',  ( 0.000000000000000000, 1.000000000000000000, -0.000000000000000000 ) ) ;
#32822=EDGE_CURVE ( 'NONE', #25300, #24596, #16944, .T. ) ;
#32826=CARTESIAN_POINT ( 'NONE',  ( 1.312623452344844566, 0.000000000000000000, 1.722945714930923744 ) ) ;
#32827=FACE_OUTER_BOUND ( 'NONE', #23134, .T. ) ;
#32832=LINE ( 'NONE', #48510, #25173 ) ;
#32835=LINE ( 'NONE', #48514, #48132 ) ;
#32837=DIRECTION ( 'NONE',  ( -0.01601477604151182663, 0.9998717552508123996, -0.000000000000000000 ) ) ;
#32840=EDGE_LOOP ( 'NONE', ( #45182, #31760, #38915, #31138 ) ) ;
#32845=AXIS2_PLACEMENT_3D ( 'NONE', #18285, #11044, #7175 ) ;
#32849=VERTEX_POINT ( 'NONE', #47432 ) ;
#32851=AXIS2_PLACEMENT_3D ( 'NONE', #34422, #3423, #30542 ) ;
#32852=CARTESIAN_POINT ( 'NONE',  ( -0.9664853984138626064, 0.008359359359691105260, 1.521674255078630633 ) ) ;
#32853=CARTESIAN_POINT ( 'NONE',  ( 0.1324246528213921248, 1.049866565067838486, -2.020365292213844199 ) ) ;
#32859=DIRECTION ( 'NONE',  ( -0.000000000000000000, -1.000000000000000000, -0.000000000000000000 ) ) ;
#32860=EDGE_CURVE ( 'NONE', #16575, #13729, #44357, .T. ) ;
#32863=CARTESIAN_POINT ( 'NONE',  ( -1.099260860659351247, 0.003500963706710694470, -1.429277301230134301 ) ) ;
#32864=DIRECTION ( 'NONE',  ( 0.9839295885986296675, 1.288287287306305530E-16, 0.1785568947986370669 ) ) ;
#32865=CARTESIAN_POINT ( 'NONE',  ( 2.823445274216730638, 1.763256531483745837, 0.8656477926280683466 ) ) ;
#32866=AXIS2_PLACEMENT_3D ( 'NONE', #7029, #34654, #18399 ) ;
#32867=EDGE_CURVE ( 'NONE', #12116, #162, #7035, .T. ) ;
#32872=ORIENTED_EDGE ( 'NONE', *, *, #47386, .T. ) ;
#32877=VERTEX_POINT ( 'NONE', #222 ) ;
#32886=ADVANCED_FACE ( 'NONE', ( #8492 ), #43587, .T. ) ;
#32889=VECTOR ( 'NONE', #38734, 39.37007874015748143 ) ;
#32891=CARTESIAN_POINT ( 'NONE',  ( 2.555365368299595323E-16, 6.692913385826772199, 2.086614173228346303 ) ) ;
#32909=DIRECTION ( 'NONE',  ( 1.160734090543304660E-16, -1.000000000000000000, -0.000000000000000000 ) ) ;
#32911=CARTESIAN_POINT ( 'NONE',  ( -0.2646829987305902576, 5.905511811023623991, -2.940868978332400463 ) ) ;
#32915=CARTESIAN_POINT ( 'NONE',  ( 0.7381027496705270252, 1.632310643118564997, -2.859439394060913298 ) ) ;
#32917=CARTESIAN_POINT ( 'NONE',  ( -2.014567149787738654, 1.675634971041569443, -0.8075478974698888646 ) ) ;
#32920=EDGE_CURVE ( 'NONE', #13018, #8462, #32769, .T. ) ;
#32923=CARTESIAN_POINT ( 'NONE',  ( -1.412929913228844203, 0.003568411354370746354, 1.063828730186929805 ) ) ;
#32925=EDGE_CURVE ( 'NONE', #2534, #39129, #35859, .T. ) ;
#32928=CARTESIAN_POINT ( 'NONE',  ( -1.929629134066536134, 1.574803149606302854, 0.9824921284572128988 ) ) ;
#32930=EDGE_CURVE ( 'NONE', #7882, #8114, #24497, .T. ) ;
#32932=AXIS2_PLACEMENT_3D ( 'NONE', #39820, #12454, #9094 ) ;
#32938=CARTESIAN_POINT ( 'NONE',  ( -1.733853452330418987, 0.0001488292986583184614, 0.1852043564780690432 ) ) ;
#32946=CARTESIAN_POINT ( 'NONE',  ( 0.000000000000000000, 6.692913385826772199, 0.000000000000000000 ) ) ;
#32947=ORIENTED_EDGE ( 'NONE', *, *, #15233, .T. ) ;
#32949=DIRECTION ( 'NONE',  ( 0.000000000000000000, 1.160734090543304660E-16, -1.000000000000000000 ) ) ;
#32953=VERTEX_POINT ( 'NONE', #28094 ) ;
#32955=CARTESIAN_POINT ( 'NONE',  ( -0.9237497744857992021, 0.5249316475426863970, 1.642046528476600153 ) ) ;
#32957=CARTESIAN_POINT ( 'NONE',  ( -1.326676825859837816, 1.205361022782829114E-17, -1.200346386814097999 ) ) ;
#32958=VECTOR ( 'NONE', #41854, 39.37007874015748143 ) ;
#32965=EDGE_CURVE ( 'NONE', #23085, #43121, #15973, .T. ) ;
#32974=LINE ( 'NONE', #13085, #40049 ) ;
#32977=AXIS2_PLACEMENT_3D ( 'NONE', #4766, #116, #16647 ) ;
#32989=EDGE_CURVE ( 'NONE', #26292, #22637, #40249, .T. ) ;
#32991=EDGE_CURVE ( 'NONE', #22720, #6064, #32507, .T. ) ;
#32992=AXIS2_PLACEMENT_3D ( 'NONE', #20641, #9539, #32797 ) ;
#32998=FACE_OUTER_BOUND ( 'NONE', #50745, .T. ) ;
#33002=ORIENTED_EDGE ( 'NONE', *, *, #15920, .T. ) ;
#33006=ORIENTED_EDGE ( 'NONE', *, *, #12488, .F. ) ;
#33007=AXIS2_PLACEMENT_3D ( 'NONE', #46512, #18674, #11178 ) ;
#33010=CARTESIAN_POINT ( 'NONE',  ( 0.002207914879453961969, 5.905511811023623991, 0.04916304461325442243 ) ) ;
#33011=ADVANCED_FACE ( 'NONE', ( #21897 ), #26813, .T. ) ;
#33013=ORIENTED_EDGE ( 'NONE', *, *, #36178, .F. ) ;
#33014=DIRECTION ( 'NONE',  ( -0.000000000000000000, -1.000000000000000000, -0.000000000000000000 ) ) ;
#33016=ORIENTED_EDGE ( 'NONE', *, *, #437, .F. ) ;
#33017=LINE ( 'NONE', #13379, #20867 ) ;
#33022=CARTESIAN_POINT ( 'NONE',  ( -2.308557526972533136, 0.000000000000000000, 1.841013194464759639 ) ) ;
#33027=VERTEX_POINT ( 'NONE', #21135 ) ;
#33032=ADVANCED_FACE ( 'NONE', ( #22155 ), #31442, .T. ) ;
#33035=CARTESIAN_POINT ( 'NONE',  ( -1.325491792074585673, 1.205361022782829114E-17, -2.638988599164751481 ) ) ;
#33039=ORIENTED_EDGE ( 'NONE', *, *, #2924, .T. ) ;
#33043=CARTESIAN_POINT ( 'NONE',  ( -1.595649168949286434, 0.0008099078524815457591, -0.7355326111394984157 ) ) ;
#33044=AXIS2_PLACEMENT_3D ( 'NONE', #26300, #37935, #14683 ) ;
#33047=LINE ( 'NONE', #1784, #13677 ) ;
#33049=CARTESIAN_POINT ( 'NONE',  ( -1.675635838109289288, 1.648255178477637140, 1.399220266318809580 ) ) ;
#33050=EDGE_CURVE ( 'NONE', #42744, #47368, #20607, .T. ) ;
#33051=CARTESIAN_POINT ( 'NONE',  ( -1.442444474601640492, 0.004816277389180329341, -1.011116641508509995 ) ) ;
#33053=VERTEX_POINT ( 'NONE', #2528 ) ;
#33055=FACE_OUTER_BOUND ( 'NONE', #31262, .T. ) ;
#33058=B_SPLINE_CURVE_WITH_KNOTS ( 'NONE', 3,
 ( #48866, #25670, #2183, #32938 ),
 .UNSPECIFIED., .F., .F.,
 ( 4, 4 ),
 ( 2.623928897500769106E-05, 0.05045977204837132774 ),
 .UNSPECIFIED. ) ;
#33059=LINE ( 'NONE', #14179, #20436 ) ;
#33064=ORIENTED_EDGE ( 'NONE', *, *, #9372, .T. ) ;
#33065=ORIENTED_EDGE ( 'NONE', *, *, #32428, .T. ) ;
#33076=DIRECTION ( 'NONE',  ( 0.000000000000000000, 0.000000000000000000, -1.000000000000000000 ) ) ;
#33082=ADVANCED_FACE ( 'NONE', ( #25002 ), #18271, .F. ) ;
#33083=DIRECTION ( 'NONE',  ( 0.000000000000000000, 0.000000000000000000, -1.000000000000000000 ) ) ;
#33084=( BOUNDED_CURVE ( )  B_SPLINE_CURVE ( 3, ( #33833, #23141, #49515, #27003 ),
 .UNSPECIFIED., .F., .F. ) 
 B_SPLINE_CURVE_WITH_KNOTS ( ( 4, 4 ),
 ( 0.1232251794661485683, 0.1739699573040163205 ),
 .UNSPECIFIED. ) 
 CURVE ( )  GEOMETRIC_REPRESENTATION_ITEM ( )  RATIONAL_B_SPLINE_CURVE ( ( 1.000000000000000000, 0.9997854254717271072, 0.9997854254717271072, 1.000000000000000000 ) ) 
 REPRESENTATION_ITEM ( '' )  );
#33085=ADVANCED_FACE ( 'NONE', ( #2272 ), #1510, .F. ) ;
#33086=CARTESIAN_POINT ( 'NONE',  ( -1.711605288297850969, 0.0005051743623580321960, -0.3401845456954783464 ) ) ;
#33089=CARTESIAN_POINT ( 'NONE',  ( -1.733526556417524622, 0.000000000000000000, 0.1851600754179555941 ) ) ;
#33090=CARTESIAN_POINT ( 'NONE',  ( 1.461782879395302048, 1.205361022782829114E-17, -1.598346982901808211 ) ) ;
#33095=EDGE_LOOP ( 'NONE', ( #1015, #190, #38512, #20397 ) ) ;
#33098=EDGE_CURVE ( 'NONE', #37445, #41115, #43354, .T. ) ;
#33099=AXIS2_PLACEMENT_3D ( 'NONE', #28334, #44336, #20339 ) ;
#33100=VERTEX_POINT ( 'NONE', #41267 ) ;
#33101=VECTOR ( 'NONE', #39665, 39.37007874015748143 ) ;
#33109=VERTEX_POINT ( 'NONE', #11289 ) ;
#33114=CARTESIAN_POINT ( 'NONE',  ( 0.4788131938641112528, 1.726726173772622941, 2.914091152102192162 ) ) ;
#33116=VECTOR ( 'NONE', #25539, 39.37007874015748143 ) ;
#33117=CARTESIAN_POINT ( 'NONE',  ( 1.152568299495707826, 1.574803149606302854, 1.833124570921553120 ) ) ;
#33120=CARTESIAN_POINT ( 'NONE',  ( 1.033334490728470723, 1.724452693827607908, -2.032317711754626277 ) ) ;
#33121=CARTESIAN_POINT ( 'NONE',  ( 1.429001793727219249, 1.049866565067837820, -1.434352145109974996 ) ) ;
#33123=VERTEX_POINT ( 'NONE', #3034 ) ;
#33127=ORIENTED_EDGE ( 'NONE', *, *, #43700, .F. ) ;
#33131=LINE ( 'NONE', #49329, #27178 ) ;
#33134=DIRECTION ( 'NONE',  ( 0.000000000000000000, 0.000000000000000000, -1.000000000000000000 ) ) ;
#33137=CARTESIAN_POINT ( 'NONE',  ( -2.867773316779185677, 1.574658946938755522, -0.7050287376752426560 ) ) ;
#33150=EDGE_CURVE ( 'NONE', #45728, #6369, #30147, .T. ) ;
#33156=ORIENTED_EDGE ( 'NONE', *, *, #23913, .T. ) ;
#33157=CARTESIAN_POINT ( 'NONE',  ( 0.8329809839909849689, 1.496921813388997435, -2.833254665166554442 ) ) ;
#33160=CARTESIAN_POINT ( 'NONE',  ( -2.158043018693463377, 1.574915981856324310, -0.1812028363557288968 ) ) ;
#33162=EDGE_CURVE ( 'NONE', #11634, #22597, #6443, .T. ) ;
#33163=ORIENTED_EDGE ( 'NONE', *, *, #17885, .T. ) ;
#33168=FACE_OUTER_BOUND ( 'NONE', #47482, .T. ) ;
#33169=CARTESIAN_POINT ( 'NONE',  ( -0.2430652128771645382, 1.574803149606302854, -2.151668812760861194 ) ) ;
#33180=ORIENTED_EDGE ( 'NONE', *, *, #9595, .T. ) ;
#33181=CONICAL_SURFACE ( 'NONE', #39750, 2.165354330708661568, 0.2617993877991570129 ) ;
#33182=ORIENTED_EDGE ( 'NONE', *, *, #31810, .F. ) ;
#33186=EDGE_LOOP ( 'NONE', ( #44285, #28765, #37369, #28620, #20621, #25486, #11144, #16326, #18364, #6910, #12993, #19827, #12954 ) ) ;
#33192=ORIENTED_EDGE ( 'NONE', *, *, #49291, .F. ) ;
#33193=VECTOR ( 'NONE', #21872, 39.37007874015748143 ) ;
#33202=CARTESIAN_POINT ( 'NONE',  ( 2.339241080213586343, 1.205361022782829114E-17, 1.802537235681917815 ) ) ;
#33203=CARTESIAN_POINT ( 'NONE',  ( -2.576863348864732117, 1.679095609600309347, 1.442554885838411849 ) ) ;
#33207=DIRECTION ( 'NONE',  ( 0.01601477604151182663, -0.9998717552508123996, 0.000000000000000000 ) ) ;
#33208=ORIENTED_EDGE ( 'NONE', *, *, #28167, .F. ) ;
#33211=CARTESIAN_POINT ( 'NONE',  ( 0.000000000000000000, 5.905511811023623991, 0.000000000000000000 ) ) ;
#33212=EDGE_CURVE ( 'NONE', #34644, #16311, #6905, .T. ) ;
#33224=VECTOR ( 'NONE', #32262, 39.37007874015748143 ) ;
#33228=CARTESIAN_POINT ( 'NONE',  ( -1.883550378546958282, 6.692913385826772199, -1.069467267250447495 ) ) ;
#33229=CIRCLE ( 'NONE', #10953, 1.743387098533651480 ) ;
#33230=VECTOR ( 'NONE', #9655, 39.37007874015748143 ) ;
#33231=FACE_OUTER_BOUND ( 'NONE', #23042, .T. ) ;
#33234=ORIENTED_EDGE ( 'NONE', *, *, #5812, .T. ) ;
#33237=VERTEX_POINT ( 'NONE', #38661 ) ;
#33238=EDGE_CURVE ( 'NONE', #22637, #22707, #34782, .T. ) ;
#33239=CARTESIAN_POINT ( 'NONE',  ( 1.602753508900452317, 0.000000000000000000, 1.341098548255033496 ) ) ;
#33241=CARTESIAN_POINT ( 'NONE',  ( 0.000000000000000000, 6.692913385826772199, 0.000000000000000000 ) ) ;
#33244=CARTESIAN_POINT ( 'NONE',  ( -1.833791099076586217, 1.574803149606302854, -1.151507526013721083 ) ) ;
#33247=ORIENTED_EDGE ( 'NONE', *, *, #15716, .T. ) ;
#33248=VERTEX_POINT ( 'NONE', #30909 ) ;
#33253=CIRCLE ( 'NONE', #29097, 1.850107469027523432 ) ;
#33256=ORIENTED_EDGE ( 'NONE', *, *, #36243, .T. ) ;
#33259=CIRCLE ( 'NONE', #1924, 2.164630168518208109 ) ;
#33261=VERTEX_POINT ( 'NONE', #7916 ) ;
#33263=DIRECTION ( 'NONE',  ( 0.01601477604151182663, -0.9998717552508123996, 0.000000000000000000 ) ) ;
#33265=ORIENTED_EDGE ( 'NONE', *, *, #50747, .T. ) ;
#33271=EDGE_CURVE ( 'NONE', #38725, #42469, #9553, .T. ) ;
#33272=CARTESIAN_POINT ( 'NONE',  ( 0.8004649005966348874, 0.000000000000000000, -1.548759025234849762 ) ) ;
#33275=CARTESIAN_POINT ( 'NONE',  ( -1.834323595590334977, 1.205361022782829114E-17, 1.151859023884900690 ) ) ;
#33283=LINE ( 'NONE', #1264, #9727 ) ;
#33284=DIRECTION ( 'NONE',  ( 9.964307797194585150E-17, -1.000000000000000000, 5.953396763000637613E-17 ) ) ;
#33287=VERTEX_POINT ( 'NONE', #20560 ) ;
#33296=ORIENTED_EDGE ( 'NONE', *, *, #43979, .F. ) ;
#33297=CONICAL_SURFACE ( 'NONE', #25874, 3.033577403570480779, 1.554780866114618743 ) ;
#33301=EDGE_CURVE ( 'NONE', #36015, #13127, #16439, .T. ) ;
#33302=DIRECTION ( 'NONE',  ( -0.1785568947986370392, 0.000000000000000000, 0.9839295885986295565 ) ) ;
#33310=ORIENTED_EDGE ( 'NONE', *, *, #27811, .T. ) ;
#33313=CARTESIAN_POINT ( 'NONE',  ( 0.4910466871075136464, 1.049866565067837820, -1.964251855984342265 ) ) ;
#33317=DIRECTION ( 'NONE',  ( -2.582876339026340310E-17, -1.000000000000000000, 1.131632063491650798E-16 ) ) ;
#33326=CARTESIAN_POINT ( 'NONE',  ( 0.08139965876239094178, 1.610780518492231694, 0.000000000000000000 ) ) ;
#33332=AXIS2_PLACEMENT_3D ( 'NONE', #48248, #17564, #49011 ) ;
#33336=VECTOR ( 'NONE', #28108, 39.37007874015748143 ) ;
#33337=DIRECTION ( 'NONE',  ( -0.000000000000000000, 1.000000000000000000, -0.000000000000000000 ) ) ;
#33338=EDGE_CURVE ( 'NONE', #28752, #2720, #43778, .T. ) ;
#33342=EDGE_CURVE ( 'NONE', #33109, #28267, #2783, .T. ) ;
#33345=EDGE_LOOP ( 'NONE', ( #47748, #46035, #12701, #31205 ) ) ;
#33348=ORIENTED_EDGE ( 'NONE', *, *, #25745, .T. ) ;
#33351=CARTESIAN_POINT ( 'NONE',  ( -2.100227814008681637, 1.559371130916006543, -2.076109931251943319 ) ) ;
#33352=VERTEX_POINT ( 'NONE', #39411 ) ;
#33353=VERTEX_POINT ( 'NONE', #32450 ) ;
#33354=CARTESIAN_POINT ( 'NONE',  ( 2.012389709219288836, 1.049866565067838264, 0.2229346560889621798 ) ) ;
#33363=VECTOR ( 'NONE', #3976, 39.37007874015748143 ) ;
#33380=FACE_OUTER_BOUND ( 'NONE', #27239, .T. ) ;
#33386=( NAMED_UNIT ( * ) PLANE_ANGLE_UNIT ( ) SI_UNIT ( $, .RADIAN. ) );
#33389=ADVANCED_FACE ( 'NONE', ( #37083 ), #49412, .F. ) ;
#33391=B_SPLINE_CURVE_WITH_KNOTS ( 'NONE', 3,
 ( #38384, #21614, #37374, #45332 ),
 .UNSPECIFIED., .F., .F.,
 ( 4, 4 ),
 ( 2.032896518363797548E-07, 0.002500497254889573386 ),
 .UNSPECIFIED. ) ;
#33392=ORIENTED_EDGE ( 'NONE', *, *, #29490, .F. ) ;
#33394=CARTESIAN_POINT ( 'NONE',  ( 0.000000000000000000, 1.574803149606302854, 0.000000000000000000 ) ) ;
#33397=CARTESIAN_POINT ( 'NONE',  ( -0.3381173457103609503, 6.692913385826772199, 2.138793126519845877 ) ) ;
#33401=CARTESIAN_POINT ( 'NONE',  ( 0.4001787029124908024, 1.205361022782829114E-17, 1.929553426015793605 ) ) ;
#33402=CARTESIAN_POINT ( 'NONE',  ( 0.1525302393087137887, 1.710345001767278994, -2.243756654240526505 ) ) ;
#33409=CARTESIAN_POINT ( 'NONE',  ( -1.232995795418201590, 5.905511811023623991, 1.780798594093551568 ) ) ;
#33412=CARTESIAN_POINT ( 'NONE',  ( 2.100227814008712723, 5.905511811023623991, -2.076109931251913565 ) ) ;
#33415=EDGE_LOOP ( 'NONE', ( #25036, #11902, #20698, #41665 ) ) ;
#33417=DIRECTION ( 'NONE',  ( -0.000000000000000000, -1.000000000000000000, -0.000000000000000000 ) ) ;
#33419=ORIENTED_EDGE ( 'NONE', *, *, #50223, .T. ) ;
#33420=LINE ( 'NONE', #32911, #27961 ) ;
#33423=CARTESIAN_POINT ( 'NONE',  ( -1.070574558570679624, 1.033102224082122600, -2.336494445557213862 ) ) ;
#33427=DIRECTION ( 'NONE',  ( 0.000000000000000000, 1.000000000000000000, 0.000000000000000000 ) ) ;
#33430=PLANE ( 'NONE',  #46299 ) ;
#33432=ORIENTED_EDGE ( 'NONE', *, *, #23139, .F. ) ;
#33437=ORIENTED_EDGE ( 'NONE', *, *, #32205, .F. ) ;
#33439=DIRECTION ( 'NONE',  ( -0.9998717552508122886, -0.01601477604151180928, 0.000000000000000000 ) ) ;
#33443=CARTESIAN_POINT ( 'NONE',  ( -2.139020239325885253, 1.673641627049041514, 0.3394120305351381872 ) ) ;
#33448=CIRCLE ( 'NONE', #16096, 1.743387098533651480 ) ;
#33449=CARTESIAN_POINT ( 'NONE',  ( 0.5433756366131596849, 1.629269058362078804, 2.902374796143934343 ) ) ;
#33454=CARTESIAN_POINT ( 'NONE',  ( 2.889674983507178219, 5.118110236220475784, -0.6090712660037604920 ) ) ;
#33455=AXIS2_PLACEMENT_3D ( 'NONE', #44941, #33611, #2100 ) ;
#33456=ORIENTED_EDGE ( 'NONE', *, *, #14637, .T. ) ;
#33458=CARTESIAN_POINT ( 'NONE',  ( 2.600183657057280051, 0.000000000000000000, 1.399218491554161892 ) ) ;
#33462=CARTESIAN_POINT ( 'NONE',  ( 0.1067246931122726866, 0.02962905676920215767, 0.000000000000000000 ) ) ;
#33466=B_SPLINE_CURVE_WITH_KNOTS ( 'NONE', 3,
 ( #49009, #13436, #41561, #18076 ),
 .UNSPECIFIED., .F., .F.,
 ( 4, 4 ),
 ( 2.174732542326846088E-07, 0.002500292828914785648 ),
 .UNSPECIFIED. ) ;
#33469=LINE ( 'NONE', #21326, #13833 ) ;
#33470=VERTEX_POINT ( 'NONE', #40696 ) ;
#33474=VERTEX_POINT ( 'NONE', #1448 ) ;
#33479=CARTESIAN_POINT ( 'NONE',  ( -1.874262219842892208, 0.5253178361172772259, 1.064469095918958219 ) ) ;
#33484=EDGE_LOOP ( 'NONE', ( #22170, #32349, #7462, #31695 ) ) ;
#33490=AXIS2_PLACEMENT_3D ( 'NONE', #39504, #20389, #40277 ) ;
#33493=VERTEX_POINT ( 'NONE', #48644 ) ;
#33494=CARTESIAN_POINT ( 'NONE',  ( 1.083598637574782142, 1.637691314537677023, 2.747180975113346246 ) ) ;
#33499=ORIENTED_EDGE ( 'NONE', *, *, #8003, .F. ) ;
#33502=EDGE_CURVE ( 'NONE', #20098, #50692, #23614, .T. ) ;
#33503=ORIENTED_EDGE ( 'NONE', *, *, #1965, .F. ) ;
#33506=ORIENTED_EDGE ( 'NONE', *, *, #2852, .F. ) ;
#33508=EDGE_CURVE ( 'NONE', #6857, #26498, #200, .T. ) ;
#33511=VERTEX_POINT ( 'NONE', #26461 ) ;
#33514=CIRCLE ( 'NONE', #7910, 2.165354330708661568 ) ;
#33517=AXIS2_PLACEMENT_3D ( 'NONE', #35694, #32090, #31830 ) ;
#33518=DIRECTION ( 'NONE',  ( 0.000000000000000000, 0.000000000000000000, -1.000000000000000000 ) ) ;
#33520=CIRCLE ( 'NONE', #46623, 2.165354330708661568 ) ;
#33522=ORIENTED_EDGE ( 'NONE', *, *, #21574, .F. ) ;
#33523=CIRCLE ( 'NONE', #6320, 2.244934639244525076 ) ;
#33524=CARTESIAN_POINT ( 'NONE',  ( 1.129748414438405124, 1.627571742414081202, 1.986830176535870907 ) ) ;
#33525=DIRECTION ( 'NONE',  ( -0.9998717552508122886, -0.01601477604151185785, 0.000000000000000000 ) ) ;
#33527=CARTESIAN_POINT ( 'NONE',  ( 2.951990591674675368, 0.000000000000000000, -0.08331184815398383348 ) ) ;
#33528=DIRECTION ( 'NONE',  ( -0.000000000000000000, 1.000000000000000000, -0.000000000000000000 ) ) ;
#33532=CARTESIAN_POINT ( 'NONE',  ( 0.7229485578905374688, 0.02618475911999341987, 1.786232274300230571 ) ) ;
#33537=VERTEX_POINT ( 'NONE', #6848 ) ;
#33539=ORIENTED_EDGE ( 'NONE', *, *, #10298, .F. ) ;
#33541=CARTESIAN_POINT ( 'NONE',  ( -2.298329623281018641, 1.584999146155742444, 1.853838580031352823 ) ) ;
#33542=CARTESIAN_POINT ( 'NONE',  ( -0.4910466871652391374, 1.049866565877818347, -1.964251856193615531 ) ) ;
#33543=CARTESIAN_POINT ( 'NONE',  ( -1.955085917952581909, 1.590347576141469377, 2.212843326005696554 ) ) ;
#33546=ORIENTED_EDGE ( 'NONE', *, *, #2852, .T. ) ;
#33554=LINE ( 'NONE', #18297, #13936 ) ;
#33558=CIRCLE ( 'NONE', #21976, 2.244934639244525076 ) ;
#33559=CARTESIAN_POINT ( 'NONE',  ( 2.034508859078114629, 0.01953464615435679050, -0.4138851785833215224 ) ) ;
#33564=ORIENTED_EDGE ( 'NONE', *, *, #50899, .T. ) ;
#33565=CARTESIAN_POINT ( 'NONE',  ( 0.08139965876239094178, 1.610780518492231694, 0.000000000000000000 ) ) ;
#33572=EDGE_CURVE ( 'NONE', #11612, #45138, #22595, .T. ) ;
#33579=ORIENTED_EDGE ( 'NONE', *, *, #30566, .T. ) ;
#33581=DIRECTION ( 'NONE',  ( -2.309260482754916270E-14, 0.000000000000000000, 1.000000000000000000 ) ) ;
#33583=CONICAL_SURFACE ( 'NONE', #17902, 2.165354330708661568, 0.2617993877991570129 ) ;
#33584=CARTESIAN_POINT ( 'NONE',  ( -2.623503965249869729, 1.569838463031876685, 1.355882097269834885 ) ) ;
#33586=VERTEX_POINT ( 'NONE', #10471 ) ;
#33587=ORIENTED_EDGE ( 'NONE', *, *, #18461, .F. ) ;
#33588=DIRECTION ( 'NONE',  ( 0.01601477604151182663, -0.9998717552508123996, 0.000000000000000000 ) ) ;
#33589=AXIS2_PLACEMENT_3D ( 'NONE', #32703, #24429, #20020 ) ;
#33594=DIRECTION ( 'NONE',  ( -0.9998717552508122886, -0.01601477604151180928, 0.000000000000000000 ) ) ;
#33595=CARTESIAN_POINT ( 'NONE',  ( 1.979793062125284830, 1.470624965921384364, 2.191257344206569257 ) ) ;
#33600=DIRECTION ( 'NONE',  ( -0.01601477604151182663, 0.9998717552508123996, -0.000000000000000000 ) ) ;
#33610=VERTEX_POINT ( 'NONE', #50165 ) ;
#33611=DIRECTION ( 'NONE',  ( 0.9959742939952384022, -1.160734090543304907E-16, 0.08963930890344089242 ) ) ;
#33612=CARTESIAN_POINT ( 'NONE',  ( 1.584529175505357212, 0.03508075509535489578, 1.200674575404337086 ) ) ;
#33617=CARTESIAN_POINT ( 'NONE',  ( 0.000000000000000000, 1.574803149606302854, 0.000000000000000000 ) ) ;
#33622=FACE_OUTER_BOUND ( 'NONE', #17504, .T. ) ;
#33625=CARTESIAN_POINT ( 'NONE',  ( -0.8949303405208606232, 5.905511811023623991, -1.971765468592543424 ) ) ;
#33627=LINE ( 'NONE', #25861, #35218 ) ;
#33630=DIRECTION ( 'NONE',  ( -0.9998717552508122886, -0.01601477604151181275, 0.000000000000000000 ) ) ;
#33635=CIRCLE ( 'NONE', #11353, 1.743387098533651480 ) ;
#33636=B_SPLINE_CURVE_WITH_KNOTS ( 'NONE', 3,
 ( #26579, #50277, #3853, #35354 ),
 .UNSPECIFIED., .F., .F.,
 ( 4, 4 ),
 ( 2.051444212662578114E-07, 0.002500220176209435544 ),
 .UNSPECIFIED. ) ;
#33637=CARTESIAN_POINT ( 'NONE',  ( -1.598711713507983578, 5.905511811023623991, -1.460438370699401522 ) ) ;
#33639=CARTESIAN_POINT ( 'NONE',  ( 0.000000000000000000, 1.574803149606302854, 0.000000000000000000 ) ) ;
#33640=ORIENTED_EDGE ( 'NONE', *, *, #24879, .F. ) ;
#33642=CARTESIAN_POINT ( 'NONE',  ( -0.4532322590609024759, 0.000000000000000000, -1.827234353172969561 ) ) ;
#33647=VECTOR ( 'NONE', #37154, 39.37007874015748143 ) ;
#33649=CARTESIAN_POINT ( 'NONE',  ( -0.8067290215918269114, 6.692913385826772199, 2.009464521518169899 ) ) ;
#33653=CARTESIAN_POINT ( 'NONE',  ( 1.215807329263347114, 1.628950133432788494, 1.938968878379255578 ) ) ;
#33661=ADVANCED_FACE ( 'NONE', ( #15604 ), #8412, .T. ) ;
#33662=CARTESIAN_POINT ( 'NONE',  ( 1.695772546416037363, 1.477242674555747426, -2.417756147381349141 ) ) ;
#33664=EDGE_LOOP ( 'NONE', ( #11361, #49014, #6452, #22362 ) ) ;
#33665=EDGE_CURVE ( 'NONE', #19894, #17400, #7858, .T. ) ;
#33666=AXIS2_PLACEMENT_3D ( 'NONE', #43313, #15958, #50760 ) ;
#33667=CARTESIAN_POINT ( 'NONE',  ( 2.919426793319799707, 5.905511811023623991, 0.4451252810446827413 ) ) ;
#33671=CARTESIAN_POINT ( 'NONE',  ( -2.151809081513409438, 6.692913385826772199, 0.2418202932658334581 ) ) ;
#33672=CARTESIAN_POINT ( 'NONE',  ( 1.008242765982022782, 0.5249316475426860640, 1.591564316133513568 ) ) ;
#33675=CARTESIAN_POINT ( 'NONE',  ( 2.932638728931774352, 5.905511811023623991, 0.3475908556738230293 ) ) ;
#33680=CARTESIAN_POINT ( 'NONE',  ( 1.202103465198962384, 0.5249316497054294928, 1.450716274357264135 ) ) ;
#33683=CARTESIAN_POINT ( 'NONE',  ( -1.416899275789439194, 0.001784216570024398704, 1.066994191199830633 ) ) ;
#33685=ORIENTED_EDGE ( 'NONE', *, *, #45074, .F. ) ;
#33692=CARTESIAN_POINT ( 'NONE',  ( -1.738955188402737440, 0.000000000000000000, -0.1273587697465547175 ) ) ;
#33693=CARTESIAN_POINT ( 'NONE',  ( 0.5756566573088583993, 1.728235332270611879, 2.896516654582643291 ) ) ;
#33696=ADVANCED_FACE ( 'NONE', ( #12491 ), #50910, .T. ) ;
#33697=VERTEX_POINT ( 'NONE', #11724 ) ;
#33698=CARTESIAN_POINT ( 'NONE',  ( 0.08119777152254364916, 1.623385212329073957, 0.000000000000000000 ) ) ;
#33699=CARTESIAN_POINT ( 'NONE',  ( 0.000000000000000000, 0.000000000000000000, 0.000000000000000000 ) ) ;
#33703=VERTEX_POINT ( 'NONE', #23856 ) ;
#33704=AXIS2_PLACEMENT_3D ( 'NONE', #41940, #22326, #18449 ) ;
#33707=DIRECTION ( 'NONE',  ( 0.000000000000000000, 0.000000000000000000, -1.000000000000000000 ) ) ;
#33711=CARTESIAN_POINT ( 'NONE',  ( 0.3381173457103291979, 1.574803149606302854, 2.138793126519850762 ) ) ;
#33717=DIRECTION ( 'NONE',  ( 0.000000000000000000, 0.000000000000000000, 1.000000000000000000 ) ) ;
#33722=CARTESIAN_POINT ( 'NONE',  ( -0.2430652128771642606, 5.905511811023623991, -2.151668812760861638 ) ) ;
#33724=CARTESIAN_POINT ( 'NONE',  ( -1.598711713507983578, 6.692913385826772199, -1.460438370699401966 ) ) ;
#33726=ORIENTED_EDGE ( 'NONE', *, *, #9783, .T. ) ;
#33729=CARTESIAN_POINT ( 'NONE',  ( 1.090138530625467839, 6.692913385826772199, 1.920534397867778020 ) ) ;
#33732=EDGE_CURVE ( 'NONE', #30403, #24144, #6984, .T. ) ;
#33734=ADVANCED_FACE ( 'NONE', ( #24111 ), #40120, .T. ) ;
#33740=CARTESIAN_POINT ( 'NONE',  ( 2.319222573356612749, 1.745048544795088308, -0.1534186080535354380 ) ) ;
#33742=VECTOR ( 'NONE', #46642, 39.37007874015748143 ) ;
#33748=CARTESIAN_POINT ( 'NONE',  ( -1.088355899089957335, 1.624853143508943942, 1.917550775237487848 ) ) ;
#33751=DIRECTION ( 'NONE',  ( 0.000000000000000000, 0.000000000000000000, -1.000000000000000000 ) ) ;
#33754=EDGE_CURVE ( 'NONE', #28752, #7505, #32127, .T. ) ;
#33756=DIRECTION ( 'NONE',  ( 0.8805955318567321166, 0.000000000000000000, 0.4738686624730094055 ) ) ;
#33757=EDGE_CURVE ( 'NONE', #43500, #36035, #20515, .T. ) ;
#33758=CARTESIAN_POINT ( 'NONE',  ( 2.437180031585944207, 1.757239404341893518, -1.667735833703099191 ) ) ;
#33760=EDGE_CURVE ( 'NONE', #34134, #48339, #25452, .T. ) ;
#33765=ORIENTED_EDGE ( 'NONE', *, *, #11327, .T. ) ;
#33770=CARTESIAN_POINT ( 'NONE',  ( 0.08139965876239094178, 1.610780518492231694, 0.000000000000000000 ) ) ;
#33773=B_SPLINE_CURVE_WITH_KNOTS ( 'NONE', 3,
 ( #19077, #46420, #39467, #42821 ),
 .UNSPECIFIED., .F., .F.,
 ( 4, 4 ),
 ( 2.034152094176694738E-07, 0.002500799499442713479 ),
 .UNSPECIFIED. ) ;
#33778=DIRECTION ( 'NONE',  ( 0.000000000000000000, 0.000000000000000000, -1.000000000000000000 ) ) ;
#33782=CARTESIAN_POINT ( 'NONE',  ( -1.530693736245496206, 6.692913385826772199, -1.531579597454065800 ) ) ;
#33790=ORIENTED_EDGE ( 'NONE', *, *, #31555, .F. ) ;
#33791=CARTESIAN_POINT ( 'NONE',  ( -0.5304089168012655620, 0.01942419597810423823, -1.736909402037482675 ) ) ;
#33792=EDGE_CURVE ( 'NONE', #50444, #24086, #5003, .T. ) ;
#33793=EDGE_LOOP ( 'NONE', ( #5031, #32614, #33296, #15305, #19175, #31163, #37049, #29035, #47001, #17887, #10981 ) ) ;
#33794=CARTESIAN_POINT ( 'NONE',  ( -1.109766902767011398, 1.694103061027446788, -2.191031250744368553 ) ) ;
#33802=CARTESIAN_POINT ( 'NONE',  ( -2.867773316779185677, 1.576133919414932638, -0.7050287376752426560 ) ) ;
#33803=ORIENTED_EDGE ( 'NONE', *, *, #49969, .F. ) ;
#33804=VERTEX_POINT ( 'NONE', #41394 ) ;
#33806=VERTEX_POINT ( 'NONE', #33412 ) ;
#33811=LINE ( 'NONE', #29918, #26424 ) ;
#33812=EDGE_CURVE ( 'NONE', #18870, #49731, #48583, .T. ) ;
#33818=DIRECTION ( 'NONE',  ( -0.1342332658176522420, 0.000000000000000000, -0.9909497617679352555 ) ) ;
#33821=AXIS2_PLACEMENT_3D ( 'NONE', #35175, #7805, #12438 ) ;
#33822=DIRECTION ( 'NONE',  ( -0.000000000000000000, 1.000000000000000000, 0.000000000000000000 ) ) ;
#33824=ORIENTED_EDGE ( 'NONE', *, *, #45541, .T. ) ;
#33827=DIRECTION ( 'NONE',  ( 0.000000000000000000, 0.000000000000000000, -1.000000000000000000 ) ) ;
#33829=ORIENTED_EDGE ( 'NONE', *, *, #20311, .T. ) ;
#33830=EDGE_LOOP ( 'NONE', ( #20864, #11994, #50589, #13215 ) ) ;
#33833=CARTESIAN_POINT ( 'NONE',  ( 2.126910391174609671, 1.205361022782829114E-17, 0.2384475364948296372 ) ) ;
#33835=B_SPLINE_CURVE_WITH_KNOTS ( 'NONE', 3,
 ( #44619, #40772, #16513, #44115 ),
 .UNSPECIFIED., .F., .F.,
 ( 4, 4 ),
 ( 2.136435329377818075E-07, 0.002500479846613039119 ),
 .UNSPECIFIED. ) ;
#33836=ORIENTED_EDGE ( 'NONE', *, *, #42206, .T. ) ;
#33839=DIRECTION ( 'NONE',  ( -0.000000000000000000, 1.000000000000000000, -0.000000000000000000 ) ) ;
#33841=CARTESIAN_POINT ( 'NONE',  ( -0.4460728916448887249, 1.700757277111965449, 2.182451250484750638 ) ) ;
#33846=CARTESIAN_POINT ( 'NONE',  ( 0.8329809839909850799, 1.732245219823249638, -2.833254665166554442 ) ) ;
#33859=B_SPLINE_CURVE_WITH_KNOTS ( 'NONE', 3,
 ( #37665, #41275, #40764, #1520 ),
 .UNSPECIFIED., .F., .F.,
 ( 4, 4 ),
 ( 6.511653002970408202E-07, 0.004414110768476271068 ),
 .UNSPECIFIED. ) ;
#33870=EDGE_LOOP ( 'NONE', ( #33002, #6744, #12693, #42938 ) ) ;
#33873=CARTESIAN_POINT ( 'NONE',  ( -1.977157105026591699, 1.676234161373136189, -0.8985969286390745880 ) ) ;
#33874=DIRECTION ( 'NONE',  ( 0.000000000000000000, 0.000000000000000000, -1.000000000000000000 ) ) ;
#33875=CARTESIAN_POINT ( 'NONE',  ( -1.383870272338435070, 0.000000000000000000, 1.124517572066690452 ) ) ;
#33876=CARTESIAN_POINT ( 'NONE',  ( 0.8291286199751974895, 1.205361022782829114E-17, -1.835126787948130556 ) ) ;
#33877=CIRCLE ( 'NONE', #10756, 2.165354330708661568 ) ;
#33878=ORIENTED_EDGE ( 'NONE', *, *, #20764, .T. ) ;
#33880=CARTESIAN_POINT ( 'NONE',  ( -1.661821349926435376, 6.692913385826772199, 1.388203579611951621 ) ) ;
#33882=ORIENTED_EDGE ( 'NONE', *, *, #47886, .F. ) ;
#33891=DIRECTION ( 'NONE',  ( 0.9998717552508121775, 0.01601477604151182663, 0.000000000000000000 ) ) ;
#33896=ORIENTED_EDGE ( 'NONE', *, *, #35053, .F. ) ;
#33903=DIRECTION ( 'NONE',  ( -0.000000000000000000, -1.000000000000000000, 0.000000000000000000 ) ) ;
#33907=AXIS2_PLACEMENT_3D ( 'NONE', #14463, #2338, #33594 ) ;
#33911=DIRECTION ( 'NONE',  ( 8.882339915255740720E-16, 0.000000000000000000, 1.000000000000000000 ) ) ;
#33915=ADVANCED_FACE ( 'NONE', ( #17642 ), #47093, .T. ) ;
#33916=DIRECTION ( 'NONE',  ( 0.8090169943749422332, 0.000000000000000000, 0.5877852522924802425 ) ) ;
#33924=DIRECTION ( 'NONE',  ( -0.8805955318567321166, 0.000000000000000000, -0.4738686624730094055 ) ) ;
#33929=DIRECTION ( 'NONE',  ( 0.000000000000000000, 0.000000000000000000, 1.000000000000000000 ) ) ;
#33930=DIRECTION ( 'NONE',  ( 0.000000000000000000, 0.000000000000000000, -1.000000000000000000 ) ) ;
#33935=ORIENTED_EDGE ( 'NONE', *, *, #47020, .T. ) ;
#33936=EDGE_LOOP ( 'NONE', ( #38024, #6994, #45365, #36068, #29527, #13724 ) ) ;
#33938=LINE ( 'NONE', #17420, #31578 ) ;
#33942=DIRECTION ( 'NONE',  ( -0.9998717552508122886, -0.01601477604151185785, 0.000000000000000000 ) ) ;
#33944=ORIENTED_EDGE ( 'NONE', *, *, #24865, .T. ) ;
#33949=CARTESIAN_POINT ( 'NONE',  ( 0.6233543567505470673, 5.905511811023623991, -2.073689640095371267 ) ) ;
#33955=CARTESIAN_POINT ( 'NONE',  ( 1.583112249919723213, 0.000000000000000000, -0.7301740747847023094 ) ) ;
#33956=PLANE ( 'NONE',  #5713 ) ;
#33958=AXIS2_PLACEMENT_3D ( 'NONE', #37040, #13287, #49114 ) ;
#33959=EDGE_CURVE ( 'NONE', #7103, #21112, #141, .T. ) ;
#33960=VECTOR ( 'NONE', #25292, 39.37007874015748143 ) ;
#33967=CARTESIAN_POINT ( 'NONE',  ( -1.661616293559047497, 0.000000000000000000, 0.5571161510599360600 ) ) ;
#33970=FACE_BOUND ( 'NONE', #8321, .T. ) ;
#33976=VERTEX_POINT ( 'NONE', #26649 ) ;
#33981=CARTESIAN_POINT ( 'NONE',  ( 0.000000000000000000, 1.574803149606302854, 0.000000000000000000 ) ) ;
#33984=VERTEX_POINT ( 'NONE', #34411 ) ;
#33986=DIRECTION ( 'NONE',  ( 0.2225209339563041788, 0.000000000000000000, 0.9749279121818259508 ) ) ;
#33987=CONICAL_SURFACE ( 'NONE', #10855, 2.244934639244524632, 1.554780866114618743 ) ;
#33990=DIRECTION ( 'NONE',  ( -0.5128992774059071280, 0.000000000000000000, 0.8584487936018655452 ) ) ;
#33991=CIRCLE ( 'NONE', #11712, 2.244934639244525076 ) ;
#33993=ORIENTED_EDGE ( 'NONE', *, *, #10201, .T. ) ;
#33997=ORIENTED_EDGE ( 'NONE', *, *, #36738, .F. ) ;
#33998=FACE_OUTER_BOUND ( 'NONE', #40716, .T. ) ;
#33999=VECTOR ( 'NONE', #25327, 39.37007874015748143 ) ;
#34005=DIRECTION ( 'NONE',  ( 1.283101021437939896E-16, 1.000000000000000000, -1.154811821032073265E-17 ) ) ;
#34008=EDGE_CURVE ( 'NONE', #38652, #22332, #49559, .T. ) ;
#34010=EDGE_CURVE ( 'NONE', #38070, #6857, #29748, .T. ) ;
#34013=CARTESIAN_POINT ( 'NONE',  ( 0.2156685157584260770, 1.624173731825095723, -2.945280361644574185 ) ) ;
#34016=DIRECTION ( 'NONE',  ( -3.986037398843765983E-20, -1.000000000000000000, -1.160734090543304660E-16 ) ) ;
#34017=CIRCLE ( 'NONE', #20814, 2.165354330708661568 ) ;
#34018=CARTESIAN_POINT ( 'NONE',  ( 2.491402175429654253, 0.000000000000000000, -1.585592796919505831 ) ) ;
#34021=CARTESIAN_POINT ( 'NONE',  ( 1.905671854841463952, 1.748959039950288341, 2.256015092822681645 ) ) ;
#34022=ORIENTED_EDGE ( 'NONE', *, *, #21569, .T. ) ;
#34033=CARTESIAN_POINT ( 'NONE',  ( -1.740398808985498258, 1.907947403895145864E-05, 0.1027251841395684928 ) ) ;
#34036=EDGE_CURVE ( 'NONE', #49090, #19294, #38538, .T. ) ;
#34037=CARTESIAN_POINT ( 'NONE',  ( -2.122091976112999490, 1.205361022782829114E-17, 0.4338754535132819390 ) ) ;
#34040=ADVANCED_FACE ( 'NONE', ( #8558 ), #48753, .T. ) ;
#34045=CARTESIAN_POINT ( 'NONE',  ( 0.2508718039770792552, 1.711920121901901348, -2.238407143905190910 ) ) ;
#34049=ORIENTED_EDGE ( 'NONE', *, *, #37160, .T. ) ;
#34051=CARTESIAN_POINT ( 'NONE',  ( -1.650279682448762886, 0.0005104048319611981764, 0.5879535613212861778 ) ) ;
#34052=ORIENTED_EDGE ( 'NONE', *, *, #8616, .T. ) ;
#34056=DIRECTION ( 'NONE',  ( -3.981026654148454344E-17, 1.000000000000000000, -1.225234019452869602E-16 ) ) ;
#34059=DIRECTION ( 'NONE',  ( -0.7227948638273978821, -8.018518666443169432E-17, 0.6910626489868580968 ) ) ;
#34060=ORIENTED_EDGE ( 'NONE', *, *, #18048, .T. ) ;
#34068=CARTESIAN_POINT ( 'NONE',  ( -0.5404877333192481537, 0.006475226164817101532, -1.773429173509019297 ) ) ;
#34069=EDGE_CURVE ( 'NONE', #33511, #2264, #4279, .T. ) ;
#34074=AXIS2_PLACEMENT_3D ( 'NONE', #48387, #13075, #44296 ) ;
#34075=CARTESIAN_POINT ( 'NONE',  ( -1.405664884363581502, 1.586962458333645021, 1.683711065981816857 ) ) ;
#34076=ORIENTED_EDGE ( 'NONE', *, *, #24693, .T. ) ;
#34078=ORIENTED_EDGE ( 'NONE', *, *, #2397, .F. ) ;
#34085=DIRECTION ( 'NONE',  ( -0.000000000000000000, -1.000000000000000000, -0.000000000000000000 ) ) ;
#34094=EDGE_CURVE ( 'NONE', #11610, #24163, #3319, .T. ) ;
#34096=ORIENTED_EDGE ( 'NONE', *, *, #34131, .F. ) ;
#34097=CARTESIAN_POINT ( 'NONE',  ( 2.947574761915768171, 2.755905511811027164, -0.1816379373804909991 ) ) ;
#34101=ORIENTED_EDGE ( 'NONE', *, *, #11410, .F. ) ;
#34103=VERTEX_POINT ( 'NONE', #46742 ) ;
#34111=CARTESIAN_POINT ( 'NONE',  ( -2.100190309385016274, 0.000000000000000000, 0.5298329251847215815 ) ) ;
#34114=VERTEX_POINT ( 'NONE', #46987 ) ;
#34120=DIRECTION ( 'NONE',  ( -0.01601477604151182663, 0.9998717552508123996, -0.000000000000000000 ) ) ;
#34125=CARTESIAN_POINT ( 'NONE',  ( -1.743516651958532115, 0.0004834999639498254787, -0.009673880220434260407 ) ) ;
#34127=FACE_OUTER_BOUND ( 'NONE', #26049, .T. ) ;
#34131=EDGE_CURVE ( 'NONE', #35860, #23592, #39797, .T. ) ;
#34132=ORIENTED_EDGE ( 'NONE', *, *, #49581, .F. ) ;
#34133=AXIS2_PLACEMENT_3D ( 'NONE', #30923, #3551, #8191 ) ;
#34134=VERTEX_POINT ( 'NONE', #24308 ) ;
#34139=B_SPLINE_CURVE_WITH_KNOTS ( 'NONE', 3,
 ( #30914, #47375, #39417, #3545 ),
 .UNSPECIFIED., .F., .F.,
 ( 4, 4 ),
 ( 0.01440155393167629264, 0.03074911278961747763 ),
 .UNSPECIFIED. ) ;
#34141=CARTESIAN_POINT ( 'NONE',  ( 1.388309139374679146, 1.631713065620022274, -1.827118126197171399 ) ) ;
#34146=AXIS2_PLACEMENT_3D ( 'NONE', #10089, #25830, #29453 ) ;
#34148=CARTESIAN_POINT ( 'NONE',  ( 2.695799277629594037, 1.662794757381320654, -1.205759334241453651 ) ) ;
#34153=CARTESIAN_POINT ( 'NONE',  ( 0.08139965876239094178, 1.610780518492231694, 0.000000000000000000 ) ) ;
#34154=CARTESIAN_POINT ( 'NONE',  ( 0.1067246931122726866, 0.02962905676920215767, 0.000000000000000000 ) ) ;
#34155=CARTESIAN_POINT ( 'NONE',  ( -1.712499999658713801, 0.5249316497054298258, -0.7854770530685656338 ) ) ;
#34157=CARTESIAN_POINT ( 'NONE',  ( 2.080833746290526420, 1.646223005948175278, -1.432513710245896243 ) ) ;
#34161=ORIENTED_EDGE ( 'NONE', *, *, #11098, .T. ) ;
#34172=ORIENTED_EDGE ( 'NONE', *, *, #25080, .F. ) ;
#34173=DIRECTION ( 'NONE',  ( -0.3513748240813305279, 0.000000000000000000, -0.9362348706397418674 ) ) ;
#34178=CARTESIAN_POINT ( 'NONE',  ( -1.068402561569949061, 5.905511811023623991, -1.884154513482187765 ) ) ;
#34179=FACE_OUTER_BOUND ( 'NONE', #36, .T. ) ;
#34181=ORIENTED_EDGE ( 'NONE', *, *, #38026, .T. ) ;
#34183=VECTOR ( 'NONE', #20878, 39.37007874015748143 ) ;
#34186=CARTESIAN_POINT ( 'NONE',  ( -1.217747569163365018, 1.597917297168418793, -2.415255414932540479 ) ) ;
#34187=DIRECTION ( 'NONE',  ( 3.986037398843765983E-20, 1.000000000000000000, 1.160734090543304660E-16 ) ) ;
#34194=ORIENTED_EDGE ( 'NONE', *, *, #22085, .T. ) ;
#34205=LINE ( 'NONE', #32752, #24764 ) ;
#34212=CIRCLE ( 'NONE', #16051, 2.244934639244525076 ) ;
#34221=AXIS2_PLACEMENT_3D ( 'NONE', #44313, #37098, #21090 ) ;
#34222=ORIENTED_EDGE ( 'NONE', *, *, #47263, .F. ) ;
#34223=DIRECTION ( 'NONE',  ( -0.01601477604151182663, 0.9998717552508123996, -0.000000000000000000 ) ) ;
#34226=ORIENTED_EDGE ( 'NONE', *, *, #22487, .T. ) ;
#34229=VERTEX_POINT ( 'NONE', #21460 ) ;
#34230=CARTESIAN_POINT ( 'NONE',  ( -0.6866523217321213179, 0.01134346163807614834, 1.689521298909904212 ) ) ;
#34232=DIRECTION ( 'NONE',  ( 0.000000000000000000, 1.000000000000000000, 0.000000000000000000 ) ) ;
#34239=DIRECTION ( 'NONE',  ( -0.9998717552508122886, -0.01601477604151185785, 0.000000000000000000 ) ) ;
#34243=ORIENTED_EDGE ( 'NONE', *, *, #14336, .F. ) ;
#34252=ADVANCED_FACE ( 'NONE', ( #16823 ), #44429, .F. ) ;
#34254=ORIENTED_EDGE ( 'NONE', *, *, #792, .F. ) ;
#34261=ORIENTED_EDGE ( 'NONE', *, *, #45704, .T. ) ;
#34262=ORIENTED_EDGE ( 'NONE', *, *, #32043, .T. ) ;
#34263=EDGE_CURVE ( 'NONE', #30628, #24596, #9583, .T. ) ;
#34267=EDGE_CURVE ( 'NONE', #8712, #47418, #49028, .T. ) ;
#34272=CARTESIAN_POINT ( 'NONE',  ( -0.5442969769572160166, 1.633567243362389565, -2.157199947919104854 ) ) ;
#34279=CARTESIAN_POINT ( 'NONE',  ( 1.836694934015037806, 1.638894784719147513, 1.401770057403159520 ) ) ;
#34281=CARTESIAN_POINT ( 'NONE',  ( 1.602753508900452317, 0.000000000000000000, 1.341098548255033496 ) ) ;
#34282=ORIENTED_EDGE ( 'NONE', *, *, #16836, .T. ) ;
#34287=VECTOR ( 'NONE', #38503, 39.37007874015748143 ) ;
#34289=FACE_OUTER_BOUND ( 'NONE', #31276, .T. ) ;
#34292=B_SPLINE_CURVE_WITH_KNOTS ( 'NONE', 3,
 ( #20187, #35954, #28189, #47776 ),
 .UNSPECIFIED., .F., .F.,
 ( 4, 4 ),
 ( 0.0001278591145448624699, 0.05010727685611865434 ),
 .UNSPECIFIED. ) ;
#34296=EDGE_CURVE ( 'NONE', #13472, #18093, #26569, .T. ) ;
#34297=CARTESIAN_POINT ( 'NONE',  ( -1.546905380132658436, 1.650317032603659140, -1.547079516075193117 ) ) ;
#34299=EDGE_CURVE ( 'NONE', #22884, #41400, #9352, .T. ) ;
#34301=CARTESIAN_POINT ( 'NONE',  ( 1.825231763105664928, 0.5249316475426857309, -0.4670754312686604681 ) ) ;
#34304=CARTESIAN_POINT ( 'NONE',  ( 0.07982360342473591996, 1.709180471932028711, 0.000000000000000000 ) ) ;
#34312=ORIENTED_EDGE ( 'NONE', *, *, #28167, .T. ) ;
#34326=DIRECTION ( 'NONE',  ( 0.000000000000000000, 1.160734090543304660E-16, -1.000000000000000000 ) ) ;
#34337=CARTESIAN_POINT ( 'NONE',  ( -2.100227814008681637, 1.559371130916006543, -2.076109931251943319 ) ) ;
#34341=EDGE_LOOP ( 'NONE', ( #35428, #8886, #32662, #17588 ) ) ;
#34344=CARTESIAN_POINT ( 'NONE',  ( 2.074656761899007051, 6.692913385826772199, -0.6223516566630626912 ) ) ;
#34348=VECTOR ( 'NONE', #37656, 39.37007874015748143 ) ;
#34352=LINE ( 'NONE', #18600, #39919 ) ;
#34355=ORIENTED_EDGE ( 'NONE', *, *, #22227, .F. ) ;
#34363=EDGE_CURVE ( 'NONE', #11539, #49795, #3224, .T. ) ;
#34370=VERTEX_POINT ( 'NONE', #3548 ) ;
#34371=CARTESIAN_POINT ( 'NONE',  ( 0.000000000000000000, 0.07874015748031502893, 1.682967650661292502 ) ) ;
#34382=CARTESIAN_POINT ( 'NONE',  ( -1.583112249919712999, 0.000000000000000000, -0.7301740747847248469 ) ) ;
#34387=DIRECTION ( 'NONE',  ( -0.000000000000000000, 1.000000000000000000, -0.000000000000000000 ) ) ;
#34388=CIRCLE ( 'NONE', #40989, 2.164630168518208109 ) ;
#34395=CARTESIAN_POINT ( 'NONE',  ( 2.988781320759228421, 2.755905511811027164, -0.1748580315756570747 ) ) ;
#34399=LINE ( 'NONE', #14010, #49806 ) ;
#34403=CARTESIAN_POINT ( 'NONE',  ( 0.3015460593140593115, 0.000000000000000000, 1.937268728265797213 ) ) ;
#34405=CARTESIAN_POINT ( 'NONE',  ( -1.522953965282238586, 0.003526770554233742919, 0.8754220627670087351 ) ) ;
#34406=ORIENTED_EDGE ( 'NONE', *, *, #10361, .T. ) ;
#34410=VERTEX_POINT ( 'NONE', #30663 ) ;
#34411=CARTESIAN_POINT ( 'NONE',  ( -0.6094175224461334528, 1.205361022782829114E-17, 1.763844451117148271 ) ) ;
#34415=ORIENTED_EDGE ( 'NONE', *, *, #23168, .T. ) ;
#34419=VECTOR ( 'NONE', #22584, 39.37007874015748854 ) ;
#34420=ADVANCED_FACE ( 'NONE', ( #22911 ), #50225, .T. ) ;
#34422=CARTESIAN_POINT ( 'NONE',  ( 0.08119777152254364916, 1.623385212329073957, 0.000000000000000000 ) ) ;
#34423=VERTEX_POINT ( 'NONE', #49979 ) ;
#34425=ADVANCED_FACE ( 'NONE', ( #15164 ), #15668, .F. ) ;
#34430=ORIENTED_EDGE ( 'NONE', *, *, #26071, .T. ) ;
#34435=ORIENTED_EDGE ( 'NONE', *, *, #39126, .F. ) ;
#34440=VERTEX_POINT ( 'NONE', #7422 ) ;
#34441=ORIENTED_EDGE ( 'NONE', *, *, #17394, .T. ) ;
#34442=EDGE_CURVE ( 'NONE', #39633, #41705, #15422, .T. ) ;
#34444=CARTESIAN_POINT ( 'NONE',  ( -1.946505901478384759, -1.354463203825560094E-16, 0.9915739042680192794 ) ) ;
#34448=VERTEX_POINT ( 'NONE', #11543 ) ;
#34450=LINE ( 'NONE', #37569, #30702 ) ;
#34455=LINE ( 'NONE', #30323, #18169 ) ;
#34458=DIRECTION ( 'NONE',  ( 1.086719731106943413E-16, -1.000000000000000000, 4.078527368698718974E-17 ) ) ;
#34462=AXIS2_PLACEMENT_3D ( 'NONE', #26806, #38698, #34326 ) ;
#34465=LINE ( 'NONE', #14840, #32547 ) ;
#34466=AXIS2_PLACEMENT_3D ( 'NONE', #37162, #29402, #17030 ) ;
#34471=ORIENTED_EDGE ( 'NONE', *, *, #32106, .F. ) ;
#34472=FACE_OUTER_BOUND ( 'NONE', #23855, .T. ) ;
#34473=AXIS2_PLACEMENT_3D ( 'NONE', #4167, #32771, #29387 ) ;
#34478=EDGE_LOOP ( 'NONE', ( #28485, #2042, #35009, #26791 ) ) ;
#34479=LINE ( 'NONE', #34728, #23842 ) ;
#34482=EDGE_CURVE ( 'NONE', #42262, #45506, #16768, .T. ) ;
#34483=ADVANCED_FACE ( 'NONE', ( #38169 ), #43785, .F. ) ;
#34485=CARTESIAN_POINT ( 'NONE',  ( 0.04921259842519690175, 0.02870789531899127500, 1.849213118431110914 ) ) ;
#34490=CARTESIAN_POINT ( 'NONE',  ( 1.930190994932111215, 1.205361022782829114E-17, -0.9827944786818438860 ) ) ;
#34497=DIRECTION ( 'NONE',  ( -2.582876339026340310E-17, -1.000000000000000000, 1.131632063491650798E-16 ) ) ;
#34498=CONICAL_SURFACE ( 'NONE', #48445, 2.244934639244524632, 1.554780866114618743 ) ;
#34500=CARTESIAN_POINT ( 'NONE',  ( 0.1450362469327829418, 5.905511811023623991, -2.160491579385212191 ) ) ;
#34501=CARTESIAN_POINT ( 'NONE',  ( -0.4161812636739087856, 0.000000000000000000, -1.692983086477939825 ) ) ;
#34503=AXIS2_PLACEMENT_3D ( 'NONE', #9590, #13975, #20685 ) ;
#34505=EDGE_CURVE ( 'NONE', #18049, #18215, #40579, .T. ) ;
#34509=DIRECTION ( 'NONE',  ( -0.9998717552508121775, -0.01601477604151182663, 0.000000000000000000 ) ) ;
#34515=AXIS2_PLACEMENT_3D ( 'NONE', #20818, #28045, #21076 ) ;
#34521=EDGE_CURVE ( 'NONE', #6492, #23952, #26129, .T. ) ;
#34522=CARTESIAN_POINT ( 'NONE',  ( 1.034308760555261886, 1.626043101691516890, -2.034340803895991812 ) ) ;
#34525=DIRECTION ( 'NONE',  ( -0.01601477604151182663, 0.9998717552508123996, -0.000000000000000000 ) ) ;
#34526=CARTESIAN_POINT ( 'NONE',  ( 1.503187667178186970, 0.5249316475426856199, 1.135806887101860729 ) ) ;
#34529=FACE_OUTER_BOUND ( 'NONE', #36698, .T. ) ;
#34542=CONICAL_SURFACE ( 'NONE', #41987, 2.244934639244524632, 1.554780866114618743 ) ;
#34544=CARTESIAN_POINT ( 'NONE',  ( -2.695799277629577162, 1.578813927010291218, -1.205759334241492731 ) ) ;
#34547=DIRECTION ( 'NONE',  ( -3.986037398843765983E-20, -1.000000000000000000, -1.160734090543304660E-16 ) ) ;
#34548=LINE ( 'NONE', #14669, #13574 ) ;
#34552=DIRECTION ( 'NONE',  ( 0.9998717552508121775, 0.01601477604151182663, 0.000000000000000000 ) ) ;
#34558=LINE ( 'NONE', #42288, #2963 ) ;
#34564=ORIENTED_EDGE ( 'NONE', *, *, #25995, .T. ) ;
#34572=ORIENTED_EDGE ( 'NONE', *, *, #41543, .T. ) ;
#34573=ORIENTED_EDGE ( 'NONE', *, *, #30155, .F. ) ;
#34576=DIRECTION ( 'NONE',  ( -0.000000000000000000, -1.000000000000000000, -0.000000000000000000 ) ) ;
#34580=ADVANCED_FACE ( 'NONE', ( #8949 ), #23667, .F. ) ;
#34582=CARTESIAN_POINT ( 'NONE',  ( -2.145579962785661543, 1.559576214923994453, -2.028675302499262312 ) ) ;
#34584=EDGE_CURVE ( 'NONE', #26794, #9867, #29093, .T. ) ;
#34587=ORIENTED_EDGE ( 'NONE', *, *, #5822, .T. ) ;
#34590=LINE ( 'NONE', #15214, #20861 ) ;
#34592=DIRECTION ( 'NONE',  ( 7.237058681235204266E-17, -1.000000000000000000, 9.074984547606538936E-17 ) ) ;
#34597=CARTESIAN_POINT ( 'NONE',  ( 2.932638728931774352, 1.205361022782829114E-17, 0.3475908556738223631 ) ) ;
#34600=LINE ( 'NONE', #50529, #21153 ) ;
#34603=EDGE_CURVE ( 'NONE', #21491, #22636, #27790, .T. ) ;
#34605=AXIS2_PLACEMENT_3D ( 'NONE', #42627, #46229, #46722 ) ;
#34610=EDGE_CURVE ( 'NONE', #50288, #21767, #5587, .T. ) ;
#34611=ORIENTED_EDGE ( 'NONE', *, *, #21304, .T. ) ;
#34613=VECTOR ( 'NONE', #45006, 39.37007874015748143 ) ;
#34615=CARTESIAN_POINT ( 'NONE',  ( 2.225020958752729872, 1.645114536686943296, 0.6712079458291126954 ) ) ;
#34621=DIRECTION ( 'NONE',  ( -0.9998717552508121775, -0.01601477604151182663, 0.000000000000000000 ) ) ;
#34629=DIRECTION ( 'NONE',  ( 0.000000000000000000, 0.000000000000000000, -1.000000000000000000 ) ) ;
#34630=B_SPLINE_CURVE_WITH_KNOTS ( 'NONE', 3,
 ( #38764, #3392, #15014, #49826 ),
 .UNSPECIFIED., .F., .F.,
 ( 4, 4 ),
 ( 4.798888246254521888E-05, 0.002548021674202805703 ),
 .UNSPECIFIED. ) ;
#34632=ORIENTED_EDGE ( 'NONE', *, *, #26974, .T. ) ;
#34635=CARTESIAN_POINT ( 'NONE',  ( 0.07982360342473591996, 1.709180471932028711, 0.000000000000000000 ) ) ;
#34636=VECTOR ( 'NONE', #20348, 39.37007874015748143 ) ;
#34641=CARTESIAN_POINT ( 'NONE',  ( -1.959565595350794220, 0.5253755374352464536, -0.8910779565606279373 ) ) ;
#34643=VERTEX_POINT ( 'NONE', #17968 ) ;
#34644=VERTEX_POINT ( 'NONE', #13595 ) ;
#34649=EDGE_LOOP ( 'NONE', ( #29055, #39074, #3356, #26969 ) ) ;
#34650=CARTESIAN_POINT ( 'NONE',  ( 0.000000000000000000, 0.000000000000000000, 0.000000000000000000 ) ) ;
#34651=DIRECTION ( 'NONE',  ( -1.118904554427321068E-16, -1.000000000000000000, -3.087980359898530052E-17 ) ) ;
#34653=CARTESIAN_POINT ( 'NONE',  ( 0.002207914879453961969, 6.692913385826772199, 0.04916304461325451958 ) ) ;
#34654=DIRECTION ( 'NONE',  ( -0.01601477604151182663, 0.9998717552508123996, -0.000000000000000000 ) ) ;
#34655=ORIENTED_EDGE ( 'NONE', *, *, #16199, .T. ) ;
#34656=CARTESIAN_POINT ( 'NONE',  ( 2.043634885149959057, 6.692913385826772199, 0.7157624142946238388 ) ) ;
#34657=DIRECTION ( 'NONE',  ( 0.01601477604151182663, -0.9998717552508123996, 0.000000000000000000 ) ) ;
#34658=ADVANCED_FACE ( 'NONE', ( #5840 ), #17212, .F. ) ;
#34672=FACE_OUTER_BOUND ( 'NONE', #50608, .T. ) ;
#34675=DIRECTION ( 'NONE',  ( -0.9998717552508121775, -0.01601477604151182316, 0.000000000000000000 ) ) ;
#34679=ORIENTED_EDGE ( 'NONE', *, *, #44155, .F. ) ;
#34683=CARTESIAN_POINT ( 'NONE',  ( -1.133754555558240673, 0.009760511380980992774, 1.372484652545675532 ) ) ;
#34690=ORIENTED_EDGE ( 'NONE', *, *, #32115, .F. ) ;
#34695=CARTESIAN_POINT ( 'NONE',  ( 0.6502734851936936566, 1.718317270777941941, -2.171228911417812046 ) ) ;
#34696=ORIENTED_EDGE ( 'NONE', *, *, #25319, .T. ) ;
#34697=DIRECTION ( 'NONE',  ( 0.000000000000000000, 0.000000000000000000, -1.000000000000000000 ) ) ;
#34700=PLANE ( 'NONE',  #27062 ) ;
#34701=CARTESIAN_POINT ( 'NONE',  ( -2.823445274216743073, 0.000000000000000000, 0.8656477926280280455 ) ) ;
#34704=CARTESIAN_POINT ( 'NONE',  ( -0.1491611873099766838, 0.5239554268833609418, -2.206323420686062686 ) ) ;
#34705=DIRECTION ( 'NONE',  ( 1.000000000000000000, 0.000000000000000000, 0.000000000000000000 ) ) ;
#34709=B_SPLINE_CURVE_WITH_KNOTS ( 'NONE', 3,
 ( #18908, #10317, #36930, #1804 ),
 .UNSPECIFIED., .F., .F.,
 ( 4, 4 ),
 ( 0.0002206499228107822511, 0.04984066487308089904 ),
 .UNSPECIFIED. ) ;
#34714=VECTOR ( 'NONE', #20589, 39.37007874015748854 ) ;
#34716=CARTESIAN_POINT ( 'NONE',  ( 2.063617991565069865, 1.675337772409502435, 1.054594607282280050 ) ) ;
#34718=CARTESIAN_POINT ( 'NONE',  ( -1.463531759593973858, 0.5244536452976792384, 1.600348737355761886 ) ) ;
#34726=CARTESIAN_POINT ( 'NONE',  ( 1.152568299495707382, 6.692913385826772199, 1.833124570921553342 ) ) ;
#34727=( BOUNDED_CURVE ( )  B_SPLINE_CURVE ( 3, ( #48507, #44153, #8795, #24543 ),
 .UNSPECIFIED., .F., .F. ) 
 B_SPLINE_CURVE_WITH_KNOTS ( ( 4, 4 ),
 ( 3.976082376286302900, 4.026957665532088448 ),
 .UNSPECIFIED. ) 
 CURVE ( )  GEOMETRIC_REPRESENTATION_ITEM ( )  RATIONAL_B_SPLINE_CURVE ( ( 1.000000000000000000, 0.9997843203757749153, 0.9997843203757749153, 1.000000000000000000 ) ) 
 REPRESENTATION_ITEM ( '' )  );
#34728=CARTESIAN_POINT ( 'NONE',  ( 1.979793062125284830, 1.205361022782829114E-17, 2.191257344206568813 ) ) ;
#34730=CARTESIAN_POINT ( 'NONE',  ( 0.07982360342473591996, 1.709180471932028711, 0.000000000000000000 ) ) ;
#34736=VERTEX_POINT ( 'NONE', #42215 ) ;
#34738=CARTESIAN_POINT ( 'NONE',  ( 0.7145799201508789000, 1.574803149606302854, 2.044048657746659448 ) ) ;
#34742=DIRECTION ( 'NONE',  ( -3.986037398843765983E-20, -1.000000000000000000, -1.160734090543304660E-16 ) ) ;
#34750=ORIENTED_EDGE ( 'NONE', *, *, #3173, .F. ) ;
#34752=CARTESIAN_POINT ( 'NONE',  ( -1.312248418042854192, 5.905511811023623991, -1.722429524498108711 ) ) ;
#34755=ORIENTED_EDGE ( 'NONE', *, *, #25041, .T. ) ;
#34758=CONICAL_SURFACE ( 'NONE', #32291, 1.850107469027523210, 0.6386652850508578450 ) ;
#34759=ORIENTED_EDGE ( 'NONE', *, *, #9791, .T. ) ;
#34765=ADVANCED_FACE ( 'NONE', ( #50665 ), #49270, .F. ) ;
#34767=EDGE_CURVE ( 'NONE', #25092, #209, #28816, .T. ) ;
#34768=CARTESIAN_POINT ( 'NONE',  ( 1.883550378546973603, 0.000000000000000000, -1.069467267250420628 ) ) ;
#34769=EDGE_CURVE ( 'NONE', #47582, #26865, #30606, .T. ) ;
#34771=DIRECTION ( 'NONE',  ( -1.267583980596137654E-16, 1.000000000000000000, -2.300325776299734791E-17 ) ) ;
#34772=CARTESIAN_POINT ( 'NONE',  ( 1.956098637639549720, 1.739232450405700847, -1.232242025355393844 ) ) ;
#34774=EDGE_LOOP ( 'NONE', ( #20990, #32816, #47224, #18383 ) ) ;
#34776=PLANE ( 'NONE',  #11019 ) ;
#34777=DIRECTION ( 'NONE',  ( -0.9749279121818259508, -0.000000000000000000, 0.2225209339563041788 ) ) ;
#34778=CARTESIAN_POINT ( 'NONE',  ( 1.669153017917641924, 1.205361022782829114E-17, 1.268159837793114031 ) ) ;
#34781=AXIS2_PLACEMENT_3D ( 'NONE', #9098, #48297, #1091 ) ;
#34782=LINE ( 'NONE', #3282, #40512 ) ;
#34784=PLANE ( 'NONE',  #23639 ) ;
#34787=CARTESIAN_POINT ( 'NONE',  ( 0.04921259842519669359, 1.617808935111010760, 2.717264019652364304 ) ) ;
#34791=CARTESIAN_POINT ( 'NONE',  ( 2.225020958752729872, 1.645114536686943296, 0.6712079458291126954 ) ) ;
#34794=FACE_OUTER_BOUND ( 'NONE', #16569, .T. ) ;
#34795=VECTOR ( 'NONE', #32383, 39.37007874015748143 ) ;
#34797=DIRECTION ( 'NONE',  ( -0.9639628606958512425, 1.288287287306305776E-16, -0.2660368455666826670 ) ) ;
#34799=ORIENTED_EDGE ( 'NONE', *, *, #22947, .T. ) ;
#34800=ORIENTED_EDGE ( 'NONE', *, *, #7130, .F. ) ;
#34811=VERTEX_POINT ( 'NONE', #34485 ) ;
#34815=AXIS2_PLACEMENT_3D ( 'NONE', #10817, #26560, #42064 ) ;
#34818=ORIENTED_EDGE ( 'NONE', *, *, #47230, .T. ) ;
#34824=AXIS2_PLACEMENT_3D ( 'NONE', #11261, #26993, #7390 ) ;
#34825=CARTESIAN_POINT ( 'NONE',  ( 2.160407304981128984, 2.755905511811027164, -0.1462862061266579361 ) ) ;
#34826=ORIENTED_EDGE ( 'NONE', *, *, #235, .F. ) ;
#34828=EDGE_CURVE ( 'NONE', #4909, #12116, #19218, .T. ) ;
#34833=LINE ( 'NONE', #15207, #38761 ) ;
#34838=CARTESIAN_POINT ( 'NONE',  ( -0.5304089168012655620, 0.01942419597810423823, -1.736909402037482675 ) ) ;
#34839=DIRECTION ( 'NONE',  ( -0.6234898018587319291, -1.160734090543304907E-16, -0.7818314824680311359 ) ) ;
#34841=CARTESIAN_POINT ( 'NONE',  ( 1.319349709118413205, 0.000000000000000000, 1.584915398547334764 ) ) ;
#34847=EDGE_CURVE ( 'NONE', #43448, #37038, #2987, .T. ) ;
#34848=VERTEX_POINT ( 'NONE', #11490 ) ;
#34851=CIRCLE ( 'NONE', #12591, 1.743387098533651480 ) ;
#34852=DIRECTION ( 'NONE',  ( -3.986037398843765983E-20, -1.000000000000000000, -1.160734090543304660E-16 ) ) ;
#34853=ORIENTED_EDGE ( 'NONE', *, *, #19408, .T. ) ;
#34856=CARTESIAN_POINT ( 'NONE',  ( 0.8449282472259149745, 1.688626626580369994, 2.111245994233534429 ) ) ;
#34864=PLANE ( 'NONE',  #10355 ) ;
#34865=FACE_OUTER_BOUND ( 'NONE', #27999, .T. ) ;
#34866=ORIENTED_EDGE ( 'NONE', *, *, #25741, .T. ) ;
#34867=CIRCLE ( 'NONE', #31595, 1.743387098533651480 ) ;
#34868=DIRECTION ( 'NONE',  ( 0.000000000000000000, 1.000000000000000000, -0.000000000000000000 ) ) ;
#34869=EDGE_LOOP ( 'NONE', ( #34060, #24242, #49510, #3530 ) ) ;
#34870=VERTEX_POINT ( 'NONE', #47573 ) ;
#34873=CARTESIAN_POINT ( 'NONE',  ( -1.420868632364155282, 0.000000000000000000, 1.070159647439151707 ) ) ;
#34877=CARTESIAN_POINT ( 'NONE',  ( -2.151809081513409438, 1.574803149606302854, 0.2418202932658341242 ) ) ;
#34878=CARTESIAN_POINT ( 'NONE',  ( 0.002207914879453961535, -5.712274067634378313E-18, 0.04916304461325374242 ) ) ;
#34880=CARTESIAN_POINT ( 'NONE',  ( 0.000000000000000000, 1.574803149606302854, 0.000000000000000000 ) ) ;
#34882=ORIENTED_EDGE ( 'NONE', *, *, #22351, .T. ) ;
#34884=VERTEX_POINT ( 'NONE', #44246 ) ;
#34887=CARTESIAN_POINT ( 'NONE',  ( 1.539674616754186820, 0.000000000000000000, -1.403993126671013059 ) ) ;
#34888=CARTESIAN_POINT ( 'NONE',  ( 1.979793062125284608, 1.651646828087945051, 2.191257344206569257 ) ) ;
#34893=AXIS2_PLACEMENT_3D ( 'NONE', #31510, #16010, #12652 ) ;
#34898=FACE_OUTER_BOUND ( 'NONE', #6116, .T. ) ;
#34906=ORIENTED_EDGE ( 'NONE', *, *, #45770, .F. ) ;
#34907=CARTESIAN_POINT ( 'NONE',  ( 1.902660579019252562, 1.639951345248664039, -1.314902632263422966 ) ) ;
#34908=DIRECTION ( 'NONE',  ( 0.000000000000000000, 1.000000000000000000, 0.000000000000000000 ) ) ;
#34910=CARTESIAN_POINT ( 'NONE',  ( -2.734482843737247038, 1.572033689214636709, -1.115254632218712016 ) ) ;
#34912=CARTESIAN_POINT ( 'NONE',  ( 0.1067246931122726866, 0.02962905676920215767, 0.000000000000000000 ) ) ;
#34920=ORIENTED_EDGE ( 'NONE', *, *, #11862, .T. ) ;
#34921=CARTESIAN_POINT ( 'NONE',  ( 2.010699302595137627, 0.01941208527870304928, -0.5094071868683279769 ) ) ;
#34931=FACE_OUTER_BOUND ( 'NONE', #20619, .T. ) ;
#34935=CARTESIAN_POINT ( 'NONE',  ( -2.142805232260984738, 5.905511811023623991, 0.3399247426648309700 ) ) ;
#34939=CONICAL_SURFACE ( 'NONE', #7699, 2.246510896728926010, 0.01601546068027819014 ) ;
#34947=CARTESIAN_POINT ( 'NONE',  ( 0.000000000000000000, 5.905511811023623991, 0.000000000000000000 ) ) ;
#34949=CIRCLE ( 'NONE', #34146, 2.164630168518208109 ) ;
#34951=DIRECTION ( 'NONE',  ( -0.9998717552508122886, -0.01601477604151181275, 0.000000000000000000 ) ) ;
#34952=ORIENTED_EDGE ( 'NONE', *, *, #3327, .T. ) ;
#34953=EDGE_LOOP ( 'NONE', ( #21238, #13721, #49178, #42815 ) ) ;
#34971=CIRCLE ( 'NONE', #19289, 2.244934639244525076 ) ;
#34972=CARTESIAN_POINT ( 'NONE',  ( -0.04921259842519706829, 1.707113721008201024, 2.241222193722145484 ) ) ;
#34973=AXIS2_PLACEMENT_3D ( 'NONE', #48063, #17629, #33134 ) ;
#34975=VECTOR ( 'NONE', #32909, 39.37007874015748143 ) ;
#34976=AXIS2_PLACEMENT_3D ( 'NONE', #31230, #23723, #27336 ) ;
#34979=CARTESIAN_POINT ( 'NONE',  ( -0.2492758785930729581, 1.703909341437327862, -2.220674960591680680 ) ) ;
#34980=CARTESIAN_POINT ( 'NONE',  ( -2.889674983507169337, 1.575089141731351505, -0.6090712660038034576 ) ) ;
#34984=VECTOR ( 'NONE', #25263, 39.37007874015748143 ) ;
#34986=CARTESIAN_POINT ( 'NONE',  ( -1.022004635462139488, 1.695497469272269964, -2.235637960992456819 ) ) ;
#34987=EDGE_LOOP ( 'NONE', ( #7304, #44621, #30442, #21168, #3288, #34078, #19054, #7838, #23797, #20797, #10196 ) ) ;
#34996=CARTESIAN_POINT ( 'NONE',  ( 1.474379988472116487, 1.633091647787944911, 1.762361831087230213 ) ) ;
#34997=CARTESIAN_POINT ( 'NONE',  ( -2.411880484304812278, 1.575048720448358752, 0.2770493584408288412 ) ) ;
#35004=CARTESIAN_POINT ( 'NONE',  ( 0.08139965876239094178, 1.610780518492231694, 0.000000000000000000 ) ) ;
#35005=CARTESIAN_POINT ( 'NONE',  ( 0.1067246931122726866, 0.02962905676920215767, 0.000000000000000000 ) ) ;
#35006=VECTOR ( 'NONE', #47797, 39.37007874015748143 ) ;
#35008=AXIS2_PLACEMENT_3D ( 'NONE', #8354, #39337, #88 ) ;
#35009=ORIENTED_EDGE ( 'NONE', *, *, #20336, .T. ) ;
#35010=DIRECTION ( 'NONE',  ( 0.01601477604151182663, -0.9998717552508123996, 0.000000000000000000 ) ) ;
#35019=ORIENTED_EDGE ( 'NONE', *, *, #19024, .F. ) ;
#35021=EDGE_CURVE ( 'NONE', #25300, #9567, #7430, .T. ) ;
#35022=EDGE_LOOP ( 'NONE', ( #27731, #12005, #29999, #9052, #13870, #23595, #31576, #34471, #40156, #45361, #33192 ) ) ;
#35026=EDGE_CURVE ( 'NONE', #596, #21677, #40721, .T. ) ;
#35028=CARTESIAN_POINT ( 'NONE',  ( -1.919487379551519490, 0.5250046931542878825, 0.9770346176326605292 ) ) ;
#35029=CARTESIAN_POINT ( 'NONE',  ( 2.734482843737263025, 1.452693199995327644, -1.115254632218672270 ) ) ;
#35039=DIRECTION ( 'NONE',  ( 7.097135778201662695E-17, 1.000000000000000000, -1.075170113095010447E-16 ) ) ;
#35040=ORIENTED_EDGE ( 'NONE', *, *, #17111, .T. ) ;
#35042=CARTESIAN_POINT ( 'NONE',  ( -1.632855683316659867, 1.205361022782829114E-17, -0.6443965869051290207 ) ) ;
#35049=DIRECTION ( 'NONE',  ( 0.000000000000000000, 0.000000000000000000, -1.000000000000000000 ) ) ;
#35053=EDGE_CURVE ( 'NONE', #50445, #9022, #43809, .T. ) ;
#35056=ORIENTED_EDGE ( 'NONE', *, *, #37933, .T. ) ;
#35057=EDGE_CURVE ( 'NONE', #45880, #50600, #33420, .T. ) ;
#35058=DIRECTION ( 'NONE',  ( -3.986037398843765983E-20, -1.000000000000000000, -1.160734090543304660E-16 ) ) ;
#35061=CARTESIAN_POINT ( 'NONE',  ( -0.04921259842519767197, 6.692913385826772199, 2.164795024401847456 ) ) ;
#35062=ORIENTED_EDGE ( 'NONE', *, *, #25476, .T. ) ;
#35066=CARTESIAN_POINT ( 'NONE',  ( 0.08119777152254364916, 1.623385212329073957, 0.000000000000000000 ) ) ;
#35068=ORIENTED_EDGE ( 'NONE', *, *, #12069, .F. ) ;
#35074=ORIENTED_EDGE ( 'NONE', *, *, #37532, .T. ) ;
#35077=EDGE_CURVE ( 'NONE', #31986, #50925, #22886, .T. ) ;
#35079=CONICAL_SURFACE ( 'NONE', #21049, 2.244934639244524632, 1.554780866114618743 ) ;
#35080=ADVANCED_FACE ( 'NONE', ( #37285 ), #17397, .F. ) ;
#35083=AXIS2_PLACEMENT_3D ( 'NONE', #22540, #42660, #7305 ) ;
#35085=DIRECTION ( 'NONE',  ( -0.000000000000000000, 1.000000000000000000, -0.000000000000000000 ) ) ;
#35089=ORIENTED_EDGE ( 'NONE', *, *, #2423, .F. ) ;
#35092=DIRECTION ( 'NONE',  ( 0.9909497617679331460, 0.000000000000000000, 0.1342332658176667026 ) ) ;
#35103=LINE ( 'NONE', #42833, #29998 ) ;
#35106=AXIS2_PLACEMENT_3D ( 'NONE', #45427, #21970, #28676 ) ;
#35109=AXIS2_PLACEMENT_3D ( 'NONE', #6354, #48904, #13593 ) ;
#35110=ORIENTED_EDGE ( 'NONE', *, *, #1761, .T. ) ;
#35113=VERTEX_POINT ( 'NONE', #6026 ) ;
#35114=EDGE_CURVE ( 'NONE', #17408, #810, #2158, .T. ) ;
#35115=DIRECTION ( 'NONE',  ( 3.586865599282426309E-17, -1.000000000000000000, -1.103923720497134591E-16 ) ) ;
#35122=B_SPLINE_CURVE_WITH_KNOTS ( 'NONE', 3,
 ( #48867, #13553, #21808, #45026 ),
 .UNSPECIFIED., .F., .F.,
 ( 4, 4 ),
 ( 2.396442697539120721E-07, 0.01971986562029358347 ),
 .UNSPECIFIED. ) ;
#35125=ORIENTED_EDGE ( 'NONE', *, *, #22092, .F. ) ;
#35130=DIRECTION ( 'NONE',  ( -0.9998717552508122886, -0.01601477604151180928, 0.000000000000000000 ) ) ;
#35132=DIRECTION ( 'NONE',  ( -0.9998717552508122886, -0.01601477604151180928, 0.000000000000000000 ) ) ;
#35135=EDGE_CURVE ( 'NONE', #6369, #2307, #18414, .T. ) ;
#35139=ORIENTED_EDGE ( 'NONE', *, *, #30289, .T. ) ;
#35145=PLANE ( 'NONE',  #34605 ) ;
#35146=VERTEX_POINT ( 'NONE', #10671 ) ;
#35150=DIRECTION ( 'NONE',  ( 0.9998717552508121775, 0.01601477604151182663, 0.000000000000000000 ) ) ;
#35158=CARTESIAN_POINT ( 'NONE',  ( 1.243113849864399656, 1.731386041893312022, 2.176571955408725056 ) ) ;
#35159=CARTESIAN_POINT ( 'NONE',  ( -1.583112249919712999, 0.000000000000000000, -0.7301740747847248469 ) ) ;
#35160=AXIS2_PLACEMENT_3D ( 'NONE', #27042, #27550, #31694 ) ;
#35169=PLANE ( 'NONE',  #6456 ) ;
#35171=CARTESIAN_POINT ( 'NONE',  ( 1.041132165474419446, 1.728185027159919951, -2.275356686326451161 ) ) ;
#35175=CARTESIAN_POINT ( 'NONE',  ( 0.07982360342473591996, 1.709180471932028711, 0.000000000000000000 ) ) ;
#35179=ORIENTED_EDGE ( 'NONE', *, *, #24499, .F. ) ;
#35192=ORIENTED_EDGE ( 'NONE', *, *, #37532, .F. ) ;
#35193=CARTESIAN_POINT ( 'NONE',  ( 0.8949303405208896001, 1.574803149606302854, -1.971765468592530102 ) ) ;
#35194=CARTESIAN_POINT ( 'NONE',  ( -0.5756566573089004768, 1.527738838675063882, 2.896516654582634853 ) ) ;
#35196=DIRECTION ( 'NONE',  ( -3.986037398843765983E-20, -1.000000000000000000, -1.160734090543304660E-16 ) ) ;
#35203=ORIENTED_EDGE ( 'NONE', *, *, #37474, .F. ) ;
#35205=DIRECTION ( 'NONE',  ( 0.000000000000000000, 0.000000000000000000, 1.000000000000000000 ) ) ;
#35206=CARTESIAN_POINT ( 'NONE',  ( 1.928178237245542492, 0.03859178796661346528, 0.5747578989280442974 ) ) ;
#35207=CARTESIAN_POINT ( 'NONE',  ( 0.4161812636739331550, 0.000000000000000000, -1.692983086477933830 ) ) ;
#35211=EDGE_LOOP ( 'NONE', ( #5792, #7481, #38208, #36852, #12708, #37990 ) ) ;
#35218=VECTOR ( 'NONE', #41616, 39.37007874015748143 ) ;
#35219=ADVANCED_FACE ( 'NONE', ( #15044 ), #50900, .F. ) ;
#35220=AXIS2_PLACEMENT_3D ( 'NONE', #32128, #44489, #27720 ) ;
#35221=DIRECTION ( 'NONE',  ( -0.01601477604151182663, 0.9998717552508123996, -0.000000000000000000 ) ) ;
#35226=EDGE_CURVE ( 'NONE', #34103, #48573, #42738, .T. ) ;
#35229=ORIENTED_EDGE ( 'NONE', *, *, #38504, .F. ) ;
#35234=DIRECTION ( 'NONE',  ( -0.01601477604151182663, 0.9998717552508123996, -0.000000000000000000 ) ) ;
#35235=CARTESIAN_POINT ( 'NONE',  ( 0.07982360342473591996, 1.709180471932028711, 0.000000000000000000 ) ) ;
#35237=ORIENTED_EDGE ( 'NONE', *, *, #36886, .F. ) ;
#35238=CARTESIAN_POINT ( 'NONE',  ( -1.129409194730853105, 1.697742047597073034, -2.458665826403365173 ) ) ;
#35239=ORIENTED_EDGE ( 'NONE', *, *, #15134, .T. ) ;
#35240=AXIS2_PLACEMENT_3D ( 'NONE', #3027, #43006, #46609 ) ;
#35242=EDGE_CURVE ( 'NONE', #30165, #23247, #4793, .T. ) ;
#35250=DIRECTION ( 'NONE',  ( -0.9998717552508121775, -0.01601477604151182316, 0.000000000000000000 ) ) ;
#35252=DIRECTION ( 'NONE',  ( 0.000000000000000000, 0.000000000000000000, 1.000000000000000000 ) ) ;
#35259=AXIS2_PLACEMENT_3D ( 'NONE', #7005, #14756, #22252 ) ;
#35261=ADVANCED_FACE ( 'NONE', ( #12431 ), #39292, .F. ) ;
#35271=DIRECTION ( 'NONE',  ( 0.9362348706397418674, 1.288287287306305776E-16, -0.3513748240813305279 ) ) ;
#35274=AXIS2_PLACEMENT_3D ( 'NONE', #39089, #7099, #38595 ) ;
#35277=CARTESIAN_POINT ( 'NONE',  ( 2.277014451362978420, 1.678755706740915343, -0.4692354975254571237 ) ) ;
#35278=EDGE_CURVE ( 'NONE', #6017, #8712, #27407, .T. ) ;
#35279=ADVANCED_FACE ( 'NONE', ( #19661 ), #46992, .F. ) ;
#35282=DIRECTION ( 'NONE',  ( -0.000000000000000000, 1.000000000000000000, -0.000000000000000000 ) ) ;
#35283=CARTESIAN_POINT ( 'NONE',  ( 2.988781320759228421, 5.118110236220475784, -0.1748580315756567971 ) ) ;
#35286=CARTESIAN_POINT ( 'NONE',  ( -2.047355983664255863, 1.576684601009278319, 0.7169714724935087879 ) ) ;
#35292=CARTESIAN_POINT ( 'NONE',  ( -1.743145509346910149, 0.000000000000000000, 0.03054797143824310862 ) ) ;
#35295=CARTESIAN_POINT ( 'NONE',  ( -1.631260293787041071, 0.0006143858728471982261, -0.6437146846949991508 ) ) ;
#35296=B_SPLINE_CURVE_WITH_KNOTS ( 'NONE', 3,
 ( #9266, #32520, #1521, #41276 ),
 .UNSPECIFIED., .F., .F.,
 ( 4, 4 ),
 ( 2.051447925150919731E-07, 0.002500220192228647109 ),
 .UNSPECIFIED. ) ;
#35297=CIRCLE ( 'NONE', #45994, 2.165354330708661568 ) ;
#35300=VERTEX_POINT ( 'NONE', #35936 ) ;
#35305=PLANE ( 'NONE',  #12752 ) ;
#35308=ADVANCED_FACE ( 'NONE', ( #31552 ), #35169, .F. ) ;
#35310=ORIENTED_EDGE ( 'NONE', *, *, #19778, .T. ) ;
#35312=CARTESIAN_POINT ( 'NONE',  ( 1.287350139463531828, 0.01584012156927684309, 1.548288944013793245 ) ) ;
#35318=VERTEX_POINT ( 'NONE', #817 ) ;
#35325=CARTESIAN_POINT ( 'NONE',  ( -1.779568955232873950, 5.905511811023623991, -1.233650562797313777 ) ) ;
#35327=B_SPLINE_CURVE_WITH_KNOTS ( 'NONE', 3,
 ( #42386, #2651, #34157, #34907 ),
 .UNSPECIFIED., .F., .F.,
 ( 4, 4 ),
 ( 2.397468562700561163E-07, 0.01627520709194900037 ),
 .UNSPECIFIED. ) ;
#35331=ORIENTED_EDGE ( 'NONE', *, *, #31451, .T. ) ;
#35336=LINE ( 'NONE', #11079, #29525 ) ;
#35338=CARTESIAN_POINT ( 'NONE',  ( 1.699531805983663935, 1.669506266544195761, -1.556832249051517181 ) ) ;
#35341=VECTOR ( 'NONE', #185, 39.37007874015748143 ) ;
#35346=EDGE_CURVE ( 'NONE', #24696, #44472, #17314, .T. ) ;
#35350=CARTESIAN_POINT ( 'NONE',  ( -0.8329809839909436686, 1.533199950842965453, -2.833254665166566877 ) ) ;
#35354=CARTESIAN_POINT ( 'NONE',  ( -2.867773316779185677, 1.576133919414932638, -0.7050287376752426560 ) ) ;
#35355=AXIS2_PLACEMENT_3D ( 'NONE', #6397, #2008, #33525 ) ;
#35362=CARTESIAN_POINT ( 'NONE',  ( 0.6423598643315989731, 1.010863969785771754, -2.512522840280564385 ) ) ;
#35364=EDGE_CURVE ( 'NONE', #17362, #35848, #15550, .T. ) ;
#35367=CYLINDRICAL_SURFACE ( 'NONE', #39456, 2.165354330708661568 ) ;
#35368=ADVANCED_FACE ( 'NONE', ( #20435 ), #16572, .F. ) ;
#35370=CARTESIAN_POINT ( 'NONE',  ( 2.031248100867566908, 0.5222577735666947829, 1.037175626315068877 ) ) ;
#35371=ORIENTED_EDGE ( 'NONE', *, *, #40455, .T. ) ;
#35372=VECTOR ( 'NONE', #32346, 39.37007874015748143 ) ;
#35378=CARTESIAN_POINT ( 'NONE',  ( 0.1170985530868079300, 0.02979521312206013725, -1.850078377359382298 ) ) ;
#35382=CARTESIAN_POINT ( 'NONE',  ( 1.930249146414562578, 0.05883613814988478824, 0.3111320644955062886 ) ) ;
#35387=CARTESIAN_POINT ( 'NONE',  ( -1.472219874544909768, 1.696317054561777171, 2.560030851058948898 ) ) ;
#35388=ORIENTED_EDGE ( 'NONE', *, *, #15489, .T. ) ;
#35393=CARTESIAN_POINT ( 'NONE',  ( -2.437180031585919782, 1.681273446161504426, -1.667735833703134718 ) ) ;
#35400=ADVANCED_FACE ( 'NONE', ( #31300 ), #5200, .F. ) ;
#35409=B_SPLINE_CURVE_WITH_KNOTS ( 'NONE', 3,
 ( #25803, #32806, #9808, #40792 ),
 .UNSPECIFIED., .F., .F.,
 ( 4, 4 ),
 ( 2.271749272631870541E-07, 0.002500337609477648517 ),
 .UNSPECIFIED. ) ;
#35411=CARTESIAN_POINT ( 'NONE',  ( 2.695799277629595370, 5.905511811023623991, -1.205759334241453429 ) ) ;
#35414=VERTEX_POINT ( 'NONE', #41340 ) ;
#35415=DIRECTION ( 'NONE',  ( -0.01601477604151182663, 0.9998717552508123996, -0.000000000000000000 ) ) ;
#35416=CARTESIAN_POINT ( 'NONE',  ( 0.6235241006192031588, 5.905511811023623991, 2.074304693190358595 ) ) ;
#35425=EDGE_CURVE ( 'NONE', #4986, #38194, #26535, .T. ) ;
#35426=ORIENTED_EDGE ( 'NONE', *, *, #231, .T. ) ;
#35428=ORIENTED_EDGE ( 'NONE', *, *, #40176, .T. ) ;
#35434=CIRCLE ( 'NONE', #2466, 2.246510896728926010 ) ;
#35435=ORIENTED_EDGE ( 'NONE', *, *, #18749, .F. ) ;
#35436=ORIENTED_EDGE ( 'NONE', *, *, #14132, .T. ) ;
#35439=DIRECTION ( 'NONE',  ( 0.000000000000000000, 0.000000000000000000, 1.000000000000000000 ) ) ;
#35444=CARTESIAN_POINT ( 'NONE',  ( 0.1067246931122726866, 0.02962905676920215767, 0.000000000000000000 ) ) ;
#35446=AXIS2_PLACEMENT_3D ( 'NONE', #23712, #7967, #12606 ) ;
#35455=ORIENTED_EDGE ( 'NONE', *, *, #9729, .T. ) ;
#35457=EDGE_LOOP ( 'NONE', ( #6643, #45693, #42351, #22154 ) ) ;
#35461=DIRECTION ( 'NONE',  ( -0.1785568947986229116, 0.000000000000000000, -0.9839295885986321100 ) ) ;
#35462=LINE ( 'NONE', #80, #14040 ) ;
#35465=VERTEX_POINT ( 'NONE', #25082 ) ;
#35466=VERTEX_POINT ( 'NONE', #25587 ) ;
#35467=ORIENTED_EDGE ( 'NONE', *, *, #47894, .F. ) ;
#35468=CARTESIAN_POINT ( 'NONE',  ( 2.949046705395566459, 1.765204021194747286, -0.1488625692542399903 ) ) ;
#35469=DIRECTION ( 'NONE',  ( -0.01601477604151182663, 0.9998717552508123996, -0.000000000000000000 ) ) ;
#35474=CARTESIAN_POINT ( 'NONE',  ( -1.709950266952966036, 0.000000000000000000, -0.3398067978735320183 ) ) ;
#35480=DIRECTION ( 'NONE',  ( -0.000000000000000000, -1.000000000000000000, -0.000000000000000000 ) ) ;
#35484=CARTESIAN_POINT ( 'NONE',  ( -1.775400203342670347, 1.593155925640307835, -2.359903268218729089 ) ) ;
#35485=ORIENTED_EDGE ( 'NONE', *, *, #10201, .F. ) ;
#35486=CARTESIAN_POINT ( 'NONE',  ( -1.087426130748108788, 0.01050254589070086231, -1.412988192946641020 ) ) ;
#35493=CARTESIAN_POINT ( 'NONE',  ( -2.122484638469143814, 1.673906474958827939, -0.4339650761337435214 ) ) ;
#35494=CARTESIAN_POINT ( 'NONE',  ( -1.152114531865843006, 1.205361022782829114E-17, 1.393499336327983729 ) ) ;
#35495=DIRECTION ( 'NONE',  ( -3.986037398843765983E-20, -1.000000000000000000, -1.160734090543304660E-16 ) ) ;
#35504=LINE ( 'NONE', #44261, #16996 ) ;
#35505=CARTESIAN_POINT ( 'NONE',  ( -2.808237744966007643, 0.000000000000000000, 0.9124517550441282321 ) ) ;
#35507=CARTESIAN_POINT ( 'NONE',  ( 1.761347130804464367, 1.743135256392197796, 2.090822154292000690 ) ) ;
#35509=VERTEX_POINT ( 'NONE', #9077 ) ;
#35511=FACE_OUTER_BOUND ( 'NONE', #20274, .T. ) ;
#35518=CARTESIAN_POINT ( 'NONE',  ( -0.5304089168012655620, 0.01942419597810423823, -1.736909402037482675 ) ) ;
#35519=B_SPLINE_CURVE_WITH_KNOTS ( 'NONE', 3,
 ( #24342, #21235, #1093, #17110 ),
 .UNSPECIFIED., .F., .F.,
 ( 4, 4 ),
 ( 0.002316997564876225116, 0.004817283094879090156 ),
 .UNSPECIFIED. ) ;
#35521=VECTOR ( 'NONE', #21390, 39.37007874015748143 ) ;
#35524=ORIENTED_EDGE ( 'NONE', *, *, #38497, .F. ) ;
#35526=B_SPLINE_CURVE_WITH_KNOTS ( 'NONE', 3,
 ( #29283, #41921, #1410, #17924 ),
 .UNSPECIFIED., .F., .F.,
 ( 4, 4 ),
 ( 2.136451552133696225E-07, 0.002500479562036453732 ),
 .UNSPECIFIED. ) ;
#35528=CIRCLE ( 'NONE', #19844, 2.165354330708661568 ) ;
#35531=LINE ( 'NONE', #48382, #38260 ) ;
#35537=CARTESIAN_POINT ( 'NONE',  ( 2.100227814008711835, 1.653522055412836700, -2.076109931251913565 ) ) ;
#35539=DIRECTION ( 'NONE',  ( -0.9998717552508122886, -0.01601477604151182316, 0.000000000000000000 ) ) ;
#35548=EDGE_CURVE ( 'NONE', #16254, #25553, #14985, .T. ) ;
#35549=DIRECTION ( 'NONE',  ( -0.01601477604151182663, 0.9998717552508123996, -0.000000000000000000 ) ) ;
#35561=CARTESIAN_POINT ( 'NONE',  ( -1.775400203342670569, 5.905511811023623991, -2.359903268218730421 ) ) ;
#35562=EDGE_LOOP ( 'NONE', ( #25102, #20475, #28120, #8415 ) ) ;
#35564=B_SPLINE_CURVE_WITH_KNOTS ( 'NONE', 3,
 ( #12199, #43426, #31829, #12710 ),
 .UNSPECIFIED., .F., .F.,
 ( 4, 4 ),
 ( 2.219309651315323410E-07, 0.002500660338287432824 ),
 .UNSPECIFIED. ) ;
#35567=EDGE_CURVE ( 'NONE', #16203, #19475, #14479, .T. ) ;
#35569=AXIS2_PLACEMENT_3D ( 'NONE', #13136, #9256, #36887 ) ;
#35570=EDGE_CURVE ( 'NONE', #2996, #3720, #7242, .T. ) ;
#35571=ORIENTED_EDGE ( 'NONE', *, *, #8635, .F. ) ;
#35575=B_SPLINE_CURVE_WITH_KNOTS ( 'NONE', 3,
 ( #45572, #30367, #49679, #41985 ),
 .UNSPECIFIED., .F., .F.,
 ( 4, 4 ),
 ( 3.456166342725411222E-07, 0.05034329717658189013 ),
 .UNSPECIFIED. ) ;
#35579=ORIENTED_EDGE ( 'NONE', *, *, #22227, .T. ) ;
#35580=LINE ( 'NONE', #8977, #25421 ) ;
#35582=VERTEX_POINT ( 'NONE', #38489 ) ;
#35583=CARTESIAN_POINT ( 'NONE',  ( 2.823445274216730638, 1.450545469922353892, 0.8656477926280681245 ) ) ;
#35588=DIRECTION ( 'NONE',  ( -0.01601477604151182663, 0.9998717552508123996, -0.000000000000000000 ) ) ;
#35591=DIRECTION ( 'NONE',  ( -0.9998717552508121775, -0.01601477604151182316, 0.000000000000000000 ) ) ;
#35596=ORIENTED_EDGE ( 'NONE', *, *, #30505, .F. ) ;
#35597=AXIS2_PLACEMENT_3D ( 'NONE', #2546, #6166, #26036 ) ;
#35600=EDGE_CURVE ( 'NONE', #3078, #25300, #45943, .T. ) ;
#35602=CONICAL_SURFACE ( 'NONE', #22412, 1.850107469027523210, 0.6386652850508578450 ) ;
#35603=CARTESIAN_POINT ( 'NONE',  ( 2.882374435144356095, 1.665690404301812588, -0.6410570582912683557 ) ) ;
#35612=B_SPLINE_CURVE_WITH_KNOTS ( 'NONE', 3,
 ( #12712, #32604, #44195, #28444 ),
 .UNSPECIFIED., .F., .F.,
 ( 4, 4 ),
 ( 2.019292134928139459E-07, 0.01591357913266653809 ),
 .UNSPECIFIED. ) ;
#35615=CARTESIAN_POINT ( 'NONE',  ( 0.08139965876239094178, 1.610780518492231694, 0.000000000000000000 ) ) ;
#35620=ORIENTED_EDGE ( 'NONE', *, *, #46976, .T. ) ;
#35622=FACE_OUTER_BOUND ( 'NONE', #20981, .T. ) ;
#35628=CARTESIAN_POINT ( 'NONE',  ( 0.04921259842519667277, 1.712470432967292622, 2.480735887547718121 ) ) ;
#35630=ORIENTED_EDGE ( 'NONE', *, *, #33754, .F. ) ;
#35633=CARTESIAN_POINT ( 'NONE',  ( -2.437180031585919782, 1.582844051365913662, -1.667735833703134718 ) ) ;
#35638=EDGE_LOOP ( 'NONE', ( #46146, #13879, #12130, #40799 ) ) ;
#35639=DIRECTION ( 'NONE',  ( 0.000000000000000000, -1.000000000000000000, -0.000000000000000000 ) ) ;
#35641=EDGE_LOOP ( 'NONE', ( #41119, #29255, #15964, #2858 ) ) ;
#35652=VERTEX_POINT ( 'NONE', #10098 ) ;
#35657=DIRECTION ( 'NONE',  ( 0.9998717552508121775, 0.01601477604151182663, 0.000000000000000000 ) ) ;
#35661=CARTESIAN_POINT ( 'NONE',  ( 2.158170387640339527, 6.692913385826772199, 0.2426819907294805456 ) ) ;
#35664=ORIENTED_EDGE ( 'NONE', *, *, #37179, .F. ) ;
#35665=CARTESIAN_POINT ( 'NONE',  ( 0.08119777152254364916, 1.623385212329073957, 0.000000000000000000 ) ) ;
#35671=CIRCLE ( 'NONE', #13422, 1.743387098533651480 ) ;
#35674=LINE ( 'NONE', #23794, #49389 ) ;
#35676=ORIENTED_EDGE ( 'NONE', *, *, #3130, .F. ) ;
#35677=CARTESIAN_POINT ( 'NONE',  ( -2.576863348864732117, 1.205361022782829114E-17, 1.442554885838412071 ) ) ;
#35678=ORIENTED_EDGE ( 'NONE', *, *, #36140, .T. ) ;
#35679=DIRECTION ( 'NONE',  ( 0.9998717552508121775, 0.01601477604151182663, 0.000000000000000000 ) ) ;
#35683=DIRECTION ( 'NONE',  ( 0.000000000000000000, 0.000000000000000000, -1.000000000000000000 ) ) ;
#35689=FACE_OUTER_BOUND ( 'NONE', #14929, .T. ) ;
#35691=ORIENTED_EDGE ( 'NONE', *, *, #6101, .F. ) ;
#35692=VERTEX_POINT ( 'NONE', #38977 ) ;
#35694=CARTESIAN_POINT ( 'NONE',  ( 0.000000000000000000, 1.574803149606302854, 0.000000000000000000 ) ) ;
#35696=EDGE_CURVE ( 'NONE', #28109, #18363, #8252, .T. ) ;
#35698=CARTESIAN_POINT ( 'NONE',  ( 1.930898218216747120, 1.205361022782829114E-17, -0.8788249315385436855 ) ) ;
#35699=CARTESIAN_POINT ( 'NONE',  ( -0.8067290215918264673, 1.574803149606302854, 2.009464521518170343 ) ) ;
#35700=CARTESIAN_POINT ( 'NONE',  ( 0.002207914879453961969, 5.905511811023623991, 0.04916304461325442243 ) ) ;
#35701=ORIENTED_EDGE ( 'NONE', *, *, #4316, .F. ) ;
#35707=EDGE_LOOP ( 'NONE', ( #22864, #15035, #7993, #33013, #12121, #2051, #8434, #41639, #45782, #15387, #46246, #22753, #28449 ) ) ;
#35713=EDGE_CURVE ( 'NONE', #12116, #12736, #4315, .T. ) ;
#35718=CONICAL_SURFACE ( 'NONE', #10143, 2.165354330708661568, 0.2617993877991570129 ) ;
#35722=FACE_OUTER_BOUND ( 'NONE', #34478, .T. ) ;
#35728=CARTESIAN_POINT ( 'NONE',  ( 2.164658444855302122, 5.905511811023623991, -0.04795272066889885720 ) ) ;
#35730=CARTESIAN_POINT ( 'NONE',  ( -2.100227814008681637, 1.686526752338742385, -2.076109931251943763 ) ) ;
#35731=CARTESIAN_POINT ( 'NONE',  ( 0.1067246931122726866, 0.02962905676920215767, 0.000000000000000000 ) ) ;
#35732=CARTESIAN_POINT ( 'NONE',  ( -0.5455270741695672498, 1.205361022782829114E-17, -1.791688814994948808 ) ) ;
#35733=ORIENTED_EDGE ( 'NONE', *, *, #30172, .F. ) ;
#35739=VECTOR ( 'NONE', #42466, 39.37007874015748143 ) ;
#35741=CARTESIAN_POINT ( 'NONE',  ( 0.000000000000000000, 1.574803149606302854, 0.000000000000000000 ) ) ;
#35742=EDGE_LOOP ( 'NONE', ( #36760, #49135, #4076, #38486 ) ) ;
#35743=CARTESIAN_POINT ( 'NONE',  ( -2.889674983507169337, 1.674218314264582785, -0.6090712660038034576 ) ) ;
#35744=CIRCLE ( 'NONE', #280, 2.165354330708661568 ) ;
#35748=VERTEX_POINT ( 'NONE', #4128 ) ;
#35749=ORIENTED_EDGE ( 'NONE', *, *, #46965, .T. ) ;
#35750=CARTESIAN_POINT ( 'NONE',  ( -2.803169890850663037, 1.572684734721109923, 0.9280490062237302107 ) ) ;
#35755=CARTESIAN_POINT ( 'NONE',  ( -2.254603722160883006, 1.577541803200882553, -0.9101444522137277504 ) ) ;
#35759=CARTESIAN_POINT ( 'NONE',  ( -1.712529581123628741, 0.0001683915352326838515, -0.3403955095013877497 ) ) ;
#35760=ORIENTED_EDGE ( 'NONE', *, *, #31290, .T. ) ;
#35761=ORIENTED_EDGE ( 'NONE', *, *, #1120, .T. ) ;
#35762=EDGE_CURVE ( 'NONE', #35318, #33053, #40280, .T. ) ;
#35769=ORIENTED_EDGE ( 'NONE', *, *, #20569, .F. ) ;
#35773=DIRECTION ( 'NONE',  ( -0.8345732537213079727, 0.000000000000000000, 0.5508969814520945363 ) ) ;
#35774=EDGE_CURVE ( 'NONE', #14656, #7588, #17221, .T. ) ;
#35780=AXIS2_PLACEMENT_3D ( 'NONE', #45289, #6070, #45796 ) ;
#35783=CARTESIAN_POINT ( 'NONE',  ( 2.134236802639954522, 0.000000000000000000, -2.040539317874581204 ) ) ;
#35794=DIRECTION ( 'NONE',  ( 0.000000000000000000, 0.000000000000000000, 1.000000000000000000 ) ) ;
#35797=CARTESIAN_POINT ( 'NONE',  ( 0.04921259842519689481, 1.205361022782829114E-17, 1.934165248549660987 ) ) ;
#35798=ORIENTED_EDGE ( 'NONE', *, *, #30590, .T. ) ;
#35800=CARTESIAN_POINT ( 'NONE',  ( -1.734268221780295827, 0.000000000000000000, 0.1852605408175444779 ) ) ;
#35803=CARTESIAN_POINT ( 'NONE',  ( 1.214996082262586485, 1.694553939843470358, 1.937611079607071130 ) ) ;
#35804=PLANE ( 'NONE',  #23488 ) ;
#35805=ADVANCED_FACE ( 'NONE', ( #1781 ), #32062, .F. ) ;
#35806=CARTESIAN_POINT ( 'NONE',  ( -0.01649396867657461699, 0.000000000000000000, 1.928239385118262650 ) ) ;
#35807=ORIENTED_EDGE ( 'NONE', *, *, #39377, .F. ) ;
#35813=ORIENTED_EDGE ( 'NONE', *, *, #26829, .F. ) ;
#35814=PRODUCT_DEFINITION_FORMATION_WITH_SPECIFIED_SOURCE ( 'ANY', '', #28122, .NOT_KNOWN. ) ;
#35821=ORIENTED_EDGE ( 'NONE', *, *, #48945, .T. ) ;
#35824=CIRCLE ( 'NONE', #23426, 1.743387098533651480 ) ;
#35825=CARTESIAN_POINT ( 'NONE',  ( -2.122091976112999490, 1.205361022782829114E-17, 0.4338754535132819390 ) ) ;
#35827=FACE_OUTER_BOUND ( 'NONE', #49723, .T. ) ;
#35828=ADVANCED_FACE ( 'NONE', ( #5910 ), #25462, .T. ) ;
#35829=CARTESIAN_POINT ( 'NONE',  ( -0.3857230305054721864, 0.000000000000000000, 1.849896105471422025 ) ) ;
#35831=B_SPLINE_CURVE_WITH_KNOTS ( 'NONE', 3,
 ( #28244, #8892, #40404, #16389 ),
 .UNSPECIFIED., .F., .F.,
 ( 4, 4 ),
 ( 0.001738546130514813902, 0.004792765071277856927 ),
 .UNSPECIFIED. ) ;
#35833=DIRECTION ( 'NONE',  ( -0.01601477604151182663, 0.9998717552508123996, -0.000000000000000000 ) ) ;
#35834=ORIENTED_EDGE ( 'NONE', *, *, #4316, .T. ) ;
#35836=VERTEX_POINT ( 'NONE', #40522 ) ;
#35837=ORIENTED_EDGE ( 'NONE', *, *, #28530, .T. ) ;
#35838=CARTESIAN_POINT ( 'NONE',  ( -1.171400696859933532, 1.590714628027123823, 1.864644694871980590 ) ) ;
#35839=CARTESIAN_POINT ( 'NONE',  ( 2.126910391174609671, 1.205361022782829114E-17, 0.2384475364948296372 ) ) ;
#35846=DIRECTION ( 'NONE',  ( -0.01601477604151182663, 0.9998717552508123996, -0.000000000000000000 ) ) ;
#35848=VERTEX_POINT ( 'NONE', #36909 ) ;
#35850=CARTESIAN_POINT ( 'NONE',  ( -1.205050450470247725, 0.008618577144216254052, 1.304493073717302165 ) ) ;
#35854=PLANE ( 'NONE',  #25206 ) ;
#35858=EDGE_CURVE ( 'NONE', #16446, #42094, #9806, .T. ) ;
#35859=LINE ( 'NONE', #27588, #11968 ) ;
#35860=VERTEX_POINT ( 'NONE', #28633 ) ;
#35863=AXIS2_PLACEMENT_3D ( 'NONE', #47728, #5169, #40031 ) ;
#35868=DIRECTION ( 'NONE',  ( 0.2660368455666826115, 0.000000000000000000, -0.9639628606958511314 ) ) ;
#35871=ORIENTED_EDGE ( 'NONE', *, *, #30071, .T. ) ;
#35873=VERTEX_POINT ( 'NONE', #17033 ) ;
#35874=CARTESIAN_POINT ( 'NONE',  ( -2.165460538733998241, 5.905511811023623991, 0.04798874274652838168 ) ) ;
#35875=EDGE_LOOP ( 'NONE', ( #12132, #38215, #8877, #20361 ) ) ;
#35878=FACE_OUTER_BOUND ( 'NONE', #28344, .T. ) ;
#35879=EDGE_CURVE ( 'NONE', #36555, #3078, #18497, .T. ) ;
#35882=EDGE_CURVE ( 'NONE', #21553, #11117, #3667, .T. ) ;
#35890=B_SPLINE_CURVE_WITH_KNOTS ( 'NONE', 3,
 ( #11827, #43053, #31457, #12344 ),
 .UNSPECIFIED., .F., .F.,
 ( 4, 4 ),
 ( 0.0001309346361729752512, 0.002631017890005541739 ),
 .UNSPECIFIED. ) ;
#35892=ORIENTED_EDGE ( 'NONE', *, *, #14847, .F. ) ;
#35902=CARTESIAN_POINT ( 'NONE',  ( 2.203200495056982788, 1.648162179384485837, 1.241478329866867458 ) ) ;
#35904=DIRECTION ( 'NONE',  ( 0.000000000000000000, 0.000000000000000000, -1.000000000000000000 ) ) ;
#35908=LINE ( 'NONE', #796, #29895 ) ;
#35909=CARTESIAN_POINT ( 'NONE',  ( -0.2483447016818748909, 1.616937350427616327, -2.942339451681899032 ) ) ;
#35910=B_SPLINE_CURVE_WITH_KNOTS ( 'NONE', 3,
 ( #48057, #8345, #27959, #39840 ),
 .UNSPECIFIED., .F., .F.,
 ( 4, 4 ),
 ( 0.0008018406558999754529, 0.003302116852321945566 ),
 .UNSPECIFIED. ) ;
#35911=CARTESIAN_POINT ( 'NONE',  ( 0.000000000000000000, 1.574803149606302854, 0.000000000000000000 ) ) ;
#35912=ORIENTED_EDGE ( 'NONE', *, *, #23246, .T. ) ;
#35913=LINE ( 'NONE', #12161, #6993 ) ;
#35915=EDGE_CURVE ( 'NONE', #20856, #21785, #31383, .T. ) ;
#35916=CARTESIAN_POINT ( 'NONE',  ( 0.000000000000000000, 2.755905511811027164, 0.000000000000000000 ) ) ;
#35917=EDGE_CURVE ( 'NONE', #50600, #38070, #47961, .T. ) ;
#35922=VECTOR ( 'NONE', #47877, 39.37007874015748143 ) ;
#35930=FACE_OUTER_BOUND ( 'NONE', #5142, .T. ) ;
#35931=CONICAL_SURFACE ( 'NONE', #38411, 3.483074324928249421, 1.244861948955335196 ) ;
#35933=B_SPLINE_CURVE_WITH_KNOTS ( 'NONE', 3,
 ( #40961, #49663, #45060, #45808 ),
 .UNSPECIFIED., .F., .F.,
 ( 4, 4 ),
 ( 6.144603567270442506E-07, 0.001441218741676510108 ),
 .UNSPECIFIED. ) ;
#35936=CARTESIAN_POINT ( 'NONE',  ( 1.472219874544873131, 1.742205712729733014, 2.560030851058970214 ) ) ;
#35938=EDGE_LOOP ( 'NONE', ( #9134, #39499, #21616, #4577 ) ) ;
#35939=CARTESIAN_POINT ( 'NONE',  ( 0.08119777152254364916, 1.623385212329073957, 0.000000000000000000 ) ) ;
#35941=CARTESIAN_POINT ( 'NONE',  ( 1.983174097826134075, 0.5219917536725240392, 1.123077076632367888 ) ) ;
#35943=CARTESIAN_POINT ( 'NONE',  ( -2.574515777086982204, 1.675047042282418852, 0.7847656960372165758 ) ) ;
#35946=EDGE_LOOP ( 'NONE', ( #7641, #25514, #15393, #23749 ) ) ;
#35951=EDGE_CURVE ( 'NONE', #44591, #38140, #20956, .T. ) ;
#35952=VERTEX_POINT ( 'NONE', #7187 ) ;
#35954=CARTESIAN_POINT ( 'NONE',  ( -1.826696687228679616, 0.5248816248417013108, -1.146824545754332680 ) ) ;
#35963=LINE ( 'NONE', #24341, #10058 ) ;
#35964=DIRECTION ( 'NONE',  ( -3.981026654148454344E-17, 1.000000000000000000, -1.225234019452869602E-16 ) ) ;
#35965=AXIS2_PLACEMENT_3D ( 'NONE', #38643, #10760, #30129 ) ;
#35971=DIRECTION ( 'NONE',  ( -0.4338837391175656699, -1.045612331811453550E-16, 0.9009688679024154823 ) ) ;
#35973=CARTESIAN_POINT ( 'NONE',  ( 1.068075307999459822, 6.692913385826772199, 1.883606783264653028 ) ) ;
#35975=DIRECTION ( 'NONE',  ( -0.04486483035050446017, 1.288287287306305283E-16, -0.9989930665413151445 ) ) ;
#35976=CARTESIAN_POINT ( 'NONE',  ( 2.919426793319799707, 1.666276233232717896, 0.4451252810446822417 ) ) ;
#35981=ORIENTED_EDGE ( 'NONE', *, *, #38739, .T. ) ;
#35984=DIRECTION ( 'NONE',  ( 0.6234898018587319291, 1.288287287306305283E-16, 0.7818314824680311359 ) ) ;
#35988=EDGE_LOOP ( 'NONE', ( #26678, #5533, #31700, #49531 ) ) ;
#35990=DIRECTION ( 'NONE',  ( 0.9909497617679331460, -1.562041240006052286E-17, 0.1342332658176667026 ) ) ;
#35991=CARTESIAN_POINT ( 'NONE',  ( 2.308557526972506047, 0.000000000000000000, 1.841013194464792724 ) ) ;
#35992=EDGE_CURVE ( 'NONE', #8114, #20465, #3058, .T. ) ;
#35995=CARTESIAN_POINT ( 'NONE',  ( 2.252332422952718183, 1.743977176619643910, -0.5645583697864726691 ) ) ;
#36000=CARTESIAN_POINT ( 'NONE',  ( 2.277873973731426638, 1.463603380278871713, 1.879489153247667632 ) ) ;
#36006=CARTESIAN_POINT ( 'NONE',  ( -0.04921259842519706829, 1.516406576848131849, 2.952755905511811108 ) ) ;
#36009=CARTESIAN_POINT ( 'NONE',  ( 0.9959141370152501116, 1.049866565877818125, 1.762829326744137948 ) ) ;
#36013=AXIS2_PLACEMENT_3D ( 'NONE', #43760, #47865, #8417 ) ;
#36014=CONICAL_SURFACE ( 'NONE', #13758, 2.244934639244524632, 1.554780866114618743 ) ;
#36015=VERTEX_POINT ( 'NONE', #14166 ) ;
#36016=VERTEX_POINT ( 'NONE', #45383 ) ;
#36019=B_SPLINE_CURVE_WITH_KNOTS ( 'NONE', 3,
 ( #3151, #15027, #30776, #15278 ),
 .UNSPECIFIED., .F., .F.,
 ( 4, 4 ),
 ( 2.330000277661172139E-07, 0.002500456362147902671 ),
 .UNSPECIFIED. ) ;
#36023=DIRECTION ( 'NONE',  ( -0.9909497617679332571, 0.000000000000000000, -0.1342332658176667304 ) ) ;
#36024=CARTESIAN_POINT ( 'NONE',  ( -1.252182360577274611, 1.655037561631665266, -1.807206635494494451 ) ) ;
#36025=CARTESIAN_POINT ( 'NONE',  ( -0.3136974817027962104, 5.905511811023624880, -2.936457595020223632 ) ) ;
#36029=DIRECTION ( 'NONE',  ( -0.9998717552508122886, -0.01601477604151182316, 0.000000000000000000 ) ) ;
#36031=CARTESIAN_POINT ( 'NONE',  ( -2.139229417893219853, 1.205361022782829114E-17, -0.3394403656973710159 ) ) ;
#36035=VERTEX_POINT ( 'NONE', #50241 ) ;
#36036=ORIENTED_EDGE ( 'NONE', *, *, #9729, .F. ) ;
#36037=CARTESIAN_POINT ( 'NONE',  ( 0.000000000000000000, 0.000000000000000000, 0.000000000000000000 ) ) ;
#36038=AXIS2_PLACEMENT_3D ( 'NONE', #20229, #20497, #5005 ) ;
#36042=B_SPLINE_CURVE_WITH_KNOTS ( 'NONE', 3,
 ( #39807, #32853, #48535, #5970 ),
 .UNSPECIFIED., .F., .F.,
 ( 4, 4 ),
 ( 0.1211775127643062444, 0.1625894504277921315 ),
 .UNSPECIFIED. ) ;
#36044=AXIS2_PLACEMENT_3D ( 'NONE', #11021, #10767, #30392 ) ;
#36061=ORIENTED_EDGE ( 'NONE', *, *, #31488, .T. ) ;
#36062=CARTESIAN_POINT ( 'NONE',  ( 1.530693736245519299, 5.905511811023623991, -1.531579597454042929 ) ) ;
#36066=EDGE_LOOP ( 'NONE', ( #25907, #26729, #22984, #12932, #18943, #41964, #16512, #41015, #8079, #1242, #49422, #37883, #25939 ) ) ;
#36068=ORIENTED_EDGE ( 'NONE', *, *, #32631, .T. ) ;
#36072=EDGE_CURVE ( 'NONE', #7052, #28425, #33554, .T. ) ;
#36078=CARTESIAN_POINT ( 'NONE',  ( 1.854041947016408010, 0.000000000000000000, 1.016381156669627694 ) ) ;
#36086=FACE_OUTER_BOUND ( 'NONE', #18555, .T. ) ;
#36091=EDGE_LOOP ( 'NONE', ( #9682, #5345, #21776, #31919, #35691, #18763 ) ) ;
#36093=EDGE_CURVE ( 'NONE', #48706, #21112, #14426, .T. ) ;
#36097=CARTESIAN_POINT ( 'NONE',  ( -2.161044708975090156, 0.000000000000000000, 0.1463148319730351032 ) ) ;
#36098=CARTESIAN_POINT ( 'NONE',  ( 2.005112362574620111, 0.03937352102360182349, 0.2219488725060905498 ) ) ;
#36099=EDGE_LOOP ( 'NONE', ( #1554, #36280, #3633, #1069 ) ) ;
#36100=CARTESIAN_POINT ( 'NONE',  ( 0.1525302393087137887, 1.710345001767278994, -2.243756654240526505 ) ) ;
#36101=ORIENTED_EDGE ( 'NONE', *, *, #37803, .F. ) ;
#36107=VERTEX_POINT ( 'NONE', #30933 ) ;
#36108=VERTEX_POINT ( 'NONE', #50735 ) ;
#36110=LINE ( 'NONE', #16231, #4844 ) ;
#36111=CARTESIAN_POINT ( 'NONE',  ( 0.08119777152254364916, 1.623385212329073957, 0.000000000000000000 ) ) ;
#36113=CARTESIAN_POINT ( 'NONE',  ( -2.164823134740036181, 5.905511811023623991, -0.04796011690018279344 ) ) ;
#36114=CARTESIAN_POINT ( 'NONE',  ( -2.867773316779185677, 1.674559808355669199, -0.7050287376752426560 ) ) ;
#36119=EDGE_CURVE ( 'NONE', #49090, #27844, #12272, .T. ) ;
#36120=CARTESIAN_POINT ( 'NONE',  ( 0.08139965876239094178, 1.610780518492231694, 0.000000000000000000 ) ) ;
#36125=ORIENTED_EDGE ( 'NONE', *, *, #8343, .F. ) ;
#36127=B_SPLINE_CURVE_WITH_KNOTS ( 'NONE', 3,
 ( #45955, #30998, #10621, #11372 ),
 .UNSPECIFIED., .F., .F.,
 ( 4, 4 ),
 ( 6.128883314497806983E-05, 0.002561329735754209504 ),
 .UNSPECIFIED. ) ;
#36128=CARTESIAN_POINT ( 'NONE',  ( -1.882988517681398966, 1.574803149606302854, 1.069164917025789530 ) ) ;
#36132=LINE ( 'NONE', #762, #33224 ) ;
#36134=ORIENTED_EDGE ( 'NONE', *, *, #11167, .T. ) ;
#36136=VERTEX_POINT ( 'NONE', #28763 ) ;
#36138=CARTESIAN_POINT ( 'NONE',  ( 2.823445274216730638, 1.763256531483745837, 0.8656477926280683466 ) ) ;
#36139=CONICAL_SURFACE ( 'NONE', #24606, 3.033577403570480779, 1.554780866114618743 ) ;
#36140=EDGE_CURVE ( 'NONE', #2179, #33261, #3559, .T. ) ;
#36141=DIRECTION ( 'NONE',  ( 0.1785568947986370669, 0.000000000000000000, -0.9839295885986296675 ) ) ;
#36143=ORIENTED_EDGE ( 'NONE', *, *, #50400, .F. ) ;
#36145=CARTESIAN_POINT ( 'NONE',  ( 2.051629384040484005, 0.01961290521451679661, 0.3275741348515084916 ) ) ;
#36152=ADVANCED_FACE ( 'NONE', ( #31185 ), #11310, .T. ) ;
#36153=VERTEX_POINT ( 'NONE', #44505 ) ;
#36155=CARTESIAN_POINT ( 'NONE',  ( -2.623503965249869729, 1.579940539283962053, 1.355882097269835107 ) ) ;
#36160=AXIS2_PLACEMENT_3D ( 'NONE', #15162, #11292, #27787 ) ;
#36169=ORIENTED_EDGE ( 'NONE', *, *, #47032, .T. ) ;
#36174=LINE ( 'NONE', #801, #42902 ) ;
#36176=CARTESIAN_POINT ( 'NONE',  ( -0.4788131938641533303, 1.711801685632677428, 2.914091152102185944 ) ) ;
#36178=EDGE_CURVE ( 'NONE', #36611, #47661, #38787, .T. ) ;
#36191=CARTESIAN_POINT ( 'NONE',  ( 1.847133430398848697, 0.5249316497054296038, -0.3711179597262244112 ) ) ;
#36192=VERTEX_POINT ( 'NONE', #4077 ) ;
#36194=ORIENTED_EDGE ( 'NONE', *, *, #29400, .F. ) ;
#36195=DIRECTION ( 'NONE',  ( 0.000000000000000000, 1.000000000000000000, -0.000000000000000000 ) ) ;
#36197=AXIS2_PLACEMENT_3D ( 'NONE', #41396, #10409, #41650 ) ;
#36198=DIRECTION ( 'NONE',  ( 0.000000000000000000, 0.000000000000000000, 1.000000000000000000 ) ) ;
#36201=CARTESIAN_POINT ( 'NONE',  ( 1.979793062125284830, 1.470624965921384364, 2.191257344206569257 ) ) ;
#36205=ORIENTED_EDGE ( 'NONE', *, *, #46796, .F. ) ;
#36209=VERTEX_POINT ( 'NONE', #39690 ) ;
#36210=CARTESIAN_POINT ( 'NONE',  ( -1.087426130748108788, 0.01050254589070086231, -1.412988192946641020 ) ) ;
#36213=EDGE_CURVE ( 'NONE', #34811, #37003, #3574, .T. ) ;
#36217=CARTESIAN_POINT ( 'NONE',  ( -0.9259623415327485896, 0.000000000000000000, 1.581646091660971143 ) ) ;
#36225=CARTESIAN_POINT ( 'NONE',  ( 1.083598637574782142, 1.491270273546293046, 2.747180975113346246 ) ) ;
#36227=EDGE_LOOP ( 'NONE', ( #603, #8352, #5468, #45792 ) ) ;
#36228=LINE ( 'NONE', #853, #44351 ) ;
#36229=DIRECTION ( 'NONE',  ( 1.000000000000000000, 0.000000000000000000, 0.000000000000000000 ) ) ;
#36231=CARTESIAN_POINT ( 'NONE',  ( 1.775400203342704986, 1.648464234653929106, -2.359903268218703332 ) ) ;
#36232=CARTESIAN_POINT ( 'NONE',  ( -0.3452076480189834040, 0.5241083961098278454, 2.177863912564995008 ) ) ;
#36237=CARTESIAN_POINT ( 'NONE',  ( 2.074656761899007495, 1.205361022782829114E-17, -0.6223516566630619140 ) ) ;
#36238=ADVANCED_FACE ( 'NONE', ( #15180 ), #17664, .T. ) ;
#36239=AXIS2_PLACEMENT_3D ( 'NONE', #39035, #7542, #19655 ) ;
#36243=EDGE_CURVE ( 'NONE', #33537, #22117, #13793, .T. ) ;
#36244=DIRECTION ( 'NONE',  ( -0.01601477604151182663, 0.9998717552508123996, -0.000000000000000000 ) ) ;
#36246=CARTESIAN_POINT ( 'NONE',  ( 2.016369045219287948, 1.641772594434526278, 1.140940039539855677 ) ) ;
#36248=EDGE_CURVE ( 'NONE', #39521, #40227, #23791, .T. ) ;
#36249=CARTESIAN_POINT ( 'NONE',  ( 0.08139965876239094178, 1.610780518492231694, 0.000000000000000000 ) ) ;
#36253=CARTESIAN_POINT ( 'NONE',  ( -2.338262049203568171, 2.755905511811027164, -0.7080022065394829811 ) ) ;
#36254=CARTESIAN_POINT ( 'NONE',  ( -1.068402561569948617, 1.205361022782829114E-17, -1.884154513482188431 ) ) ;
#36255=DIRECTION ( 'NONE',  ( -0.000000000000000000, -1.000000000000000000, -0.000000000000000000 ) ) ;
#36261=ORIENTED_EDGE ( 'NONE', *, *, #27076, .T. ) ;
#36269=DIRECTION ( 'NONE',  ( 0.2660368455666826115, 0.000000000000000000, -0.9639628606958511314 ) ) ;
#36270=ORIENTED_EDGE ( 'NONE', *, *, #20764, .F. ) ;
#36271=VERTEX_POINT ( 'NONE', #33169 ) ;
#36272=DIRECTION ( 'NONE',  ( -1.105928667600727183E-16, 1.000000000000000000, 6.607616187506045307E-17 ) ) ;
#36274=EDGE_LOOP ( 'NONE', ( #47934, #5236, #37121, #24450 ) ) ;
#36278=PLANE ( 'NONE',  #15408 ) ;
#36280=ORIENTED_EDGE ( 'NONE', *, *, #26840, .F. ) ;
#36290=EDGE_CURVE ( 'NONE', #4750, #42832, #6034, .T. ) ;
#36291=DIRECTION ( 'NONE',  ( 0.000000000000000000, 0.000000000000000000, -1.000000000000000000 ) ) ;
#36292=VERTEX_POINT ( 'NONE', #29276 ) ;
#36294=PLANE ( 'NONE',  #44022 ) ;
#36297=DIRECTION ( 'NONE',  ( -0.01601477604151182663, 0.9998717552508123996, -0.000000000000000000 ) ) ;
#36304=EDGE_CURVE ( 'NONE', #30628, #25553, #2396, .T. ) ;
#36305=CIRCLE ( 'NONE', #3309, 1.850107469027523432 ) ;
#36306=CARTESIAN_POINT ( 'NONE',  ( -2.150518151785907772, 1.673457466938482296, -0.2530435858860717313 ) ) ;
#36315=LINE ( 'NONE', #28550, #46245 ) ;
#36316=EDGE_LOOP ( 'NONE', ( #41923, #44706, #1738, #840 ) ) ;
#36319=ORIENTED_EDGE ( 'NONE', *, *, #36702, .T. ) ;
#36322=CARTESIAN_POINT ( 'NONE',  ( -1.748857564167104472, 1.593560878921895352, -2.379187624385278532 ) ) ;
#36323=ORIENTED_EDGE ( 'NONE', *, *, #21854, .T. ) ;
#36325=ORIENTED_EDGE ( 'NONE', *, *, #13860, .T. ) ;
#36327=CARTESIAN_POINT ( 'NONE',  ( 1.571584482197274202, 0.9990897620696875814, -2.079374994526344000 ) ) ;
#36328=CARTESIAN_POINT ( 'NONE',  ( -0.9916727432047125479, 0.5239746995928241668, -1.945806201603022645 ) ) ;
#36334=ORIENTED_EDGE ( 'NONE', *, *, #47386, .F. ) ;
#36338=CARTESIAN_POINT ( 'NONE',  ( 1.236813753895252166, 1.487789312410982445, -2.681693691597563767 ) ) ;
#36349=B_SPLINE_CURVE_WITH_KNOTS ( 'NONE', 3,
 ( #28346, #44348, #5629, #48442 ),
 .UNSPECIFIED., .F., .F.,
 ( 4, 4 ),
 ( 0.01475822760527119651, 0.03075144468528176467 ),
 .UNSPECIFIED. ) ;
#36354=ORIENTED_EDGE ( 'NONE', *, *, #47007, .T. ) ;
#36359=ORIENTED_EDGE ( 'NONE', *, *, #35713, .T. ) ;
#36360=CARTESIAN_POINT ( 'NONE',  ( 2.755905511811024056, 2.913385826771657250, -1.023622047244094224 ) ) ;
#36363=PLANE ( 'NONE',  #35446 ) ;
#36366=CARTESIAN_POINT ( 'NONE',  ( 0.000000000000000000, 6.692913385826772199, 0.000000000000000000 ) ) ;
#36370=DIRECTION ( 'NONE',  ( -0.9998717552508122886, -0.01601477604151181275, 0.000000000000000000 ) ) ;
#36371=DIRECTION ( 'NONE',  ( 0.9639628606958549062, 0.000000000000000000, -0.2660368455666687892 ) ) ;
#36386=LINE ( 'NONE', #4629, #27700 ) ;
#36387=EDGE_LOOP ( 'NONE', ( #22467, #4318, #2572, #19123 ) ) ;
#36388=CARTESIAN_POINT ( 'NONE',  ( 1.775400203342704986, 1.648464234653929106, -2.359903268218703332 ) ) ;
#36389=B_SPLINE_CURVE_WITH_KNOTS ( 'NONE', 3,
 ( #16180, #8940, #40190, #939 ),
 .UNSPECIFIED., .F., .F.,
 ( 4, 4 ),
 ( 0.01369329263415524495, 0.03074394281915088928 ),
 .UNSPECIFIED. ) ;
#36399=EDGE_CURVE ( 'NONE', #2009, #29934, #25945, .T. ) ;
#36400=FACE_OUTER_BOUND ( 'NONE', #3142, .T. ) ;
#36401=CARTESIAN_POINT ( 'NONE',  ( 2.150824344285287459, 1.742351338968239238, -0.8657870173518766865 ) ) ;
#36404=CIRCLE ( 'NONE', #10823, 2.165354330708661568 ) ;
#36405=AXIS2_PLACEMENT_3D ( 'NONE', #36031, #1420, #24667 ) ;
#36406=CARTESIAN_POINT ( 'NONE',  ( 2.793030215715258446, 5.118110236220475784, 0.9592557174602684977 ) ) ;
#36411=CARTESIAN_POINT ( 'NONE',  ( -2.576863348864732117, 1.580667355030889620, 1.442554885838411849 ) ) ;
#36412=VECTOR ( 'NONE', #23620, 39.37007874015748143 ) ;
#36417=DIRECTION ( 'NONE',  ( 0.3513748240813304724, 0.000000000000000000, 0.9362348706397417564 ) ) ;
#36418=AXIS2_PLACEMENT_3D ( 'NONE', #30536, #42647, #38039 ) ;
#36421=CARTESIAN_POINT ( 'NONE',  ( 0.07982360342473591996, 1.709180471932028711, 0.000000000000000000 ) ) ;
#36422=DIRECTION ( 'NONE',  ( -0.8805955318567321166, 5.503865196449042635E-17, -0.4738686624730094055 ) ) ;
#36424=ORIENTED_EDGE ( 'NONE', *, *, #35879, .T. ) ;
#36425=LINE ( 'NONE', #40554, #28257 ) ;
#36431=B_SPLINE_CURVE_WITH_KNOTS ( 'NONE', 3,
 ( #22983, #27345, #43599, #19096 ),
 .UNSPECIFIED., .F., .F.,
 ( 4, 4 ),
 ( 0.1211775127643062999, 0.1625894504277921315 ),
 .UNSPECIFIED. ) ;
#36433=ADVANCED_FACE ( 'NONE', ( #26197 ), #33956, .F. ) ;
#36439=EDGE_LOOP ( 'NONE', ( #20678, #15951, #30561, #23234, #45950, #17407 ) ) ;
#36441=VERTEX_POINT ( 'NONE', #6330 ) ;
#36445=CARTESIAN_POINT ( 'NONE',  ( 1.984304711592181691, 1.049866565877818125, -0.4024264095323374368 ) ) ;
#36447=AXIS2_PLACEMENT_3D ( 'NONE', #7060, #50365, #7313 ) ;
#36451=VECTOR ( 'NONE', #3767, 39.37007874015748854 ) ;
#36454=EDGE_CURVE ( 'NONE', #3395, #16985, #6531, .T. ) ;
#36455=AXIS2_PLACEMENT_3D ( 'NONE', #23157, #11296, #50724 ) ;
#36461=ORIENTED_EDGE ( 'NONE', *, *, #47745, .F. ) ;
#36462=CARTESIAN_POINT ( 'NONE',  ( -1.738885967245169306, 1.688171000478772887, 2.065113283993135429 ) ) ;
#36464=EDGE_LOOP ( 'NONE', ( #10130, #32692, #24330, #31935 ) ) ;
#36465=CARTESIAN_POINT ( 'NONE',  ( -1.105178190331685961, 1.205361022782829114E-17, -1.437421806808603542 ) ) ;
#36467=DIRECTION ( 'NONE',  ( -0.9909497617679331460, 0.000000000000000000, -0.1342332658176667026 ) ) ;
#36471=CARTESIAN_POINT ( 'NONE',  ( -2.160407304981126320, 1.574879494900809584, -0.1462862061266896330 ) ) ;
#36474=EDGE_LOOP ( 'NONE', ( #32512, #14942, #9374, #47864, #3230, #43553, #43419, #45344, #15137, #27172, #24008 ) ) ;
#36478=ORIENTED_EDGE ( 'NONE', *, *, #1265, .T. ) ;
#36481=CARTESIAN_POINT ( 'NONE',  ( -0.9971138720282235468, 1.601380608780962778, 2.516743141396816430 ) ) ;
#36489=CARTESIAN_POINT ( 'NONE',  ( 2.193564619503452828, 1.644610705845120258, 0.7644775380370429918 ) ) ;
#36495=VECTOR ( 'NONE', #2078, 39.37007874015748143 ) ;
#36496=EDGE_CURVE ( 'NONE', #12681, #28527, #44428, .T. ) ;
#36497=CARTESIAN_POINT ( 'NONE',  ( 2.437180031585944207, 1.757239404341893518, -1.667735833703099191 ) ) ;
#36500=ORIENTED_EDGE ( 'NONE', *, *, #32965, .T. ) ;
#36502=CARTESIAN_POINT ( 'NONE',  ( -1.743145509346916588, 0.000000000000000000, 0.000000000000000000 ) ) ;
#36507=CARTESIAN_POINT ( 'NONE',  ( -1.064142702668968932, 0.000000000000000000, -1.380941303491921346 ) ) ;
#36513=CARTESIAN_POINT ( 'NONE',  ( -1.010509689441836390, 0.01173450346422093109, -1.474572740271697047 ) ) ;
#36515=CARTESIAN_POINT ( 'NONE',  ( 1.333043869570198714, 0.03249744100148316966, 1.450993329683806676 ) ) ;
#36522=EDGE_CURVE ( 'NONE', #26498, #48342, #41978, .T. ) ;
#36532=DIRECTION ( 'NONE',  ( -0.01601477604151182663, 0.9998717552508123996, -0.000000000000000000 ) ) ;
#36534=EDGE_CURVE ( 'NONE', #46444, #47197, #15087, .T. ) ;
#36536=AXIS2_PLACEMENT_3D ( 'NONE', #32304, #24545, #44916 ) ;
#36541=CARTESIAN_POINT ( 'NONE',  ( -0.04921259842519689481, 0.009044826170997494544, 1.897191039754219988 ) ) ;
#36553=VERTEX_POINT ( 'NONE', #26945 ) ;
#36554=CARTESIAN_POINT ( 'NONE',  ( 0.07982360342473591996, 1.709180471932028711, 0.000000000000000000 ) ) ;
#36555=VERTEX_POINT ( 'NONE', #23838 ) ;
#36557=CARTESIAN_POINT ( 'NONE',  ( 0.7697289541298216742, 1.632794381801279116, -2.850711116225059794 ) ) ;
#36558=CARTESIAN_POINT ( 'NONE',  ( 2.138597145901430352, 6.692913385826772199, 0.3393547186367261159 ) ) ;
#36559=CARTESIAN_POINT ( 'NONE',  ( 2.823445274216730638, 1.664781993127344872, 0.8656477926280681245 ) ) ;
#36560=AXIS2_PLACEMENT_3D ( 'NONE', #3127, #18881, #43873 ) ;
#36561=DIRECTION ( 'NONE',  ( -0.9839295885986295565, 2.076492729081308301E-17, -0.1785568947986370392 ) ) ;
#36566=LINE ( 'NONE', #5066, #33101 ) ;
#36569=EDGE_LOOP ( 'NONE', ( #8665, #24075, #36978, #39593 ) ) ;
#36573=ORIENTED_EDGE ( 'NONE', *, *, #2535, .F. ) ;
#36576=DIRECTION ( 'NONE',  ( -0.3090169943749447312, 0.000000000000000000, -0.9510565162951544194 ) ) ;
#36577=EDGE_CURVE ( 'NONE', #1678, #24825, #49176, .T. ) ;
#36581=DIRECTION ( 'NONE',  ( 0.000000000000000000, 0.000000000000000000, -1.000000000000000000 ) ) ;
#36582=ORIENTED_EDGE ( 'NONE', *, *, #30629, .T. ) ;
#36587=CARTESIAN_POINT ( 'NONE',  ( 2.059921668671832240, 5.905511811023623991, 0.7210543110491621777 ) ) ;
#36590=CARTESIAN_POINT ( 'NONE',  ( -1.088226697794229869, 1.657663611856292185, 1.917334528692921758 ) ) ;
#36592=EDGE_CURVE ( 'NONE', #33511, #10224, #23083, .T. ) ;
#36593=CARTESIAN_POINT ( 'NONE',  ( 0.08119777152254364916, 1.623385212329073957, 0.000000000000000000 ) ) ;
#36594=VERTEX_POINT ( 'NONE', #3460 ) ;
#36595=DIRECTION ( 'NONE',  ( 0.01601477604151182663, -0.9998717552508123996, 0.000000000000000000 ) ) ;
#36599=ADVANCED_FACE ( 'NONE', ( #39079 ), #18062, .T. ) ;
#36600=AXIS2_PLACEMENT_3D ( 'NONE', #13058, #23898, #32949 ) ;
#36601=CARTESIAN_POINT ( 'NONE',  ( 1.232995795418176055, 1.205361022782829114E-17, 1.780798594093568221 ) ) ;
#36602=ORIENTED_EDGE ( 'NONE', *, *, #46960, .F. ) ;
#36604=CARTESIAN_POINT ( 'NONE',  ( 0.000000000000000000, 6.692913385826772199, 0.000000000000000000 ) ) ;
#36608=AXIS2_PLACEMENT_3D ( 'NONE', #5111, #47674, #12351 ) ;
#36611=VERTEX_POINT ( 'NONE', #44712 ) ;
#36613=AXIS2_PLACEMENT_3D ( 'NONE', #36955, #48516, #9320 ) ;
#36619=ORIENTED_EDGE ( 'NONE', *, *, #40489, .F. ) ;
#36620=DIRECTION ( 'NONE',  ( -0.6579387259397027066, 8.743779800425989470E-17, -0.7530714660036196273 ) ) ;
#36624=CARTESIAN_POINT ( 'NONE',  ( 0.07982360342473591996, 1.709180471932028711, 0.000000000000000000 ) ) ;
#36625=CARTESIAN_POINT ( 'NONE',  ( -2.101347671104863313, 1.674245022174266406, -0.5300970854448181502 ) ) ;
#36628=DIRECTION ( 'NONE',  ( -0.9998717552508121775, -0.01601477604151182316, 0.000000000000000000 ) ) ;
#36633=CARTESIAN_POINT ( 'NONE',  ( -0.8515791614234526907, 0.000000000000000000, 1.521253268579204398 ) ) ;
#36637=ORIENTED_EDGE ( 'NONE', *, *, #224, .T. ) ;
#36640=AXIS2_PLACEMENT_3D ( 'NONE', #37281, #33417, #13781 ) ;
#36642=CIRCLE ( 'NONE', #2844, 2.244934639244525076 ) ;
#36652=ORIENTED_EDGE ( 'NONE', *, *, #45684, .F. ) ;
#36656=FACE_OUTER_BOUND ( 'NONE', #7115, .T. ) ;
#36658=EDGE_LOOP ( 'NONE', ( #10226, #16997, #39800, #46152 ) ) ;
#36666=CARTESIAN_POINT ( 'NONE',  ( 0.4161812636739331550, 0.000000000000000000, -1.692983086477933830 ) ) ;
#36670=DIRECTION ( 'NONE',  ( 0.000000000000000000, 0.000000000000000000, 1.000000000000000000 ) ) ;
#36673=ORIENTED_EDGE ( 'NONE', *, *, #43425, .T. ) ;
#36677=CONICAL_SURFACE ( 'NONE', #4413, 2.165354330708661568, 0.2617993877991570129 ) ;
#36678=CARTESIAN_POINT ( 'NONE',  ( 2.164823134740036625, 5.118110236220475784, -0.04796011690015051371 ) ) ;
#36681=ORIENTED_EDGE ( 'NONE', *, *, #38802, .F. ) ;
#36684=DIRECTION ( 'NONE',  ( 0.9998717552508121775, 0.01601477604151182663, 0.000000000000000000 ) ) ;
#36689=CARTESIAN_POINT ( 'NONE',  ( 0.6551740444401462637, 0.000000000000000000, 1.885762267972743711 ) ) ;
#36691=EDGE_CURVE ( 'NONE', #40889, #31073, #8990, .T. ) ;
#36692=ORIENTED_EDGE ( 'NONE', *, *, #46326, .T. ) ;
#36695=EDGE_CURVE ( 'NONE', #37948, #16316, #20862, .T. ) ;
#36697=EDGE_CURVE ( 'NONE', #40266, #16563, #40612, .T. ) ;
#36698=EDGE_LOOP ( 'NONE', ( #45094, #2598, #24968, #34679, #46638, #10091, #26558, #31201, #9324, #22449, #26299, #45654, #40736 ) ) ;
#36699=CARTESIAN_POINT ( 'NONE',  ( 2.274988110810610031, 1.744340048923221920, -0.4687729985174870495 ) ) ;
#36702=EDGE_CURVE ( 'NONE', #20337, #10224, #8601, .T. ) ;
#36703=AXIS2_PLACEMENT_3D ( 'NONE', #9313, #22216, #30716 ) ;
#36704=CONICAL_SURFACE ( 'NONE', #14447, 3.033577403570480779, 1.554780866114618743 ) ;
#36706=VECTOR ( 'NONE', #20617, 39.37007874015748143 ) ;
#36710=ORIENTED_EDGE ( 'NONE', *, *, #12033, .T. ) ;
#36711=CARTESIAN_POINT ( 'NONE',  ( 1.427293369312940152, 0.000000000000000000, -1.001115484471646111 ) ) ;
#36714=ORIENTED_EDGE ( 'NONE', *, *, #3228, .T. ) ;
#36720=VERTEX_POINT ( 'NONE', #4475 ) ;
#36721=VERTEX_POINT ( 'NONE', #35976 ) ;
#36725=CARTESIAN_POINT ( 'NONE',  ( 2.422542647548854511, 1.750080673592185665, 0.7353866329521624445 ) ) ;
#36727=CARTESIAN_POINT ( 'NONE',  ( -0.04921259842519708910, 1.718497255264965551, 2.952755905511811108 ) ) ;
#36731=VERTEX_POINT ( 'NONE', #43952 ) ;
#36738=EDGE_CURVE ( 'NONE', #23605, #40028, #9162, .T. ) ;
#36742=EDGE_LOOP ( 'NONE', ( #1736, #9434, #22938, #39525 ) ) ;
#36744=VECTOR ( 'NONE', #15661, 39.37007874015748143 ) ;
#36748=DIRECTION ( 'NONE',  ( 0.1785568947986370392, 1.142009442734629415E-16, -0.9839295885986295565 ) ) ;
#36760=ORIENTED_EDGE ( 'NONE', *, *, #50951, .T. ) ;
#36764=ORIENTED_EDGE ( 'NONE', *, *, #30650, .T. ) ;
#36766=ADVANCED_FACE ( 'NONE', ( #28724 ), #48521, .T. ) ;
#36767=FACE_OUTER_BOUND ( 'NONE', #47764, .T. ) ;
#36768=EDGE_LOOP ( 'NONE', ( #4648, #43712, #23930, #5517 ) ) ;
#36770=CARTESIAN_POINT ( 'NONE',  ( 2.947574761915769059, 5.905511811023623991, -0.1816379373804906106 ) ) ;
#36782=VECTOR ( 'NONE', #1238, 39.37007874015748143 ) ;
#36788=CARTESIAN_POINT ( 'NONE',  ( -1.711605288297850969, 0.0005051743623580321960, -0.3401845456954783464 ) ) ;
#36793=VECTOR ( 'NONE', #12629, 39.37007874015748143 ) ;
#36796=VERTEX_POINT ( 'NONE', #17881 ) ;
#36802=ORIENTED_EDGE ( 'NONE', *, *, #5822, .F. ) ;
#36806=B_SPLINE_CURVE_WITH_KNOTS ( 'NONE', 3,
 ( #50249, #6938, #31701, #47401 ),
 .UNSPECIFIED., .F., .F.,
 ( 4, 4 ),
 ( 0.1211873102087489551, 0.1625992483279400103 ),
 .UNSPECIFIED. ) ;
#36808=ORIENTED_EDGE ( 'NONE', *, *, #3106, .F. ) ;
#36810=ORIENTED_EDGE ( 'NONE', *, *, #42197, .F. ) ;
#36813=CARTESIAN_POINT ( 'NONE',  ( 0.8952071785065199849, 1.205361022782829114E-17, 1.972340328593147785 ) ) ;
#36815=ADVANCED_FACE ( 'NONE', ( #5750 ), #44969, .F. ) ;
#36817=CARTESIAN_POINT ( 'NONE',  ( 1.135809427359538271, 0.01508310756785651019, -1.647033034181351052 ) ) ;
#36820=AXIS2_PLACEMENT_3D ( 'NONE', #30723, #22972, #10344 ) ;
#36842=DIRECTION ( 'NONE',  ( 0.000000000000000000, -1.000000000000000000, 0.000000000000000000 ) ) ;
#36846=EDGE_LOOP ( 'NONE', ( #9749, #14606, #5711 ) ) ;
#36850=EDGE_LOOP ( 'NONE', ( #23261, #29614, #33824, #48428, #50777, #3321, #46350, #3996 ) ) ;
#36851=DIRECTION ( 'NONE',  ( 0.9998717552508121775, 0.01601477604151182663, 0.000000000000000000 ) ) ;
#36852=ORIENTED_EDGE ( 'NONE', *, *, #51006, .F. ) ;
#36856=CARTESIAN_POINT ( 'NONE',  ( -2.157989646284840468, 1.673342082170779621, -0.1819910592820468964 ) ) ;
#36859=CARTESIAN_POINT ( 'NONE',  ( 0.7381027496705272473, 1.730766751998747521, -2.859439394060913298 ) ) ;
#36860=ORIENTED_EDGE ( 'NONE', *, *, #26883, .F. ) ;
#36861=B_SPLINE_CURVE_WITH_KNOTS ( 'NONE', 3,
 ( #27699, #23575, #11959, #31589 ),
 .UNSPECIFIED., .F., .F.,
 ( 4, 4 ),
 ( 2.032841336367455452E-07, 0.01843528932679509152 ),
 .UNSPECIFIED. ) ;
#36863=EDGE_CURVE ( 'NONE', #17189, #47793, #45975, .T. ) ;
#36865=EDGE_CURVE ( 'NONE', #40614, #12124, #45216, .T. ) ;
#36867=ORIENTED_EDGE ( 'NONE', *, *, #41438, .F. ) ;
#36869=CARTESIAN_POINT ( 'NONE',  ( -2.464291103507775915, 0.000000000000000000, -1.626664315311338260 ) ) ;
#36870=EDGE_CURVE ( 'NONE', #19430, #13784, #15616, .T. ) ;
#36872=CARTESIAN_POINT ( 'NONE',  ( -0.4358240471401270688, 1.708633904392455660, 2.677201428532125949 ) ) ;
#36876=B_SPLINE_CURVE_WITH_KNOTS ( 'NONE', 3,
 ( #46431, #50041, #26088, #11102 ),
 .UNSPECIFIED., .F., .F.,
 ( 4, 4 ),
 ( 4.094226701244036431E-07, 0.04399192588115360264 ),
 .UNSPECIFIED. ) ;
#36877=ORIENTED_EDGE ( 'NONE', *, *, #6525, .T. ) ;
#36880=ORIENTED_EDGE ( 'NONE', *, *, #30853, .T. ) ;
#36883=EDGE_CURVE ( 'NONE', #50795, #24825, #33131, .T. ) ;
#36884=CARTESIAN_POINT ( 'NONE',  ( 1.785493683324574254, 0.000000000000000000, -1.119626681005672530 ) ) ;
#36886=EDGE_CURVE ( 'NONE', #11192, #16625, #46604, .T. ) ;
#36887=DIRECTION ( 'NONE',  ( -0.4738686624729965269, 0.000000000000000000, -0.8805955318567391110 ) ) ;
#36888=ORIENTED_EDGE ( 'NONE', *, *, #22756, .T. ) ;
#36891=VECTOR ( 'NONE', #41649, 39.37007874015748143 ) ;
#36894=ORIENTED_EDGE ( 'NONE', *, *, #37870, .T. ) ;
#36896=LINE ( 'NONE', #1517, #34183 ) ;
#36897=EDGE_CURVE ( 'NONE', #39028, #26405, #30006, .T. ) ;
#36900=CARTESIAN_POINT ( 'NONE',  ( 0.002207914879453961969, 5.905511811023623991, 0.04916304461325442243 ) ) ;
#36902=CARTESIAN_POINT ( 'NONE',  ( 2.009930929872536964, 1.574803149606302854, -0.8055662819783826478 ) ) ;
#36906=CARTESIAN_POINT ( 'NONE',  ( 0.9442395380435398833, 1.624600478255878055, -2.074157072296122450 ) ) ;
#36907=DIRECTION ( 'NONE',  ( 0.000000000000000000, 0.000000000000000000, 1.000000000000000000 ) ) ;
#36909=CARTESIAN_POINT ( 'NONE',  ( 2.755905511811024056, 2.913385826771657250, 1.023622047244094446 ) ) ;
#36910=VECTOR ( 'NONE', #19960, 39.37007874015748854 ) ;
#36913=CARTESIAN_POINT ( 'NONE',  ( 2.455254121193349182, 1.659040775461701811, -1.640354758330454077 ) ) ;
#36914=DIRECTION ( 'NONE',  ( -0.7818314824680221431, 7.240175090764046435E-17, -0.6234898018587431423 ) ) ;
#36915=CARTESIAN_POINT ( 'NONE',  ( -2.254539048594918604, 1.675968636652996224, -0.9101168094050288149 ) ) ;
#36918=LINE ( 'NONE', #25291, #11967 ) ;
#36919=CARTESIAN_POINT ( 'NONE',  ( 0.9838852166858930159, 5.905511811023623991, 1.929635236160318179 ) ) ;
#36930=CARTESIAN_POINT ( 'NONE',  ( -1.883118996231724962, 1.042646074230517472, -1.732359575492526504 ) ) ;
#36935=ORIENTED_EDGE ( 'NONE', *, *, #13159, .T. ) ;
#36936=DIRECTION ( 'NONE',  ( -9.701723960855733411E-17, 1.000000000000000000, -8.476140964546406840E-17 ) ) ;
#36938=CARTESIAN_POINT ( 'NONE',  ( -1.597750071202345135, 0.000000000000000000, -0.7364305798568749895 ) ) ;
#36941=ORIENTED_EDGE ( 'NONE', *, *, #19262, .F. ) ;
#36942=B_SPLINE_CURVE_WITH_KNOTS ( 'NONE', 3,
 ( #18345, #40259, #50786, #15729 ),
 .UNSPECIFIED., .F., .F.,
 ( 4, 4 ),
 ( 2.472934783152532252E-07, 0.01680610193886662024 ),
 .UNSPECIFIED. ) ;
#36948=CIRCLE ( 'NONE', #34473, 2.165354330708661568 ) ;
#36950=CARTESIAN_POINT ( 'NONE',  ( -1.905671854841497259, 1.205361022782829114E-17, 2.256015092822653667 ) ) ;
#36951=ADVANCED_FACE ( 'NONE', ( #15764 ), #35145, .T. ) ;
#36952=FACE_OUTER_BOUND ( 'NONE', #10216, .T. ) ;
#36953=CARTESIAN_POINT ( 'NONE',  ( 2.138597145901430352, 1.574803149606302854, 0.3393547186367255608 ) ) ;
#36955=CARTESIAN_POINT ( 'NONE',  ( 0.1155636338427008941, -0.5222242541845523167, 0.000000000000000000 ) ) ;
#36956=DIRECTION ( 'NONE',  ( -0.000000000000000000, 1.000000000000000000, -0.000000000000000000 ) ) ;
#36957=EDGE_CURVE ( 'NONE', #6865, #43780, #3393, .T. ) ;
#36959=ORIENTED_EDGE ( 'NONE', *, *, #38843, .F. ) ;
#36962=CIRCLE ( 'NONE', #29551, 2.165354330708661568 ) ;
#36964=ORIENTED_EDGE ( 'NONE', *, *, #22072, .F. ) ;
#36972=CIRCLE ( 'NONE', #30377, 2.164630168518208109 ) ;
#36975=VERTEX_POINT ( 'NONE', #47217 ) ;
#36976=CARTESIAN_POINT ( 'NONE',  ( -1.572100079625529556, 1.686782128119526325, 1.874211475136934535 ) ) ;
#36978=ORIENTED_EDGE ( 'NONE', *, *, #48817, .T. ) ;
#36981=CARTESIAN_POINT ( 'NONE',  ( -2.903572669614648660, 5.118110236220475784, 1.294565943894125937 ) ) ;
#36983=ORIENTED_EDGE ( 'NONE', *, *, #36213, .F. ) ;
#36995=LENGTH_MEASURE_WITH_UNIT ( LENGTH_MEASURE( 0.02539999999999999897 ), #48052 );
#36997=CARTESIAN_POINT ( 'NONE',  ( -1.232620761116186126, 1.574803149606302854, -1.780282403660753410 ) ) ;
#36998=( BOUNDED_CURVE ( )  B_SPLINE_CURVE ( 3, ( #1769, #45370, #48968, #10031 ),
 .UNSPECIFIED., .F., .F. ) 
 B_SPLINE_CURVE_WITH_KNOTS ( ( 4, 4 ),
 ( 4.674186630050075841, 4.725131524484309509 ),
 .UNSPECIFIED. ) 
 CURVE ( )  GEOMETRIC_REPRESENTATION_ITEM ( )  RATIONAL_B_SPLINE_CURVE ( ( 1.000000000000000000, 0.9997837298384644189, 0.9997837298384644189, 1.000000000000000000 ) ) 
 REPRESENTATION_ITEM ( '' )  );
#37000=DIRECTION ( 'NONE',  ( -1.045785279492541006E-16, -1.000000000000000000, -5.036236473261559574E-17 ) ) ;
#37003=VERTEX_POINT ( 'NONE', #38269 ) ;
#37005=CARTESIAN_POINT ( 'NONE',  ( -2.100227814008681637, 0.000000000000000000, -2.076109931251943763 ) ) ;
#37006=CIRCLE ( 'NONE', #8134, 2.165354330708661568 ) ;
#37010=VECTOR ( 'NONE', #40850, 39.37007874015748854 ) ;
#37020=ORIENTED_EDGE ( 'NONE', *, *, #30489, .T. ) ;
#37023=FACE_OUTER_BOUND ( 'NONE', #7702, .T. ) ;
#37024=VERTEX_POINT ( 'NONE', #39010 ) ;
#37026=CARTESIAN_POINT ( 'NONE',  ( 2.074634995449671226, 0.01972627099085171726, -0.1424341672639439782 ) ) ;
#37038=VERTEX_POINT ( 'NONE', #3902 ) ;
#37040=CARTESIAN_POINT ( 'NONE',  ( 0.08139965876239094178, 1.610780518492231694, 0.000000000000000000 ) ) ;
#37049=ORIENTED_EDGE ( 'NONE', *, *, #43663, .F. ) ;
#37057=VERTEX_POINT ( 'NONE', #18 ) ;
#37060=ORIENTED_EDGE ( 'NONE', *, *, #49327, .F. ) ;
#37062=CARTESIAN_POINT ( 'NONE',  ( -1.252725762389900188, 0.005294869427718575626, -1.265815002325405336 ) ) ;
#37063=EDGE_CURVE ( 'NONE', #50100, #22707, #18643, .T. ) ;
#37064=EDGE_CURVE ( 'NONE', #4522, #30941, #13188, .T. ) ;
#37065=ORIENTED_EDGE ( 'NONE', *, *, #32021, .T. ) ;
#37066=CARTESIAN_POINT ( 'NONE',  ( 2.145573199472960546, 1.752687626240418073, -2.028682376369756568 ) ) ;
#37069=ORIENTED_EDGE ( 'NONE', *, *, #50377, .F. ) ;
#37070=LINE ( 'NONE', #33202, #22004 ) ;
#37073=VECTOR ( 'NONE', #43357, 39.37007874015748143 ) ;
#37076=CARTESIAN_POINT ( 'NONE',  ( -2.009930929872524974, 5.905511811023623991, -0.8055662819784118467 ) ) ;
#37078=CARTESIAN_POINT ( 'NONE',  ( 0.1067246931122726866, 0.02962905676920215767, 0.000000000000000000 ) ) ;
#37083=FACE_OUTER_BOUND ( 'NONE', #47131, .T. ) ;
#37084=CARTESIAN_POINT ( 'NONE',  ( 0.000000000000000000, 1.574803149606302854, 0.000000000000000000 ) ) ;
#37085=ORIENTED_EDGE ( 'NONE', *, *, #14336, .T. ) ;
#37096=CARTESIAN_POINT ( 'NONE',  ( 1.775400203342704764, 1.475394431724762478, -2.359903268218703332 ) ) ;
#37098=DIRECTION ( 'NONE',  ( -3.986037398843765983E-20, -1.000000000000000000, -1.160734090543304660E-16 ) ) ;
#37099=ORIENTED_EDGE ( 'NONE', *, *, #49539, .T. ) ;
#37102=ORIENTED_EDGE ( 'NONE', *, *, #33338, .T. ) ;
#37111=B_SPLINE_CURVE_WITH_KNOTS ( 'NONE', 3,
 ( #19973, #39865, #12762, #4757 ),
 .UNSPECIFIED., .F., .F.,
 ( 4, 4 ),
 ( 2.925317793448864180E-05, 0.02001440658342761025 ),
 .UNSPECIFIED. ) ;
#37114=B_SPLINE_CURVE_WITH_KNOTS ( 'NONE', 3,
 ( #41879, #22764, #14766, #30515 ),
 .UNSPECIFIED., .F., .F.,
 ( 4, 4 ),
 ( 0.001750221845292458797, 0.004250273344973329141 ),
 .UNSPECIFIED. ) ;
#37120=VECTOR ( 'NONE', #7340, 39.37007874015748143 ) ;
#37121=ORIENTED_EDGE ( 'NONE', *, *, #3978, .F. ) ;
#37126=VERTEX_POINT ( 'NONE', #17064 ) ;
#37128=CARTESIAN_POINT ( 'NONE',  ( 2.121469926805689354, 6.692913385826772199, -0.4337334748181388422 ) ) ;
#37130=CARTESIAN_POINT ( 'NONE',  ( -2.574535399664545920, 1.576620825002011061, 0.7847720717991576445 ) ) ;
#37131=DIRECTION ( 'NONE',  ( 0.000000000000000000, 1.000000000000000000, 0.000000000000000000 ) ) ;
#37133=B_SPLINE_CURVE_WITH_KNOTS ( 'NONE', 3,
 ( #11254, #35507, #26983, #4015 ),
 .UNSPECIFIED., .F., .F.,
 ( 4, 4 ),
 ( 2.656726248922481073E-07, 0.01672130471895163367 ),
 .UNSPECIFIED. ) ;
#37134=B_SPLINE_CURVE_WITH_KNOTS ( 'NONE', 3,
 ( #17143, #43976, #40635, #21014 ),
 .UNSPECIFIED., .F., .F.,
 ( 4, 4 ),
 ( 0.1211775127643062860, 0.1625894504277921315 ),
 .UNSPECIFIED. ) ;
#37137=EDGE_LOOP ( 'NONE', ( #32368, #41009, #43100, #4882 ) ) ;
#37142=CARTESIAN_POINT ( 'NONE',  ( 0.9836083787002611878, 1.574803149606302854, -1.929060376159698720 ) ) ;
#37146=CARTESIAN_POINT ( 'NONE',  ( 0.07982360342473591996, 1.709180471932028711, 0.000000000000000000 ) ) ;
#37152=CARTESIAN_POINT ( 'NONE',  ( -1.712991727494380223, 1.205361022782829114E-17, -0.3405009913947248945 ) ) ;
#37153=CONICAL_SURFACE ( 'NONE', #43711, 2.246510896728926010, 0.01601546068027819014 ) ;
#37154=DIRECTION ( 'NONE',  ( 0.9959742939952384022, -1.044444007753810152E-17, 0.08963930890344089242 ) ) ;
#37155=VECTOR ( 'NONE', #581, 39.37007874015748143 ) ;
#37156=EDGE_CURVE ( 'NONE', #48863, #36721, #20763, .T. ) ;
#37157=CARTESIAN_POINT ( 'NONE',  ( -1.779568955232875060, 1.574803149606302854, -1.233650562797313555 ) ) ;
#37158=DIRECTION ( 'NONE',  ( 0.000000000000000000, -1.000000000000000000, 0.000000000000000000 ) ) ;
#37159=ORIENTED_EDGE ( 'NONE', *, *, #13904, .F. ) ;
#37160=EDGE_CURVE ( 'NONE', #36720, #43500, #12154, .T. ) ;
#37162=CARTESIAN_POINT ( 'NONE',  ( 0.000000000000000000, 6.692913385826772199, 0.000000000000000000 ) ) ;
#37168=FACE_OUTER_BOUND ( 'NONE', #1668, .T. ) ;
#37171=ADVANCED_FACE ( 'NONE', ( #8792 ), #40034, .T. ) ;
#37173=ORIENTED_EDGE ( 'NONE', *, *, #18099, .T. ) ;
#37176=LINE ( 'NONE', #5672, #33116 ) ;
#37179=EDGE_CURVE ( 'NONE', #45778, #39028, #793, .T. ) ;
#37182=VERTEX_POINT ( 'NONE', #25306 ) ;
#37183=ORIENTED_EDGE ( 'NONE', *, *, #24207, .F. ) ;
#37189=ORIENTED_EDGE ( 'NONE', *, *, #33212, .F. ) ;
#37190=ORIENTED_EDGE ( 'NONE', *, *, #21364, .T. ) ;
#37192=FACE_OUTER_BOUND ( 'NONE', #45754, .T. ) ;
#37193=VECTOR ( 'NONE', #45606, 39.37007874015748143 ) ;
#37196=DIRECTION ( 'NONE',  ( -0.3090169943749582204, -0.000000000000000000, 0.9510565162951500895 ) ) ;
#37197=CARTESIAN_POINT ( 'NONE',  ( -1.325491792074585673, 1.205361022782829114E-17, -2.638988599164751481 ) ) ;
#37206=DIRECTION ( 'NONE',  ( -0.9998717552508122886, -0.01601477604151182316, 0.000000000000000000 ) ) ;
#37212=ORIENTED_EDGE ( 'NONE', *, *, #38947, .F. ) ;
#37217=ADVANCED_FACE ( 'NONE', ( #10076 ), #13160, .F. ) ;
#37228=VERTEX_POINT ( 'NONE', #45412 ) ;
#37231=ORIENTED_EDGE ( 'NONE', *, *, #44017, .T. ) ;
#37236=LINE ( 'NONE', #26363, #7885 ) ;
#37237=EDGE_CURVE ( 'NONE', #15540, #21218, #29438, .T. ) ;
#37248=EDGE_CURVE ( 'NONE', #12736, #42295, #3271, .T. ) ;
#37255=CARTESIAN_POINT ( 'NONE',  ( -1.391094485341343390, 0.5249441293655172647, 1.667033902411208413 ) ) ;
#37259=CARTESIAN_POINT ( 'NONE',  ( -1.645270756471820528, 1.587191622466853413, 1.808365756894092069 ) ) ;
#37262=LINE ( 'NONE', #14014, #30076 ) ;
#37265=LINE ( 'NONE', #25124, #12675 ) ;
#37266=CARTESIAN_POINT ( 'NONE',  ( -0.3465944589516569141, 6.692913385826772199, 2.185505870675811035 ) ) ;
#37275=VECTOR ( 'NONE', #25135, 39.37007874015748143 ) ;
#37280=CARTESIAN_POINT ( 'NONE',  ( -1.661821349926435376, 6.692913385826772199, 1.388203579611951621 ) ) ;
#37281=CARTESIAN_POINT ( 'NONE',  ( 0.000000000000000000, 0.000000000000000000, 0.000000000000000000 ) ) ;
#37282=ADVANCED_FACE ( 'NONE', ( #21954 ), #6567, .T. ) ;
#37285=FACE_OUTER_BOUND ( 'NONE', #31715, .T. ) ;
#37286=CARTESIAN_POINT ( 'NONE',  ( 0.3382312733057610266, 6.692913385826772199, -2.139420919314966252 ) ) ;
#37287=VERTEX_POINT ( 'NONE', #41824 ) ;
#37288=DIRECTION ( 'NONE',  ( -0.4738686624729965269, 0.000000000000000000, -0.8805955318567391110 ) ) ;
#37291=LINE ( 'NONE', #2164, #34613 ) ;
#37294=VERTEX_POINT ( 'NONE', #49013 ) ;
#37295=ORIENTED_EDGE ( 'NONE', *, *, #19697, .T. ) ;
#37303=VECTOR ( 'NONE', #19431, 39.37007874015748143 ) ;
#37305=ADVANCED_FACE ( 'NONE', ( #1562 ), #4121, .T. ) ;
#37306=CARTESIAN_POINT ( 'NONE',  ( -1.741748233172855320, 0.000000000000000000, -0.08495931630248562683 ) ) ;
#37312=AXIS2_PLACEMENT_3D ( 'NONE', #21164, #1535, #56 ) ;
#37315=B_SPLINE_CURVE_WITH_KNOTS ( 'NONE', 3,
 ( #43392, #39276, #35158, #27389 ),
 .UNSPECIFIED., .F., .F.,
 ( 4, 4 ),
 ( 2.330467117010365678E-07, 0.01702404298823860518 ),
 .UNSPECIFIED. ) ;
#37327=EDGE_LOOP ( 'NONE', ( #39986, #30284, #34759, #1703 ) ) ;
#37329=CARTESIAN_POINT ( 'NONE',  ( 1.004206812140325145, 1.632800078982482139, 2.535642212739530610 ) ) ;
#37333=DIRECTION ( 'NONE',  ( 1.283101021437939896E-16, 1.000000000000000000, -1.154811821032073265E-17 ) ) ;
#37343=CARTESIAN_POINT ( 'NONE',  ( -1.727163557247779480, 0.000000000000000000, 0.2505061835542949922 ) ) ;
#37344=CARTESIAN_POINT ( 'NONE',  ( 1.945791886572777685, 0.000000000000000000, -0.8495516078614956390 ) ) ;
#37345=AXIS2_PLACEMENT_3D ( 'NONE', #11758, #27496, #26986 ) ;
#37346=EDGE_CURVE ( 'NONE', #32538, #50196, #44803, .T. ) ;
#37358=EDGE_CURVE ( 'NONE', #5201, #10800, #461, .T. ) ;
#37361=AXIS2_PLACEMENT_3D ( 'NONE', #37078, #9707, #25443 ) ;
#37362=CARTESIAN_POINT ( 'NONE',  ( -1.088485032206041980, 1.592042674141829650, 1.917766907668551069 ) ) ;
#37363=VERTEX_POINT ( 'NONE', #38463 ) ;
#37365=B_SPLINE_CURVE_WITH_KNOTS ( 'NONE', 3,
 ( #14774, #37771, #50089, #26635 ),
 .UNSPECIFIED., .F., .F.,
 ( 4, 4 ),
 ( 2.472189838406668358E-07, 0.01917498170529582241 ),
 .UNSPECIFIED. ) ;
#37366=ORIENTED_EDGE ( 'NONE', *, *, #14132, .F. ) ;
#37367=DIRECTION ( 'NONE',  ( -0.9998717552508122886, -0.01601477604151181275, 0.000000000000000000 ) ) ;
#37369=ORIENTED_EDGE ( 'NONE', *, *, #43479, .F. ) ;
#37371=CARTESIAN_POINT ( 'NONE',  ( 2.823445274216730638, 5.905511811023623991, 0.8656477926280686797 ) ) ;
#37374=CARTESIAN_POINT ( 'NONE',  ( -0.5110942157764869487, 1.711289833164726160, 2.908233010320107059 ) ) ;
#37388=CARTESIAN_POINT ( 'NONE',  ( 1.478089240774732582, 0.05159396975604255142, 1.241682111880268558 ) ) ;
#37390=FACE_OUTER_BOUND ( 'NONE', #21034, .T. ) ;
#37392=VECTOR ( 'NONE', #35990, 39.37007874015748854 ) ;
#37393=EDGE_LOOP ( 'NONE', ( #40080, #34355, #28380, #18028 ) ) ;
#37395=DIRECTION ( 'NONE',  ( -0.1342332658176522420, 1.150282676381580509E-16, -0.9909497617679352555 ) ) ;
#37403=CARTESIAN_POINT ( 'NONE',  ( -1.531732224425391253, 1.205361022782829114E-17, 0.8801458454442117052 ) ) ;
#37408=ADVANCED_FACE ( 'NONE', ( #7218 ), #23093, .T. ) ;
#37409=CARTESIAN_POINT ( 'NONE',  ( -0.8238130908517355966, 1.694707076513333410, 2.054984861273213337 ) ) ;
#37413=ORIENTED_EDGE ( 'NONE', *, *, #4971, .F. ) ;
#37415=LINE ( 'NONE', #45378, #17543 ) ;
#37418=CARTESIAN_POINT ( 'NONE',  ( -2.120026437385223783, 1.579675233831871806, 1.196720460861670610 ) ) ;
#37422=CARTESIAN_POINT ( 'NONE',  ( 1.759095177328794168, 1.049866565877818125, 1.002495067636045345 ) ) ;
#37423=ORIENTED_EDGE ( 'NONE', *, *, #32822, .T. ) ;
#37425=AXIS2_PLACEMENT_3D ( 'NONE', #5881, #33528, #2267 ) ;
#37426=CARTESIAN_POINT ( 'NONE',  ( -2.932638728931780125, 1.673548413681422042, 0.3475908556737793420 ) ) ;
#37429=CARTESIAN_POINT ( 'NONE',  ( 1.052882392248851273, 1.735662962607948057, 2.758708974802636327 ) ) ;
#37434=ORIENTED_EDGE ( 'NONE', *, *, #15237, .T. ) ;
#37435=CARTESIAN_POINT ( 'NONE',  ( -1.442444474601640492, 0.004816277389180329341, -1.011116641508509995 ) ) ;
#37444=EDGE_CURVE ( 'NONE', #22025, #16346, #34833, .T. ) ;
#37445=VERTEX_POINT ( 'NONE', #31214 ) ;
#37447=B_SPLINE_CURVE_WITH_KNOTS ( 'NONE', 3,
 ( #8207, #4327, #16463, #32218 ),
 .UNSPECIFIED., .F., .F.,
 ( 4, 4 ),
 ( 0.01122604379886785533, 0.03073620398351814553 ),
 .UNSPECIFIED. ) ;
#37455=CIRCLE ( 'NONE', #20927, 1.850107469027523432 ) ;
#37456=CARTESIAN_POINT ( 'NONE',  ( -0.1450362469327504955, 6.692913385826772199, -2.160491579385213967 ) ) ;
#37461=CONICAL_SURFACE ( 'NONE', #8541, 1.850107469027523210, 0.6386652850508578450 ) ;
#37462=LINE ( 'NONE', #49019, #30107 ) ;
#37464=ADVANCED_FACE ( 'NONE', ( #20609 ), #36363, .F. ) ;
#37465=LINE ( 'NONE', #49527, #12436 ) ;
#37466=AXIS2_PLACEMENT_3D ( 'NONE', #50775, #27591, #15222 ) ;
#37469=ORIENTED_EDGE ( 'NONE', *, *, #21088, .T. ) ;
#37470=DIRECTION ( 'NONE',  ( -0.01601477604151182663, 0.9998717552508123996, -0.000000000000000000 ) ) ;
#37471=FACE_OUTER_BOUND ( 'NONE', #25784, .T. ) ;
#37474=EDGE_CURVE ( 'NONE', #8450, #18246, #32237, .T. ) ;
#37492=CARTESIAN_POINT ( 'NONE',  ( 0.000000000000000000, 6.692913385826772199, 0.000000000000000000 ) ) ;
#37493=DIRECTION ( 'NONE',  ( -3.986037398843765983E-20, -1.000000000000000000, -1.160734090543304660E-16 ) ) ;
#37494=AXIS2_PLACEMENT_3D ( 'NONE', #7928, #19536, #27286 ) ;
#37500=ORIENTED_EDGE ( 'NONE', *, *, #8525, .T. ) ;
#37501=PLANE ( 'NONE',  #29026 ) ;
#37514=EDGE_CURVE ( 'NONE', #2835, #7511, #214, .T. ) ;
#37515=CARTESIAN_POINT ( 'NONE',  ( -0.7330548839819540641, 1.630543939889479210, 2.093275022833150700 ) ) ;
#37518=FACE_OUTER_BOUND ( 'NONE', #33793, .T. ) ;
#37520=CARTESIAN_POINT ( 'NONE',  ( 0.000000000000000000, 1.574803149606302854, 0.000000000000000000 ) ) ;
#37522=ORIENTED_EDGE ( 'NONE', *, *, #18585, .T. ) ;
#37526=VECTOR ( 'NONE', #4419, 39.37007874015748143 ) ;
#37527=ADVANCED_FACE ( 'NONE', ( #8733 ), #39568, .T. ) ;
#37532=EDGE_CURVE ( 'NONE', #24163, #14608, #15963, .T. ) ;
#37533=CARTESIAN_POINT ( 'NONE',  ( 1.775400203342704764, 1.475394431724762478, -2.359903268218703332 ) ) ;
#37537=LINE ( 'NONE', #14030, #25063 ) ;
#37542=B_SPLINE_CURVE_WITH_KNOTS ( 'NONE', 3,
 ( #26209, #44793, #9449, #25698 ),
 .UNSPECIFIED., .F., .F.,
 ( 4, 4 ),
 ( 2.767189446683712919E-07, 0.002500421657723224042 ),
 .UNSPECIFIED. ) ;
#37543=CARTESIAN_POINT ( 'NONE',  ( 2.555365368299595323E-16, 6.692913385826772199, 2.086614173228346303 ) ) ;
#37545=CARTESIAN_POINT ( 'NONE',  ( -2.823445274216743073, 1.675250974312822105, 0.8656477926280276014 ) ) ;
#37548=CARTESIAN_POINT ( 'NONE',  ( 0.002207914879453961969, 5.905511811023623991, -2.115467123904953617 ) ) ;
#37551=ORIENTED_EDGE ( 'NONE', *, *, #30595, .T. ) ;
#37554=ORIENTED_EDGE ( 'NONE', *, *, #37156, .F. ) ;
#37561=CARTESIAN_POINT ( 'NONE',  ( -2.055928985459924530, 5.905511811023623991, 0.7197570096327607914 ) ) ;
#37567=ORIENTED_EDGE ( 'NONE', *, *, #24865, .F. ) ;
#37569=CARTESIAN_POINT ( 'NONE',  ( 2.437180031585944207, 1.205361022782829114E-17, -1.667735833703099413 ) ) ;
#37575=VECTOR ( 'NONE', #37998, 39.37007874015748143 ) ;
#37577=CARTESIAN_POINT ( 'NONE',  ( 0.2878729406458415685, 0.5249316497054297148, 1.861923634248271231 ) ) ;
#37579=ORIENTED_EDGE ( 'NONE', *, *, #6125, .F. ) ;
#37583=DIRECTION ( 'NONE',  ( -0.9998717552508122886, -0.01601477604151182316, 0.000000000000000000 ) ) ;
#37585=DIRECTION ( 'NONE',  ( 5.779879058770898378E-18, 1.000000000000000000, 1.286990067732318227E-16 ) ) ;
#37587=DIRECTION ( 'NONE',  ( 3.986037398843765983E-20, 1.000000000000000000, 1.160734090543304660E-16 ) ) ;
#37590=DIRECTION ( 'NONE',  ( -7.993605777301125513E-15, 0.000000000000000000, 1.000000000000000000 ) ) ;
#37591=DIRECTION ( 'NONE',  ( 0.000000000000000000, 0.000000000000000000, -1.000000000000000000 ) ) ;
#37594=EDGE_CURVE ( 'NONE', #49287, #6252, #39975, .T. ) ;
#37599=CARTESIAN_POINT ( 'NONE',  ( 2.734482843737263025, 1.452693199995327644, -1.115254632218672270 ) ) ;
#37601=CIRCLE ( 'NONE', #25207, 2.165354330708661568 ) ;
#37602=EDGE_CURVE ( 'NONE', #13729, #50819, #360, .T. ) ;
#37609=CARTESIAN_POINT ( 'NONE',  ( 0.1067246931122726866, 0.02962905676920215767, 0.000000000000000000 ) ) ;
#37615=CARTESIAN_POINT ( 'NONE',  ( -2.101391096692225791, 1.575819129783617489, -0.5301069970517552354 ) ) ;
#37620=ORIENTED_EDGE ( 'NONE', *, *, #16951, .T. ) ;
#37624=PLANE ( 'NONE',  #23208 ) ;
#37627=AXIS2_PLACEMENT_3D ( 'NONE', #39530, #3658, #19892 ) ;
#37629=VERTEX_POINT ( 'NONE', #28858 ) ;
#37636=B_SPLINE_CURVE_WITH_KNOTS ( 'NONE', 3,
 ( #1435, #17191, #43637, #39014 ),
 .UNSPECIFIED., .F., .F.,
 ( 4, 4 ),
 ( 0.001674362740038782627, 0.004174460773670277645 ),
 .UNSPECIFIED. ) ;
#37637=CARTESIAN_POINT ( 'NONE',  ( 1.387820626701303572, 1.664513642032426466, -1.826445746185616503 ) ) ;
#37638=CIRCLE ( 'NONE', #33517, 2.165354330708661568 ) ;
#37642=EDGE_CURVE ( 'NONE', #16311, #22056, #47780, .T. ) ;
#37649=CARTESIAN_POINT ( 'NONE',  ( 2.069752515245542046, 1.205361022782829114E-17, -0.5228856972975560735 ) ) ;
#37651=CARTESIAN_POINT ( 'NONE',  ( 2.823445274216730638, 1.664781993127344872, 0.8656477926280681245 ) ) ;
#37652=LINE ( 'NONE', #45864, #35521 ) ;
#37654=CARTESIAN_POINT ( 'NONE',  ( 0.1067246931122726866, 0.02962905676920215767, 0.000000000000000000 ) ) ;
#37655=EDGE_CURVE ( 'NONE', #10470, #45968, #51042, .T. ) ;
#37656=DIRECTION ( 'NONE',  ( 0.7818314824680221431, 0.000000000000000000, 0.6234898018587431423 ) ) ;
#37661=FACE_OUTER_BOUND ( 'NONE', #22629, .T. ) ;
#37662=B_SPLINE_CURVE_WITH_KNOTS ( 'NONE', 3,
 ( #33584, #15147, #35028, #46602 ),
 .UNSPECIFIED., .F., .F.,
 ( 4, 4 ),
 ( 3.737662051086792397E-07, 0.05012529773801908256 ),
 .UNSPECIFIED. ) ;
#37663=EDGE_CURVE ( 'NONE', #37629, #33123, #14131, .T. ) ;
#37665=CARTESIAN_POINT ( 'NONE',  ( 1.726519710923990480, 1.205361022782829114E-17, -1.198633063221572481 ) ) ;
#37667=FACE_OUTER_BOUND ( 'NONE', #6759, .T. ) ;
#37668=CARTESIAN_POINT ( 'NONE',  ( -1.833791099076586217, 5.905511811023623991, -1.151507526013721305 ) ) ;
#37677=B_SPLINE_CURVE_WITH_KNOTS ( 'NONE', 3,
 ( #307, #21661, #37422, #4952 ),
 .UNSPECIFIED., .F., .F.,
 ( 4, 4 ),
 ( 0.1211873102087489551, 0.1625992483279400380 ),
 .UNSPECIFIED. ) ;
#37679=AXIS2_PLACEMENT_3D ( 'NONE', #44534, #40683, #13572 ) ;
#37682=CARTESIAN_POINT ( 'NONE',  ( -2.623503965249869729, 0.000000000000000000, 1.355882097269835107 ) ) ;
#37688=CONICAL_SURFACE ( 'NONE', #26137, 2.165354330708661568, 0.2617993877991570129 ) ;
#37689=LINE ( 'NONE', #2301, #19759 ) ;
#37696=CARTESIAN_POINT ( 'NONE',  ( -0.2156685157583827228, 5.905511811023623991, -2.945280361644577294 ) ) ;
#37700=DIRECTION ( 'NONE',  ( 8.902872254220023478E-17, 1.000000000000000000, -9.311674343991161395E-17 ) ) ;
#37701=ORIENTED_EDGE ( 'NONE', *, *, #15834, .F. ) ;
#37702=VERTEX_POINT ( 'NONE', #21882 ) ;
#37703=VERTEX_POINT ( 'NONE', #29882 ) ;
#37708=VECTOR ( 'NONE', #9647, 39.37007874015748854 ) ;
#37709=CARTESIAN_POINT ( 'NONE',  ( 0.5343643221173207669, 1.723869505195006147, 2.668977133226676290 ) ) ;
#37713=ORIENTED_EDGE ( 'NONE', *, *, #21192, .F. ) ;
#37715=VECTOR ( 'NONE', #36561, 39.37007874015748854 ) ;
#37718=CARTESIAN_POINT ( 'NONE',  ( -0.4461448448314593307, 1.667947728109364647, 2.182847745222971092 ) ) ;
#37732=DIRECTION ( 'NONE',  ( 0.3513748240813304724, 0.000000000000000000, 0.9362348706397417564 ) ) ;
#37737=VECTOR ( 'NONE', #20196, 39.37007874015748143 ) ;
#37740=ORIENTED_EDGE ( 'NONE', *, *, #39136, .T. ) ;
#37749=ADVANCED_FACE ( 'NONE', ( #1496 ), #28847, .T. ) ;
#37752=CARTESIAN_POINT ( 'NONE',  ( 1.530693736245518854, 1.574803149606302854, -1.531579597454043373 ) ) ;
#37755=CARTESIAN_POINT ( 'NONE',  ( -2.715141060683412100, 0.000000000000000000, -1.160506983230102040 ) ) ;
#37764=EDGE_CURVE ( 'NONE', #13212, #9488, #21322, .T. ) ;
#37765=DIRECTION ( 'NONE',  ( 0.08963930890342654279, 0.000000000000000000, 0.9959742939952397345 ) ) ;
#37766=ORIENTED_EDGE ( 'NONE', *, *, #4932, .T. ) ;
#37771=CARTESIAN_POINT ( 'NONE',  ( -1.547867290569560961, 1.691170706622086017, -2.214182027291666355 ) ) ;
#37774=AXIS2_PLACEMENT_3D ( 'NONE', #38174, #46379, #42535 ) ;
#37775=CARTESIAN_POINT ( 'NONE',  ( 1.695772546416037363, 1.477242674555747426, -2.417756147381349141 ) ) ;
#37779=CARTESIAN_POINT ( 'NONE',  ( 0.000000000000000000, 6.692913385826772199, 0.000000000000000000 ) ) ;
#37780=CARTESIAN_POINT ( 'NONE',  ( 1.557927422371225612, 0.000000000000000000, 0.7824709080581413456 ) ) ;
#37783=EDGE_LOOP ( 'NONE', ( #24893, #27738, #38348, #13237 ) ) ;
#37785=CARTESIAN_POINT ( 'NONE',  ( 0.08119777152254364916, 1.623385212329073957, 0.000000000000000000 ) ) ;
#37787=PLANE ( 'NONE',  #2405 ) ;
#37792=ORIENTED_EDGE ( 'NONE', *, *, #26253, .F. ) ;
#37794=LINE ( 'NONE', #30033, #47976 ) ;
#37796=AXIS2_PLACEMENT_3D ( 'NONE', #6273, #29247, #45733 ) ;
#37798=EDGE_CURVE ( 'NONE', #44880, #41924, #7650, .T. ) ;
#37803=EDGE_CURVE ( 'NONE', #50692, #6941, #7405, .T. ) ;
#37805=ORIENTED_EDGE ( 'NONE', *, *, #10975, .F. ) ;
#37811=FACE_OUTER_BOUND ( 'NONE', #19373, .T. ) ;
#37816=AXIS2_PLACEMENT_3D ( 'NONE', #38183, #35058, #26541 ) ;
#37822=EDGE_LOOP ( 'NONE', ( #15179, #21834, #21212, #45159, #14062, #35229, #24459, #12530, #37102, #47087, #39158, #28755, #16754, #41658, #7620, #43090, #49987, #23632, #44266, #16913, #3611, #26150, #4773, #10100, #42201, #2951, #301, #25872, #45456, #48976, #33256, #39699, #26891, #28503, #43198, #42819, #27149, #595, #5294, #36877, #30510, #49613, #50468, #13208, #20918, #40880, #32809, #27494, #27430, #50988, #28305, #40027, #15938, #25532, #17035, #39253, #40216, #20958, #8348, #36319, #11935, #14072, #17744, #42912, #45429, #21600, #45170, #10598, #29824, #206, #18233, #8981, #29264, #6403, #27996, #49184 ) ) ;
#37823=CARTESIAN_POINT ( 'NONE',  ( 0.5756566573088583993, 1.629780628454260194, 2.896516654582643291 ) ) ;
#37827=EDGE_CURVE ( 'NONE', #17626, #31910, #23132, .T. ) ;
#37830=CIRCLE ( 'NONE', #32027, 2.244934639244525076 ) ;
#37832=PLANE ( 'NONE',  #42082 ) ;
#37835=EDGE_CURVE ( 'NONE', #11648, #1706, #39772, .T. ) ;
#37843=DIRECTION ( 'NONE',  ( -8.032339854997460071E-17, 1.000000000000000000, 1.007223559679395367E-16 ) ) ;
#37844=CARTESIAN_POINT ( 'NONE',  ( 0.4788131938641111973, 1.504819983455083277, 2.914091152102192162 ) ) ;
#37849=ORIENTED_EDGE ( 'NONE', *, *, #41563, .F. ) ;
#37861=ORIENTED_EDGE ( 'NONE', *, *, #38319, .F. ) ;
#37862=CARTESIAN_POINT ( 'NONE',  ( 2.949782676795221992, 0.000000000000000000, -0.1324748927672375898 ) ) ;
#37869=DIRECTION ( 'NONE',  ( 1.042246309068005903E-16, 1.000000000000000000, -7.572362681945165783E-17 ) ) ;
#37870=EDGE_CURVE ( 'NONE', #21120, #24910, #28708, .T. ) ;
#37876=AXIS2_PLACEMENT_3D ( 'NONE', #31359, #14856, #38852 ) ;
#37883=ORIENTED_EDGE ( 'NONE', *, *, #15879, .T. ) ;
#37885=ORIENTED_EDGE ( 'NONE', *, *, #27896, .F. ) ;
#37887=EDGE_CURVE ( 'NONE', #26436, #24660, #10765, .T. ) ;
#37888=ADVANCED_FACE ( 'NONE', ( #6647 ), #15149, .F. ) ;
#37890=VERTEX_POINT ( 'NONE', #36306 ) ;
#37896=CARTESIAN_POINT ( 'NONE',  ( -1.733526556417524622, 0.000000000000000000, 0.1851600754179555941 ) ) ;
#37898=CARTESIAN_POINT ( 'NONE',  ( -1.735432873265435161, 1.581680620477750931, 1.321016258651915409 ) ) ;
#37900=DIRECTION ( 'NONE',  ( -0.4738686624729965269, 1.022326139627305519E-16, -0.8805955318567391110 ) ) ;
#37901=CARTESIAN_POINT ( 'NONE',  ( -0.2304536187657762192, 1.049866565067838264, -2.011542525589492758 ) ) ;
#37905=AXIS2_PLACEMENT_3D ( 'NONE', #45502, #9915, #14038 ) ;
#37906=CARTESIAN_POINT ( 'NONE',  ( -1.312623452344869657, 1.205361022782829114E-17, 1.722945714930904648 ) ) ;
#37908=ORIENTED_EDGE ( 'NONE', *, *, #44054, .F. ) ;
#37911=ORIENTED_EDGE ( 'NONE', *, *, #49103, .F. ) ;
#37912=DIRECTION ( 'NONE',  ( 0.8345732537213079727, 0.000000000000000000, -0.5508969814520945363 ) ) ;
#37916=DIRECTION ( 'NONE',  ( 0.9639628606958511314, 0.000000000000000000, 0.2660368455666826115 ) ) ;
#37917=CARTESIAN_POINT ( 'NONE',  ( -1.547009873100170907, 1.617506960006209527, -1.547179421581643011 ) ) ;
#37920=CARTESIAN_POINT ( 'NONE',  ( 2.099568260077706583, 1.574803149606302854, -0.5296909464895790398 ) ) ;
#37922=EDGE_LOOP ( 'NONE', ( #16003, #43592, #46723, #31477 ) ) ;
#37925=ORIENTED_EDGE ( 'NONE', *, *, #31290, .F. ) ;
#37926=ORIENTED_EDGE ( 'NONE', *, *, #23845, .T. ) ;
#37933=EDGE_CURVE ( 'NONE', #26292, #27844, #33877, .T. ) ;
#37934=AXIS2_PLACEMENT_3D ( 'NONE', #5875, #37131, #13883 ) ;
#37935=DIRECTION ( 'NONE',  ( 0.1342332658176667304, 1.288287287306305530E-16, -0.9909497617679332571 ) ) ;
#37940=ORIENTED_EDGE ( 'NONE', *, *, #7683, .T. ) ;
#37941=CARTESIAN_POINT ( 'NONE',  ( 0.1736737122991879045, 1.616004489590360693, -2.478679879797507368 ) ) ;
#37948=VERTEX_POINT ( 'NONE', #4804 ) ;
#37962=CARTESIAN_POINT ( 'NONE',  ( -0.7331725592709618100, 1.597733653658881758, 2.093588567519426569 ) ) ;
#37963=DIRECTION ( 'NONE',  ( -0.9998717552508122886, -0.01601477604151180928, 0.000000000000000000 ) ) ;
#37966=DIRECTION ( 'NONE',  ( 0.6910626489868580968, 0.000000000000000000, 0.7227948638273978821 ) ) ;
#37967=CARTESIAN_POINT ( 'NONE',  ( -0.6734335508564485151, 1.704902552214879963, -2.625115814727751129 ) ) ;
#37968=B_SPLINE_CURVE_WITH_KNOTS ( 'NONE', 3,
 ( #41064, #49764, #21435, #17813 ),
 .UNSPECIFIED., .F., .F.,
 ( 4, 4 ),
 ( 0.001800744595756896896, 0.004300762518479772645 ),
 .UNSPECIFIED. ) ;
#37971=DIRECTION ( 'NONE',  ( -3.986037398843765983E-20, -1.000000000000000000, -1.160734090543304660E-16 ) ) ;
#37972=DIRECTION ( 'NONE',  ( -0.9998717552508122886, -0.01601477604151180928, 0.000000000000000000 ) ) ;
#37973=ORIENTED_EDGE ( 'NONE', *, *, #32454, .F. ) ;
#37984=ORIENTED_EDGE ( 'NONE', *, *, #34263, .T. ) ;
#37986=DIRECTION ( 'NONE',  ( -2.582876339026174526E-17, -1.000000000000000000, -1.131632063491654496E-16 ) ) ;
#37988=ADVANCED_FACE ( 'NONE', ( #16685 ), #32438, .F. ) ;
#37990=ORIENTED_EDGE ( 'NONE', *, *, #4177, .F. ) ;
#37991=ORIENTED_EDGE ( 'NONE', *, *, #11103, .F. ) ;
#37992=LINE ( 'NONE', #2613, #32958 ) ;
#37995=CARTESIAN_POINT ( 'NONE',  ( -0.8306416476351717870, 0.009809765579796675752, -1.611421686139382192 ) ) ;
#37998=DIRECTION ( 'NONE',  ( -0.8805955318567391110, 0.000000000000000000, 0.4738686624729965269 ) ) ;
#38006=B_SPLINE_CURVE_WITH_KNOTS ( 'NONE', 3,
 ( #12902, #12642, #21161, #22366 ),
 .UNSPECIFIED., .F., .F.,
 ( 4, 4 ),
 ( 0.001559031566645303814, 0.04607411539233744607 ),
 .UNSPECIFIED. ) ;
#38008=DIRECTION ( 'NONE',  ( 0.2660368455666688448, 0.000000000000000000, 0.9639628606958550172 ) ) ;
#38009=PLANE ( 'NONE',  #2139 ) ;
#38019=DIRECTION ( 'NONE',  ( 0.000000000000000000, -1.000000000000000000, 0.000000000000000000 ) ) ;
#38024=ORIENTED_EDGE ( 'NONE', *, *, #8010, .F. ) ;
#38026=EDGE_CURVE ( 'NONE', #36594, #22069, #9703, .T. ) ;
#38028=CARTESIAN_POINT ( 'NONE',  ( 1.081562861160096700, 0.04524287409729283588, -1.572369041216798768 ) ) ;
#38033=DIRECTION ( 'NONE',  ( 1.241861098869888840E-16, 1.000000000000000000, -3.427318860986102267E-17 ) ) ;
#38036=EDGE_CURVE ( 'NONE', #19894, #20329, #17702, .T. ) ;
#38039=DIRECTION ( 'NONE',  ( 0.000000000000000000, 0.000000000000000000, -1.000000000000000000 ) ) ;
#38046=CARTESIAN_POINT ( 'NONE',  ( -2.823445274216743073, 0.000000000000000000, 0.8656477926280280455 ) ) ;
#38052=CARTESIAN_POINT ( 'NONE',  ( -1.971834065208965203, 0.000000000000000000, 0.8963217522329899323 ) ) ;
#38055=( BOUNDED_CURVE ( )  B_SPLINE_CURVE ( 3, ( #42881, #50580, #3148, #7023 ),
 .UNSPECIFIED., .F., .F. ) 
 B_SPLINE_CURVE_WITH_KNOTS ( ( 4, 4 ),
 ( 0.3208970237599759745, 0.3716576335890542926 ),
 .UNSPECIFIED. ) 
 CURVE ( )  GEOMETRIC_REPRESENTATION_ITEM ( )  RATIONAL_B_SPLINE_CURVE ( ( 1.000000000000000000, 0.9997852915667326812, 0.9997852915667326812, 1.000000000000000000 ) ) 
 REPRESENTATION_ITEM ( '' )  );
#38056=ADVANCED_FACE ( 'NONE', ( #16945 ), #9954, .F. ) ;
#38061=ORIENTED_EDGE ( 'NONE', *, *, #21088, .F. ) ;
#38067=PLANE ( 'NONE',  #41977 ) ;
#38068=DIRECTION ( 'NONE',  ( 0.4338837391175656699, 0.000000000000000000, -0.9009688679024154823 ) ) ;
#38070=VERTEX_POINT ( 'NONE', #21829 ) ;
#38071=DIRECTION ( 'NONE',  ( 0.7818314824680311359, 0.000000000000000000, -0.6234898018587319291 ) ) ;
#38075=EDGE_LOOP ( 'NONE', ( #37295, #18750, #16499, #46702 ) ) ;
#38079=AXIS2_PLACEMENT_3D ( 'NONE', #13077, #29583, #49158 ) ;
#38086=AXIS2_PLACEMENT_3D ( 'NONE', #42037, #22171, #10038 ) ;
#38087=AXIS2_PLACEMENT_3D ( 'NONE', #26051, #6180, #33818 ) ;
#38088=ORIENTED_EDGE ( 'NONE', *, *, #49256, .F. ) ;
#38091=CARTESIAN_POINT ( 'NONE',  ( -2.318785326816343861, 1.683110758435957477, 1.828187939119067851 ) ) ;
#38094=EDGE_CURVE ( 'NONE', #28481, #38735, #44068, .T. ) ;
#38097=DIRECTION ( 'NONE',  ( -0.01601477604151182663, 0.9998717552508123996, -0.000000000000000000 ) ) ;
#38099=DIRECTION ( 'NONE',  ( 0.9009688679024154823, 0.000000000000000000, 0.4338837391175656699 ) ) ;
#38103=CARTESIAN_POINT ( 'NONE',  ( 2.491402175429654253, 1.659612532563349285, -1.585592796919505831 ) ) ;
#38107=CARTESIAN_POINT ( 'NONE',  ( -1.734268221780295827, 0.000000000000000000, 0.1852605408175444779 ) ) ;
#38108=CARTESIAN_POINT ( 'NONE',  ( 0.7381027496705270252, 1.499047760149736952, -2.859439394060913298 ) ) ;
#38113=DIRECTION ( 'NONE',  ( -0.01601477604151182663, 0.9998717552508123996, -0.000000000000000000 ) ) ;
#38114=EDGE_CURVE ( 'NONE', #23605, #11539, #47783, .T. ) ;
#38119=VECTOR ( 'NONE', #27932, 39.37007874015748143 ) ;
#38121=ORIENTED_EDGE ( 'NONE', *, *, #7759, .T. ) ;
#38126=DIRECTION ( 'NONE',  ( -1.105928667600717569E-16, 1.000000000000000000, -6.607616187506203079E-17 ) ) ;
#38129=VECTOR ( 'NONE', #46873, 39.37007874015748143 ) ;
#38130=ORIENTED_EDGE ( 'NONE', *, *, #42786, .F. ) ;
#38134=CARTESIAN_POINT ( 'NONE',  ( -2.142805232260985182, -3.932816271735134525E-17, 0.3399247426648318582 ) ) ;
#38135=ORIENTED_EDGE ( 'NONE', *, *, #11622, .F. ) ;
#38140=VERTEX_POINT ( 'NONE', #17444 ) ;
#38141=CARTESIAN_POINT ( 'NONE',  ( 2.193564619503452828, 1.644610705845120258, 0.7644775380370429918 ) ) ;
#38143=DIRECTION ( 'NONE',  ( 0.000000000000000000, -1.000000000000000000, -0.000000000000000000 ) ) ;
#38147=ADVANCED_FACE ( 'NONE', ( #22582 ), #37153, .T. ) ;
#38148=CARTESIAN_POINT ( 'NONE',  ( -0.4788131938641531637, 1.205361022782829114E-17, 2.914091152102186388 ) ) ;
#38149=EDGE_CURVE ( 'NONE', #24903, #41095, #48973, .T. ) ;
#38150=CONICAL_SURFACE ( 'NONE', #30731, 3.033577403570480779, 1.554780866114618743 ) ;
#38154=DIRECTION ( 'NONE',  ( 0.000000000000000000, 0.000000000000000000, 1.000000000000000000 ) ) ;
#38161=ORIENTED_EDGE ( 'NONE', *, *, #6282, .F. ) ;
#38164=VERTEX_POINT ( 'NONE', #45542 ) ;
#38165=CARTESIAN_POINT ( 'NONE',  ( 2.339241080213585899, 1.657243480315735873, 1.802537235681917815 ) ) ;
#38167=B_SPLINE_CURVE_WITH_KNOTS ( 'NONE', 3,
 ( #3348, #42088, #18851, #2594 ),
 .UNSPECIFIED., .F., .F.,
 ( 4, 4 ),
 ( 2.007585174703544570E-07, 0.002500777222804251645 ),
 .UNSPECIFIED. ) ;
#38169=FACE_OUTER_BOUND ( 'NONE', #19587, .T. ) ;
#38170=EDGE_CURVE ( 'NONE', #196, #46048, #24425, .T. ) ;
#38174=CARTESIAN_POINT ( 'NONE',  ( 0.08119777152254364916, 1.623385212329073957, 0.000000000000000000 ) ) ;
#38175=ADVANCED_FACE ( 'NONE', ( #47227, #26453 ), #50155, .T. ) ;
#38179=EDGE_CURVE ( 'NONE', #20106, #7882, #31531, .T. ) ;
#38183=CARTESIAN_POINT ( 'NONE',  ( 0.002207914879453961535, -5.712274067634378313E-18, 0.04916304461325374242 ) ) ;
#38192=AXIS2_PLACEMENT_3D ( 'NONE', #18694, #23308, #19426 ) ;
#38194=VERTEX_POINT ( 'NONE', #10715 ) ;
#38206=AXIS2_PLACEMENT_3D ( 'NONE', #17448, #18212, #10210 ) ;
#38207=DIRECTION ( 'NONE',  ( 7.097135778201662695E-17, 1.000000000000000000, -1.075170113095010447E-16 ) ) ;
#38208=ORIENTED_EDGE ( 'NONE', *, *, #6864, .T. ) ;
#38213=DIRECTION ( 'NONE',  ( 0.8345732537213079727, 6.391122427287080193E-17, -0.5508969814520945363 ) ) ;
#38215=ORIENTED_EDGE ( 'NONE', *, *, #3647, .F. ) ;
#38220=DIRECTION ( 'NONE',  ( 0.8805955318567321166, -5.503865196449042635E-17, 0.4738686624730094055 ) ) ;
#38223=DIRECTION ( 'NONE',  ( -0.9998717552508121775, -0.01601477604151182316, 0.000000000000000000 ) ) ;
#38224=LINE ( 'NONE', #46182, #43169 ) ;
#38225=AXIS2_PLACEMENT_3D ( 'NONE', #39248, #31261, #23498 ) ;
#38233=CARTESIAN_POINT ( 'NONE',  ( 2.755905511811024056, 2.913385826771657250, -1.023622047244094224 ) ) ;
#38234=AXIS2_PLACEMENT_3D ( 'NONE', #45604, #41264, #49459 ) ;
#38235=FACE_OUTER_BOUND ( 'NONE', #38386, .T. ) ;
#38236=EDGE_CURVE ( 'NONE', #27703, #19989, #28062, .T. ) ;
#38240=VERTEX_POINT ( 'NONE', #8031 ) ;
#38242=ORIENTED_EDGE ( 'NONE', *, *, #32822, .F. ) ;
#38244=CARTESIAN_POINT ( 'NONE',  ( 1.542217245295272932, 0.05262109711011796892, 1.166931937029544564 ) ) ;
#38247=ORIENTED_EDGE ( 'NONE', *, *, #18967, .F. ) ;
#38252=CARTESIAN_POINT ( 'NONE',  ( 0.002207914879453961969, 5.905511811023623991, 0.04916304461325442243 ) ) ;
#38255=CARTESIAN_POINT ( 'NONE',  ( -1.690941099774203815, 0.0008361491594236539725, -0.4364244636917575804 ) ) ;
#38257=ORIENTED_EDGE ( 'NONE', *, *, #35346, .F. ) ;
#38258=FACE_OUTER_BOUND ( 'NONE', #46192, .T. ) ;
#38259=AXIS2_PLACEMENT_3D ( 'NONE', #25180, #30069, #6326 ) ;
#38260=VECTOR ( 'NONE', #13069, 39.37007874015748143 ) ;
#38268=CARTESIAN_POINT ( 'NONE',  ( 1.776015598323502198, 0.5249316497054298258, 0.6288076369129006471 ) ) ;
#38269=CARTESIAN_POINT ( 'NONE',  ( 0.04921259842519670746, 1.514263714023589502, 2.952755905511811108 ) ) ;
#38271=VERTEX_POINT ( 'NONE', #30083 ) ;
#38277=B_SPLINE_CURVE_WITH_KNOTS ( 'NONE', 3,
 ( #42506, #6887, #26503, #31147 ),
 .UNSPECIFIED., .F., .F.,
 ( 4, 4 ),
 ( 2.102951466402419151E-07, 0.002500239283416568880 ),
 .UNSPECIFIED. ) ;
#38280=CARTESIAN_POINT ( 'NONE',  ( -2.882375110776534299, 1.574243653623555339, -0.6410540981532866223 ) ) ;
#38284=FACE_OUTER_BOUND ( 'NONE', #25812, .T. ) ;
#38305=DIRECTION ( 'NONE',  ( -0.9998717552508122886, -0.01601477604151180928, 0.000000000000000000 ) ) ;
#38312=ORIENTED_EDGE ( 'NONE', *, *, #12937, .F. ) ;
#38314=DIRECTION ( 'NONE',  ( -0.000000000000000000, 1.000000000000000000, -0.000000000000000000 ) ) ;
#38315=CARTESIAN_POINT ( 'NONE',  ( -0.4349608091551073197, 1.574803149606302854, 2.121218629000295230 ) ) ;
#38319=EDGE_CURVE ( 'NONE', #23810, #17176, #47742, .T. ) ;
#38324=DIRECTION ( 'NONE',  ( 7.097135778201508621E-17, 1.000000000000000000, 1.075170113095020677E-16 ) ) ;
#38328=ORIENTED_EDGE ( 'NONE', *, *, #42236, .F. ) ;
#38329=DIRECTION ( 'NONE',  ( 0.000000000000000000, 0.000000000000000000, 1.000000000000000000 ) ) ;
#38330=VERTEX_POINT ( 'NONE', #12417 ) ;
#38333=LINE ( 'NONE', #2953, #19323 ) ;
#38335=CARTESIAN_POINT ( 'NONE',  ( 2.277873973731426194, 1.754757658573260048, 1.879489153247668076 ) ) ;
#38337=ORIENTED_EDGE ( 'NONE', *, *, #40026, .F. ) ;
#38338=CIRCLE ( 'NONE', #46544, 2.165354330708661568 ) ;
#38339=VERTEX_POINT ( 'NONE', #28928 ) ;
#38343=EDGE_CURVE ( 'NONE', #4293, #4534, #24808, .T. ) ;
#38344=CARTESIAN_POINT ( 'NONE',  ( -1.472219874544909768, 1.597879704547665369, 2.560030851058948898 ) ) ;
#38346=DIRECTION ( 'NONE',  ( -0.9998717552508122886, -0.01601477604151181275, 0.000000000000000000 ) ) ;
#38348=ORIENTED_EDGE ( 'NONE', *, *, #11458, .F. ) ;
#38355=CARTESIAN_POINT ( 'NONE',  ( -0.7145799201509074328, 1.574803149606302854, 2.044048657746648789 ) ) ;
#38360=ORIENTED_EDGE ( 'NONE', *, *, #5851, .F. ) ;
#38366=ORIENTED_EDGE ( 'NONE', *, *, #37764, .F. ) ;
#38369=CARTESIAN_POINT ( 'NONE',  ( -1.068402561569949283, 6.692913385826772199, -1.884154513482188209 ) ) ;
#38372=DIRECTION ( 'NONE',  ( -3.986037398843765983E-20, -1.000000000000000000, -1.160734090543304660E-16 ) ) ;
#38373=EDGE_CURVE ( 'NONE', #50100, #29332, #36174, .T. ) ;
#38377=VERTEX_POINT ( 'NONE', #47996 ) ;
#38378=CARTESIAN_POINT ( 'NONE',  ( 2.793030215715258446, 0.000000000000000000, 0.9592557174602679426 ) ) ;
#38382=ORIENTED_EDGE ( 'NONE', *, *, #40456, .F. ) ;
#38384=CARTESIAN_POINT ( 'NONE',  ( -0.5756566573089004768, 1.710292258889409833, 2.896516654582634853 ) ) ;
#38386=EDGE_LOOP ( 'NONE', ( #4439, #36959, #49231, #27567, #2319, #4704, #46123, #34132, #21160, #20894, #18359, #23686, #2933 ) ) ;
#38389=ORIENTED_EDGE ( 'NONE', *, *, #44196, .T. ) ;
#38391=CARTESIAN_POINT ( 'NONE',  ( 1.661821349926414282, 6.692913385826772199, 1.388203579611976712 ) ) ;
#38392=DIRECTION ( 'NONE',  ( -0.2660368455666687892, 0.000000000000000000, -0.9639628606958549062 ) ) ;
#38393=ADVANCED_FACE ( 'NONE', ( #17071 ), #11623, .T. ) ;
#38394=DIRECTION ( 'NONE',  ( -0.01601477604151182663, 0.9998717552508123996, -0.000000000000000000 ) ) ;
#38396=CARTESIAN_POINT ( 'NONE',  ( -0.5441960870438705689, 1.666377258251801941, -2.156834381528191180 ) ) ;
#38397=CARTESIAN_POINT ( 'NONE',  ( 1.943616526632303110, 1.647544198063666476, -1.926374208805734956 ) ) ;
#38399=EDGE_CURVE ( 'NONE', #26794, #31047, #31403, .T. ) ;
#38401=CARTESIAN_POINT ( 'NONE',  ( 0.000000000000000000, 1.574803149606302854, 0.000000000000000000 ) ) ;
#38408=CARTESIAN_POINT ( 'NONE',  ( -1.790681247139289889, 1.679220913509628543, -1.240985722462402352 ) ) ;
#38411=AXIS2_PLACEMENT_3D ( 'NONE', #16849, #48290, #12974 ) ;
#38418=CARTESIAN_POINT ( 'NONE',  ( -2.456292249654252302, 1.578478270180400322, -1.103389117635475536 ) ) ;
#38424=EDGE_CURVE ( 'NONE', #25218, #8605, #37465, .T. ) ;
#38425=DIRECTION ( 'NONE',  ( -0.01601477604151182663, 0.9998717552508123996, -0.000000000000000000 ) ) ;
#38428=LINE ( 'NONE', #18554, #21298 ) ;
#38435=EDGE_CURVE ( 'NONE', #9734, #24599, #20721, .T. ) ;
#38439=EDGE_CURVE ( 'NONE', #39932, #29652, #29957, .T. ) ;
#38443=VERTEX_POINT ( 'NONE', #13957 ) ;
#38445=CARTESIAN_POINT ( 'NONE',  ( 0.1525789431699052512, 1.677537385366203448, -2.244297798459045534 ) ) ;
#38452=EDGE_LOOP ( 'NONE', ( #41152, #28921, #17020, #39262 ) ) ;
#38457=EDGE_CURVE ( 'NONE', #31511, #35836, #15144, .T. ) ;
#38463=CARTESIAN_POINT ( 'NONE',  ( -1.442444474601640492, 0.004816277389180329341, -1.011116641508509995 ) ) ;
#38464=EDGE_CURVE ( 'NONE', #30125, #49795, #29768, .T. ) ;
#38468=LINE ( 'NONE', #6465, #50979 ) ;
#38472=CARTESIAN_POINT ( 'NONE',  ( -2.165354330708661568, 1.574803149606301966, -0.01597875172474143637 ) ) ;
#38473=DIRECTION ( 'NONE',  ( -1.288287287306305283E-16, 1.000000000000000000, 0.000000000000000000 ) ) ;
#38475=CARTESIAN_POINT ( 'NONE',  ( 2.734482843737263025, 2.755905511811027164, -1.115254632218672493 ) ) ;
#38480=VECTOR ( 'NONE', #13068, 39.37007874015748143 ) ;
#38481=ORIENTED_EDGE ( 'NONE', *, *, #22560, .F. ) ;
#38483=CARTESIAN_POINT ( 'NONE',  ( -1.790900357307437352, 1.580792207208895128, -1.241130355818072406 ) ) ;
#38485=CONICAL_SURFACE ( 'NONE', #16216, 2.244934639244524632, 1.554780866114618743 ) ;
#38486=ORIENTED_EDGE ( 'NONE', *, *, #22756, .F. ) ;
#38489=CARTESIAN_POINT ( 'NONE',  ( 2.043634885149959057, 5.118110236220475784, 0.7157624142946238388 ) ) ;
#38494=ORIENTED_EDGE ( 'NONE', *, *, #39966, .F. ) ;
#38497=EDGE_CURVE ( 'NONE', #16641, #11793, #41039, .T. ) ;
#38500=CARTESIAN_POINT ( 'NONE',  ( 2.122900538649399316, 1.653866144572175179, -2.052396120437094407 ) ) ;
#38501=CARTESIAN_POINT ( 'NONE',  ( 1.236813753895252166, 1.640077341046696890, -2.681693691597563767 ) ) ;
#38503=DIRECTION ( 'NONE',  ( -0.1785568947986370392, 0.000000000000000000, 0.9839295885986295565 ) ) ;
#38504=EDGE_CURVE ( 'NONE', #21474, #45901, #49781, .T. ) ;
#38511=CYLINDRICAL_SURFACE ( 'NONE', #9280, 2.165354330708661568 ) ;
#38512=ORIENTED_EDGE ( 'NONE', *, *, #21228, .T. ) ;
#38515=DIRECTION ( 'NONE',  ( 0.9639628606958512425, -1.160734090543304660E-16, 0.2660368455666826670 ) ) ;
#38519=CARTESIAN_POINT ( 'NONE',  ( 1.905671854841463730, 1.650492703781866632, 2.256015092822682089 ) ) ;
#38522=ORIENTED_EDGE ( 'NONE', *, *, #24504, .F. ) ;
#38524=EDGE_CURVE ( 'NONE', #11129, #26516, #8309, .T. ) ;
#38527=LINE ( 'NONE', #26140, #49639 ) ;
#38528=CARTESIAN_POINT ( 'NONE',  ( -1.152895553066196843, 6.692913385826772199, -1.833672301139088301 ) ) ;
#38535=B_SPLINE_CURVE_WITH_KNOTS ( 'NONE', 3,
 ( #20868, #27138, #8738, #28607 ),
 .UNSPECIFIED., .F., .F.,
 ( 4, 4 ),
 ( 2.271247561980464994E-07, 0.002500295238063529428 ),
 .UNSPECIFIED. ) ;
#38536=CARTESIAN_POINT ( 'NONE',  ( 0.07982360342473591996, 1.709180471932028711, 0.000000000000000000 ) ) ;
#38538=LINE ( 'NONE', #3160, #30667 ) ;
#38545=EDGE_LOOP ( 'NONE', ( #39284, #8591, #37926, #30229 ) ) ;
#38547=VERTEX_POINT ( 'NONE', #42581 ) ;
#38550=CARTESIAN_POINT ( 'NONE',  ( -0.2492758785930729581, 1.703909341437327862, -2.220674960591680680 ) ) ;
#38555=EDGE_LOOP ( 'NONE', ( #1565, #37766, #34415, #14162 ) ) ;
#38559=EDGE_CURVE ( 'NONE', #37038, #47957, #33636, .T. ) ;
#38561=DIRECTION ( 'NONE',  ( -0.01601477604151182663, 0.9998717552508123996, -0.000000000000000000 ) ) ;
#38563=CARTESIAN_POINT ( 'NONE',  ( -1.743268982565497449, 0.0004610889948519912205, -0.02902809809614041725 ) ) ;
#38564=CONICAL_SURFACE ( 'NONE', #31146, 2.165354330708661568, 0.2617993877991570129 ) ;
#38568=CARTESIAN_POINT ( 'NONE',  ( 0.8069532150559736161, 1.205361022782829114E-17, -2.010061882867131278 ) ) ;
#38571=EDGE_CURVE ( 'NONE', #36108, #41559, #50204, .T. ) ;
#38576=DIRECTION ( 'NONE',  ( -0.000000000000000000, -1.000000000000000000, -0.000000000000000000 ) ) ;
#38577=EDGE_LOOP ( 'NONE', ( #43286, #21974, #7514, #44995 ) ) ;
#38580=PLANE ( 'NONE',  #26703 ) ;
#38582=EDGE_CURVE ( 'NONE', #21621, #5433, #47041, .T. ) ;
#38583=CONICAL_SURFACE ( 'NONE', #23743, 2.165354330708661568, 0.2617993877991570129 ) ;
#38584=CONICAL_SURFACE ( 'NONE', #16309, 2.165354330708661568, 0.2617993877991570129 ) ;
#38585=CARTESIAN_POINT ( 'NONE',  ( 0.1067246931122726866, 0.02962905676920215767, 0.000000000000000000 ) ) ;
#38587=EDGE_LOOP ( 'NONE', ( #23865, #16274, #39193 ) ) ;
#38589=VECTOR ( 'NONE', #5159, 39.37007874015748143 ) ;
#38591=CARTESIAN_POINT ( 'NONE',  ( -0.2198976605848039223, 1.205361022782829114E-17, -1.894256224240784103 ) ) ;
#38593=VECTOR ( 'NONE', #24223, 39.37007874015748143 ) ;
#38595=DIRECTION ( 'NONE',  ( 0.000000000000000000, 0.000000000000000000, 1.000000000000000000 ) ) ;
#38597=CARTESIAN_POINT ( 'NONE',  ( -1.979793062125317471, 1.556934451446513545, 2.191257344206539504 ) ) ;
#38602=DIRECTION ( 'NONE',  ( 0.4338837391175656699, 0.000000000000000000, -0.9009688679024154823 ) ) ;
#38608=ORIENTED_EDGE ( 'NONE', *, *, #23112, .T. ) ;
#38615=EDGE_LOOP ( 'NONE', ( #9941, #23317, #28176, #16169 ) ) ;
#38616=ORIENTED_EDGE ( 'NONE', *, *, #49685, .T. ) ;
#38617=FACE_OUTER_BOUND ( 'NONE', #19782, .T. ) ;
#38619=ADVANCED_FACE ( 'NONE', ( #15219 ), #11094, .T. ) ;
#38624=ADVANCED_FACE ( 'NONE', ( #19332 ), #2843, .F. ) ;
#38625=DIRECTION ( 'NONE',  ( -0.9998717552508122886, -0.01601477604151181275, 0.000000000000000000 ) ) ;
#38636=CARTESIAN_POINT ( 'NONE',  ( -1.909828200256540987, 1.049866565067838042, 0.6722859868850896703 ) ) ;
#38642=VERTEX_POINT ( 'NONE', #7470 ) ;
#38643=CARTESIAN_POINT ( 'NONE',  ( -0.5272349255865267370, 0.000000000000000000, 2.905303903342410621 ) ) ;
#38644=ADVANCED_FACE ( 'NONE', ( #27330 ), #7718, .T. ) ;
#38650=DIRECTION ( 'NONE',  ( 0.9998717552508121775, 0.01601477604151182663, 0.000000000000000000 ) ) ;
#38651=CARTESIAN_POINT ( 'NONE',  ( 2.951990591674676256, 1.447429260878886348, -0.08331184815398369470 ) ) ;
#38652=VERTEX_POINT ( 'NONE', #24495 ) ;
#38653=CARTESIAN_POINT ( 'NONE',  ( 1.426808618753927282, 0.05077261674489902399, -1.296082183384024811 ) ) ;
#38656=ADVANCED_FACE ( 'NONE', ( #27842 ), #9003, .F. ) ;
#38659=VECTOR ( 'NONE', #10552, 39.37007874015748854 ) ;
#38661=CARTESIAN_POINT ( 'NONE',  ( 0.9432913529151772947, 1.723010488186151878, -2.072188145589165753 ) ) ;
#38665=CARTESIAN_POINT ( 'NONE',  ( 0.04921259842519669359, 1.621581020286960051, 2.952755905511811108 ) ) ;
#38670=ORIENTED_EDGE ( 'NONE', *, *, #27877, .F. ) ;
#38672=EDGE_CURVE ( 'NONE', #33027, #10178, #4089, .T. ) ;
#38674=CARTESIAN_POINT ( 'NONE',  ( 0.08139965876239094178, 1.610780518492231694, 0.000000000000000000 ) ) ;
#38679=ORIENTED_EDGE ( 'NONE', *, *, #13325, .T. ) ;
#38685=ORIENTED_EDGE ( 'NONE', *, *, #3106, .T. ) ;
#38687=LINE ( 'NONE', #3308, #47867 ) ;
#38688=CIRCLE ( 'NONE', #25484, 2.164630168518208109 ) ;
#38691=FACE_OUTER_BOUND ( 'NONE', #31722, .T. ) ;
#38693=ORIENTED_EDGE ( 'NONE', *, *, #47592, .T. ) ;
#38698=DIRECTION ( 'NONE',  ( -3.986037398843765983E-20, -1.000000000000000000, -1.160734090543304660E-16 ) ) ;
#38704=VERTEX_POINT ( 'NONE', #8233 ) ;
#38706=FACE_OUTER_BOUND ( 'NONE', #16153, .T. ) ;
#38707=ORIENTED_EDGE ( 'NONE', *, *, #41574, .F. ) ;
#38711=DIRECTION ( 'NONE',  ( -0.9998717552508121775, -0.01601477604151182316, 0.000000000000000000 ) ) ;
#38712=ORIENTED_EDGE ( 'NONE', *, *, #41310, .F. ) ;
#38721=LINE ( 'NONE', #30469, #42482 ) ;
#38725=VERTEX_POINT ( 'NONE', #32506 ) ;
#38733=EDGE_CURVE ( 'NONE', #7184, #40673, #43473, .T. ) ;
#38734=DIRECTION ( 'NONE',  ( 1.558091277195102803E-17, -1.000000000000000000, 1.150229170499808965E-16 ) ) ;
#38735=VERTEX_POINT ( 'NONE', #48200 ) ;
#38738=ORIENTED_EDGE ( 'NONE', *, *, #5321, .T. ) ;
#38739=EDGE_CURVE ( 'NONE', #40626, #31520, #20064, .T. ) ;
#38742=EDGE_CURVE ( 'NONE', #11117, #45160, #15971, .T. ) ;
#38745=DIRECTION ( 'NONE',  ( -0.01601477604151182663, 0.9998717552508123996, -0.000000000000000000 ) ) ;
#38749=DIRECTION ( 'NONE',  ( 0.000000000000000000, 1.160734090543304660E-16, -1.000000000000000000 ) ) ;
#38752=CYLINDRICAL_SURFACE ( 'NONE', #14662, 2.165354330708661568 ) ;
#38755=ORIENTED_EDGE ( 'NONE', *, *, #33959, .F. ) ;
#38758=ORIENTED_EDGE ( 'NONE', *, *, #35548, .T. ) ;
#38761=VECTOR ( 'NONE', #38213, 39.37007874015748143 ) ;
#38764=CARTESIAN_POINT ( 'NONE',  ( -2.047355983664255863, 1.576684601009278319, 0.7169714724935087879 ) ) ;
#38768=CARTESIAN_POINT ( 'NONE',  ( -0.2810210260976235830, 1.616428356993893978, -2.939398529254692694 ) ) ;
#38769=DIRECTION ( 'NONE',  ( -0.01601477604151182663, 0.9998717552508123996, -0.000000000000000000 ) ) ;
#38774=EDGE_CURVE ( 'NONE', #11918, #38951, #2807, .T. ) ;
#38776=ADVANCED_FACE ( 'NONE', ( #1252 ), #10018, .T. ) ;
#38777=CARTESIAN_POINT ( 'NONE',  ( 1.929629134066521923, 1.574803149606302854, 0.9824921284572415425 ) ) ;
#38781=DIRECTION ( 'NONE',  ( -0.9998717552508121775, -0.01601477604151182663, 0.000000000000000000 ) ) ;
#38786=CARTESIAN_POINT ( 'NONE',  ( 0.5439123932328762123, 0.000000000000000000, -1.909459815214741729 ) ) ;
#38787=B_SPLINE_CURVE_WITH_KNOTS ( 'NONE', 3,
 ( #43292, #27293, #23421, #39177 ),
 .UNSPECIFIED., .F., .F.,
 ( 4, 4 ),
 ( 0.01204075435466551991, 0.03073748598634059442 ),
 .UNSPECIFIED. ) ;
#38790=ORIENTED_EDGE ( 'NONE', *, *, #5812, .F. ) ;
#38792=ADVANCED_FACE ( 'NONE', ( #41765 ), #2014, .F. ) ;
#38794=PLANE ( 'NONE',  #31198 ) ;
#38797=CARTESIAN_POINT ( 'NONE',  ( -0.2922236155267554092, 1.710885387309459160, -2.697863400512623855 ) ) ;
#38802=EDGE_CURVE ( 'NONE', #36553, #19989, #17763, .T. ) ;
#38805=ORIENTED_EDGE ( 'NONE', *, *, #47966, .F. ) ;
#38810=ORIENTED_EDGE ( 'NONE', *, *, #15642, .T. ) ;
#38813=CARTESIAN_POINT ( 'NONE',  ( -1.172858943013145749, 5.905511811023623991, 1.867085387823100850 ) ) ;
#38814=B_SPLINE_CURVE_WITH_KNOTS ( 'NONE', 3,
 ( #7906, #3274, #19772, #27777 ),
 .UNSPECIFIED., .F., .F.,
 ( 4, 4 ),
 ( 6.300333842480880930E-07, 0.002724228881262062436 ),
 .UNSPECIFIED. ) ;
#38818=CARTESIAN_POINT ( 'NONE',  ( 2.734482843737263025, 1.663397001319319113, -1.115254632218672493 ) ) ;
#38819=LINE ( 'NONE', #15317, #45558 ) ;
#38821=VERTEX_POINT ( 'NONE', #21894 ) ;
#38824=CARTESIAN_POINT ( 'NONE',  ( 2.947574761915768171, 1.666714435463287236, -0.1816379373804911379 ) ) ;
#38825=ORIENTED_EDGE ( 'NONE', *, *, #18724, .T. ) ;
#38827=FACE_OUTER_BOUND ( 'NONE', #537, .T. ) ;
#38828=DIRECTION ( 'NONE',  ( 0.01601477604151182663, -0.9998717552508123996, 0.000000000000000000 ) ) ;
#38829=DIRECTION ( 'NONE',  ( -0.000000000000000000, 1.000000000000000000, -0.000000000000000000 ) ) ;
#38831=CARTESIAN_POINT ( 'NONE',  ( 0.08139965876239094178, 1.610780518492231694, 0.000000000000000000 ) ) ;
#38839=EDGE_CURVE ( 'NONE', #17350, #51046, #37652, .T. ) ;
#38840=DIRECTION ( 'NONE',  ( 0.7818314824680221431, 0.000000000000000000, 0.6234898018587431423 ) ) ;
#38843=EDGE_CURVE ( 'NONE', #20385, #4443, #9511, .T. ) ;
#38844=CARTESIAN_POINT ( 'NONE',  ( -1.901641471869980782, 6.692913385826772199, 1.079202499698819429 ) ) ;
#38846=CARTESIAN_POINT ( 'NONE',  ( 2.164823134740037069, 1.574803149606302854, -0.04796011690015113127 ) ) ;
#38851=CARTESIAN_POINT ( 'NONE',  ( -1.232620761116185681, 6.692913385826772199, -1.780282403660753410 ) ) ;
#38852=DIRECTION ( 'NONE',  ( 0.2225209339563041788, 0.000000000000000000, 0.9749279121818259508 ) ) ;
#38853=FACE_OUTER_BOUND ( 'NONE', #13055, .T. ) ;
#38857=DIRECTION ( 'NONE',  ( -0.9998717552508122886, -0.01601477604151185785, 0.000000000000000000 ) ) ;
#38859=FACE_OUTER_BOUND ( 'NONE', #43315, .T. ) ;
#38863=VERTEX_POINT ( 'NONE', #25256 ) ;
#38866=CARTESIAN_POINT ( 'NONE',  ( -1.530693736245496872, 1.574803149606302854, -1.531579597454065800 ) ) ;
#38876=CARTESIAN_POINT ( 'NONE',  ( 1.412396057062171639, 5.905511811023623991, 1.691415513056039321 ) ) ;
#38878=VECTOR ( 'NONE', #45625, 39.37007874015748143 ) ;
#38880=FACE_OUTER_BOUND ( 'NONE', #17376, .T. ) ;
#38881=ORIENTED_EDGE ( 'NONE', *, *, #27947, .T. ) ;
#38884=EDGE_CURVE ( 'NONE', #2673, #13810, #916, .T. ) ;
#38890=LINE ( 'NONE', #34768, #45015 ) ;
#38891=CARTESIAN_POINT ( 'NONE',  ( 2.278027606577265107, 1.645963535160160696, -0.4694667435916627385 ) ) ;
#38893=DIRECTION ( 'NONE',  ( 0.000000000000000000, 1.000000000000000000, 0.000000000000000000 ) ) ;
#38894=CARTESIAN_POINT ( 'NONE',  ( 2.620071330711824853, 0.9846937227970387063, -0.06840533695594305796 ) ) ;
#38899=CARTESIAN_POINT ( 'NONE',  ( 1.748857742733975096, 1.746506983082525499, -2.379187494648852930 ) ) ;
#38900=LINE ( 'NONE', #39154, #28983 ) ;
#38901=EDGE_CURVE ( 'NONE', #32706, #33100, #48954, .T. ) ;
#38902=VECTOR ( 'NONE', #8107, 39.37007874015748143 ) ;
#38911=CARTESIAN_POINT ( 'NONE',  ( 1.472219874544873131, 1.482402307789154161, 2.560030851058970214 ) ) ;
#38912=VECTOR ( 'NONE', #38314, 39.37007874015748143 ) ;
#38915=ORIENTED_EDGE ( 'NONE', *, *, #46856, .T. ) ;
#38917=DIRECTION ( 'NONE',  ( -0.9998717552508121775, -0.01601477604151182316, 0.000000000000000000 ) ) ;
#38918=AXIS2_PLACEMENT_3D ( 'NONE', #1833, #32317, #25076 ) ;
#38919=LINE ( 'NONE', #3047, #2030 ) ;
#38924=ORIENTED_EDGE ( 'NONE', *, *, #34767, .T. ) ;
#38926=VERTEX_POINT ( 'NONE', #23399 ) ;
#38928=CARTESIAN_POINT ( 'NONE',  ( 1.751183565766393890, 0.5249316497054296038, -0.6949723510457602726 ) ) ;
#38929=DIRECTION ( 'NONE',  ( -0.1342332658176667026, -1.150175664618034464E-16, 0.9909497617679331460 ) ) ;
#38938=ORIENTED_EDGE ( 'NONE', *, *, #4675, .F. ) ;
#38939=EDGE_CURVE ( 'NONE', #35652, #18885, #10000, .T. ) ;
#38944=CARTESIAN_POINT ( 'NONE',  ( 2.074656761899007051, 5.905511811023623991, -0.6223516566630625801 ) ) ;
#38945=CONICAL_SURFACE ( 'NONE', #16703, 2.165354330708661568, 0.2617993877991570129 ) ;
#38947=EDGE_CURVE ( 'NONE', #50130, #24742, #39738, .T. ) ;
#38950=DIRECTION ( 'NONE',  ( -0.9998717552508121775, -0.01601477604151182663, 0.000000000000000000 ) ) ;
#38951=VERTEX_POINT ( 'NONE', #23149 ) ;
#38952=CARTESIAN_POINT ( 'NONE',  ( -2.168245791271168343, 1.560742704294596495, -2.004968704497279486 ) ) ;
#38953=AXIS2_PLACEMENT_3D ( 'NONE', #13020, #28238, #8632 ) ;
#38954=DIRECTION ( 'NONE',  ( -0.9998717552508122886, -0.01601477604151185785, 0.000000000000000000 ) ) ;
#38956=EDGE_LOOP ( 'NONE', ( #19120, #36673, #21804, #7237 ) ) ;
#38957=ORIENTED_EDGE ( 'NONE', *, *, #28475, .T. ) ;
#38959=CARTESIAN_POINT ( 'NONE',  ( -2.951990591674674480, 1.673246673531018525, -0.08331184815402598032 ) ) ;
#38961=LINE ( 'NONE', #39982, #13603 ) ;
#38976=ORIENTED_EDGE ( 'NONE', *, *, #34131, .T. ) ;
#38977=CARTESIAN_POINT ( 'NONE',  ( -2.919426793319806368, 1.673754417692067564, 0.4451252810446391095 ) ) ;
#38978=VECTOR ( 'NONE', #335, 39.37007874015748143 ) ;
#38983=CYLINDRICAL_SURFACE ( 'NONE', #44545, 2.164630168518208109 ) ;
#38984=EDGE_CURVE ( 'NONE', #35848, #2274, #38900, .T. ) ;
#38987=DIRECTION ( 'NONE',  ( -0.9362348706397418674, -1.160734090543305153E-16, 0.3513748240813305279 ) ) ;
#38994=ORIENTED_EDGE ( 'NONE', *, *, #19717, .T. ) ;
#38995=ADVANCED_FACE ( 'NONE', ( #46366 ), #26514, .F. ) ;
#38996=CARTESIAN_POINT ( 'NONE',  ( -0.5662636741187642153, 0.000000000000000000, 1.648861433446455971 ) ) ;
#38997=DIRECTION ( 'NONE',  ( -0.000000000000000000, 1.000000000000000000, -0.000000000000000000 ) ) ;
#38999=VERTEX_POINT ( 'NONE', #50711 ) ;
#39003=VERTEX_POINT ( 'NONE', #15415 ) ;
#39007=DIRECTION ( 'NONE',  ( -0.9998717552508122886, -0.01601477604151181275, 0.000000000000000000 ) ) ;
#39010=CARTESIAN_POINT ( 'NONE',  ( -1.738955188402737440, 0.000000000000000000, -0.1273587697465547175 ) ) ;
#39011=EDGE_LOOP ( 'NONE', ( #3930, #22046, #34282, #580, #7168, #29086, #10871, #25842, #20595, #35237, #15449, #17821, #36461 ) ) ;
#39014=CARTESIAN_POINT ( 'NONE',  ( -1.790900357307437352, 1.580792207208895128, -1.241130355818072406 ) ) ;
#39017=VERTEX_POINT ( 'NONE', #19020 ) ;
#39027=VECTOR ( 'NONE', #15842, 39.37007874015748143 ) ;
#39028=VERTEX_POINT ( 'NONE', #28293 ) ;
#39035=CARTESIAN_POINT ( 'NONE',  ( 0.000000000000000000, 6.692913385826772199, 0.000000000000000000 ) ) ;
#39036=ORIENTED_EDGE ( 'NONE', *, *, #43911, .F. ) ;
#39038=DIRECTION ( 'NONE',  ( 0.000000000000000000, 1.160734090543304660E-16, -1.000000000000000000 ) ) ;
#39049=CARTESIAN_POINT ( 'NONE',  ( 0.000000000000000000, 6.692913385826772199, -2.086614173228346303 ) ) ;
#39053=VECTOR ( 'NONE', #41153, 39.37007874015748143 ) ;
#39056=FACE_OUTER_BOUND ( 'NONE', #43033, .T. ) ;
#39062=FACE_OUTER_BOUND ( 'NONE', #35707, .T. ) ;
#39063=LINE ( 'NONE', #34444, #39825 ) ;
#39066=ORIENTED_EDGE ( 'NONE', *, *, #22085, .F. ) ;
#39067=CARTESIAN_POINT ( 'NONE',  ( 0.1067246931122726866, 0.02962905676920215767, 0.000000000000000000 ) ) ;
#39070=CONICAL_SURFACE ( 'NONE', #6089, 3.033577403570480779, 1.554780866114618743 ) ;
#39072=FACE_OUTER_BOUND ( 'NONE', #38577, .T. ) ;
#39074=ORIENTED_EDGE ( 'NONE', *, *, #50978, .F. ) ;
#39078=CARTESIAN_POINT ( 'NONE',  ( -2.024313280741415255, 1.050020262844681751, -0.04164981208090088455 ) ) ;
#39079=FACE_OUTER_BOUND ( 'NONE', #23483, .T. ) ;
#39082=EDGE_CURVE ( 'NONE', #11815, #10495, #21277, .T. ) ;
#39086=EDGE_CURVE ( 'NONE', #29782, #2720, #36315, .T. ) ;
#39089=CARTESIAN_POINT ( 'NONE',  ( 0.000000000000000000, 1.574803149606302854, 0.000000000000000000 ) ) ;
#39090=ORIENTED_EDGE ( 'NONE', *, *, #41295, .T. ) ;
#39092=EDGE_CURVE ( 'NONE', #1553, #13738, #36566, .T. ) ;
#39095=CIRCLE ( 'NONE', #16846, 2.165354330708661568 ) ;
#39097=AXIS2_PLACEMENT_3D ( 'NONE', #32650, #13273, #5521 ) ;
#39098=VECTOR ( 'NONE', #2846, 39.37007874015748143 ) ;
#39099=ORIENTED_EDGE ( 'NONE', *, *, #21913, .F. ) ;
#39104=CARTESIAN_POINT ( 'NONE',  ( -2.889674983507169337, 1.205361022782829114E-17, -0.6090712660038032356 ) ) ;
#39106=VECTOR ( 'NONE', #23467, 39.37007874015748143 ) ;
#39107=ORIENTED_EDGE ( 'NONE', *, *, #31488, .F. ) ;
#39108=CARTESIAN_POINT ( 'NONE',  ( 0.07982360342473591996, 1.709180471932028711, 0.000000000000000000 ) ) ;
#39111=FACE_OUTER_BOUND ( 'NONE', #30382, .T. ) ;
#39114=ORIENTED_EDGE ( 'NONE', *, *, #10361, .F. ) ;
#39115=CARTESIAN_POINT ( 'NONE',  ( -1.030301126714985971, 0.000000000000000000, -1.501813316714599500 ) ) ;
#39119=DIRECTION ( 'NONE',  ( -0.01601477604151182663, 0.9998717552508123996, -0.000000000000000000 ) ) ;
#39120=DIRECTION ( 'NONE',  ( 0.9510565162951545304, 0.000000000000000000, -0.3090169943749447867 ) ) ;
#39126=EDGE_CURVE ( 'NONE', #50130, #29859, #49544, .T. ) ;
#39129=VERTEX_POINT ( 'NONE', #28039 ) ;
#39133=ORIENTED_EDGE ( 'NONE', *, *, #47084, .T. ) ;
#39135=DIRECTION ( 'NONE',  ( 0.3090169943749582204, 1.288287287306305283E-16, -0.9510565162951500895 ) ) ;
#39136=EDGE_CURVE ( 'NONE', #6492, #34811, #29218, .T. ) ;
#39140=FACE_OUTER_BOUND ( 'NONE', #10191, .T. ) ;
#39143=DIRECTION ( 'NONE',  ( 0.000000000000000000, 0.000000000000000000, 1.000000000000000000 ) ) ;
#39144=LINE ( 'NONE', #30641, #17031 ) ;
#39145=CARTESIAN_POINT ( 'NONE',  ( -2.932638728931780125, 1.673548413681422042, 0.3475908556737793420 ) ) ;
#39149=FACE_OUTER_BOUND ( 'NONE', #26937, .T. ) ;
#39154=CARTESIAN_POINT ( 'NONE',  ( 2.755905511811024056, 2.913385826771657250, 1.023622047244094446 ) ) ;
#39158=ORIENTED_EDGE ( 'NONE', *, *, #18280, .T. ) ;
#39161=VECTOR ( 'NONE', #34651, 39.37007874015748143 ) ;
#39165=VERTEX_POINT ( 'NONE', #420 ) ;
#39166=CARTESIAN_POINT ( 'NONE',  ( 2.110884035022549732, 1.741711621820001943, -0.9557545615714394538 ) ) ;
#39168=FACE_OUTER_BOUND ( 'NONE', #50438, .T. ) ;
#39170=CARTESIAN_POINT ( 'NONE',  ( 2.623503965249849301, 1.661669217907264740, 1.355882097269874187 ) ) ;
#39176=ORIENTED_EDGE ( 'NONE', *, *, #48007, .T. ) ;
#39177=CARTESIAN_POINT ( 'NONE',  ( -0.9914495361339012991, 1.703811331058339373, 2.781765111341808705 ) ) ;
#39184=ORIENTED_EDGE ( 'NONE', *, *, #24809, .T. ) ;
#39186=EDGE_LOOP ( 'NONE', ( #46884, #1780, #35596, #30320, #5251, #34222, #50355, #11507, #11596, #3512, #6316 ) ) ;
#39187=CARTESIAN_POINT ( 'NONE',  ( 0.9218113296639885990, 0.000000000000000000, -1.800737481590852118 ) ) ;
#39191=ADVANCED_FACE ( 'NONE', ( #29057 ), #5079, .T. ) ;
#39192=ORIENTED_EDGE ( 'NONE', *, *, #23578, .F. ) ;
#39193=ORIENTED_EDGE ( 'NONE', *, *, #43069, .F. ) ;
#39200=CONICAL_SURFACE ( 'NONE', #27652, 1.850107469027523210, 0.6386652850508578450 ) ;
#39205=AXIS2_PLACEMENT_3D ( 'NONE', #42853, #3884, #11874 ) ;
#39206=CARTESIAN_POINT ( 'NONE',  ( -2.165668409223900692, 1.578950121022790531, 1.109510278747024348 ) ) ;
#39207=ORIENTED_EDGE ( 'NONE', *, *, #38802, .T. ) ;
#39209=VECTOR ( 'NONE', #50361, 39.37007874015748143 ) ;
#39214=CARTESIAN_POINT ( 'NONE',  ( 1.485598995959308333, -1.845608808797952187E-16, 1.625606721701626345 ) ) ;
#39215=CARTESIAN_POINT ( 'NONE',  ( 0.08139965876239094178, 1.610780518492231694, 0.000000000000000000 ) ) ;
#39226=B_SPLINE_CURVE_WITH_KNOTS ( 'NONE', 3,
 ( #26008, #5877, #29113, #29885 ),
 .UNSPECIFIED., .F., .F.,
 ( 4, 4 ),
 ( 2.220043001603228065E-07, 0.002500468287160468196 ),
 .UNSPECIFIED. ) ;
#39227=AXIS2_PLACEMENT_3D ( 'NONE', #24817, #29454, #41083 ) ;
#39230=ORIENTED_EDGE ( 'NONE', *, *, #21845, .F. ) ;
#39232=VECTOR ( 'NONE', #12265, 39.37007874015748143 ) ;
#39233=ORIENTED_EDGE ( 'NONE', *, *, #39839, .T. ) ;
#39235=CARTESIAN_POINT ( 'NONE',  ( 0.002207914879453961969, 6.692913385826772199, 0.04916304461325451958 ) ) ;
#39240=ORIENTED_EDGE ( 'NONE', *, *, #25009, .F. ) ;
#39248=CARTESIAN_POINT ( 'NONE',  ( -2.952069331832154919, 5.118110236220475784, 1.181102362204724310 ) ) ;
#39249=EDGE_CURVE ( 'NONE', #28752, #28376, #36404, .T. ) ;
#39251=ORIENTED_EDGE ( 'NONE', *, *, #23139, .T. ) ;
#39253=ORIENTED_EDGE ( 'NONE', *, *, #32920, .T. ) ;
#39255=SHAPE_DEFINITION_REPRESENTATION ( #42939, #8330 ) ;
#39262=ORIENTED_EDGE ( 'NONE', *, *, #47556, .F. ) ;
#39265=FACE_OUTER_BOUND ( 'NONE', #50538, .T. ) ;
#39267=CARTESIAN_POINT ( 'NONE',  ( -2.951990591674674480, 1.673246673531018525, -0.08331184815402598032 ) ) ;
#39269=CARTESIAN_POINT ( 'NONE',  ( 2.889674983507178219, 1.665813060096536402, -0.6090712660037608250 ) ) ;
#39272=CARTESIAN_POINT ( 'NONE',  ( -1.528548437492483814, 1.596993453424210063, 2.526376101412316721 ) ) ;
#39273=VECTOR ( 'NONE', #30326, 39.37007874015748143 ) ;
#39276=CARTESIAN_POINT ( 'NONE',  ( 1.357666866036842945, 1.736795568944660362, 2.368301409647881162 ) ) ;
#39278=VECTOR ( 'NONE', #36467, 39.37007874015748854 ) ;
#39280=CARTESIAN_POINT ( 'NONE',  ( 0.1067246931122726866, 0.02962905676920215767, 0.000000000000000000 ) ) ;
#39284=ORIENTED_EDGE ( 'NONE', *, *, #36399, .T. ) ;
#39286=DIRECTION ( 'NONE',  ( -0.3513748240813305279, 0.000000000000000000, -0.9362348706397418674 ) ) ;
#39287=CARTESIAN_POINT ( 'NONE',  ( 1.528548638510035307, 1.743074481295564082, 2.526375981309921581 ) ) ;
#39289=B_SPLINE_CURVE_WITH_KNOTS ( 'NONE', 3,
 ( #15802, #3687, #33049, #48729 ),
 .UNSPECIFIED., .F., .F.,
 ( 4, 4 ),
 ( 0.0001991432653589252772, 0.002699267682809819522 ),
 .UNSPECIFIED. ) ;
#39292=PLANE ( 'NONE',  #49298 ) ;
#39294=DIRECTION ( 'NONE',  ( 8.741157232058247392E-17, -1.000000000000000000, -7.636919086868415696E-17 ) ) ;
#39301=VERTEX_POINT ( 'NONE', #13327 ) ;
#39302=ORIENTED_EDGE ( 'NONE', *, *, #39340, .T. ) ;
#39306=DIRECTION ( 'NONE',  ( -0.000000000000000000, -1.000000000000000000, -0.000000000000000000 ) ) ;
#39314=CARTESIAN_POINT ( 'NONE',  ( 2.919426793319799707, 2.755905511811027164, 0.4451252810446823527 ) ) ;
#39319=EDGE_CURVE ( 'NONE', #17488, #22117, #20735, .T. ) ;
#39321=DIRECTION ( 'NONE',  ( -0.9998717552508121775, -0.01601477604151182316, 0.000000000000000000 ) ) ;
#39322=DIRECTION ( 'NONE',  ( 0.000000000000000000, 0.000000000000000000, -1.000000000000000000 ) ) ;
#39327=ORIENTED_EDGE ( 'NONE', *, *, #29572, .F. ) ;
#39329=DIRECTION ( 'NONE',  ( -0.4338837391175526803, 0.000000000000000000, -0.9009688679024218105 ) ) ;
#39331=CARTESIAN_POINT ( 'NONE',  ( 0.07982360342473591996, 1.709180471932028711, 0.000000000000000000 ) ) ;
#39332=CARTESIAN_POINT ( 'NONE',  ( 0.5484938309455573702, 0.5249316497054296038, -1.802438616747610745 ) ) ;
#39333=ORIENTED_EDGE ( 'NONE', *, *, #42965, .F. ) ;
#39335=VERTEX_POINT ( 'NONE', #6602 ) ;
#39336=CARTESIAN_POINT ( 'NONE',  ( 2.950518648759354434, 1.765226948982748123, -0.1160872037111668892 ) ) ;
#39337=DIRECTION ( 'NONE',  ( 0.3513748240813434620, 0.000000000000000000, -0.9362348706397368714 ) ) ;
#39339=AXIS2_PLACEMENT_3D ( 'NONE', #10472, #49161, #1705 ) ;
#39340=EDGE_CURVE ( 'NONE', #42191, #44778, #2161, .T. ) ;
#39342=FACE_OUTER_BOUND ( 'NONE', #45003, .T. ) ;
#39343=CONICAL_SURFACE ( 'NONE', #17097, 2.244934639244524632, 1.554780866114618743 ) ;
#39352=FACE_OUTER_BOUND ( 'NONE', #28168, .T. ) ;
#39360=B_SPLINE_CURVE_WITH_KNOTS ( 'NONE', 3,
 ( #5036, #20782, #36541, #16918 ),
 .UNSPECIFIED., .F., .F.,
 ( 4, 4 ),
 ( 0.03514866506299903909, 0.03730642777952080519 ),
 .UNSPECIFIED. ) ;
#39363=DIRECTION ( 'NONE',  ( -0.3513748240813434620, -1.086579671787963332E-16, 0.9362348706397368714 ) ) ;
#39368=ORIENTED_EDGE ( 'NONE', *, *, #5595, .F. ) ;
#39370=LINE ( 'NONE', #4254, #18856 ) ;
#39371=B_SPLINE_CURVE_WITH_KNOTS ( 'NONE', 3,
 ( #15217, #18085, #2841, #18595 ),
 .UNSPECIFIED., .F., .F.,
 ( 4, 4 ),
 ( 0.01297872134738276700, 0.03074049562890820986 ),
 .UNSPECIFIED. ) ;
#39377=EDGE_CURVE ( 'NONE', #22056, #48706, #50408, .T. ) ;
#39382=AXIS2_PLACEMENT_3D ( 'NONE', #26657, #18417, #14035 ) ;
#39383=CONICAL_SURFACE ( 'NONE', #17129, 3.483074324928249421, 1.244861948955335196 ) ;
#39390=ORIENTED_EDGE ( 'NONE', *, *, #21188, .F. ) ;
#39393=CARTESIAN_POINT ( 'NONE',  ( -0.5354483489059734813, 0.01294997333450623005, -1.755169374176263730 ) ) ;
#39399=CONICAL_SURFACE ( 'NONE', #35274, 2.165354330708661568, 0.2617993877991570129 ) ;
#39402=CARTESIAN_POINT ( 'NONE',  ( 1.661821349926414282, 6.692913385826772199, 1.388203579611976712 ) ) ;
#39411=CARTESIAN_POINT ( 'NONE',  ( 0.000000000000000000, 1.574803149606302854, -2.165354330708661568 ) ) ;
#39414=ORIENTED_EDGE ( 'NONE', *, *, #6780, .T. ) ;
#39417=CARTESIAN_POINT ( 'NONE',  ( 2.258212185701618857, 1.750938538929015076, -1.549600192960912004 ) ) ;
#39419=DIRECTION ( 'NONE',  ( -0.7818314824680221431, 0.000000000000000000, -0.6234898018587431423 ) ) ;
#39424=CARTESIAN_POINT ( 'NONE',  ( 0.1067246931122726866, 0.02962905676920215767, 0.000000000000000000 ) ) ;
#39426=CARTESIAN_POINT ( 'NONE',  ( -2.952069331832154919, 5.118110236220475784, 1.181102362204724310 ) ) ;
#39436=AXIS2_PLACEMENT_3D ( 'NONE', #41016, #29124, #36628 ) ;
#39445=ORIENTED_EDGE ( 'NONE', *, *, #1533, .T. ) ;
#39450=CARTESIAN_POINT ( 'NONE',  ( 2.168245791271197209, 1.466194936398640181, -2.004968704497248400 ) ) ;
#39451=ORIENTED_EDGE ( 'NONE', *, *, #2847, .T. ) ;
#39453=CARTESIAN_POINT ( 'NONE',  ( 2.803166786255866239, 1.450263284045836709, 0.9280585611840251881 ) ) ;
#39454=CARTESIAN_POINT ( 'NONE',  ( -0.2906532981117672110, 1.205361022782829114E-17, 1.877244666688175245 ) ) ;
#39456=AXIS2_PLACEMENT_3D ( 'NONE', #11609, #15731, #46937 ) ;
#39458=VERTEX_POINT ( 'NONE', #27973 ) ;
#39459=FACE_OUTER_BOUND ( 'NONE', #16324, .T. ) ;
#39460=DIRECTION ( 'NONE',  ( -0.01601477604151182663, 0.9998717552508123996, -0.000000000000000000 ) ) ;
#39461=VECTOR ( 'NONE', #28008, 39.37007874015748143 ) ;
#39464=CIRCLE ( 'NONE', #28783, 2.246510896728926010 ) ;
#39467=CARTESIAN_POINT ( 'NONE',  ( 0.5433595661824232037, 1.502645338999371249, 2.902377712497140827 ) ) ;
#39469=B_SPLINE_CURVE_WITH_KNOTS ( 'NONE', 3,
 ( #32957, #13318, #29051, #21320 ),
 .UNSPECIFIED., .F., .F.,
 ( 4, 4 ),
 ( 6.049486680839438895E-07, 0.0005306152659298648405 ),
 .UNSPECIFIED. ) ;
#39472=DIRECTION ( 'NONE',  ( -0.9510565162951500895, 0.000000000000000000, -0.3090169943749582204 ) ) ;
#39474=DIRECTION ( 'NONE',  ( -3.986037398843765983E-20, -1.000000000000000000, -1.160734090543304660E-16 ) ) ;
#39481=EDGE_LOOP ( 'NONE', ( #42947, #34755, #37522, #49123 ) ) ;
#39482=EDGE_CURVE ( 'NONE', #4093, #39165, #8365, .T. ) ;
#39485=CONICAL_SURFACE ( 'NONE', #12296, 3.033577403570480779, 1.554780866114618743 ) ;
#39486=ORIENTED_EDGE ( 'NONE', *, *, #25084, .T. ) ;
#39491=AXIS2_PLACEMENT_3D ( 'NONE', #10374, #1858, #49055 ) ;
#39493=DIRECTION ( 'NONE',  ( 0.01601477604151182663, -0.9998717552508123996, 0.000000000000000000 ) ) ;
#39496=VECTOR ( 'NONE', #19225, 39.37007874015748143 ) ;
#39498=CARTESIAN_POINT ( 'NONE',  ( 0.04921259842519667277, 1.720031199985617265, 2.952755905511811108 ) ) ;
#39499=ORIENTED_EDGE ( 'NONE', *, *, #25364, .T. ) ;
#39503=CARTESIAN_POINT ( 'NONE',  ( -1.843283979527560623, 1.678378384481335139, -1.157773721536293765 ) ) ;
#39504=CARTESIAN_POINT ( 'NONE',  ( 0.000000000000000000, 0.000000000000000000, 0.000000000000000000 ) ) ;
#39514=B_SPLINE_CURVE_WITH_KNOTS ( 'NONE', 3,
 ( #35486, #4755, #32132, #4499 ),
 .UNSPECIFIED., .F., .F.,
 ( 4, 4 ),
 ( 0.0003353342934138906894, 0.04951278680019933348 ),
 .UNSPECIFIED. ) ;
#39515=ADVANCED_FACE ( 'NONE', ( #24369 ), #40118, .F. ) ;
#39518=CARTESIAN_POINT ( 'NONE',  ( 1.883550378546972937, 5.905511811023623991, -1.069467267250421072 ) ) ;
#39521=VERTEX_POINT ( 'NONE', #7856 ) ;
#39524=CARTESIAN_POINT ( 'NONE',  ( 0.07982360342473591996, 1.709180471932028711, 0.000000000000000000 ) ) ;
#39525=ORIENTED_EDGE ( 'NONE', *, *, #50499, .T. ) ;
#39526=CARTESIAN_POINT ( 'NONE',  ( 2.889674983507178219, 1.764288196056212454, -0.6090712660037608250 ) ) ;
#39530=CARTESIAN_POINT ( 'NONE',  ( 2.755905511811024056, 2.913385826771657250, 1.023622047244094446 ) ) ;
#39533=CARTESIAN_POINT ( 'NONE',  ( 2.074049943651431693, 6.692913385826772199, 0.6221544894624241318 ) ) ;
#39535=EDGE_CURVE ( 'NONE', #26405, #4443, #32315, .T. ) ;
#39542=DIRECTION ( 'NONE',  ( 0.000000000000000000, 0.000000000000000000, -1.000000000000000000 ) ) ;
#39545=EDGE_CURVE ( 'NONE', #16076, #31910, #5110, .T. ) ;
#39546=EDGE_LOOP ( 'NONE', ( #14710, #28569, #14883, #49771, #9656, #35068, #3903, #44527, #41434, #41566, #13266 ) ) ;
#39547=CARTESIAN_POINT ( 'NONE',  ( 0.5567409167160404238, 0.02445386360714798396, -1.832321260915883210 ) ) ;
#39549=DIRECTION ( 'NONE',  ( 0.000000000000000000, 1.160734090543304660E-16, -1.000000000000000000 ) ) ;
#39550=VERTEX_POINT ( 'NONE', #32380 ) ;
#39552=CARTESIAN_POINT ( 'NONE',  ( 0.7381027496705272473, 1.730766751998747521, -2.859439394060913298 ) ) ;
#39554=EDGE_CURVE ( 'NONE', #17224, #45778, #43459, .T. ) ;
#39556=B_SPLINE_CURVE_WITH_KNOTS ( 'NONE', 3,
 ( #4501, #47571, #32389, #48082 ),
 .UNSPECIFIED., .F., .F.,
 ( 4, 4 ),
 ( 0.01260738023649243464, 0.03073908182205475209 ),
 .UNSPECIFIED. ) ;
#39563=VERTEX_POINT ( 'NONE', #24626 ) ;
#39564=EDGE_CURVE ( 'NONE', #38926, #14656, #5167, .T. ) ;
#39565=CARTESIAN_POINT ( 'NONE',  ( -1.882988517681399188, 6.692913385826772199, 1.069164917025788863 ) ) ;
#39568=CONICAL_SURFACE ( 'NONE', #21450, 2.244934639244524632, 1.554780866114618743 ) ;
#39577=FACE_OUTER_BOUND ( 'NONE', #1079, .T. ) ;
#39579=ORIENTED_EDGE ( 'NONE', *, *, #35425, .F. ) ;
#39580=CARTESIAN_POINT ( 'NONE',  ( 0.07982360342473591996, 1.709180471932028711, 0.000000000000000000 ) ) ;
#39584=DIRECTION ( 'NONE',  ( -1.105928667600727183E-16, 1.000000000000000000, 6.607616187506045307E-17 ) ) ;
#39586=ADVANCED_FACE ( 'NONE', ( #3986 ), #23853, .F. ) ;
#39589=CARTESIAN_POINT ( 'NONE',  ( 0.5110594979943910987, 0.000000000000000000, -1.666798357583575418 ) ) ;
#39593=ORIENTED_EDGE ( 'NONE', *, *, #16845, .T. ) ;
#39595=FACE_OUTER_BOUND ( 'NONE', #7092, .T. ) ;
#39599=ORIENTED_EDGE ( 'NONE', *, *, #24436, .T. ) ;
#39607=CARTESIAN_POINT ( 'NONE',  ( 2.867773316779195447, 1.763947033723992641, -0.7050287376752004675 ) ) ;
#39608=CARTESIAN_POINT ( 'NONE',  ( 2.919426793319799707, 1.764751637901927905, 0.4451252810446822417 ) ) ;
#39612=EDGE_CURVE ( 'NONE', #25030, #16032, #13009, .T. ) ;
#39617=DIRECTION ( 'NONE',  ( 0.000000000000000000, 0.000000000000000000, -1.000000000000000000 ) ) ;
#39625=CARTESIAN_POINT ( 'NONE',  ( -1.843472447131334624, 1.579950168977349412, -1.157898127912315944 ) ) ;
#39632=ORIENTED_EDGE ( 'NONE', *, *, #44479, .F. ) ;
#39633=VERTEX_POINT ( 'NONE', #20744 ) ;
#39635=LINE ( 'NONE', #12274, #29884 ) ;
#39641=CARTESIAN_POINT ( 'NONE',  ( 2.734482843737263025, 1.761870738172414796, -1.115254632218672493 ) ) ;
#39642=ORIENTED_EDGE ( 'NONE', *, *, #32727, .F. ) ;
#39643=ORIENTED_EDGE ( 'NONE', *, *, #31398, .F. ) ;
#39651=ORIENTED_EDGE ( 'NONE', *, *, #1965, .T. ) ;
#39652=LINE ( 'NONE', #47097, #23613 ) ;
#39655=CONICAL_SURFACE ( 'NONE', #62, 2.244934639244524632, 1.554780866114618743 ) ;
#39656=CARTESIAN_POINT ( 'NONE',  ( -1.068075307999487578, 1.574803149606302854, 1.883606783264637485 ) ) ;
#39657=CARTESIAN_POINT ( 'NONE',  ( 0.002207914879453961969, 6.692913385826772199, 0.04916304461325451958 ) ) ;
#39658=DIRECTION ( 'NONE',  ( 0.9998717552508121775, 0.01601477604151182663, 0.000000000000000000 ) ) ;
#39665=DIRECTION ( 'NONE',  ( -0.000000000000000000, 1.000000000000000000, -0.000000000000000000 ) ) ;
#39667=ORIENTED_EDGE ( 'NONE', *, *, #18228, .T. ) ;
#39672=CARTESIAN_POINT ( 'NONE',  ( 2.867773316779195447, 1.449472587384593725, -0.7050287376752005786 ) ) ;
#39683=DIRECTION ( 'NONE',  ( -0.9998717552508122886, -0.01601477604151180928, 0.000000000000000000 ) ) ;
#39685=VERTEX_POINT ( 'NONE', #36502 ) ;
#39688=CARTESIAN_POINT ( 'NONE',  ( 1.319349709118413205, 0.000000000000000000, 1.584915398547334764 ) ) ;
#39690=CARTESIAN_POINT ( 'NONE',  ( 0.7381027496705270252, 1.632310643118564997, -2.859439394060913298 ) ) ;
#39692=CARTESIAN_POINT ( 'NONE',  ( 0.2430652128771959297, 1.574803149606302854, -2.151668812760857641 ) ) ;
#39695=AXIS2_PLACEMENT_3D ( 'NONE', #37654, #9513, #25257 ) ;
#39698=CARTESIAN_POINT ( 'NONE',  ( 2.100227814008711835, 1.653522055412836700, -2.076109931251913565 ) ) ;
#39699=ORIENTED_EDGE ( 'NONE', *, *, #39319, .F. ) ;
#39702=B_SPLINE_CURVE_WITH_KNOTS ( 'NONE', 3,
 ( #44860, #16756, #5383, #48205 ),
 .UNSPECIFIED., .F., .F.,
 ( 4, 4 ),
 ( 2.220059668071660630E-07, 0.002500468552710426520 ),
 .UNSPECIFIED. ) ;
#39704=EDGE_CURVE ( 'NONE', #6926, #26859, #43919, .T. ) ;
#39705=EDGE_CURVE ( 'NONE', #2996, #30054, #17384, .T. ) ;
#39707=VERTEX_POINT ( 'NONE', #29517 ) ;
#39710=CARTESIAN_POINT ( 'NONE',  ( 2.066011418817629952, 0.01968689263637172018, 0.2301982101820274906 ) ) ;
#39727=DIRECTION ( 'NONE',  ( -5.207613805428889878E-18, -1.000000000000000000, 1.159565308550899675E-16 ) ) ;
#39729=AXIS2_PLACEMENT_3D ( 'NONE', #31804, #11660, #31545 ) ;
#39733=CARTESIAN_POINT ( 'NONE',  ( -1.695772546416001836, 1.594396608463251486, -2.417756147381374010 ) ) ;
#39736=LINE ( 'NONE', #27338, #45675 ) ;
#39738=B_SPLINE_CURVE_WITH_KNOTS ( 'NONE', 3,
 ( #30653, #7414, #6903, #18529 ),
 .UNSPECIFIED., .F., .F.,
 ( 4, 4 ),
 ( 8.019549856696441979E-05, 0.0001436088897228033647 ),
 .UNSPECIFIED. ) ;
#39740=CARTESIAN_POINT ( 'NONE',  ( 0.5465852118371267165, 0.5227683204652883164, -2.165491180797212589 ) ) ;
#39741=CARTESIAN_POINT ( 'NONE',  ( -1.514466370293032549, 5.905511811023623991, 2.534789744887398388 ) ) ;
#39743=ORIENTED_EDGE ( 'NONE', *, *, #4490, .F. ) ;
#39744=CARTESIAN_POINT ( 'NONE',  ( -1.977278193622379332, 1.577807025067274882, -0.8986486843887250275 ) ) ;
#39746=DIRECTION ( 'NONE',  ( -0.000000000000000000, 1.000000000000000000, -0.000000000000000000 ) ) ;
#39747=VERTEX_POINT ( 'NONE', #6279 ) ;
#39750=AXIS2_PLACEMENT_3D ( 'NONE', #7510, #19622, #27622 ) ;
#39751=VECTOR ( 'NONE', #9798, 39.37007874015748143 ) ;
#39752=CARTESIAN_POINT ( 'NONE',  ( 1.929629134066521701, 6.692913385826772199, 0.9824921284572420976 ) ) ;
#39753=ORIENTED_EDGE ( 'NONE', *, *, #31071, .T. ) ;
#39754=EDGE_LOOP ( 'NONE', ( #15191, #48528, #8004, #43885 ) ) ;
#39759=ORIENTED_EDGE ( 'NONE', *, *, #4123, .T. ) ;
#39760=DIRECTION ( 'NONE',  ( 0.9998717552508121775, 0.01601477604151182663, 0.000000000000000000 ) ) ;
#39761=CARTESIAN_POINT ( 'NONE',  ( 2.600183657057279607, 5.905511811023623991, 1.399218491554162336 ) ) ;
#39762=VERTEX_POINT ( 'NONE', #10405 ) ;
#39770=DIRECTION ( 'NONE',  ( 0.9510565162951500895, 0.000000000000000000, 0.3090169943749582204 ) ) ;
#39771=CARTESIAN_POINT ( 'NONE',  ( 0.8013550346897827525, 1.731743580627177925, -2.841982872583248998 ) ) ;
#39772=B_SPLINE_CURVE_WITH_KNOTS ( 'NONE', 3,
 ( #37898, #2519, #46606, #30134 ),
 .UNSPECIFIED., .F., .F.,
 ( 4, 4 ),
 ( 0.01111952476426258593, 0.03073605569767426729 ),
 .UNSPECIFIED. ) ;
#39775=ORIENTED_EDGE ( 'NONE', *, *, #37803, .T. ) ;
#39777=CARTESIAN_POINT ( 'NONE',  ( -2.084291548511494785, 5.905511811023623991, 0.6254821886024592992 ) ) ;
#39783=VECTOR ( 'NONE', #40024, 39.37007874015748143 ) ;
#39785=LINE ( 'NONE', #20416, #42447 ) ;
#39797=LINE ( 'NONE', #8042, #43871 ) ;
#39799=CARTESIAN_POINT ( 'NONE',  ( 2.121469926805689354, 1.574803149606302854, -0.4337334748181394528 ) ) ;
#39800=ORIENTED_EDGE ( 'NONE', *, *, #25290, .T. ) ;
#39806=DIRECTION ( 'NONE',  ( 0.000000000000000000, 0.000000000000000000, -1.000000000000000000 ) ) ;
#39807=CARTESIAN_POINT ( 'NONE',  ( 0.1450362469327826365, 1.574803149606302854, -2.160491579385212191 ) ) ;
#39811=ORIENTED_EDGE ( 'NONE', *, *, #33757, .F. ) ;
#39812=PLANE ( 'NONE',  #14993 ) ;
#39820=CARTESIAN_POINT ( 'NONE',  ( 0.002207914879453961535, -5.712274067634378313E-18, 0.04916304461325374242 ) ) ;
#39822=CARTESIAN_POINT ( 'NONE',  ( -0.1450934409768894484, 5.905511811023623991, 2.161127057262024920 ) ) ;
#39824=DIRECTION ( 'NONE',  ( 0.000000000000000000, 0.000000000000000000, -1.000000000000000000 ) ) ;
#39825=VECTOR ( 'NONE', #11445, 39.37007874015748143 ) ;
#39826=CARTESIAN_POINT ( 'NONE',  ( -0.7514907335614920969, 0.005366325807348728584, -1.673910055625482451 ) ) ;
#39829=EDGE_CURVE ( 'NONE', #33976, #3507, #8822, .T. ) ;
#39831=ORIENTED_EDGE ( 'NONE', *, *, #14475, .F. ) ;
#39835=ADVANCED_FACE ( 'NONE', ( #10905 ), #33987, .T. ) ;
#39838=DIRECTION ( 'NONE',  ( 1.241861098869884156E-16, 1.000000000000000000, 3.427318860986280993E-17 ) ) ;
#39839=EDGE_CURVE ( 'NONE', #36136, #47107, #34709, .T. ) ;
#39840=CARTESIAN_POINT ( 'NONE',  ( 0.3546377434558362074, 1.615156926475952881, 2.229828021450985798 ) ) ;
#39844=ORIENTED_EDGE ( 'NONE', *, *, #2535, .T. ) ;
#39851=DIRECTION ( 'NONE',  ( -0.1342332658176667304, -1.160734090543304907E-16, 0.9909497617679332571 ) ) ;
#39853=VERTEX_POINT ( 'NONE', #49001 ) ;
#39854=DIRECTION ( 'NONE',  ( -0.000000000000000000, -1.000000000000000000, -0.000000000000000000 ) ) ;
#39858=DIRECTION ( 'NONE',  ( -0.000000000000000000, 1.000000000000000000, -0.000000000000000000 ) ) ;
#39863=CARTESIAN_POINT ( 'NONE',  ( 0.000000000000000000, 1.574803149606302854, 0.000000000000000000 ) ) ;
#39864=CARTESIAN_POINT ( 'NONE',  ( 2.298322628623565400, 1.462353850267382738, 1.853847351054373371 ) ) ;
#39865=CARTESIAN_POINT ( 'NONE',  ( -2.688839661887661325, 1.574817859957791999, -0.07149372627020672555 ) ) ;
#39877=CARTESIAN_POINT ( 'NONE',  ( -1.675546303352015709, 1.681065010344670041, 1.399148864732502995 ) ) ;
#39887=FACE_OUTER_BOUND ( 'NONE', #36227, .T. ) ;
#39888=DIRECTION ( 'NONE',  ( -0.01601477604151182663, 0.9998717552508123996, -0.000000000000000000 ) ) ;
#39890=ORIENTED_EDGE ( 'NONE', *, *, #2655, .F. ) ;
#39891=DIRECTION ( 'NONE',  ( -1.729310098865080642E-17, 1.000000000000000000, 1.276627980444840260E-16 ) ) ;
#39894=FACE_OUTER_BOUND ( 'NONE', #17317, .T. ) ;
#39896=ORIENTED_EDGE ( 'NONE', *, *, #32335, .F. ) ;
#39897=CARTESIAN_POINT ( 'NONE',  ( 1.771435203777392386, 1.736274727556916808, 1.475617711110977615 ) ) ;
#39898=ORIENTED_EDGE ( 'NONE', *, *, #18195, .T. ) ;
#39900=CARTESIAN_POINT ( 'NONE',  ( 2.491402175429654253, 1.758084086496218612, -1.585592796919505609 ) ) ;
#39901=ADVANCED_FACE ( 'NONE', ( #20915 ), #28906, .T. ) ;
#39903=ORIENTED_EDGE ( 'NONE', *, *, #45021, .F. ) ;
#39906=EDGE_CURVE ( 'NONE', #12681, #18049, #32244, .T. ) ;
#39907=VERTEX_POINT ( 'NONE', #13179 ) ;
#39909=VECTOR ( 'NONE', #37196, 39.37007874015748143 ) ;
#39912=CARTESIAN_POINT ( 'NONE',  ( 0.8013550346330908791, 1.633286922350572379, -2.841982872598894705 ) ) ;
#39913=CARTESIAN_POINT ( 'NONE',  ( -0.4433489891367859981, 5.905511811023623991, 2.167441310503416041 ) ) ;
#39914=VECTOR ( 'NONE', #22306, 39.37007874015748143 ) ;
#39917=LINE ( 'NONE', #43519, #37715 ) ;
#39919=VECTOR ( 'NONE', #6722, 39.37007874015748143 ) ;
#39926=DIRECTION ( 'NONE',  ( 0.000000000000000000, 1.000000000000000000, 0.000000000000000000 ) ) ;
#39929=EDGE_CURVE ( 'NONE', #47107, #20029, #21686, .T. ) ;
#39930=DIRECTION ( 'NONE',  ( 0.000000000000000000, 0.000000000000000000, 1.000000000000000000 ) ) ;
#39932=VERTEX_POINT ( 'NONE', #2063 ) ;
#39933=ORIENTED_EDGE ( 'NONE', *, *, #21921, .T. ) ;
#39938=DIRECTION ( 'NONE',  ( -0.6910626489868685329, 1.288287287306305776E-16, 0.7227948638273880011 ) ) ;
#39939=EDGE_CURVE ( 'NONE', #18246, #27191, #41068, .T. ) ;
#39940=B_SPLINE_CURVE_WITH_KNOTS ( 'NONE', 3,
 ( #44375, #48722, #29137, #36906 ),
 .UNSPECIFIED., .F., .F.,
 ( 4, 4 ),
 ( 2.220417365849702369E-07, 0.01713232808254949724 ),
 .UNSPECIFIED. ) ;
#39945=CARTESIAN_POINT ( 'NONE',  ( 1.223349603905365068, 0.04751384826852676074, 1.475034436811822669 ) ) ;
#39946=ORIENTED_EDGE ( 'NONE', *, *, #2313, .F. ) ;
#39948=AXIS2_PLACEMENT_3D ( 'NONE', #9973, #38113, #10484 ) ;
#39952=AXIS2_PLACEMENT_3D ( 'NONE', #1256, #1762, #28616 ) ;
#39956=CARTESIAN_POINT ( 'NONE',  ( 2.932638728931774352, 1.447899366913586672, 0.3475908556738225297 ) ) ;
#39957=CONICAL_SURFACE ( 'NONE', #17705, 2.165354330708661568, 0.2617993877991570129 ) ;
#39961=EDGE_CURVE ( 'NONE', #19788, #25553, #46800, .T. ) ;
#39966=EDGE_CURVE ( 'NONE', #18328, #37294, #30335, .T. ) ;
#39971=DIRECTION ( 'NONE',  ( -0.01601477604151182663, 0.9998717552508123996, -0.000000000000000000 ) ) ;
#39972=VERTEX_POINT ( 'NONE', #11077 ) ;
#39975=LINE ( 'NONE', #4606, #34636 ) ;
#39978=CARTESIAN_POINT ( 'NONE',  ( 0.000000000000000000, 0.000000000000000000, 0.000000000000000000 ) ) ;
#39982=CARTESIAN_POINT ( 'NONE',  ( 0.8069532150559727279, 5.905511811023623991, -2.010061882867130834 ) ) ;
#39985=DIRECTION ( 'NONE',  ( -0.000000000000000000, 1.000000000000000000, -0.000000000000000000 ) ) ;
#39986=ORIENTED_EDGE ( 'NONE', *, *, #26950, .T. ) ;
#39989=AXIS2_PLACEMENT_3D ( 'NONE', #42868, #15760, #46963 ) ;
#39993=ADVANCED_FACE ( 'NONE', ( #50758 ), #2570, .T. ) ;
#39999=ORIENTED_EDGE ( 'NONE', *, *, #1851, .F. ) ;
#40000=EDGE_CURVE ( 'NONE', #32953, #36796, #3131, .T. ) ;
#40001=CARTESIAN_POINT ( 'NONE',  ( -2.153807523435208093, -5.072058324879254713E-17, 0.2420910006175685525 ) ) ;
#40017=EDGE_CURVE ( 'NONE', #17176, #30581, #12582, .T. ) ;
#40018=CIRCLE ( 'NONE', #46585, 2.246510896728926010 ) ;
#40021=DIRECTION ( 'NONE',  ( -6.394449067488625930E-17, -1.000000000000000000, 9.687176266499597757E-17 ) ) ;
#40024=DIRECTION ( 'NONE',  ( 0.000000000000000000, -1.000000000000000000, -0.000000000000000000 ) ) ;
#40026=EDGE_CURVE ( 'NONE', #49387, #42296, #3077, .T. ) ;
#40027=ORIENTED_EDGE ( 'NONE', *, *, #730, .T. ) ;
#40028=VERTEX_POINT ( 'NONE', #3580 ) ;
#40031=DIRECTION ( 'NONE',  ( 0.000000000000000000, 0.000000000000000000, 1.000000000000000000 ) ) ;
#40034=CYLINDRICAL_SURFACE ( 'NONE', #23871, 2.165354330708661568 ) ;
#40036=ORIENTED_EDGE ( 'NONE', *, *, #43911, .T. ) ;
#40044=PLANE ( 'NONE',  #37627 ) ;
#40046=STYLED_ITEM('',(#51080),#23876);
#40049=VECTOR ( 'NONE', #25205, 39.37007874015748143 ) ;
#40051=AXIS2_PLACEMENT_3D ( 'NONE', #47587, #36023, #8135 ) ;
#40054=DIRECTION ( 'NONE',  ( -0.9362348706397417564, 0.000000000000000000, 0.3513748240813304724 ) ) ;
#40055=DIRECTION ( 'NONE',  ( -0.000000000000000000, 1.000000000000000000, -0.000000000000000000 ) ) ;
#40061=EDGE_CURVE ( 'NONE', #50100, #22884, #10573, .T. ) ;
#40064=ORIENTED_EDGE ( 'NONE', *, *, #21321, .F. ) ;
#40071=ORIENTED_EDGE ( 'NONE', *, *, #44896, .T. ) ;
#40073=CARTESIAN_POINT ( 'NONE',  ( 0.9542980589831819849, 0.02856680792132131746, 1.693175744540320604 ) ) ;
#40074=ORIENTED_EDGE ( 'NONE', *, *, #14285, .T. ) ;
#40075=ORIENTED_EDGE ( 'NONE', *, *, #22351, .F. ) ;
#40076=CARTESIAN_POINT ( 'NONE',  ( -1.557927422371237158, 0.000000000000000000, 0.7824709080581183640 ) ) ;
#40078=LINE ( 'NONE', #12201, #39278 ) ;
#40080=ORIENTED_EDGE ( 'NONE', *, *, #35696, .F. ) ;
#40081=ADVANCED_FACE ( 'NONE', ( #30951 ), #13868, .T. ) ;
#40084=CARTESIAN_POINT ( 'NONE',  ( 0.000000000000000000, 0.000000000000000000, 0.000000000000000000 ) ) ;
#40085=VECTOR ( 'NONE', #13257, 39.37007874015748143 ) ;
#40089=CIRCLE ( 'NONE', #6302, 1.850107469027523432 ) ;
#40091=CONICAL_SURFACE ( 'NONE', #46651, 3.483074324928249421, 1.244861948955335196 ) ;
#40092=EDGE_CURVE ( 'NONE', #48279, #46197, #35890, .T. ) ;
#40093=CARTESIAN_POINT ( 'NONE',  ( 2.951990591674675368, 5.118110236220475784, -0.08331184815398323673 ) ) ;
#40095=ORIENTED_EDGE ( 'NONE', *, *, #31170, .F. ) ;
#40096=LINE ( 'NONE', #44211, #44391 ) ;
#40102=FACE_OUTER_BOUND ( 'NONE', #44128, .T. ) ;
#40103=CARTESIAN_POINT ( 'NONE',  ( 2.823445274216730638, 1.664781993127344872, 0.8656477926280681245 ) ) ;
#40104=VERTEX_POINT ( 'NONE', #39454 ) ;
#40109=ORIENTED_EDGE ( 'NONE', *, *, #43479, .T. ) ;
#40112=B_SPLINE_CURVE_WITH_KNOTS ( 'NONE', 3,
 ( #108, #19472, #16640, #23864 ),
 .UNSPECIFIED., .F., .F.,
 ( 4, 4 ),
 ( 2.271941954864058199E-07, 0.002500388579452512972 ),
 .UNSPECIFIED. ) ;
#40116=ORIENTED_EDGE ( 'NONE', *, *, #8777, .T. ) ;
#40117=DIRECTION ( 'NONE',  ( 0.000000000000000000, -1.000000000000000000, 0.000000000000000000 ) ) ;
#40118=PLANE ( 'NONE',  #43824 ) ;
#40120=CYLINDRICAL_SURFACE ( 'NONE', #6750, 2.164630168518208109 ) ;
#40125=CARTESIAN_POINT ( 'NONE',  ( -1.735196932040237394, 1.680109596358665636, 1.320828101803479315 ) ) ;
#40130=EDGE_CURVE ( 'NONE', #1426, #41559, #19565, .T. ) ;
#40141=CARTESIAN_POINT ( 'NONE',  ( -0.8919566823238733733, 0.004617306369309737146, 1.588833855319179200 ) ) ;
#40143=EDGE_CURVE ( 'NONE', #35414, #13810, #24826, .T. ) ;
#40144=B_SPLINE_CURVE_WITH_KNOTS ( 'NONE', 3,
 ( #30520, #37515, #2641, #14772 ),
 .UNSPECIFIED., .F., .F.,
 ( 4, 4 ),
 ( 0.0005826651466654904138, 0.003082939193993071859 ),
 .UNSPECIFIED. ) ;
#40145=VECTOR ( 'NONE', #24396, 39.37007874015748143 ) ;
#40146=VERTEX_POINT ( 'NONE', #40936 ) ;
#40148=CARTESIAN_POINT ( 'NONE',  ( -2.793030215715272213, 1.573188339825353665, 0.9592557174602283077 ) ) ;
#40151=CARTESIAN_POINT ( 'NONE',  ( 1.695772546416037363, 1.745688802946234297, -2.417756147381349141 ) ) ;
#40153=CARTESIAN_POINT ( 'NONE',  ( 1.973323729629757217, 0.000000000000000000, -0.7899196136953162695 ) ) ;
#40156=ORIENTED_EDGE ( 'NONE', *, *, #28097, .F. ) ;
#40161=CARTESIAN_POINT ( 'NONE',  ( 0.1155636338427008941, -0.5222242541845523167, 0.000000000000000000 ) ) ;
#40163=ORIENTED_EDGE ( 'NONE', *, *, #3900, .F. ) ;
#40167=ORIENTED_EDGE ( 'NONE', *, *, #32645, .F. ) ;
#40168=PLANE ( 'NONE',  #23381 ) ;
#40176=EDGE_CURVE ( 'NONE', #36441, #45968, #8188, .T. ) ;
#40177=LINE ( 'NONE', #43254, #27693 ) ;
#40185=CYLINDRICAL_SURFACE ( 'NONE', #18607, 2.164630168518208109 ) ;
#40186=CARTESIAN_POINT ( 'NONE',  ( 1.940243258758003853, 1.049866565067838264, 0.5786780620529168306 ) ) ;
#40187=ORIENTED_EDGE ( 'NONE', *, *, #15654, .F. ) ;
#40189=B_SPLINE_CURVE_WITH_KNOTS ( 'NONE', 3,
 ( #18820, #6946, #30693, #7203 ),
 .UNSPECIFIED., .F., .F.,
 ( 4, 4 ),
 ( 0.1211775127643062860, 0.1625894504277921315 ),
 .UNSPECIFIED. ) ;
#40190=CARTESIAN_POINT ( 'NONE',  ( 1.228430781948798955, 1.636319860738493892, -2.437439334865536544 ) ) ;
#40195=EDGE_CURVE ( 'NONE', #9022, #32849, #43568, .T. ) ;
#40196=ORIENTED_EDGE ( 'NONE', *, *, #20263, .F. ) ;
#40198=B_SPLINE_CURVE_WITH_KNOTS ( 'NONE', 3,
 ( #29878, #25747, #37637, #45594 ),
 .UNSPECIFIED., .F., .F.,
 ( 4, 4 ),
 ( 0.0003817749841608031802, 0.002881981116852952267 ),
 .UNSPECIFIED. ) ;
#40203=CARTESIAN_POINT ( 'NONE',  ( -0.8244711865321519006, 0.01471425056033665718, -1.598608591632243892 ) ) ;
#40208=ORIENTED_EDGE ( 'NONE', *, *, #22092, .T. ) ;
#40209=VERTEX_POINT ( 'NONE', #16221 ) ;
#40212=CARTESIAN_POINT ( 'NONE',  ( -0.6982598466389058345, 0.000000000000000000, 1.720449438420079691 ) ) ;
#40216=ORIENTED_EDGE ( 'NONE', *, *, #29873, .F. ) ;
#40220=EDGE_CURVE ( 'NONE', #45649, #39707, #27825, .T. ) ;
#40222=ORIENTED_EDGE ( 'NONE', *, *, #12739, .T. ) ;
#40227=VERTEX_POINT ( 'NONE', #3838 ) ;
#40230=CARTESIAN_POINT ( 'NONE',  ( 2.875073879018141376, 1.764051760264652824, -0.6730428845924211201 ) ) ;
#40232=ORIENTED_EDGE ( 'NONE', *, *, #30471, .T. ) ;
#40233=CARTESIAN_POINT ( 'NONE',  ( -0.8067290215918264673, 1.574803149606302854, 2.009464521518170343 ) ) ;
#40235=AXIS2_PLACEMENT_3D ( 'NONE', #887, #48088, #37288 ) ;
#40239=CARTESIAN_POINT ( 'NONE',  ( -1.478009596860490715, 1.585803725363800210, 1.616919955472289727 ) ) ;
#40240=CARTESIAN_POINT ( 'NONE',  ( 1.952332965905436701, 0.01912591429768871476, 0.6860966224282102344 ) ) ;
#40243=ADVANCED_FACE ( 'NONE', ( #38706 ), #18799, .T. ) ;
#40246=EDGE_CURVE ( 'NONE', #24535, #36108, #35336, .T. ) ;
#40249=LINE ( 'NONE', #4875, #36706 ) ;
#40250=ORIENTED_EDGE ( 'NONE', *, *, #48564, .T. ) ;
#40254=CARTESIAN_POINT ( 'NONE',  ( 1.068402561569974818, 6.692913385826772199, -1.884154513482173776 ) ) ;
#40258=CARTESIAN_POINT ( 'NONE',  ( 0.000000000000000000, 0.000000000000000000, 0.000000000000000000 ) ) ;
#40259=CARTESIAN_POINT ( 'NONE',  ( 1.566178811999271892, 1.641618931010494498, -2.239385674323774555 ) ) ;
#40260=DIRECTION ( 'NONE',  ( 0.000000000000000000, 0.000000000000000000, -1.000000000000000000 ) ) ;
#40261=CARTESIAN_POINT ( 'NONE',  ( 2.889674983507178219, 1.448941827424379936, -0.6090712660037606030 ) ) ;
#40262=ORIENTED_EDGE ( 'NONE', *, *, #17394, .F. ) ;
#40266=VERTEX_POINT ( 'NONE', #34825 ) ;
#40269=DIRECTION ( 'NONE',  ( -0.9909497617679331460, 0.000000000000000000, -0.1342332658176667026 ) ) ;
#40271=AXIS2_PLACEMENT_3D ( 'NONE', #32209, #27802, #43548 ) ;
#40272=CARTESIAN_POINT ( 'NONE',  ( -2.150518151785907772, 1.673457466938482296, -0.2530435858860717313 ) ) ;
#40274=ORIENTED_EDGE ( 'NONE', *, *, #33757, .T. ) ;
#40276=DIRECTION ( 'NONE',  ( 1.283101021437938170E-16, 1.000000000000000000, 1.154811821032258155E-17 ) ) ;
#40277=DIRECTION ( 'NONE',  ( 3.197442310920450836E-14, 0.000000000000000000, 1.000000000000000000 ) ) ;
#40280=CIRCLE ( 'NONE', #5676, 2.165354330708661568 ) ;
#40290=EDGE_CURVE ( 'NONE', #24532, #11539, #49273, .T. ) ;
#40292=CARTESIAN_POINT ( 'NONE',  ( -2.151809081513409438, 1.575012187087082127, 0.2418202932658340965 ) ) ;
#40294=AXIS2_PLACEMENT_3D ( 'NONE', #42076, #3090, #37963 ) ;
#40295=EDGE_CURVE ( 'NONE', #50819, #18042, #13016, .T. ) ;
#40298=DIRECTION ( 'NONE',  ( -0.000000000000000000, -1.000000000000000000, -0.000000000000000000 ) ) ;
#40299=ORIENTED_EDGE ( 'NONE', *, *, #50499, .F. ) ;
#40301=CARTESIAN_POINT ( 'NONE',  ( 2.099568260077707027, 5.905511811023623991, -0.5296909464895783737 ) ) ;
#40307=( BOUNDED_CURVE ( )  B_SPLINE_CURVE ( 3, ( #28199, #16600, #32350, #48043 ),
 .UNSPECIFIED., .F., .F. ) 
 B_SPLINE_CURVE_WITH_KNOTS ( ( 4, 4 ),
 ( 5.042641131756091077, 5.093548817700087383 ),
 .UNSPECIFIED. ) 
 CURVE ( )  GEOMETRIC_REPRESENTATION_ITEM ( )  RATIONAL_B_SPLINE_CURVE ( ( 1.000000000000000000, 0.9997840456193998193, 0.9997840456193998193, 1.000000000000000000 ) ) 
 REPRESENTATION_ITEM ( '' )  );
#40313=CARTESIAN_POINT ( 'NONE',  ( -1.247273217833388514, 0.007942302252338809612, -1.260601835943744087 ) ) ;
#40315=B_SPLINE_CURVE_WITH_KNOTS ( 'NONE', 3,
 ( #24039, #10271, #6406, #10777 ),
 .UNSPECIFIED., .F., .F.,
 ( 4, 4 ),
 ( 2.559138052676411348E-07, 0.01633353498065875237 ),
 .UNSPECIFIED. ) ;
#40320=AXIS2_PLACEMENT_3D ( 'NONE', #19292, #23943, #5021 ) ;
#40323=LINE ( 'NONE', #20681, #23032 ) ;
#40324=VERTEX_POINT ( 'NONE', #3582 ) ;
#40325=EDGE_CURVE ( 'NONE', #45901, #50834, #18828, .T. ) ;
#40330=ORIENTED_EDGE ( 'NONE', *, *, #45027, .F. ) ;
#40331=AXIS2_PLACEMENT_3D ( 'NONE', #34912, #11419, #42892 ) ;
#40332=CARTESIAN_POINT ( 'NONE',  ( 0.8668862056626265300, 0.04180443457634609727, -1.686684286392636789 ) ) ;
#40334=DIRECTION ( 'NONE',  ( -0.000000000000000000, -1.000000000000000000, -0.000000000000000000 ) ) ;
#40335=DIRECTION ( 'NONE',  ( -0.01601477604151182663, 0.9998717552508123996, -0.000000000000000000 ) ) ;
#40343=CARTESIAN_POINT ( 'NONE',  ( -0.8004649005966125719, 0.000000000000000000, -1.548759025234861753 ) ) ;
#40346=ORIENTED_EDGE ( 'NONE', *, *, #41814, .F. ) ;
#40349=DIRECTION ( 'NONE',  ( -0.000000000000000000, 1.000000000000000000, -0.000000000000000000 ) ) ;
#40354=ORIENTED_EDGE ( 'NONE', *, *, #16951, .F. ) ;
#40356=DIRECTION ( 'NONE',  ( 0.7818314824680221431, -7.240175090764046435E-17, 0.6234898018587431423 ) ) ;
#40358=VECTOR ( 'NONE', #48568, 39.37007874015748143 ) ;
#40359=B_SPLINE_CURVE_WITH_KNOTS ( 'NONE', 3,
 ( #35042, #35295, #15667, #47117 ),
 .UNSPECIFIED., .F., .F.,
 ( 4, 4 ),
 ( 5.991603428212694306E-07, 0.0001408512246855418704 ),
 .UNSPECIFIED. ) ;
#40360=DIRECTION ( 'NONE',  ( -3.986037398843765983E-20, -1.000000000000000000, -1.160734090543304660E-16 ) ) ;
#40363=CARTESIAN_POINT ( 'NONE',  ( 2.867773316779195447, 5.905511811023623991, -0.7050287376751999124 ) ) ;
#40369=CARTESIAN_POINT ( 'NONE',  ( -1.556712866041157106, 5.905511811023623991, 2.509548638715848323 ) ) ;
#40371=EDGE_LOOP ( 'NONE', ( #5599, #4976, #33546, #38242 ) ) ;
#40373=CARTESIAN_POINT ( 'NONE',  ( 1.028983995711348021, 0.000000000000000000, 1.754363299348386862 ) ) ;
#40375=B_SPLINE_CURVE_WITH_KNOTS ( 'NONE', 3,
 ( #50035, #3094, #46180, #30968 ),
 .UNSPECIFIED., .F., .F.,
 ( 4, 4 ),
 ( 0.001414413680292015644, 0.004800578680812093990 ),
 .UNSPECIFIED. ) ;
#40381=ADVANCED_FACE ( 'NONE', ( #20076 ), #8960, .T. ) ;
#40384=CARTESIAN_POINT ( 'NONE',  ( -0.5756566573089003658, 1.611847391933241669, 2.896516654582634853 ) ) ;
#40386=CARTESIAN_POINT ( 'NONE',  ( -1.738921996492520661, 6.764728787913346618E-05, 0.1249482579781430736 ) ) ;
#40397=DIRECTION ( 'NONE',  ( -0.000000000000000000, 1.000000000000000000, -0.000000000000000000 ) ) ;
#40399=EDGE_CURVE ( 'NONE', #8450, #34440, #36972, .T. ) ;
#40404=CARTESIAN_POINT ( 'NONE',  ( 0.6418034415187964248, 0.01259213821865694249, 1.850136423892497994 ) ) ;
#40406=ORIENTED_EDGE ( 'NONE', *, *, #35992, .F. ) ;
#40407=CARTESIAN_POINT ( 'NONE',  ( 2.734482843737263025, 0.000000000000000000, -1.115254632218672937 ) ) ;
#40410=CARTESIAN_POINT ( 'NONE',  ( 1.565700802531847957, 1.740062672906616204, -2.238727750734997191 ) ) ;
#40413=CARTESIAN_POINT ( 'NONE',  ( 0.9914495361338626633, 0.000000000000000000, 2.781765111341823360 ) ) ;
#40414=CARTESIAN_POINT ( 'NONE',  ( 1.944213194762889119, 0.05905979794000976862, 0.2136995197171435157 ) ) ;
#40421=DIRECTION ( 'NONE',  ( -1.267583980596137654E-16, 1.000000000000000000, -2.300325776299734791E-17 ) ) ;
#40423=ORIENTED_EDGE ( 'NONE', *, *, #40971, .F. ) ;
#40427=FACE_OUTER_BOUND ( 'NONE', #20908, .T. ) ;
#40430=LINE ( 'NONE', #407, #4677 ) ;
#40431=ORIENTED_EDGE ( 'NONE', *, *, #44067, .T. ) ;
#40432=EDGE_CURVE ( 'NONE', #5041, #6926, #24737, .T. ) ;
#40436=EDGE_CURVE ( 'NONE', #22884, #30932, #21723, .T. ) ;
#40437=FACE_OUTER_BOUND ( 'NONE', #22504, .T. ) ;
#40438=VECTOR ( 'NONE', #22642, 39.37007874015748143 ) ;
#40441=CARTESIAN_POINT ( 'NONE',  ( 0.9836083787002616319, 5.905511811023623991, -1.929060376159698054 ) ) ;
#40447=ORIENTED_EDGE ( 'NONE', *, *, #5742, .F. ) ;
#40450=DIRECTION ( 'NONE',  ( 0.000000000000000000, 0.000000000000000000, -1.000000000000000000 ) ) ;
#40455=EDGE_CURVE ( 'NONE', #38863, #32449, #28470, .T. ) ;
#40456=EDGE_CURVE ( 'NONE', #25755, #26859, #48737, .T. ) ;
#40475=DIRECTION ( 'NONE',  ( 0.9959742939952397345, 0.000000000000000000, -0.08963930890342654279 ) ) ;
#40476=ORIENTED_EDGE ( 'NONE', *, *, #41594, .F. ) ;
#40478=EDGE_LOOP ( 'NONE', ( #3506, #8223, #39251, #19438 ) ) ;
#40481=DIRECTION ( 'NONE',  ( -5.207613805427244364E-18, -1.000000000000000000, -1.159565308550900415E-16 ) ) ;
#40484=CARTESIAN_POINT ( 'NONE',  ( 0.002207914879453961969, 6.692913385826772199, 0.04916304461325451958 ) ) ;
#40488=FACE_OUTER_BOUND ( 'NONE', #543, .T. ) ;
#40489=EDGE_CURVE ( 'NONE', #43816, #26794, #44083, .T. ) ;
#40493=LINE ( 'NONE', #17258, #44297 ) ;
#40494=CARTESIAN_POINT ( 'NONE',  ( 2.481910067697468580, 1.652579973978634653, -0.5160015848849505149 ) ) ;
#40495=DIRECTION ( 'NONE',  ( -0.000000000000000000, 1.000000000000000000, -0.000000000000000000 ) ) ;
#40497=CARTESIAN_POINT ( 'NONE',  ( 0.4519983648154151656, 1.649524736702080441, 2.215103298928671638 ) ) ;
#40498=AXIS2_PLACEMENT_3D ( 'NONE', #7975, #50523, #18596 ) ;
#40499=AXIS2_PLACEMENT_3D ( 'NONE', #10501, #26244, #34509 ) ;
#40503=CARTESIAN_POINT ( 'NONE',  ( -0.7117868624172403180, 0.000000000000000000, -1.591464117667691580 ) ) ;
#40504=CARTESIAN_POINT ( 'NONE',  ( -2.160407304981126764, 5.905511811023623991, -0.1462862061266901326 ) ) ;
#40509=ORIENTED_EDGE ( 'NONE', *, *, #43972, .F. ) ;
#40511=CARTESIAN_POINT ( 'NONE',  ( -1.693234526714950228, 0.000000000000000000, -0.4369479234249735167 ) ) ;
#40512=VECTOR ( 'NONE', #11537, 39.37007874015748143 ) ;
#40513=CARTESIAN_POINT ( 'NONE',  ( -1.979793062125317471, 1.589971192595758698, 2.191257344206539948 ) ) ;
#40515=CARTESIAN_POINT ( 'NONE',  ( 0.2156685157584260770, 1.510622172706404864, -2.945280361644574185 ) ) ;
#40517=EDGE_CURVE ( 'NONE', #7509, #23296, #10584, .T. ) ;
#40519=B_SPLINE_CURVE_WITH_KNOTS ( 'NONE', 3,
 ( #33494, #28571, #25219, #49181 ),
 .UNSPECIFIED., .F., .F.,
 ( 4, 4 ),
 ( 2.136451542541482466E-07, 0.002500479364714848496 ),
 .UNSPECIFIED. ) ;
#40522=CARTESIAN_POINT ( 'NONE',  ( -0.8241443283111672402, 1.596276574288824301, 2.055867440327626916 ) ) ;
#40527=CARTESIAN_POINT ( 'NONE',  ( 0.1067246931122726866, 0.02962905676920215767, 0.000000000000000000 ) ) ;
#40530=CARTESIAN_POINT ( 'NONE',  ( -2.996855935080999345, 5.118110236220475784, 0.1838511574193322229 ) ) ;
#40534=VECTOR ( 'NONE', #41266, 39.37007874015748143 ) ;
#40536=CARTESIAN_POINT ( 'NONE',  ( -1.393175312147127531, 0.000000000000000000, 1.048074961516273218 ) ) ;
#40537=DIRECTION ( 'NONE',  ( 0.6579387259397027066, -8.743779800425989470E-17, 0.7530714660036196273 ) ) ;
#40538=ORIENTED_EDGE ( 'NONE', *, *, #30938, .F. ) ;
#40539=CARTESIAN_POINT ( 'NONE',  ( 0.000000000000000000, 5.905511811023623991, 0.000000000000000000 ) ) ;
#40541=ORIENTED_EDGE ( 'NONE', *, *, #3933, .T. ) ;
#40543=VECTOR ( 'NONE', #2562, 39.37007874015748143 ) ;
#40547=VECTOR ( 'NONE', #27464, 39.37007874015748143 ) ;
#40554=CARTESIAN_POINT ( 'NONE',  ( -0.04921259842519767197, 6.692913385826772199, -2.165433070866142007 ) ) ;
#40557=DIRECTION ( 'NONE',  ( 0.9195277725514489076, 0.000000000000000000, 0.3930250316539278810 ) ) ;
#40565=VECTOR ( 'NONE', #13770, 39.37007874015748143 ) ;
#40568=AXIS2_PLACEMENT_3D ( 'NONE', #23500, #31263, #2881 ) ;
#40571=EDGE_CURVE ( 'NONE', #29332, #41869, #26256, .T. ) ;
#40579=CIRCLE ( 'NONE', #20795, 2.246510896728926010 ) ;
#40583=EDGE_CURVE ( 'NONE', #6769, #21621, #40198, .T. ) ;
#40587=CYLINDRICAL_SURFACE ( 'NONE', #6557, 2.165354330708661568 ) ;
#40595=ORIENTED_EDGE ( 'NONE', *, *, #16404, .F. ) ;
#40600=CARTESIAN_POINT ( 'NONE',  ( -2.659122809025360024, 1.575291203863115275, 0.4098647105644042110 ) ) ;
#40601=LINE ( 'NONE', #20199, #31852 ) ;
#40602=DIRECTION ( 'NONE',  ( 0.000000000000000000, 0.000000000000000000, -1.000000000000000000 ) ) ;
#40605=CARTESIAN_POINT ( 'NONE',  ( 0.5286458662987449930, 5.905511811023623991, 2.100489422084715674 ) ) ;
#40608=DIRECTION ( 'NONE',  ( -3.986037398843765983E-20, -1.000000000000000000, -1.160734090543304660E-16 ) ) ;
#40612=LINE ( 'NONE', #17120, #40358 ) ;
#40614=VERTEX_POINT ( 'NONE', #21622 ) ;
#40615=VECTOR ( 'NONE', #33756, 39.37007874015748854 ) ;
#40616=EDGE_CURVE ( 'NONE', #40227, #5560, #18517, .T. ) ;
#40620=DIRECTION ( 'NONE',  ( -0.000000000000000000, 1.000000000000000000, 0.000000000000000000 ) ) ;
#40622=CONICAL_SURFACE ( 'NONE', #14224, 2.246510896728926010, 0.01601546068027819014 ) ;
#40626=VERTEX_POINT ( 'NONE', #9497 ) ;
#40631=CARTESIAN_POINT ( 'NONE',  ( 2.457479397754350536, 1.750633465154818991, -0.6113818280758235302 ) ) ;
#40635=CARTESIAN_POINT ( 'NONE',  ( -0.2878729405423523513, 0.5249316475426858419, 1.861923633677847079 ) ) ;
#40636=LINE ( 'NONE', #5010, #34975 ) ;
#40638=CARTESIAN_POINT ( 'NONE',  ( 1.930898218216747120, 1.205361022782829114E-17, -0.8788249315385436855 ) ) ;
#40639=CARTESIAN_POINT ( 'NONE',  ( 0.2156685157584260770, 1.624173731825095723, -2.945280361644574185 ) ) ;
#40644=DIRECTION ( 'NONE',  ( 1.687538997430237941E-14, 0.000000000000000000, 1.000000000000000000 ) ) ;
#40650=ORIENTED_EDGE ( 'NONE', *, *, #37887, .F. ) ;
#40654=ORIENTED_EDGE ( 'NONE', *, *, #36178, .T. ) ;
#40661=ORIENTED_EDGE ( 'NONE', *, *, #41419, .F. ) ;
#40673=VERTEX_POINT ( 'NONE', #30897 ) ;
#40677=EDGE_LOOP ( 'NONE', ( #24923, #4591, #38707, #5588, #29116, #29153, #31490, #48897, #45680, #39579, #12379 ) ) ;
#40683=DIRECTION ( 'NONE',  ( -0.000000000000000000, -1.000000000000000000, -0.000000000000000000 ) ) ;
#40686=B_SPLINE_CURVE_WITH_KNOTS ( 'NONE', 3,
 ( #8622, #361, #24372, #876 ),
 .UNSPECIFIED., .F., .F.,
 ( 4, 4 ),
 ( 2.075011172033926488E-07, 0.002500489681420431202 ),
 .UNSPECIFIED. ) ;
#40687=CONICAL_SURFACE ( 'NONE', #18422, 2.165354330708661568, 0.2617993877991570129 ) ;
#40695=ORIENTED_EDGE ( 'NONE', *, *, #12907, .F. ) ;
#40696=CARTESIAN_POINT ( 'NONE',  ( 2.298708793198899869, 5.118110236220475784, 1.181102362204724754 ) ) ;
#40700=CARTESIAN_POINT ( 'NONE',  ( 1.834499544866850851, 1.737284818394516206, 1.400019292979238772 ) ) ;
#40701=CARTESIAN_POINT ( 'NONE',  ( 2.112725606141798718, 1.676124320423267866, -0.9565416868427374375 ) ) ;
#40703=VERTEX_POINT ( 'NONE', #38391 ) ;
#40705=B_SPLINE_CURVE_WITH_KNOTS ( 'NONE', 3,
 ( #20460, #40600, #20198, #8335 ),
 .UNSPECIFIED., .F., .F.,
 ( 4, 4 ),
 ( 6.908975551891818311E-06, 0.02000310376711551125 ),
 .UNSPECIFIED. ) ;
#40706=ORIENTED_EDGE ( 'NONE', *, *, #5150, .T. ) ;
#40713=ORIENTED_EDGE ( 'NONE', *, *, #32437, .T. ) ;
#40716=EDGE_LOOP ( 'NONE', ( #5688, #29548, #46159, #27296 ) ) ;
#40718=ORIENTED_EDGE ( 'NONE', *, *, #38839, .T. ) ;
#40721=B_SPLINE_CURVE_WITH_KNOTS ( 'NONE', 3,
 ( #40638, #5777, #1393, #25146 ),
 .UNSPECIFIED., .F., .F.,
 ( 4, 4 ),
 ( 6.537091799742329783E-07, 0.004672429636363999335 ),
 .UNSPECIFIED. ) ;
#40722=ORIENTED_EDGE ( 'NONE', *, *, #8781, .T. ) ;
#40724=CIRCLE ( 'NONE', #1129, 1.743387098533651480 ) ;
#40733=EDGE_CURVE ( 'NONE', #17198, #9822, #38277, .T. ) ;
#40734=B_SPLINE_CURVE_WITH_KNOTS ( 'NONE', 3,
 ( #35493, #7614, #635, #35743 ),
 .UNSPECIFIED., .F., .F.,
 ( 4, 4 ),
 ( 0.01074804989555521069, 0.03073582135077717464 ),
 .UNSPECIFIED. ) ;
#40736=ORIENTED_EDGE ( 'NONE', *, *, #22330, .T. ) ;
#40747=CARTESIAN_POINT ( 'NONE',  ( 1.700185224778670401, 1.636708331897141377, -1.557456981387029149 ) ) ;
#40752=CARTESIAN_POINT ( 'NONE',  ( 1.726519710923990480, 1.205361022782829114E-17, -1.198633063221572481 ) ) ;
#40762=VECTOR ( 'NONE', #24864, 39.37007874015748143 ) ;
#40764=CARTESIAN_POINT ( 'NONE',  ( 1.634516194504713527, 0.03557717711494950280, -1.137902073757964816 ) ) ;
#40765=AXIS2_PLACEMENT_3D ( 'NONE', #8753, #24509, #40260 ) ;
#40766=DIRECTION ( 'NONE',  ( -0.000000000000000000, -1.000000000000000000, -0.000000000000000000 ) ) ;
#40768=LINE ( 'NONE', #13148, #33647 ) ;
#40770=CARTESIAN_POINT ( 'NONE',  ( -2.151809081513409438, 1.575012187087082127, 0.2418202932658340965 ) ) ;
#40772=CARTESIAN_POINT ( 'NONE',  ( -1.052882153134559129, 1.702845081222334578, 2.758709064543730438 ) ) ;
#40776=EDGE_CURVE ( 'NONE', #50201, #43816, #44397, .T. ) ;
#40777=ORIENTED_EDGE ( 'NONE', *, *, #30938, .T. ) ;
#40778=CARTESIAN_POINT ( 'NONE',  ( 1.368795924897367566, 1.049866565067838486, 1.491914849661855502 ) ) ;
#40780=EDGE_CURVE ( 'NONE', #20664, #1280, #6265, .T. ) ;
#40781=CARTESIAN_POINT ( 'NONE',  ( 1.090138530625468283, -2.244369135793855756E-16, 1.920534397867776910 ) ) ;
#40782=CARTESIAN_POINT ( 'NONE',  ( 2.793030215715258446, 1.762782749918499814, 0.9592557174602684977 ) ) ;
#40784=DIRECTION ( 'NONE',  ( -0.01601477604151182663, 0.9998717552508123996, -0.000000000000000000 ) ) ;
#40785=ORIENTED_EDGE ( 'NONE', *, *, #28356, .F. ) ;
#40787=PLANE ( 'NONE',  #6226 ) ;
#40788=PLANE ( 'NONE',  #11671 ) ;
#40792=CARTESIAN_POINT ( 'NONE',  ( -2.576863348864732117, 1.568913320674888201, 1.442554885838411849 ) ) ;
#40794=CARTESIAN_POINT ( 'NONE',  ( 0.002207914879453961969, 6.692913385826772199, 0.04916304461325451958 ) ) ;
#40799=ORIENTED_EDGE ( 'NONE', *, *, #16649, .F. ) ;
#40809=ORIENTED_EDGE ( 'NONE', *, *, #39829, .F. ) ;
#40812=DIRECTION ( 'NONE',  ( 0.2225209339563184452, 0.000000000000000000, -0.9749279121818227312 ) ) ;
#40819=VERTEX_POINT ( 'NONE', #23385 ) ;
#40823=ORIENTED_EDGE ( 'NONE', *, *, #13214, .T. ) ;
#40830=CIRCLE ( 'NONE', #16097, 1.850107469027523432 ) ;
#40833=VERTEX_POINT ( 'NONE', #12807 ) ;
#40840=ORIENTED_EDGE ( 'NONE', *, *, #33150, .F. ) ;
#40841=EDGE_LOOP ( 'NONE', ( #26460, #33016, #24326, #38790 ) ) ;
#40845=ORIENTED_EDGE ( 'NONE', *, *, #46976, .F. ) ;
#40848=DIRECTION ( 'NONE',  ( -0.000000000000000000, -1.000000000000000000, -0.000000000000000000 ) ) ;
#40850=DIRECTION ( 'NONE',  ( 0.5877852522924684742, -9.392878985996986848E-17, 0.8090169943749506709 ) ) ;
#40854=ORIENTED_EDGE ( 'NONE', *, *, #46193, .F. ) ;
#40855=B_SPLINE_CURVE_WITH_KNOTS ( 'NONE', 3,
 ( #47987, #16797, #24796, #21182 ),
 .UNSPECIFIED., .F., .F.,
 ( 4, 4 ),
 ( 0.002222465192948955282, 0.004722220330562246909 ),
 .UNSPECIFIED. ) ;
#40857=CARTESIAN_POINT ( 'NONE',  ( 1.882988517681382756, 6.692913385826772199, 1.069164917025817951 ) ) ;
#40858=DIRECTION ( 'NONE',  ( -3.986037398843765983E-20, -1.000000000000000000, -1.160734090543304660E-16 ) ) ;
#40862=ADVANCED_FACE ( 'NONE', ( #44533 ), #8420, .F. ) ;
#40868=AXIS2_PLACEMENT_3D ( 'NONE', #30097, #11235, #26966 ) ;
#40872=ADVANCED_FACE ( 'NONE', ( #4545 ), #927, .T. ) ;
#40878=LINE ( 'NONE', #25888, #669 ) ;
#40880=ORIENTED_EDGE ( 'NONE', *, *, #46443, .T. ) ;
#40885=ORIENTED_EDGE ( 'NONE', *, *, #31338, .T. ) ;
#40888=CARTESIAN_POINT ( 'NONE',  ( 0.002207914879453961969, 6.692913385826772199, 0.04916304461325451958 ) ) ;
#40889=VERTEX_POINT ( 'NONE', #670 ) ;
#40896=DIRECTION ( 'NONE',  ( -0.01601477604151182663, 0.9998717552508123996, -0.000000000000000000 ) ) ;
#40909=EDGE_CURVE ( 'NONE', #20873, #5560, #1318, .T. ) ;
#40911=CIRCLE ( 'NONE', #21116, 1.850107469027523432 ) ;
#40913=DIRECTION ( 'NONE',  ( -0.9998717552508121775, -0.01601477604151182663, 0.000000000000000000 ) ) ;
#40914=CARTESIAN_POINT ( 'NONE',  ( -1.805735793713946435, 1.049866565877818347, 0.9158222790674427349 ) ) ;
#40930=ORIENTED_EDGE ( 'NONE', *, *, #11157, .F. ) ;
#40936=CARTESIAN_POINT ( 'NONE',  ( -2.734482843737247038, 1.676638068352269029, -1.115254632218712016 ) ) ;
#40939=LINE ( 'NONE', #41699, #38480 ) ;
#40943=EDGE_CURVE ( 'NONE', #19430, #16862, #16139, .T. ) ;
#40947=DIRECTION ( 'NONE',  ( -0.9959742939952397345, 1.288287287306305530E-16, 0.08963930890342654279 ) ) ;
#40950=LINE ( 'NONE', #41707, #48871 ) ;
#40959=CIRCLE ( 'NONE', #30223, 1.850107469027523432 ) ;
#40961=CARTESIAN_POINT ( 'NONE',  ( -0.6094175224461334528, 1.205361022782829114E-17, 1.763844451117148271 ) ) ;
#40971=EDGE_CURVE ( 'NONE', #35836, #31431, #39464, .T. ) ;
#40977=ORIENTED_EDGE ( 'NONE', *, *, #33502, .T. ) ;
#40985=VERTEX_POINT ( 'NONE', #30519 ) ;
#40987=CIRCLE ( 'NONE', #12962, 1.743387098533651480 ) ;
#40988=CARTESIAN_POINT ( 'NONE',  ( -0.6380732109764247761, 1.697682040615038801, -2.127022210610377773 ) ) ;
#40989=AXIS2_PLACEMENT_3D ( 'NONE', #45351, #33014, #25497 ) ;
#40998=EDGE_LOOP ( 'NONE', ( #24267, #14057, #36637, #774 ) ) ;
#41001=CARTESIAN_POINT ( 'NONE',  ( -2.325625524897931840, 1.576417212481815211, 0.7038963509006195274 ) ) ;
#41002=B_SPLINE_CURVE_WITH_KNOTS ( 'NONE', 3,
 ( #6754, #50556, #29990, #7508 ),
 .UNSPECIFIED., .F., .F.,
 ( 4, 4 ),
 ( 2.655964760909496045E-07, 0.002500437657294805275 ),
 .UNSPECIFIED. ) ;
#41007=CARTESIAN_POINT ( 'NONE',  ( 0.1067246931122726866, 0.02962905676920215767, 0.000000000000000000 ) ) ;
#41009=ORIENTED_EDGE ( 'NONE', *, *, #11327, .F. ) ;
#41010=CARTESIAN_POINT ( 'NONE',  ( 1.129748414438405124, 1.627571742414081202, 1.986830176535870907 ) ) ;
#41011=CARTESIAN_POINT ( 'NONE',  ( 1.556712866041120247, 1.480457248723645591, 2.509548638715870084 ) ) ;
#41012=CARTESIAN_POINT ( 'NONE',  ( 1.746845460392688620, 0.000000000000000000, -1.172799208037324847 ) ) ;
#41015=ORIENTED_EDGE ( 'NONE', *, *, #18777, .F. ) ;
#41016=CARTESIAN_POINT ( 'NONE',  ( 0.1067246931122726866, 0.02962905676920215767, 0.000000000000000000 ) ) ;
#41027=CARTESIAN_POINT ( 'NONE',  ( -0.6690177265809421625, 0.000000000000000000, 1.735666008086750089 ) ) ;
#41028=EDGE_CURVE ( 'NONE', #1621, #20851, #37636, .T. ) ;
#41029=DIRECTION ( 'NONE',  ( -0.000000000000000000, 1.000000000000000000, -0.000000000000000000 ) ) ;
#41035=ADVANCED_FACE ( 'NONE', ( #39265 ), #8283, .T. ) ;
#41036=VERTEX_POINT ( 'NONE', #11900 ) ;
#41039=B_SPLINE_CURVE_WITH_KNOTS ( 'NONE', 3,
 ( #6213, #26081, #13446, #6469 ),
 .UNSPECIFIED., .F., .F.,
 ( 4, 4 ),
 ( 0.002601184284654935782, 0.004660285992363409451 ),
 .UNSPECIFIED. ) ;
#41045=DIRECTION ( 'NONE',  ( -0.9998717552508121775, -0.01601477604151182663, 0.000000000000000000 ) ) ;
#41048=DIRECTION ( 'NONE',  ( 1.142080616180678453E-16, -1.000000000000000000, 2.072570748943325363E-17 ) ) ;
#41049=CARTESIAN_POINT ( 'NONE',  ( 2.298708793198899425, 2.755905511811027164, 1.181102362204724088 ) ) ;
#41054=AXIS2_PLACEMENT_3D ( 'NONE', #46818, #11492, #50921 ) ;
#41056=VERTEX_POINT ( 'NONE', #8026 ) ;
#41060=VERTEX_POINT ( 'NONE', #31277 ) ;
#41061=ORIENTED_EDGE ( 'NONE', *, *, #27757, .F. ) ;
#41064=CARTESIAN_POINT ( 'NONE',  ( -2.101347671104863313, 1.674245022174266406, -0.5300970854448181502 ) ) ;
#41068=CIRCLE ( 'NONE', #47613, 2.164630168518208109 ) ;
#41072=CARTESIAN_POINT ( 'NONE',  ( 0.5756566573088583993, 5.905511811023623991, 2.896516654582643291 ) ) ;
#41074=EDGE_CURVE ( 'NONE', #26643, #17294, #17969, .T. ) ;
#41079=CARTESIAN_POINT ( 'NONE',  ( 0.3595914698493179462, 0.000000000000000000, 1.705899337635486290 ) ) ;
#41083=DIRECTION ( 'NONE',  ( 0.000000000000000000, 1.160734090543304660E-16, -1.000000000000000000 ) ) ;
#41088=EDGE_CURVE ( 'NONE', #21474, #28376, #50576, .T. ) ;
#41090=VERTEX_POINT ( 'NONE', #31787 ) ;
#41093=CARTESIAN_POINT ( 'NONE',  ( 1.733526556417521958, 0.000000000000000000, 0.1851600754179809072 ) ) ;
#41095=VERTEX_POINT ( 'NONE', #15271 ) ;
#41099=VECTOR ( 'NONE', #12863, 39.37007874015748143 ) ;
#41105=ORIENTED_EDGE ( 'NONE', *, *, #38739, .F. ) ;
#41106=CARTESIAN_POINT ( 'NONE',  ( -2.456251886791057437, 1.676905504490172838, -1.103371865719809275 ) ) ;
#41107=PLANE ( 'NONE',  #507 ) ;
#41111=ORIENTED_EDGE ( 'NONE', *, *, #16649, .T. ) ;
#41114=CARTESIAN_POINT ( 'NONE',  ( 3.937007874015748143, 2.913385826771657250, -1.023622047244094224 ) ) ;
#41115=VERTEX_POINT ( 'NONE', #47484 ) ;
#41117=DIRECTION ( 'NONE',  ( 0.9998717552508121775, 0.01601477604151182663, 0.000000000000000000 ) ) ;
#41118=FACE_OUTER_BOUND ( 'NONE', #4761, .T. ) ;
#41119=ORIENTED_EDGE ( 'NONE', *, *, #49416, .T. ) ;
#41139=B_SPLINE_CURVE_WITH_KNOTS ( 'NONE', 3,
 ( #2159, #29008, #48845, #25394 ),
 .UNSPECIFIED., .F., .F.,
 ( 4, 4 ),
 ( 0.1211775127643062860, 0.1625894504277921315 ),
 .UNSPECIFIED. ) ;
#41143=CARTESIAN_POINT ( 'NONE',  ( 1.329442508636073939, 1.634319695305515463, 2.129162132572615551 ) ) ;
#41146=CARTESIAN_POINT ( 'NONE',  ( 0.2483449720853004861, 1.723125804968587360, -2.942339427345150860 ) ) ;
#41147=VERTEX_POINT ( 'NONE', #47993 ) ;
#41150=EDGE_CURVE ( 'NONE', #39017, #27844, #4925, .T. ) ;
#41152=ORIENTED_EDGE ( 'NONE', *, *, #12396, .T. ) ;
#41153=DIRECTION ( 'NONE',  ( 7.237058681235334921E-17, -1.000000000000000000, -9.074984547606431700E-17 ) ) ;
#41157=CARTESIAN_POINT ( 'NONE',  ( -2.154836593528564492, 1.574965465101147766, -0.2160053639259867930 ) ) ;
#41158=CARTESIAN_POINT ( 'NONE',  ( -0.1450362469327511061, 1.574803149606302854, -2.160491579385214411 ) ) ;
#41161=CARTESIAN_POINT ( 'NONE',  ( -1.891495399494460106, 1.644797792086550858, 1.073742665334450175 ) ) ;
#41163=CARTESIAN_POINT ( 'NONE',  ( -2.047355983664255863, 1.576684601009278319, 0.7169714724935087879 ) ) ;
#41165=ADVANCED_FACE ( 'NONE', ( #32827 ), #8797, .F. ) ;
#41166=DIRECTION ( 'NONE',  ( -0.9362348706397368714, -1.160734090543304413E-16, -0.3513748240813434620 ) ) ;
#41168=ORIENTED_EDGE ( 'NONE', *, *, #42297, .F. ) ;
#41169=DIRECTION ( 'NONE',  ( -0.9998717552508122886, -0.01601477604151181275, 0.000000000000000000 ) ) ;
#41170=CARTESIAN_POINT ( 'NONE',  ( -1.723188456408593527, 6.692913385826772199, 1.311251662046200472 ) ) ;
#41188=ORIENTED_EDGE ( 'NONE', *, *, #46447, .T. ) ;
#41192=CARTESIAN_POINT ( 'NONE',  ( 1.478089240774732582, 0.05159396975604255142, 1.241682111880268558 ) ) ;
#41194=ORIENTED_EDGE ( 'NONE', *, *, #32737, .F. ) ;
#41197=ORIENTED_EDGE ( 'NONE', *, *, #2616, .F. ) ;
#41199=CARTESIAN_POINT ( 'NONE',  ( 1.083598637574782142, 1.637691314537677023, 2.747180975113346246 ) ) ;
#41203=EDGE_CURVE ( 'NONE', #23878, #10495, #29605, .T. ) ;
#41206=ORIENTED_EDGE ( 'NONE', *, *, #8003, .T. ) ;
#41207=DIRECTION ( 'NONE',  ( 0.000000000000000000, -1.000000000000000000, -0.000000000000000000 ) ) ;
#41214=DIRECTION ( 'NONE',  ( 0.000000000000000000, 1.160734090543304660E-16, -1.000000000000000000 ) ) ;
#41216=CARTESIAN_POINT ( 'NONE',  ( 1.930898218216747120, 1.205361022782829114E-17, -0.8788249315385436855 ) ) ;
#41230=ORIENTED_EDGE ( 'NONE', *, *, #9889, .F. ) ;
#41232=ORIENTED_EDGE ( 'NONE', *, *, #40246, .F. ) ;
#41234=DIRECTION ( 'NONE',  ( -0.000000000000000000, -1.000000000000000000, -0.000000000000000000 ) ) ;
#41242=EDGE_CURVE ( 'NONE', #46048, #19150, #10833, .T. ) ;
#41247=CIRCLE ( 'NONE', #23909, 2.165354330708661568 ) ;
#41249=ORIENTED_EDGE ( 'NONE', *, *, #7903, .F. ) ;
#41250=DIRECTION ( 'NONE',  ( -0.9998717552508122886, -0.01601477604151185785, 0.000000000000000000 ) ) ;
#41255=EDGE_CURVE ( 'NONE', #17122, #43876, #17332, .T. ) ;
#41257=EDGE_CURVE ( 'NONE', #32688, #29455, #26575, .T. ) ;
#41258=ORIENTED_EDGE ( 'NONE', *, *, #48108, .F. ) ;
#41262=ORIENTED_EDGE ( 'NONE', *, *, #8495, .T. ) ;
#41264=DIRECTION ( 'NONE',  ( -0.000000000000000000, -1.000000000000000000, -0.000000000000000000 ) ) ;
#41265=CARTESIAN_POINT ( 'NONE',  ( 1.662320194739496770, 5.905511811023623991, -1.388601395075552247 ) ) ;
#41266=DIRECTION ( 'NONE',  ( -9.701723960855857903E-17, 1.000000000000000000, 8.476140964546263859E-17 ) ) ;
#41267=CARTESIAN_POINT ( 'NONE',  ( 1.979793062125284608, 1.651646828087945051, 2.191257344206569257 ) ) ;
#41270=DIRECTION ( 'NONE',  ( -2.582876339026340310E-17, -1.000000000000000000, 1.131632063491650798E-16 ) ) ;
#41275=CARTESIAN_POINT ( 'NONE',  ( 1.680518189209764479, 0.01778946649618510026, -1.168267724599023838 ) ) ;
#41276=CARTESIAN_POINT ( 'NONE',  ( -2.889674983507169337, 1.674218314264582785, -0.6090712660038034576 ) ) ;
#41285=CARTESIAN_POINT ( 'NONE',  ( -1.891607981616729495, 1.579179190298960256, 1.073803248357834139 ) ) ;
#41289=PLANE ( 'NONE',  #11215 ) ;
#41291=DIRECTION ( 'NONE',  ( 0.6910626489868684219, 0.000000000000000000, -0.7227948638273878901 ) ) ;
#41295=EDGE_CURVE ( 'NONE', #39335, #40266, #38468, .T. ) ;
#41298=VERTEX_POINT ( 'NONE', #22213 ) ;
#41304=ORIENTED_EDGE ( 'NONE', *, *, #45612, .T. ) ;
#41306=CARTESIAN_POINT ( 'NONE',  ( -1.232620761116186126, 1.574803149606302854, -1.780282403660753410 ) ) ;
#41310=EDGE_CURVE ( 'NONE', #643, #33237, #15450, .T. ) ;
#41313=AXIS2_PLACEMENT_3D ( 'NONE', #1755, #22151, #17511 ) ;
#41317=CARTESIAN_POINT ( 'NONE',  ( -0.9836083787002332102, 1.574803149606302854, -1.929060376159713375 ) ) ;
#41320=ORIENTED_EDGE ( 'NONE', *, *, #33572, .T. ) ;
#41322=LINE ( 'NONE', #37456, #36495 ) ;
#41331=DIRECTION ( 'NONE',  ( -1.729310098865080642E-17, 1.000000000000000000, 1.276627980444840260E-16 ) ) ;
#41333=CARTESIAN_POINT ( 'NONE',  ( 1.548545842648739956, 1.732704746525083772, 1.697655184951773810 ) ) ;
#41338=ORIENTED_EDGE ( 'NONE', *, *, #46744, .T. ) ;
#41340=CARTESIAN_POINT ( 'NONE',  ( -0.04921259842519689481, 0.000000000000000000, 1.742692369722729895 ) ) ;
#41343=DIRECTION ( 'NONE',  ( -0.000000000000000000, -1.000000000000000000, -0.000000000000000000 ) ) ;
#41345=ORIENTED_EDGE ( 'NONE', *, *, #13281, .F. ) ;
#41351=ORIENTED_EDGE ( 'NONE', *, *, #6030, .T. ) ;
#41353=LINE ( 'NONE', #14232, #1757 ) ;
#41354=CARTESIAN_POINT ( 'NONE',  ( 1.900276455977023549, 1.738338356005314722, -1.313328886422038710 ) ) ;
#41356=CARTESIAN_POINT ( 'NONE',  ( 2.164658444855302122, 5.905511811023623991, -0.04795272066889885720 ) ) ;
#41359=ORIENTED_EDGE ( 'NONE', *, *, #5253, .F. ) ;
#41360=CARTESIAN_POINT ( 'NONE',  ( 1.232995795418176943, 5.905511811023623991, 1.780798594093568221 ) ) ;
#41364=CARTESIAN_POINT ( 'NONE',  ( -2.307846990702095535, 5.118110236220475784, -0.8016101313716829102 ) ) ;
#41367=ORIENTED_EDGE ( 'NONE', *, *, #47753, .F. ) ;
#41375=ORIENTED_EDGE ( 'NONE', *, *, #26098, .T. ) ;
#41376=EDGE_CURVE ( 'NONE', #9179, #28139, #47427, .T. ) ;
#41377=CARTESIAN_POINT ( 'NONE',  ( -0.4424051356154121706, 0.01394701979125833637, -1.788003152444398225 ) ) ;
#41380=CARTESIAN_POINT ( 'NONE',  ( 2.099568260077707027, 2.755905511811027164, -0.5296909464895783737 ) ) ;
#41383=CARTESIAN_POINT ( 'NONE',  ( 2.326943258702977246, 1.646747008850265370, -0.05524094006260020506 ) ) ;
#41385=CIRCLE ( 'NONE', #43863, 2.165354330708661568 ) ;
#41390=VECTOR ( 'NONE', #49440, 39.37007874015748143 ) ;
#41391=DIRECTION ( 'NONE',  ( 3.986037398843765983E-20, 1.000000000000000000, 1.160734090543304660E-16 ) ) ;
#41392=ORIENTED_EDGE ( 'NONE', *, *, #13556, .T. ) ;
#41394=CARTESIAN_POINT ( 'NONE',  ( -1.613340714851948965, 1.583636149837539975, -1.474425128113891814 ) ) ;
#41395=CARTESIAN_POINT ( 'NONE',  ( 1.461363083917469163, 6.692913385826772199, 1.597866488315585087 ) ) ;
#41396=CARTESIAN_POINT ( 'NONE',  ( 0.000000000000000000, 1.595182601976580683, 0.000000000000000000 ) ) ;
#41398=DIRECTION ( 'NONE',  ( 0.000000000000000000, 1.000000000000000000, 0.000000000000000000 ) ) ;
#41400=VERTEX_POINT ( 'NONE', #46672 ) ;
#41402=CARTESIAN_POINT ( 'NONE',  ( 2.867773316779195447, 1.205361022782829114E-17, -0.7050287376752006896 ) ) ;
#41403=EDGE_LOOP ( 'NONE', ( #36582, #26108, #24181, #43126 ) ) ;
#41404=DIRECTION ( 'NONE',  ( -0.9362348706397417564, 0.000000000000000000, 0.3513748240813304724 ) ) ;
#41407=CARTESIAN_POINT ( 'NONE',  ( -1.171161938979115025, 1.656335251912683271, 1.864245081490210731 ) ) ;
#41412=CARTESIAN_POINT ( 'NONE',  ( -1.408960544533061299, 0.005352583808700523381, 1.060663264281380025 ) ) ;
#41415=VERTEX_POINT ( 'NONE', #4357 ) ;
#41416=LINE ( 'NONE', #6042, #1996 ) ;
#41418=CARTESIAN_POINT ( 'NONE',  ( 2.277873973731426194, 1.656288013650806912, 1.879489153247668076 ) ) ;
#41419=EDGE_CURVE ( 'NONE', #22594, #15665, #6505, .T. ) ;
#41423=DIRECTION ( 'NONE',  ( -0.9909497617679352555, 0.000000000000000000, 0.1342332658176522697 ) ) ;
#41426=ADVANCED_FACE ( 'NONE', ( #15967 ), #23205, .T. ) ;
#41434=ORIENTED_EDGE ( 'NONE', *, *, #13263, .F. ) ;
#41438=EDGE_CURVE ( 'NONE', #42820, #36594, #6808, .T. ) ;
#41452=B_SPLINE_CURVE_WITH_KNOTS ( 'NONE', 3,
 ( #1633, #44986, #41143, #33653 ),
 .UNSPECIFIED., .F., .F.,
 ( 4, 4 ),
 ( 2.330467837939416791E-07, 0.01688764880552376044 ),
 .UNSPECIFIED. ) ;
#41459=ORIENTED_EDGE ( 'NONE', *, *, #5112, .T. ) ;
#41464=ORIENTED_EDGE ( 'NONE', *, *, #12782, .T. ) ;
#41465=AXIS2_PLACEMENT_3D ( 'NONE', #29742, #21489, #13999 ) ;
#41469=FACE_OUTER_BOUND ( 'NONE', #1734, .T. ) ;
#41472=CARTESIAN_POINT ( 'NONE',  ( 0.6584127755596609344, 0.000000000000000000, 1.614277297217986851 ) ) ;
#41474=ORIENTED_EDGE ( 'NONE', *, *, #22635, .T. ) ;
#41477=CARTESIAN_POINT ( 'NONE',  ( -2.919165122154194769, 1.575328909575085090, 0.4450898352768660748 ) ) ;
#41478=ORIENTED_EDGE ( 'NONE', *, *, #27587, .F. ) ;
#41483=CARTESIAN_POINT ( 'NONE',  ( -2.932638728931780125, 1.673548413681422042, 0.3475908556737793420 ) ) ;
#41485=LINE ( 'NONE', #42492, #19866 ) ;
#41487=CARTESIAN_POINT ( 'NONE',  ( -1.172858943013144861, -2.300834904144050480E-16, 1.867085387823100628 ) ) ;
#41492=CARTESIAN_POINT ( 'NONE',  ( -0.2492758785930729581, 1.703909341437327862, -2.220674960591680680 ) ) ;
#41493=AXIS2_PLACEMENT_3D ( 'NONE', #5735, #25353, #25104 ) ;
#41495=CIRCLE ( 'NONE', #3569, 2.164630168518208109 ) ;
#41497=CARTESIAN_POINT ( 'NONE',  ( 1.306035350298335729, 1.696012099853481336, -1.881328916909827065 ) ) ;
#41498=AXIS2_PLACEMENT_3D ( 'NONE', #42870, #30761, #18887 ) ;
#41499=VECTOR ( 'NONE', #2080, 39.37007874015748143 ) ;
#41506=ORIENTED_EDGE ( 'NONE', *, *, #32040, .T. ) ;
#41509=CARTESIAN_POINT ( 'NONE',  ( 2.742591780645512234, 1.758546389883244965, -0.07390773670709777088 ) ) ;
#41510=EDGE_CURVE ( 'NONE', #40324, #8605, #24490, .T. ) ;
#41516=EDGE_CURVE ( 'NONE', #38951, #39747, #29582, .T. ) ;
#41518=ORIENTED_EDGE ( 'NONE', *, *, #20324, .F. ) ;
#41526=CARTESIAN_POINT ( 'NONE',  ( -2.165460538733998241, 1.205361022782829114E-17, 0.04798874274652762534 ) ) ;
#41539=CONICAL_SURFACE ( 'NONE', #13496, 3.483074324928249421, 1.244861948955335196 ) ;
#41543=EDGE_CURVE ( 'NONE', #48519, #48829, #40493, .T. ) ;
#41548=PLANE ( 'NONE',  #38087 ) ;
#41551=DIRECTION ( 'NONE',  ( 0.7818314824680221431, 0.000000000000000000, 0.6234898018587431423 ) ) ;
#41554=ORIENTED_EDGE ( 'NONE', *, *, #34505, .F. ) ;
#41555=CARTESIAN_POINT ( 'NONE',  ( -0.5373920265435009336, 0.5242596937404421231, -2.132180421997459607 ) ) ;
#41558=EDGE_LOOP ( 'NONE', ( #24732, #28494, #6085, #21427, #18977, #32060, #37908, #36983, #10746, #41345, #6951, #16594, #7480 ) ) ;
#41559=VERTEX_POINT ( 'NONE', #48694 ) ;
#41561=CARTESIAN_POINT ( 'NONE',  ( -2.721590468760166193, 1.571075366034202947, -1.145417842932506147 ) ) ;
#41563=EDGE_CURVE ( 'NONE', #20029, #33804, #16031, .T. ) ;
#41564=DIRECTION ( 'NONE',  ( -0.9998717552508121775, -0.01601477604151182663, 0.000000000000000000 ) ) ;
#41565=ORIENTED_EDGE ( 'NONE', *, *, #38901, .T. ) ;
#41566=ORIENTED_EDGE ( 'NONE', *, *, #39082, .F. ) ;
#41569=CARTESIAN_POINT ( 'NONE',  ( -0.3382312733057311060, 1.205361022782829114E-17, -2.139420919314970693 ) ) ;
#41570=AXIS2_PLACEMENT_3D ( 'NONE', #31273, #27375, #35904 ) ;
#41572=AXIS2_PLACEMENT_3D ( 'NONE', #24192, #24956, #5078 ) ;
#41574=EDGE_CURVE ( 'NONE', #23260, #33703, #36349, .T. ) ;
#41576=CARTESIAN_POINT ( 'NONE',  ( -0.5440951526915226433, 1.699187271209207983, -2.156468654116168171 ) ) ;
#41579=DIRECTION ( 'NONE',  ( 0.000000000000000000, -1.000000000000000000, 0.000000000000000000 ) ) ;
#41580=EDGE_CURVE ( 'NONE', #33697, #37057, #45548, .T. ) ;
#41585=FACE_OUTER_BOUND ( 'NONE', #8260, .T. ) ;
#41591=B_SPLINE_CURVE_WITH_KNOTS ( 'NONE', 3,
 ( #9121, #1376, #14016, #48577 ),
 .UNSPECIFIED., .F., .F.,
 ( 4, 4 ),
 ( 0.1211775127643062860, 0.1625894504277921315 ),
 .UNSPECIFIED. ) ;
#41594=EDGE_CURVE ( 'NONE', #20385, #47699, #36110, .T. ) ;
#41601=B_SPLINE_CURVE_WITH_KNOTS ( 'NONE', 3,
 ( #7997, #35628, #30742, #39498 ),
 .UNSPECIFIED., .F., .F.,
 ( 4, 4 ),
 ( 0.04362072447804023201, 0.06160699411348036225 ),
 .UNSPECIFIED. ) ;
#41602=PLANE ( 'NONE',  #46926 ) ;
#41604=ADVANCED_FACE ( 'NONE', ( #4868 ), #31989, .T. ) ;
#41606=ORIENTED_EDGE ( 'NONE', *, *, #43979, .T. ) ;
#41609=PLANE ( 'NONE',  #30264 ) ;
#41612=B_SPLINE_CURVE_WITH_KNOTS ( 'NONE', 3,
 ( #6954, #23444, #42816, #11832 ),
 .UNSPECIFIED., .F., .F.,
 ( 4, 4 ),
 ( 2.766355543619157244E-07, 0.002500607986718841793 ),
 .UNSPECIFIED. ) ;
#41613=VERTEX_POINT ( 'NONE', #28089 ) ;
#41616=DIRECTION ( 'NONE',  ( 0.000000000000000000, -1.000000000000000000, -0.000000000000000000 ) ) ;
#41623=ORIENTED_EDGE ( 'NONE', *, *, #13449, .T. ) ;
#41625=CARTESIAN_POINT ( 'NONE',  ( 0.3546377434558362074, 1.615156926475952881, 2.229828021450985798 ) ) ;
#41626=CARTESIAN_POINT ( 'NONE',  ( 2.043634885149959501, 1.574803149606302854, 0.7157624142946232837 ) ) ;
#41627=CARTESIAN_POINT ( 'NONE',  ( 0.7516222819726512405, 1.687132160473688636, 2.142747677857361310 ) ) ;
#41628=ORIENTED_EDGE ( 'NONE', *, *, #19843, .F. ) ;
#41630=LINE ( 'NONE', #18137, #47303 ) ;
#41639=ORIENTED_EDGE ( 'NONE', *, *, #45617, .F. ) ;
#41640=AXIS2_PLACEMENT_3D ( 'NONE', #9058, #1570, #13956 ) ;
#41644=VECTOR ( 'NONE', #39985, 39.37007874015748143 ) ;
#41646=CIRCLE ( 'NONE', #7001, 2.246510896728926010 ) ;
#41649=DIRECTION ( 'NONE',  ( -1.288287287306305283E-16, 1.000000000000000000, 0.000000000000000000 ) ) ;
#41650=DIRECTION ( 'NONE',  ( 0.000000000000000000, 0.000000000000000000, 1.000000000000000000 ) ) ;
#41651=ORIENTED_EDGE ( 'NONE', *, *, #29575, .T. ) ;
#41654=ORIENTED_EDGE ( 'NONE', *, *, #45617, .T. ) ;
#41657=ADVANCED_FACE ( 'NONE', ( #6649 ), #26508, .T. ) ;
#41658=ORIENTED_EDGE ( 'NONE', *, *, #28715, .F. ) ;
#41661=ADVANCED_FACE ( 'NONE', ( #29377 ), #1445, .F. ) ;
#41665=ORIENTED_EDGE ( 'NONE', *, *, #43252, .T. ) ;
#41678=CARTESIAN_POINT ( 'NONE',  ( 0.9845150457423212931, 0.000000000000000000, -1.438794182654551390 ) ) ;
#41682=VECTOR ( 'NONE', #34777, 39.37007874015748143 ) ;
#41684=AXIS2_PLACEMENT_3D ( 'NONE', #7255, #30495, #34621 ) ;
#41694=DIRECTION ( 'NONE',  ( 0.9839295885986321100, 1.288287287306305037E-16, -0.1785568947986229116 ) ) ;
#41699=CARTESIAN_POINT ( 'NONE',  ( 1.174087487603958202, -2.119814714969965171E-16, 1.869141625116386818 ) ) ;
#41702=EDGE_CURVE ( 'NONE', #36271, #23504, #12939, .T. ) ;
#41704=CARTESIAN_POINT ( 'NONE',  ( 0.000000000000000000, 0.000000000000000000, 0.000000000000000000 ) ) ;
#41705=VERTEX_POINT ( 'NONE', #34021 ) ;
#41706=EDGE_CURVE ( 'NONE', #45979, #24001, #10012, .T. ) ;
#41707=CARTESIAN_POINT ( 'NONE',  ( 2.074049943651431693, 6.692913385826772199, 0.6221544894624241318 ) ) ;
#41710=ORIENTED_EDGE ( 'NONE', *, *, #34010, .T. ) ;
#41717=DIRECTION ( 'NONE',  ( 0.000000000000000000, 0.000000000000000000, 1.000000000000000000 ) ) ;
#41719=VECTOR ( 'NONE', #41717, 39.37007874015748143 ) ;
#41720=VERTEX_POINT ( 'NONE', #6137 ) ;
#41725=CARTESIAN_POINT ( 'NONE',  ( 0.08139965876239094178, 1.610780518492231694, 0.000000000000000000 ) ) ;
#41727=EDGE_CURVE ( 'NONE', #50444, #42699, #49964, .T. ) ;
#41732=ORIENTED_EDGE ( 'NONE', *, *, #49862, .T. ) ;
#41735=DIRECTION ( 'NONE',  ( -0.9998717552508122886, -0.01601477604151180928, 0.000000000000000000 ) ) ;
#41737=CARTESIAN_POINT ( 'NONE',  ( -1.428156070725274951, 1.693047415430531721, 2.294380806141768758 ) ) ;
#41741=ORIENTED_EDGE ( 'NONE', *, *, #1851, .T. ) ;
#41743=ORIENTED_EDGE ( 'NONE', *, *, #826, .T. ) ;
#41744=ORIENTED_EDGE ( 'NONE', *, *, #24420, .F. ) ;
#41749=VECTOR ( 'NONE', #44925, 39.37007874015748854 ) ;
#41759=CARTESIAN_POINT ( 'NONE',  ( -1.281152772984899713, 5.905511811023623991, -2.660341145381166506 ) ) ;
#41762=CARTESIAN_POINT ( 'NONE',  ( 0.5344736634771639627, 1.625426382409501436, 2.669579653780858930 ) ) ;
#41764=CARTESIAN_POINT ( 'NONE',  ( 2.951990591674675368, 1.765258879000601855, -0.08331184815398361143 ) ) ;
#41765=FACE_OUTER_BOUND ( 'NONE', #6235, .T. ) ;
#41766=ADVANCED_FACE ( 'NONE', ( #1748 ), #4728, .T. ) ;
#41771=ORIENTED_EDGE ( 'NONE', *, *, #47020, .F. ) ;
#41774=B_SPLINE_CURVE_WITH_KNOTS ( 'NONE', 3,
 ( #42224, #22866, #46577, #2738 ),
 .UNSPECIFIED., .F., .F.,
 ( 4, 4 ),
 ( 7.087756405766085514E-05, 0.002570929063738525318 ),
 .UNSPECIFIED. ) ;
#41775=DIRECTION ( 'NONE',  ( -0.8345732537212999791, 0.000000000000000000, -0.5508969814521065267 ) ) ;
#41781=LINE ( 'NONE', #2794, #26749 ) ;
#41784=ORIENTED_EDGE ( 'NONE', *, *, #12405, .F. ) ;
#41787=AXIS2_PLACEMENT_3D ( 'NONE', #13886, #34525, #27264 ) ;
#41790=DIRECTION ( 'NONE',  ( -0.000000000000000000, 1.000000000000000000, -0.000000000000000000 ) ) ;
#41798=EDGE_CURVE ( 'NONE', #44322, #42262, #50447, .T. ) ;
#41800=B_SPLINE_CURVE_WITH_KNOTS ( 'NONE', 3,
 ( #25771, #33541, #21649, #48459 ),
 .UNSPECIFIED., .F., .F.,
 ( 4, 4 ),
 ( 2.558223237824230539E-07, 0.002500373809894031792 ),
 .UNSPECIFIED. ) ;
#41804=CARTESIAN_POINT ( 'NONE',  ( 0.2156685157584260770, 1.624173731825095723, -2.945280361644574185 ) ) ;
#41807=EDGE_CURVE ( 'NONE', #25781, #6769, #15399, .T. ) ;
#41808=CARTESIAN_POINT ( 'NONE',  ( 0.9432913529151772947, 1.723010488186151878, -2.072188145589165753 ) ) ;
#41810=VERTEX_POINT ( 'NONE', #31664 ) ;
#41812=DIRECTION ( 'NONE',  ( 0.000000000000000000, 0.000000000000000000, 1.000000000000000000 ) ) ;
#41814=EDGE_CURVE ( 'NONE', #27359, #50834, #12038, .T. ) ;
#41815=ORIENTED_EDGE ( 'NONE', *, *, #28855, .F. ) ;
#41818=EDGE_CURVE ( 'NONE', #29455, #41810, #38814, .T. ) ;
#41824=CARTESIAN_POINT ( 'NONE',  ( -1.477691947303356290, 1.684234009953186728, 1.616556376299586706 ) ) ;
#41827=CARTESIAN_POINT ( 'NONE',  ( -0.8192648851572477131, 1.600279018255590158, 2.322980749500460185 ) ) ;
#41829=CARTESIAN_POINT ( 'NONE',  ( 1.785493683324574254, 0.000000000000000000, -1.119626681005672530 ) ) ;
#41831=CARTESIAN_POINT ( 'NONE',  ( -0.2627480064045953911, 0.000000000000000000, 1.723473835155032274 ) ) ;
#41832=CARTESIAN_POINT ( 'NONE',  ( 0.000000000000000000, 1.574803149606302854, 0.000000000000000000 ) ) ;
#41833=EDGE_CURVE ( 'NONE', #42163, #1464, #27087, .T. ) ;
#41835=EDGE_CURVE ( 'NONE', #31188, #21069, #24639, .T. ) ;
#41841=ORIENTED_EDGE ( 'NONE', *, *, #47110, .F. ) ;
#41851=EDGE_CURVE ( 'NONE', #47418, #50807, #6389, .T. ) ;
#41853=VERTEX_POINT ( 'NONE', #11281 ) ;
#41854=DIRECTION ( 'NONE',  ( -5.207613805427244364E-18, -1.000000000000000000, -1.159565308550900415E-16 ) ) ;
#41856=VERTEX_POINT ( 'NONE', #18772 ) ;
#41860=DIRECTION ( 'NONE',  ( -0.4738686624730094055, 0.000000000000000000, 0.8805955318567321166 ) ) ;
#41861=AXIS2_PLACEMENT_3D ( 'NONE', #12917, #16789, #39760 ) ;
#41862=EDGE_CURVE ( 'NONE', #39550, #25006, #7407, .T. ) ;
#41864=ADVANCED_FACE ( 'NONE', ( #39149 ), #38564, .T. ) ;
#41867=FACE_OUTER_BOUND ( 'NONE', #47133, .T. ) ;
#41869=VERTEX_POINT ( 'NONE', #3785 ) ;
#41871=DIRECTION ( 'NONE',  ( -0.000000000000000000, -1.000000000000000000, -0.000000000000000000 ) ) ;
#41872=FACE_OUTER_BOUND ( 'NONE', #28887, .T. ) ;
#41875=ORIENTED_EDGE ( 'NONE', *, *, #45770, .T. ) ;
#41879=CARTESIAN_POINT ( 'NONE',  ( -1.977157105026591699, 1.676234161373136189, -0.8985969286390745880 ) ) ;
#41881=CARTESIAN_POINT ( 'NONE',  ( 1.950008968278537091, -1.129616514605691021E-16, 0.9934589848971179249 ) ) ;
#41883=ORIENTED_EDGE ( 'NONE', *, *, #6, .T. ) ;
#41894=DIRECTION ( 'NONE',  ( -3.986037398843765983E-20, -1.000000000000000000, -1.160734090543304660E-16 ) ) ;
#41895=VERTEX_POINT ( 'NONE', #24174 ) ;
#41899=ORIENTED_EDGE ( 'NONE', *, *, #41376, .F. ) ;
#41905=AXIS2_PLACEMENT_3D ( 'NONE', #35783, #47868, #24164 ) ;
#41908=DIRECTION ( 'NONE',  ( 0.000000000000000000, -1.000000000000000000, -0.000000000000000000 ) ) ;
#41921=CARTESIAN_POINT ( 'NONE',  ( -1.022165783835742969, 1.604882761207047759, 2.770237110760823462 ) ) ;
#41923=ORIENTED_EDGE ( 'NONE', *, *, #14181, .T. ) ;
#41924=VERTEX_POINT ( 'NONE', #43772 ) ;
#41927=CARTESIAN_POINT ( 'NONE',  ( 0.000000000000000000, 1.574803149606302854, 0.000000000000000000 ) ) ;
#41929=PLANE ( 'NONE',  #5772 ) ;
#41940=CARTESIAN_POINT ( 'NONE',  ( 0.08139965876239094178, 1.610780518492231694, 0.000000000000000000 ) ) ;
#41941=CARTESIAN_POINT ( 'NONE',  ( -2.437180031585919782, 1.566133505135788750, -1.667735833703134274 ) ) ;
#41942=EDGE_CURVE ( 'NONE', #13750, #12775, #50992, .T. ) ;
#41944=DIRECTION ( 'NONE',  ( -0.9998717552508122886, -0.01601477604151180928, 0.000000000000000000 ) ) ;
#41946=CARTESIAN_POINT ( 'NONE',  ( 0.07982360342473591996, 1.709180471932028711, 0.000000000000000000 ) ) ;
#41959=EDGE_LOOP ( 'NONE', ( #22066, #4, #5426, #35179, #25723, #9277, #17496, #10503, #35701, #710, #45063 ) ) ;
#41960=CARTESIAN_POINT ( 'NONE',  ( 1.281152772984937682, 0.000000000000000000, -2.660341145381147854 ) ) ;
#41962=EDGE_CURVE ( 'NONE', #35465, #25743, #4808, .T. ) ;
#41964=ORIENTED_EDGE ( 'NONE', *, *, #23702, .F. ) ;
#41968=CARTESIAN_POINT ( 'NONE',  ( -1.738729679588005617, 0.000000000000000000, -0.1273486421340072894 ) ) ;
#41969=AXIS2_PLACEMENT_3D ( 'NONE', #47840, #24134, #4513 ) ;
#41977=AXIS2_PLACEMENT_3D ( 'NONE', #21546, #5798, #2684 ) ;
#41978=CIRCLE ( 'NONE', #8175, 2.246510896728926010 ) ;
#41984=CARTESIAN_POINT ( 'NONE',  ( 1.761907912426849521, 1.644691605102268195, 2.091464020505111154 ) ) ;
#41985=CARTESIAN_POINT ( 'NONE',  ( -1.676283831994445306, 0.001070912127414903967, 0.4929124452910598198 ) ) ;
#41986=LINE ( 'NONE', #17289, #7084 ) ;
#41987=AXIS2_PLACEMENT_3D ( 'NONE', #49353, #25138, #14026 ) ;
#41990=ORIENTED_EDGE ( 'NONE', *, *, #31451, .F. ) ;
#41997=EDGE_LOOP ( 'NONE', ( #3663, #17805, #3056, #48180 ) ) ;
#41998=ORIENTED_EDGE ( 'NONE', *, *, #36119, .F. ) ;
#42011=CARTESIAN_POINT ( 'NONE',  ( 1.243905582186644043, 1.632961070568905715, 2.177897092110659294 ) ) ;
#42015=DIRECTION ( 'NONE',  ( -0.000000000000000000, -1.000000000000000000, -0.000000000000000000 ) ) ;
#42022=CARTESIAN_POINT ( 'NONE',  ( 2.074049943651431693, 6.692913385826772199, 0.6221544894624241318 ) ) ;
#42025=CARTESIAN_POINT ( 'NONE',  ( -1.002140947543763705, 1.626234033651570821, -1.967543651896755508 ) ) ;
#42027=ORIENTED_EDGE ( 'NONE', *, *, #21898, .F. ) ;
#42029=ORIENTED_EDGE ( 'NONE', *, *, #48495, .F. ) ;
#42031=CARTESIAN_POINT ( 'NONE',  ( -1.312248418042854192, 6.692913385826772199, -1.722429524498108933 ) ) ;
#42037=CARTESIAN_POINT ( 'NONE',  ( 0.08139965876239094178, 1.610780518492231694, 0.000000000000000000 ) ) ;
#42038=ORIENTED_EDGE ( 'NONE', *, *, #25936, .T. ) ;
#42041=ORIENTED_EDGE ( 'NONE', *, *, #11922, .F. ) ;
#42050=ORIENTED_EDGE ( 'NONE', *, *, #49746, .F. ) ;
#42053=CARTESIAN_POINT ( 'NONE',  ( 0.1526763070133267952, 1.611922144458495687, -2.245379599360889600 ) ) ;
#42061=EDGE_CURVE ( 'NONE', #34736, #26467, #33469, .T. ) ;
#42064=DIRECTION ( 'NONE',  ( 0.000000000000000000, 0.000000000000000000, 1.000000000000000000 ) ) ;
#42068=ORIENTED_EDGE ( 'NONE', *, *, #10557, .F. ) ;
#42071=EDGE_CURVE ( 'NONE', #21408, #23810, #46716, .T. ) ;
#42076=CARTESIAN_POINT ( 'NONE',  ( 0.07982360342473591996, 1.709180471932028711, 0.000000000000000000 ) ) ;
#42080=CARTESIAN_POINT ( 'NONE',  ( -0.6087643519215788501, 1.702044864518692746, -2.390792234956752083 ) ) ;
#42082=AXIS2_PLACEMENT_3D ( 'NONE', #36869, #10194, #18707 ) ;
#42084=ADVANCED_FACE ( 'NONE', ( #49406 ), #3949, .T. ) ;
#42088=CARTESIAN_POINT ( 'NONE',  ( -0.2483604914213126402, 1.519985912000072936, -2.942338030579628061 ) ) ;
#42091=EDGE_CURVE ( 'NONE', #20029, #46385, #37542, .T. ) ;
#42093=DIRECTION ( 'NONE',  ( -0.9749279121818227312, 0.000000000000000000, -0.2225209339563184452 ) ) ;
#42094=VERTEX_POINT ( 'NONE', #33722 ) ;
#42095=VERTEX_POINT ( 'NONE', #37076 ) ;
#42099=CARTESIAN_POINT ( 'NONE',  ( 0.8446807076687119498, 1.721431058233622746, 2.110586427442081803 ) ) ;
#42104=CARTESIAN_POINT ( 'NONE',  ( -2.152441353505195387, 0.000000000000000000, -0.2419059403265113872 ) ) ;
#42105=CARTESIAN_POINT ( 'NONE',  ( 0.04921259842519667971, 1.708690180665275005, 2.244725876464058523 ) ) ;
#42109=VECTOR ( 'NONE', #6402, 39.37007874015748854 ) ;
#42112=DIRECTION ( 'NONE',  ( -0.01601477604151182663, 0.9998717552508123996, -0.000000000000000000 ) ) ;
#42114=ADVANCED_FACE ( 'NONE', ( #10463 ), #29832, .T. ) ;
#42117=ORIENTED_EDGE ( 'NONE', *, *, #29274, .F. ) ;
#42120=ORIENTED_EDGE ( 'NONE', *, *, #37064, .F. ) ;
#42129=CARTESIAN_POINT ( 'NONE',  ( -0.8329809839909438907, 1.607838722253305486, -2.833254665166566877 ) ) ;
#42131=PLANE ( 'NONE',  #29075 ) ;
#42132=LINE ( 'NONE', #23023, #46543 ) ;
#42133=ADVANCED_FACE ( 'NONE', ( #1951 ), #4762, .T. ) ;
#42134=DIRECTION ( 'NONE',  ( 0.000000000000000000, 1.160734090543304660E-16, -1.000000000000000000 ) ) ;
#42141=EDGE_CURVE ( 'NONE', #25262, #41036, #30758, .T. ) ;
#42143=EDGE_LOOP ( 'NONE', ( #41741, #47680, #13772, #17768 ) ) ;
#42155=ORIENTED_EDGE ( 'NONE', *, *, #43252, .F. ) ;
#42157=EDGE_CURVE ( 'NONE', #975, #29609, #33635, .T. ) ;
#42162=ORIENTED_EDGE ( 'NONE', *, *, #40432, .F. ) ;
#42163=VERTEX_POINT ( 'NONE', #46553 ) ;
#42168=CARTESIAN_POINT ( 'NONE',  ( -0.3465944589516558594, -2.479472480830696451E-16, 2.185505870675810147 ) ) ;
#42179=CARTESIAN_POINT ( 'NONE',  ( 0.08139965876239094178, 1.610780518492231694, 0.000000000000000000 ) ) ;
#42183=ORIENTED_EDGE ( 'NONE', *, *, #28940, .F. ) ;
#42184=CARTESIAN_POINT ( 'NONE',  ( 0.1155636338427008941, -0.5222242541845523167, 0.000000000000000000 ) ) ;
#42187=FACE_OUTER_BOUND ( 'NONE', #6875, .T. ) ;
#42191=VERTEX_POINT ( 'NONE', #31097 ) ;
#42197=EDGE_CURVE ( 'NONE', #1553, #37294, #21524, .T. ) ;
#42198=CARTESIAN_POINT ( 'NONE',  ( -1.500384104969938459, 1.597432260198647480, 2.543203506735845831 ) ) ;
#42201=ORIENTED_EDGE ( 'NONE', *, *, #38424, .T. ) ;
#42204=VERTEX_POINT ( 'NONE', #22585 ) ;
#42206=EDGE_CURVE ( 'NONE', #44848, #2534, #9182, .T. ) ;
#42208=ORIENTED_EDGE ( 'NONE', *, *, #10921, .F. ) ;
#42213=CARTESIAN_POINT ( 'NONE',  ( -1.977157105026591699, 1.676234161373136189, -0.8985969286390745880 ) ) ;
#42215=CARTESIAN_POINT ( 'NONE',  ( 1.695772546416037807, 5.905511811023623991, -2.417756147381349141 ) ) ;
#42218=CONICAL_SURFACE ( 'NONE', #3457, 2.244934639244524632, 1.554780866114618743 ) ;
#42224=CARTESIAN_POINT ( 'NONE',  ( 2.150824344285287459, 1.742351338968239238, -0.8657870173518766865 ) ) ;
#42228=ADVANCED_FACE ( 'NONE', ( #39342 ), #39399, .T. ) ;
#42230=DIRECTION ( 'NONE',  ( 0.01601477604151182663, -0.9998717552508123996, 0.000000000000000000 ) ) ;
#42235=CARTESIAN_POINT ( 'NONE',  ( -2.708693778673423758, 1.578604444535609108, -1.175591149347226194 ) ) ;
#42236=EDGE_CURVE ( 'NONE', #48626, #30224, #18415, .T. ) ;
#42242=ORIENTED_EDGE ( 'NONE', *, *, #23933, .F. ) ;
#42245=CARTESIAN_POINT ( 'NONE',  ( -2.164823134740036181, 1.574803149606301966, 0.000000000000000000 ) ) ;
#42248=AXIS2_PLACEMENT_3D ( 'NONE', #18883, #18634, #50813 ) ;
#42249=( BOUNDED_CURVE ( )  B_SPLINE_CURVE ( 3, ( #6805, #18687, #42420, #7063 ),
 .UNSPECIFIED., .F., .F. ) 
 B_SPLINE_CURVE_WITH_KNOTS ( ( 4, 4 ),
 ( 5.231528604247587033, 5.282403893493373026 ),
 .UNSPECIFIED. ) 
 CURVE ( )  GEOMETRIC_REPRESENTATION_ITEM ( )  RATIONAL_B_SPLINE_CURVE ( ( 1.000000000000000000, 0.9997843203757749153, 0.9997843203757749153, 1.000000000000000000 ) ) 
 REPRESENTATION_ITEM ( '' )  );
#42250=CARTESIAN_POINT ( 'NONE',  ( -1.152568299495734694, 6.692913385826772199, 1.833124570921535801 ) ) ;
#42251=CONICAL_SURFACE ( 'NONE', #32365, 1.850107469027523210, 0.6386652850508578450 ) ;
#42252=DIRECTION ( 'NONE',  ( 0.000000000000000000, 0.000000000000000000, 1.000000000000000000 ) ) ;
#42259=CARTESIAN_POINT ( 'NONE',  ( 1.625502936149584077, 0.000000000000000000, 1.317350029429052771 ) ) ;
#42262=VERTEX_POINT ( 'NONE', #43197 ) ;
#42280=ORIENTED_EDGE ( 'NONE', *, *, #24751, .T. ) ;
#42285=VERTEX_POINT ( 'NONE', #26455 ) ;
#42287=EDGE_CURVE ( 'NONE', #30224, #17224, #584, .T. ) ;
#42288=CARTESIAN_POINT ( 'NONE',  ( 0.8949303405208902662, 6.692913385826772199, -1.971765468592529880 ) ) ;
#42289=ORIENTED_EDGE ( 'NONE', *, *, #48756, .F. ) ;
#42295=VERTEX_POINT ( 'NONE', #5246 ) ;
#42296=VERTEX_POINT ( 'NONE', #24621 ) ;
#42297=EDGE_CURVE ( 'NONE', #20924, #344, #93, .T. ) ;
#42298=CYLINDRICAL_SURFACE ( 'NONE', #7547, 2.164630168518208109 ) ;
#42300=VERTEX_POINT ( 'NONE', #27970 ) ;
#42306=B_SPLINE_CURVE_WITH_KNOTS ( 'NONE', 3,
 ( #14461, #30205, #45925, #10590 ),
 .UNSPECIFIED., .F., .F.,
 ( 4, 4 ),
 ( 2.137724770886416802E-07, 0.002500774150297437569 ),
 .UNSPECIFIED. ) ;
#42309=DIRECTION ( 'NONE',  ( -0.000000000000000000, -1.000000000000000000, -0.000000000000000000 ) ) ;
#42310=ORIENTED_EDGE ( 'NONE', *, *, #13681, .F. ) ;
#42317=EDGE_LOOP ( 'NONE', ( #24779, #2564, #10291, #33765 ) ) ;
#42320=LINE ( 'NONE', #6965, #29931 ) ;
#42321=CARTESIAN_POINT ( 'NONE',  ( 0.1155636338427008941, -0.5222242541845523167, 0.000000000000000000 ) ) ;
#42322=CARTESIAN_POINT ( 'NONE',  ( 2.164658444855302122, 5.905511811023623991, -0.04795272066889885720 ) ) ;
#42323=CARTESIAN_POINT ( 'NONE',  ( 1.372667653987894809, 0.000000000000000000, 1.546304799276380981 ) ) ;
#42326=ADVANCED_FACE ( 'NONE', ( #613 ), #48325, .F. ) ;
#42328=DIRECTION ( 'NONE',  ( 0.000000000000000000, -0.000000000000000000, 1.000000000000000000 ) ) ;
#42335=VERTEX_POINT ( 'NONE', #36246 ) ;
#42336=CARTESIAN_POINT ( 'NONE',  ( 1.068075307999459822, 6.692913385826772199, 1.883606783264653028 ) ) ;
#42337=VECTOR ( 'NONE', #37395, 39.37007874015748854 ) ;
#42338=CARTESIAN_POINT ( 'NONE',  ( 0.8314045656493375125, 1.724861346829795750, 2.355326812497060107 ) ) ;
#42340=EDGE_CURVE ( 'NONE', #30098, #39633, #8612, .T. ) ;
#42351=ORIENTED_EDGE ( 'NONE', *, *, #14442, .F. ) ;
#42354=CARTESIAN_POINT ( 'NONE',  ( 1.325491792074624087, 1.641458297549746037, -2.638988599164732385 ) ) ;
#42358=CARTESIAN_POINT ( 'NONE',  ( 2.808237744965994320, 5.905511811023623991, 0.9124517550441686442 ) ) ;
#42359=PLANE ( 'NONE',  #36560 ) ;
#42361=ORIENTED_EDGE ( 'NONE', *, *, #11485, .F. ) ;
#42363=VECTOR ( 'NONE', #27443, 39.37007874015748143 ) ;
#42364=AXIS2_PLACEMENT_3D ( 'NONE', #24682, #4038, #31926 ) ;
#42370=AXIS2_PLACEMENT_3D ( 'NONE', #26832, #43075, #19839 ) ;
#42379=ORIENTED_EDGE ( 'NONE', *, *, #38114, .T. ) ;
#42382=CARTESIAN_POINT ( 'NONE',  ( 2.138649790787681138, 0.000000000000000000, -0.1124749717369803448 ) ) ;
#42386=CARTESIAN_POINT ( 'NONE',  ( 2.437180031585944207, 1.658768335924418080, -1.667735833703099191 ) ) ;
#42389=DIRECTION ( 'NONE',  ( -0.9998717552508122886, -0.01601477604151181275, 0.000000000000000000 ) ) ;
#42393=CARTESIAN_POINT ( 'NONE',  ( -0.7145799201509080989, 6.692913385826772199, 2.044048657746648789 ) ) ;
#42396=ORIENTED_EDGE ( 'NONE', *, *, #29572, .T. ) ;
#42397=EDGE_CURVE ( 'NONE', #17674, #2006, #47558, .T. ) ;
#42399=AXIS2_PLACEMENT_3D ( 'NONE', #14829, #30576, #48307 ) ;
#42408=CIRCLE ( 'NONE', #39952, 2.164630168518208109 ) ;
#42409=CARTESIAN_POINT ( 'NONE',  ( -1.772999178993743152, 5.118110236220475784, -1.009977129983215427 ) ) ;
#42415=ORIENTED_EDGE ( 'NONE', *, *, #48601, .T. ) ;
#42420=CARTESIAN_POINT ( 'NONE',  ( 1.219713223144859748, 0.000000000000000000, -1.650995057222538254 ) ) ;
#42421=CARTESIAN_POINT ( 'NONE',  ( 1.958513403246152640, 1.640845930445798073, -1.233835998176425308 ) ) ;
#42423=B_SPLINE_CURVE_WITH_KNOTS ( 'NONE', 3,
 ( #5930, #17807, #41555, #14184 ),
 .UNSPECIFIED., .F., .F.,
 ( 4, 4 ),
 ( 3.460281517023109080E-07, 0.04793831677642486355 ),
 .UNSPECIFIED. ) ;
#42426=CARTESIAN_POINT ( 'NONE',  ( 0.1067246931122726866, 0.02962905676920215767, 0.000000000000000000 ) ) ;
#42428=EDGE_CURVE ( 'NONE', #28289, #6369, #48828, .T. ) ;
#42429=CARTESIAN_POINT ( 'NONE',  ( 1.599172890215259546, 0.000000000000000000, 1.460879300779193590 ) ) ;
#42432=DIRECTION ( 'NONE',  ( -0.000000000000000000, -1.000000000000000000, -0.000000000000000000 ) ) ;
#42433=B_SPLINE_CURVE_WITH_KNOTS ( 'NONE', 3,
 ( #23159, #33794, #14408, #42533 ),
 .UNSPECIFIED., .F., .F.,
 ( 4, 4 ),
 ( 0.01179318187808457187, 0.03073709326239987966 ),
 .UNSPECIFIED. ) ;
#42440=EDGE_CURVE ( 'NONE', #30165, #18246, #45164, .T. ) ;
#42441=CARTESIAN_POINT ( 'NONE',  ( -1.738955188402737440, 0.000000000000000000, -0.1273587697465547175 ) ) ;
#42446=ADVANCED_FACE ( 'NONE', ( #17381 ), #22131, .T. ) ;
#42447=VECTOR ( 'NONE', #44417, 39.37007874015748143 ) ;
#42448=ORIENTED_EDGE ( 'NONE', *, *, #7192, .T. ) ;
#42450=CARTESIAN_POINT ( 'NONE',  ( -2.277873973731453727, 1.683757167080951245, 1.879489153247634992 ) ) ;
#42451=VECTOR ( 'NONE', #21023, 39.37007874015748143 ) ;
#42455=AXIS2_PLACEMENT_3D ( 'NONE', #34635, #7766, #39007 ) ;
#42459=ADVANCED_FACE ( 'NONE', ( #49342 ), #13512, .T. ) ;
#42463=CARTESIAN_POINT ( 'NONE',  ( -1.175769893759974538, 0.000000000000000000, 1.370616677507177972 ) ) ;
#42464=CARTESIAN_POINT ( 'NONE',  ( -1.547114303032252502, 1.584696887024839906, -1.547279266820049237 ) ) ;
#42466=DIRECTION ( 'NONE',  ( 2.866708903754509961E-17, 1.000000000000000000, -1.255987235303920130E-16 ) ) ;
#42469=VERTEX_POINT ( 'NONE', #10401 ) ;
#42471=ORIENTED_EDGE ( 'NONE', *, *, #45281, .F. ) ;
#42479=DIRECTION ( 'NONE',  ( 0.1785568947986229116, 0.000000000000000000, 0.9839295885986321100 ) ) ;
#42480=B_SPLINE_CURVE_WITH_KNOTS ( 'NONE', 3,
 ( #33137, #17126, #29506, #25373 ),
 .UNSPECIFIED., .F., .F.,
 ( 4, 4 ),
 ( 3.370817529537171183E-07, 0.05037949722401796615 ),
 .UNSPECIFIED. ) ;
#42482=VECTOR ( 'NONE', #19334, 39.37007874015748143 ) ;
#42484=CARTESIAN_POINT ( 'NONE',  ( 0.5662636741187413447, 0.000000000000000000, 1.648861433446464186 ) ) ;
#42491=EDGE_CURVE ( 'NONE', #19150, #38271, #45450, .T. ) ;
#42492=CARTESIAN_POINT ( 'NONE',  ( 2.706338173250262269, 5.118110236220475784, -1.181102362204724310 ) ) ;
#42494=ORIENTED_EDGE ( 'NONE', *, *, #49675, .F. ) ;
#42495=DIRECTION ( 'NONE',  ( -0.9998717552508121775, -0.01601477604151182316, 0.000000000000000000 ) ) ;
#42498=EDGE_CURVE ( 'NONE', #2006, #970, #40878, .T. ) ;
#42503=CARTESIAN_POINT ( 'NONE',  ( 0.5544985201248122664, 1.716783259433079856, -2.194164409418295048 ) ) ;
#42504=B_SPLINE_CURVE_WITH_KNOTS ( 'NONE', 3,
 ( #46593, #38636, #11512, #27246 ),
 .UNSPECIFIED., .F., .F.,
 ( 4, 4 ),
 ( 0.1211775127643062860, 0.1625894504277921315 ),
 .UNSPECIFIED. ) ;
#42505=B_SPLINE_CURVE_WITH_KNOTS ( 'NONE', 3,
 ( #37533, #9900, #2153, #33662 ),
 .UNSPECIFIED., .F., .F.,
 ( 4, 4 ),
 ( 2.471499816278681188E-07, 0.002500687884645799025 ),
 .UNSPECIFIED. ) ;
#42506=CARTESIAN_POINT ( 'NONE',  ( -2.793030215715272213, 1.577298709702483093, 0.9592557174602283077 ) ) ;
#42510=DIRECTION ( 'NONE',  ( 0.01601477604151182663, -0.9998717552508123996, 0.000000000000000000 ) ) ;
#42511=CARTESIAN_POINT ( 'NONE',  ( 1.645881266606342708, 1.741324525431280135, -2.181635745336127474 ) ) ;
#42512=AXIS2_PLACEMENT_3D ( 'NONE', #15538, #46984, #11656 ) ;
#42513=ORIENTED_EDGE ( 'NONE', *, *, #24296, .T. ) ;
#42514=DIRECTION ( 'NONE',  ( -3.986037398843765983E-20, -1.000000000000000000, -1.160734090543304660E-16 ) ) ;
#42515=CARTESIAN_POINT ( 'NONE',  ( -1.780101451746625152, 0.000000000000000000, 1.234002060668493828 ) ) ;
#42525=CIRCLE ( 'NONE', #26023, 2.164630168518208109 ) ;
#42529=AXIS2_PLACEMENT_3D ( 'NONE', #2426, #22299, #18168 ) ;
#42533=CARTESIAN_POINT ( 'NONE',  ( -1.325491792074585451, 1.698604322780517650, -2.638988599164751481 ) ) ;
#42535=DIRECTION ( 'NONE',  ( -0.9998717552508122886, -0.01601477604151185785, 0.000000000000000000 ) ) ;
#42537=CARTESIAN_POINT ( 'NONE',  ( 2.151809081513405442, 6.692913385826772199, 0.2418202932658665705 ) ) ;
#42538=ORIENTED_EDGE ( 'NONE', *, *, #37474, .T. ) ;
#42541=ORIENTED_EDGE ( 'NONE', *, *, #27058, .F. ) ;
#42542=CYLINDRICAL_SURFACE ( 'NONE', #37816, 2.164630168518208109 ) ;
#42549=VECTOR ( 'NONE', #47747, 39.37007874015748143 ) ;
#42558=VECTOR ( 'NONE', #34187, 39.37007874015748143 ) ;
#42560=EDGE_CURVE ( 'NONE', #11282, #23897, #21276, .T. ) ;
#42563=VERTEX_POINT ( 'NONE', #34405 ) ;
#42564=CARTESIAN_POINT ( 'NONE',  ( -0.6233543567505162031, 1.574803149606302854, -2.073689640095379705 ) ) ;
#42572=CARTESIAN_POINT ( 'NONE',  ( 0.08119777152254364916, 1.623385212329073957, 0.000000000000000000 ) ) ;
#42575=EDGE_LOOP ( 'NONE', ( #30349, #31954, #1669, #49305 ) ) ;
#42577=CARTESIAN_POINT ( 'NONE',  ( -2.947574761915765063, 1.673315526576397261, -0.1816379373805333819 ) ) ;
#42578=CARTESIAN_POINT ( 'NONE',  ( -2.946551303128973842, 1.574890269766889617, -0.1815919737934194866 ) ) ;
#42580=FACE_OUTER_BOUND ( 'NONE', #40998, .T. ) ;
#42581=CARTESIAN_POINT ( 'NONE',  ( 0.04921259842519689481, 0.000000000000000000, 1.742692369722729895 ) ) ;
#42584=LINE ( 'NONE', #225, #16851 ) ;
#42587=AXIS2_PLACEMENT_3D ( 'NONE', #41007, #26262, #22142 ) ;
#42594=DIRECTION ( 'NONE',  ( 1.160706738777435820E-16, 1.000000000000000000, 5.589669052740852391E-17 ) ) ;
#42602=DIRECTION ( 'NONE',  ( 0.2225209339563041788, -1.160734090543304660E-16, 0.9749279121818259508 ) ) ;
#42609=DIRECTION ( 'NONE',  ( 0.9998717552508121775, 0.01601477604151182663, 0.000000000000000000 ) ) ;
#42614=CONICAL_SURFACE ( 'NONE', #29436, 1.850107469027523210, 0.6386652850508578450 ) ;
#42616=DIRECTION ( 'NONE',  ( 0.000000000000000000, 0.000000000000000000, 1.000000000000000000 ) ) ;
#42621=ORIENTED_EDGE ( 'NONE', *, *, #2423, .T. ) ;
#42624=DIRECTION ( 'NONE',  ( -0.000000000000000000, 1.000000000000000000, -0.000000000000000000 ) ) ;
#42627=CARTESIAN_POINT ( 'NONE',  ( -2.010517631316633747, 1.205361022782829114E-17, 0.8058170502102087740 ) ) ;
#42628=ORIENTED_EDGE ( 'NONE', *, *, #31167, .T. ) ;
#42630=CARTESIAN_POINT ( 'NONE',  ( 2.100190309385009169, 1.205361022782829114E-17, 0.5298329251847523347 ) ) ;
#42631=DIRECTION ( 'NONE',  ( 0.000000000000000000, 0.000000000000000000, 1.000000000000000000 ) ) ;
#42633=ORIENTED_EDGE ( 'NONE', *, *, #21188, .T. ) ;
#42635=CARTESIAN_POINT ( 'NONE',  ( -2.867773316779185677, 1.574658946938755522, -0.7050287376752426560 ) ) ;
#42638=CARTESIAN_POINT ( 'NONE',  ( -0.2783729501556720387, 0.02346101323895649626, 1.809574371873096110 ) ) ;
#42647=DIRECTION ( 'NONE',  ( -3.986037398843765983E-20, -1.000000000000000000, -1.160734090543304660E-16 ) ) ;
#42648=CARTESIAN_POINT ( 'NONE',  ( 0.5762653268100312864, 0.000000000000000000, -1.903066372058335620 ) ) ;
#42650=ORIENTED_EDGE ( 'NONE', *, *, #31422, .F. ) ;
#42653=AXIS2_PLACEMENT_3D ( 'NONE', #18719, #50157, #30337 ) ;
#42658=EDGE_CURVE ( 'NONE', #44522, #14656, #15514, .T. ) ;
#42659=ORIENTED_EDGE ( 'NONE', *, *, #37764, .T. ) ;
#42660=DIRECTION ( 'NONE',  ( -0.000000000000000000, 1.000000000000000000, -0.000000000000000000 ) ) ;
#42662=CARTESIAN_POINT ( 'NONE',  ( 2.158170387640339527, -2.691217175373896062E-17, 0.2426819907294796574 ) ) ;
#42663=VERTEX_POINT ( 'NONE', #31029 ) ;
#42680=FACE_OUTER_BOUND ( 'NONE', #6439, .T. ) ;
#42682=ORIENTED_EDGE ( 'NONE', *, *, #12605, .T. ) ;
#42689=EDGE_CURVE ( 'NONE', #50201, #2264, #47247, .T. ) ;
#42690=DIRECTION ( 'NONE',  ( 0.9998717552508121775, 0.01601477604151182663, 0.000000000000000000 ) ) ;
#42694=DIRECTION ( 'NONE',  ( -0.9998717552508122886, -0.01601477604151182316, 0.000000000000000000 ) ) ;
#42699=VERTEX_POINT ( 'NONE', #25004 ) ;
#42703=AXIS2_PLACEMENT_3D ( 'NONE', #18825, #22950, #46661 ) ;
#42713=CARTESIAN_POINT ( 'NONE',  ( 1.561199273709754642, 0.01720004865961270724, 1.307960151495090262 ) ) ;
#42714=FACE_OUTER_BOUND ( 'NONE', #4442, .T. ) ;
#42721=EDGE_LOOP ( 'NONE', ( #30075, #35807, #4769, #27628, #8922, #43759 ) ) ;
#42722=CARTESIAN_POINT ( 'NONE',  ( -0.4460728916448887249, 1.700757277111965449, 2.182451250484750638 ) ) ;
#42731=EDGE_CURVE ( 'NONE', #44818, #42300, #20792, .T. ) ;
#42735=FACE_OUTER_BOUND ( 'NONE', #4430, .T. ) ;
#42738=CIRCLE ( 'NONE', #46797, 2.165354330708661568 ) ;
#42741=CARTESIAN_POINT ( 'NONE',  ( 1.556712866041120247, 1.743522182421873401, 2.509548638715870084 ) ) ;
#42744=VERTEX_POINT ( 'NONE', #44359 ) ;
#42747=EDGE_LOOP ( 'NONE', ( #34172, #46345, #11587, #40476 ) ) ;
#42751=EDGE_LOOP ( 'NONE', ( #44337, #27566, #46330, #48037 ) ) ;
#42754=EDGE_CURVE ( 'NONE', #41115, #47582, #49724, .T. ) ;
#42755=CARTESIAN_POINT ( 'NONE',  ( 2.565025421079572876, 0.9854942283129086711, -0.5349721219160458174 ) ) ;
#42757=CARTESIAN_POINT ( 'NONE',  ( 0.5756566573088583993, 1.728235332270611879, 2.896516654582643291 ) ) ;
#42761=DIRECTION ( 'NONE',  ( -0.000000000000000000, 1.000000000000000000, -0.000000000000000000 ) ) ;
#42769=ORIENTED_EDGE ( 'NONE', *, *, #8184, .F. ) ;
#42771=CARTESIAN_POINT ( 'NONE',  ( -2.491402175429631605, 1.205361022782829114E-17, -1.585592796919542025 ) ) ;
#42772=ORIENTED_EDGE ( 'NONE', *, *, #30788, .F. ) ;
#42779=DIRECTION ( 'NONE',  ( -1.495358972789985422E-32, 1.160734090543304660E-16, -1.000000000000000000 ) ) ;
#42780=ADVANCED_FACE ( 'NONE', ( #23784 ), #31186, .T. ) ;
#42782=EDGE_CURVE ( 'NONE', #15190, #24926, #17190, .T. ) ;
#42786=EDGE_CURVE ( 'NONE', #21618, #50651, #36948, .T. ) ;
#42798=ORIENTED_EDGE ( 'NONE', *, *, #28064, .F. ) ;
#42805=AXIS2_PLACEMENT_3D ( 'NONE', #19446, #31086, #7587 ) ;
#42809=EDGE_CURVE ( 'NONE', #11414, #24015, #17515, .T. ) ;
#42813=ORIENTED_EDGE ( 'NONE', *, *, #7491, .F. ) ;
#42815=ORIENTED_EDGE ( 'NONE', *, *, #28012, .F. ) ;
#42816=CARTESIAN_POINT ( 'NONE',  ( 2.122891901563675354, 1.466501505047771436, -2.052405154120522379 ) ) ;
#42819=ORIENTED_EDGE ( 'NONE', *, *, #8616, .F. ) ;
#42820=VERTEX_POINT ( 'NONE', #18274 ) ;
#42821=CARTESIAN_POINT ( 'NONE',  ( 0.5756566573088583993, 1.502670515430445386, 2.896516654582643291 ) ) ;
#42823=DIRECTION ( 'NONE',  ( -3.986037398843765983E-20, -1.000000000000000000, -1.160734090543304660E-16 ) ) ;
#42824=CARTESIAN_POINT ( 'NONE',  ( -2.735162923786631950, 2.755905511811027164, -0.4201650439732181885 ) ) ;
#42832=VERTEX_POINT ( 'NONE', #10530 ) ;
#42833=CARTESIAN_POINT ( 'NONE',  ( -2.952069331832154919, 2.755905511811027164, -1.181102362204724088 ) ) ;
#42841=ORIENTED_EDGE ( 'NONE', *, *, #6165, .F. ) ;
#42845=FACE_OUTER_BOUND ( 'NONE', #1720, .T. ) ;
#42847=VERTEX_POINT ( 'NONE', #38165 ) ;
#42853=CARTESIAN_POINT ( 'NONE',  ( 0.000000000000000000, 6.692913385826772199, 0.000000000000000000 ) ) ;
#42854=B_SPLINE_CURVE_WITH_KNOTS ( 'NONE', 3,
 ( #18501, #45330, #17991, #33758 ),
 .UNSPECIFIED., .F., .F.,
 ( 4, 4 ),
 ( 2.396528199383891172E-07, 0.002500331713901011391 ),
 .UNSPECIFIED. ) ;
#42863=EDGE_CURVE ( 'NONE', #42295, #162, #45995, .T. ) ;
#42865=EDGE_LOOP ( 'NONE', ( #3028, #33803, #8023, #27855 ) ) ;
#42868=CARTESIAN_POINT ( 'NONE',  ( 0.000000000000000000, 0.000000000000000000, 0.000000000000000000 ) ) ;
#42870=CARTESIAN_POINT ( 'NONE',  ( 0.000000000000000000, 5.905511811023623991, 0.000000000000000000 ) ) ;
#42871=CIRCLE ( 'NONE', #15686, 2.165354330708661568 ) ;
#42881=CARTESIAN_POINT ( 'NONE',  ( 2.042485253772177156, 1.205361022782829114E-17, 0.6118985000151695441 ) ) ;
#42887=CARTESIAN_POINT ( 'NONE',  ( -0.04921259842519689481, 2.794703227806734062E-17, 1.924024829198930364 ) ) ;
#42888=B_SPLINE_CURVE_WITH_KNOTS ( 'NONE', 3,
 ( #30095, #34230, #25707, #5835 ),
 .UNSPECIFIED., .F., .F.,
 ( 4, 4 ),
 ( 0.001714960275793771249, 0.003045713467573901712 ),
 .UNSPECIFIED. ) ;
#42892=DIRECTION ( 'NONE',  ( -0.9998717552508122886, -0.01601477604151182316, 0.000000000000000000 ) ) ;
#42893=ORIENTED_EDGE ( 'NONE', *, *, #38236, .T. ) ;
#42896=ORIENTED_EDGE ( 'NONE', *, *, #40130, .F. ) ;
#42901=EDGE_LOOP ( 'NONE', ( #4414, #48485, #41351, #43913 ) ) ;
#42902=VECTOR ( 'NONE', #4928, 39.37007874015748143 ) ;
#42904=CARTESIAN_POINT ( 'NONE',  ( 1.466506618346834934, 1.205361022782829114E-17, -1.470210429041567401 ) ) ;
#42907=VERTEX_POINT ( 'NONE', #26022 ) ;
#42909=EDGE_LOOP ( 'NONE', ( #32652, #8746, #31384, #24814 ) ) ;
#42912=ORIENTED_EDGE ( 'NONE', *, *, #16036, .T. ) ;
#42913=ORIENTED_EDGE ( 'NONE', *, *, #20932, .F. ) ;
#42914=CARTESIAN_POINT ( 'NONE',  ( 0.4001787029124908024, 1.205361022782829114E-17, 1.929553426015793605 ) ) ;
#42915=CARTESIAN_POINT ( 'NONE',  ( 2.932638728931774352, 5.118110236220475784, 0.3475908556738230293 ) ) ;
#42929=CARTESIAN_POINT ( 'NONE',  ( -1.088097428176262760, 1.690474079180120492, 1.917118167796188821 ) ) ;
#42933=FACE_OUTER_BOUND ( 'NONE', #19609, .T. ) ;
#42934=CYLINDRICAL_SURFACE ( 'NONE', #7440, 2.165354330708661568 ) ;
#42938=ORIENTED_EDGE ( 'NONE', *, *, #49675, .T. ) ;
#42939=PRODUCT_DEFINITION_SHAPE ( 'NONE', 'NONE',  #23739 ) ;
#42946=CARTESIAN_POINT ( 'NONE',  ( 0.9243200180699869817, 1.726337457326624580, 2.322784611151789136 ) ) ;
#42947=ORIENTED_EDGE ( 'NONE', *, *, #35278, .T. ) ;
#42949=AXIS2_PLACEMENT_3D ( 'NONE', #33565, #25034, #45140 ) ;
#42950=DIRECTION ( 'NONE',  ( 0.9909497617679331460, 0.000000000000000000, 0.1342332658176667026 ) ) ;
#42954=DIRECTION ( 'NONE',  ( 0.000000000000000000, 1.000000000000000000, -0.000000000000000000 ) ) ;
#42957=LINE ( 'NONE', #15610, #49813 ) ;
#42965=EDGE_CURVE ( 'NONE', #18815, #40626, #14911, .T. ) ;
#42966=CARTESIAN_POINT ( 'NONE',  ( 0.000000000000000000, 1.585169487999011917, 0.000000000000000000 ) ) ;
#42968=ADVANCED_FACE ( 'NONE', ( #5889 ), #28740, .F. ) ;
#42969=B_SPLINE_CURVE_WITH_KNOTS ( 'NONE', 3,
 ( #12102, #8229, #24489, #40239 ),
 .UNSPECIFIED., .F., .F.,
 ( 4, 4 ),
 ( 0.001547042765121542287, 0.004047202068159086626 ),
 .UNSPECIFIED. ) ;
#42971=VERTEX_POINT ( 'NONE', #23925 ) ;
#42973=CARTESIAN_POINT ( 'NONE',  ( 1.700185224778670401, 1.636708331897141377, -1.557456981387029149 ) ) ;
#42976=DIRECTION ( 'NONE',  ( -0.9998717552508122886, -0.01601477604151185785, 0.000000000000000000 ) ) ;
#42982=CARTESIAN_POINT ( 'NONE',  ( 2.950518610523430674, 1.446690190534351661, -0.1160880551001583216 ) ) ;
#42986=EDGE_LOOP ( 'NONE', ( #45482, #14473, #716, #30425 ) ) ;
#42992=DIRECTION ( 'NONE',  ( -0.9998717552508122886, -0.01601477604151182316, 0.000000000000000000 ) ) ;
#42994=EDGE_LOOP ( 'NONE', ( #31718, #9911, #41506, #11309 ) ) ;
#42999=B_SPLINE_CURVE_WITH_KNOTS ( 'NONE', 3,
 ( #24334, #1343, #48036, #21227 ),
 .UNSPECIFIED., .F., .F.,
 ( 4, 4 ),
 ( 0.01435888398627585376, 0.03074837528792711411 ),
 .UNSPECIFIED. ) ;
#43000=EDGE_CURVE ( 'NONE', #22173, #7931, #22906, .T. ) ;
#43003=DIRECTION ( 'NONE',  ( -0.9998717552508122886, -0.01601477604151181275, 0.000000000000000000 ) ) ;
#43004=B_SPLINE_CURVE_WITH_KNOTS ( 'NONE', 3,
 ( #43922, #570, #50854, #24061 ),
 .UNSPECIFIED., .F., .F.,
 ( 4, 4 ),
 ( 0.0006814467624810971891, 0.003181736896792887459 ),
 .UNSPECIFIED. ) ;
#43006=DIRECTION ( 'NONE',  ( -3.986037398843765983E-20, -1.000000000000000000, -1.160734090543304660E-16 ) ) ;
#43014=CARTESIAN_POINT ( 'NONE',  ( 2.154397719472966433, 0.9909074813825916594, -1.481072863788291949 ) ) ;
#43022=ORIENTED_EDGE ( 'NONE', *, *, #3617, .T. ) ;
#43023=CARTESIAN_POINT ( 'NONE',  ( -1.247273217833388514, 0.007942302252338809612, -1.260601835943744087 ) ) ;
#43025=CARTESIAN_POINT ( 'NONE',  ( 1.325491792074624087, 1.739919523179865202, -2.638988599164732385 ) ) ;
#43033=EDGE_LOOP ( 'NONE', ( #48569, #19226, #33247, #8170 ) ) ;
#43041=CARTESIAN_POINT ( 'NONE',  ( 2.093903048064389427, 0.000000000000000000, -0.4274415146361335571 ) ) ;
#43046=CIRCLE ( 'NONE', #7615, 1.850107469027523432 ) ;
#43053=CARTESIAN_POINT ( 'NONE',  ( -1.843409664576977303, 1.612759574255218986, -1.157856685511029715 ) ) ;
#43057=EDGE_CURVE ( 'NONE', #30156, #50385, #31164, .T. ) ;
#43059=DIRECTION ( 'NONE',  ( 8.741157232058135226E-17, -1.000000000000000000, 7.636919086868543885E-17 ) ) ;
#43061=AXIS2_PLACEMENT_3D ( 'NONE', #9568, #34085, #30463 ) ;
#43068=CARTESIAN_POINT ( 'NONE',  ( -0.6313959120844663264, 0.5236499866080164267, -2.102827561452275784 ) ) ;
#43069=EDGE_CURVE ( 'NONE', #27482, #39685, #50488, .T. ) ;
#43070=CARTESIAN_POINT ( 'NONE',  ( 2.309000164489917406, 1.744884814208895296, 0.2631132722234555410 ) ) ;
#43071=ADVANCED_FACE ( 'NONE', ( #7419 ), #49312, .F. ) ;
#43072=CARTESIAN_POINT ( 'NONE',  ( -0.4350747367504783636, 0.000000000000000000, -2.121846421795421378 ) ) ;
#43074=ORIENTED_EDGE ( 'NONE', *, *, #37663, .F. ) ;
#43075=DIRECTION ( 'NONE',  ( -3.986037398843765983E-20, -1.000000000000000000, -1.160734090543304660E-16 ) ) ;
#43076=ORIENTED_EDGE ( 'NONE', *, *, #4490, .T. ) ;
#43090=ORIENTED_EDGE ( 'NONE', *, *, #40517, .F. ) ;
#43091=CIRCLE ( 'NONE', #15110, 2.164630168518208109 ) ;
#43093=PLANE ( 'NONE',  #16140 ) ;
#43096=ORIENTED_EDGE ( 'NONE', *, *, #14852, .F. ) ;
#43100=ORIENTED_EDGE ( 'NONE', *, *, #31140, .T. ) ;
#43101=CARTESIAN_POINT ( 'NONE',  ( -0.4414517166633473710, 0.5234905560015207238, 2.156986477457879747 ) ) ;
#43103=CARTESIAN_POINT ( 'NONE',  ( 2.951990591674675368, 1.765258879000601855, -0.08331184815398361143 ) ) ;
#43106=DIRECTION ( 'NONE',  ( -0.01601477604151182663, 0.9998717552508123996, -0.000000000000000000 ) ) ;
#43114=EDGE_LOOP ( 'NONE', ( #18729, #30836, #32589, #11602 ) ) ;
#43115=DIRECTION ( 'NONE',  ( 0.000000000000000000, 1.160734090543304660E-16, -1.000000000000000000 ) ) ;
#43121=VERTEX_POINT ( 'NONE', #36062 ) ;
#43124=CARTESIAN_POINT ( 'NONE',  ( -2.427212287055287909, 1.673239622219053535, -0.05974402731829655394 ) ) ;
#43125=VECTOR ( 'NONE', #12244, 39.37007874015748143 ) ;
#43126=ORIENTED_EDGE ( 'NONE', *, *, #39545, .T. ) ;
#43129=AXIS2_PLACEMENT_3D ( 'NONE', #12868, #474, #16226 ) ;
#43133=DIRECTION ( 'NONE',  ( -0.4338837391175656699, 0.000000000000000000, 0.9009688679024154823 ) ) ;
#43137=DIRECTION ( 'NONE',  ( -0.9998717552508121775, -0.01601477604151182316, 0.000000000000000000 ) ) ;
#43140=ORIENTED_EDGE ( 'NONE', *, *, #17304, .F. ) ;
#43148=EDGE_CURVE ( 'NONE', #13391, #23287, #28300, .T. ) ;
#43150=DIRECTION ( 'NONE',  ( 0.000000000000000000, 1.160734090543304660E-16, -1.000000000000000000 ) ) ;
#43152=DIRECTION ( 'NONE',  ( -0.7530714660036196273, -1.160734090543304907E-16, 0.6579387259397027066 ) ) ;
#43154=CARTESIAN_POINT ( 'NONE',  ( -1.236813753895213086, 1.601547340627394567, -2.681693691597581974 ) ) ;
#43164=ORIENTED_EDGE ( 'NONE', *, *, #33508, .F. ) ;
#43167=CARTESIAN_POINT ( 'NONE',  ( -2.145839806594207033, 0.5252136644077377570, -0.04710757465011475298 ) ) ;
#43169=VECTOR ( 'NONE', #14465, 39.37007874015748143 ) ;
#43172=PLANE ( 'NONE',  #3204 ) ;
#43181=ORIENTED_EDGE ( 'NONE', *, *, #12033, .F. ) ;
#43184=CARTESIAN_POINT ( 'NONE',  ( 2.949782676795221992, 0.000000000000000000, -0.1324748927672375898 ) ) ;
#43189=ORIENTED_EDGE ( 'NONE', *, *, #146, .T. ) ;
#43190=ORIENTED_EDGE ( 'NONE', *, *, #48119, .T. ) ;
#43194=CARTESIAN_POINT ( 'NONE',  ( 1.087963734054938625, 1.205361022782829114E-17, 1.724994741719410918 ) ) ;
#43197=CARTESIAN_POINT ( 'NONE',  ( 1.956192433058983493, 0.05925166736471587647, -0.03859050128386512513 ) ) ;
#43198=ORIENTED_EDGE ( 'NONE', *, *, #48842, .T. ) ;
#43200=B_SPLINE_CURVE_WITH_KNOTS ( 'NONE', 3,
 ( #11275, #27511, #37709, #42757 ),
 .UNSPECIFIED., .F., .F.,
 ( 4, 4 ),
 ( 0.01311645403109486761, 0.03074129349619527524 ),
 .UNSPECIFIED. ) ;
#43209=CARTESIAN_POINT ( 'NONE',  ( 2.323794147221719175, 1.745121766917047790, -0.05509951330290247667 ) ) ;
#43210=CARTESIAN_POINT ( 'NONE',  ( -0.3595914698493425377, 0.000000000000000000, 1.705899337635481405 ) ) ;
#43216=B_SPLINE_CURVE_WITH_KNOTS ( 'NONE', 3,
 ( #529, #35902, #24794, #44145 ),
 .UNSPECIFIED., .F., .F.,
 ( 4, 4 ),
 ( 0.01457548150641458512, 0.03074977565575078009 ),
 .UNSPECIFIED. ) ;
#43220=ORIENTED_EDGE ( 'NONE', *, *, #16532, .F. ) ;
#43232=DIRECTION ( 'NONE',  ( 0.4738686624729965269, 1.288287287306305283E-16, 0.8805955318567391110 ) ) ;
#43233=ORIENTED_EDGE ( 'NONE', *, *, #36454, .T. ) ;
#43237=CONICAL_SURFACE ( 'NONE', #48964, 3.483074324928249421, 1.244861948955335196 ) ;
#43239=CARTESIAN_POINT ( 'NONE',  ( 2.150824344285287459, 1.742351338968239238, -0.8657870173518766865 ) ) ;
#43247=ORIENTED_EDGE ( 'NONE', *, *, #22577, .T. ) ;
#43252=EDGE_CURVE ( 'NONE', #43798, #50288, #20122, .T. ) ;
#43253=CARTESIAN_POINT ( 'NONE',  ( 1.915720322920900331, 0.05860343245220329955, -0.3867724703730804348 ) ) ;
#43254=CARTESIAN_POINT ( 'NONE',  ( 0.2431224069212723493, 0.000000000000000000, 2.152304290637673034 ) ) ;
#43256=CARTESIAN_POINT ( 'NONE',  ( 2.276001286114500477, 1.711547877995502231, -0.4690042491690135096 ) ) ;
#43257=ADVANCED_FACE ( 'NONE', ( #12309 ), #24947, .F. ) ;
#43258=DIRECTION ( 'NONE',  ( -0.8584487936018655452, 0.000000000000000000, -0.5128992774059071280 ) ) ;
#43261=ORIENTED_EDGE ( 'NONE', *, *, #18900, .T. ) ;
#43268=B_SPLINE_CURVE_WITH_KNOTS ( 'NONE', 3,
 ( #46215, #11627, #10872, #26614 ),
 .UNSPECIFIED., .F., .F.,
 ( 4, 4 ),
 ( 0.1211775127643062444, 0.1625894504277921315 ),
 .UNSPECIFIED. ) ;
#43269=ADVANCED_FACE ( 'NONE', ( #6851 ), #2721, .T. ) ;
#43275=VECTOR ( 'NONE', #38220, 39.37007874015748854 ) ;
#43286=ORIENTED_EDGE ( 'NONE', *, *, #26829, .T. ) ;
#43287=AXIS2_PLACEMENT_3D ( 'NONE', #43730, #24897, #40644 ) ;
#43292=CARTESIAN_POINT ( 'NONE',  ( -0.7328193673159020260, 1.696164507524817511, 2.092647490920610309 ) ) ;
#43293=FACE_OUTER_BOUND ( 'NONE', #33936, .T. ) ;
#43300=ORIENTED_EDGE ( 'NONE', *, *, #32860, .F. ) ;
#43302=CARTESIAN_POINT ( 'NONE',  ( 0.4435105686220199295, 5.905511811023623991, 2.168331686854577889 ) ) ;
#43303=ORIENTED_EDGE ( 'NONE', *, *, #15940, .T. ) ;
#43313=CARTESIAN_POINT ( 'NONE',  ( 0.1067246931122726866, 0.02962905676920215767, 0.000000000000000000 ) ) ;
#43315=EDGE_LOOP ( 'NONE', ( #22813, #30509, #12322, #48774, #28418, #27747, #17675, #24827, #45712, #19651, #41459 ) ) ;
#43316=DIRECTION ( 'NONE',  ( -0.7818314824680309139, 0.000000000000000000, 0.6234898018587318180 ) ) ;
#43320=VECTOR ( 'NONE', #32802, 39.37007874015748143 ) ;
#43329=DIRECTION ( 'NONE',  ( 0.3513748240813434620, 1.086579671787963332E-16, -0.9362348706397368714 ) ) ;
#43331=DIRECTION ( 'NONE',  ( -0.000000000000000000, -1.000000000000000000, -0.000000000000000000 ) ) ;
#43340=B_SPLINE_CURVE_WITH_KNOTS ( 'NONE', 3,
 ( #27788, #11789, #7420, #18786 ),
 .UNSPECIFIED., .F., .F.,
 ( 4, 4 ),
 ( 0.001850897396926462404, 0.04526678932488142210 ),
 .UNSPECIFIED. ) ;
#43343=EDGE_CURVE ( 'NONE', #12429, #18859, #42888, .T. ) ;
#43354=B_SPLINE_CURVE_WITH_KNOTS ( 'NONE', 3,
 ( #21639, #17765, #33532, #45359 ),
 .UNSPECIFIED., .F., .F.,
 ( 4, 4 ),
 ( 6.352633626275700509E-07, 0.003169472943232748419 ),
 .UNSPECIFIED. ) ;
#43355=EDGE_LOOP ( 'NONE', ( #37991, #13760, #18308, #45846, #40595, #35467, #4053, #40718, #39903, #36808, #17042, #5211, #28849, #16586, #27940, #21210, #10166, #35676, #32301, #43247, #18196, #10368, #43974, #13141, #3738, #37792, #31399, #3146, #8773, #9856, #39844, #43303, #7016, #39114, #5498, #20654, #20125, #46730, #19108, #21397, #4985, #32217, #23549, #3971, #31818, #22576, #30862, #2279, #18852, #17743, #13271, #3346, #41628, #27253, #34262, #22664, #21609, #11370, #24419, #8831, #10754, #7925, #20768, #3374, #4368, #43521, #8476, #22674, #29356, #19542, #2916 ) ) ;
#43357=DIRECTION ( 'NONE',  ( 0.04486483035050446017, -1.159583191840067383E-16, 0.9989930665413151445 ) ) ;
#43367=CARTESIAN_POINT ( 'NONE',  ( -1.500384104887378278, 1.695869373643325906, 2.543203506785173040 ) ) ;
#43378=EDGE_CURVE ( 'NONE', #18328, #29362, #10904, .T. ) ;
#43380=ORIENTED_EDGE ( 'NONE', *, *, #50402, .F. ) ;
#43381=ORIENTED_EDGE ( 'NONE', *, *, #27706, .F. ) ;
#43389=DIRECTION ( 'NONE',  ( -0.000000000000000000, 1.000000000000000000, -0.000000000000000000 ) ) ;
#43392=CARTESIAN_POINT ( 'NONE',  ( 1.472219874544873131, 1.742205712729733014, 2.560030851058970214 ) ) ;
#43400=CARTESIAN_POINT ( 'NONE',  ( -1.628069513120385503, 0.001843152681973240061, -0.6423508795876955446 ) ) ;
#43405=ORIENTED_EDGE ( 'NONE', *, *, #47556, .T. ) ;
#43408=CARTESIAN_POINT ( 'NONE',  ( 2.164658444855302122, 5.905511811023623991, -0.04795272066889885720 ) ) ;
#43409=ADVANCED_FACE ( 'NONE', ( #39352 ), #103, .F. ) ;
#43411=CARTESIAN_POINT ( 'NONE',  ( 2.576863348864710801, 1.456480680773285741, 1.442554885838449596 ) ) ;
#43412=FACE_OUTER_BOUND ( 'NONE', #29031, .T. ) ;
#43413=CARTESIAN_POINT ( 'NONE',  ( 0.000000000000000000, 0.000000000000000000, 2.952755905511811108 ) ) ;
#43414=ADVANCED_FACE ( 'NONE', ( #7360 ), #46563, .T. ) ;
#43416=CIRCLE ( 'NONE', #5481, 2.086614173228346303 ) ;
#43418=ORIENTED_EDGE ( 'NONE', *, *, #29880, .F. ) ;
#43419=ORIENTED_EDGE ( 'NONE', *, *, #45465, .F. ) ;
#43422=DIRECTION ( 'NONE',  ( -0.9998717552508122886, -0.01601477604151180928, 0.000000000000000000 ) ) ;
#43424=VERTEX_POINT ( 'NONE', #38355 ) ;
#43425=EDGE_CURVE ( 'NONE', #47197, #35113, #11985, .T. ) ;
#43426=CARTESIAN_POINT ( 'NONE',  ( -1.266385247993056185, 1.541563538762524166, -2.667452810599844071 ) ) ;
#43430=DIRECTION ( 'NONE',  ( -0.6234898018587431423, -1.160734090543304660E-16, 0.7818314824680221431 ) ) ;
#43433=DIRECTION ( 'NONE',  ( 0.000000000000000000, 0.000000000000000000, -1.000000000000000000 ) ) ;
#43436=DIRECTION ( 'NONE',  ( -0.01601477604151182663, 0.9998717552508123996, -0.000000000000000000 ) ) ;
#43438=CYLINDRICAL_SURFACE ( 'NONE', #20823, 2.165354330708661568 ) ;
#43441=DIRECTION ( 'NONE',  ( -0.01601477604151182663, 0.9998717552508123996, -0.000000000000000000 ) ) ;
#43444=CARTESIAN_POINT ( 'NONE',  ( -0.4788131938641533303, 1.525670379232220375, 2.914091152102185944 ) ) ;
#43448=VERTEX_POINT ( 'NONE', #34980 ) ;
#43451=FACE_OUTER_BOUND ( 'NONE', #39754, .T. ) ;
#43456=VECTOR ( 'NONE', #37587, 39.37007874015748143 ) ;
#43458=LINE ( 'NONE', #43967, #46442 ) ;
#43459=LINE ( 'NONE', #44233, #38902 ) ;
#43460=ORIENTED_EDGE ( 'NONE', *, *, #49947, .T. ) ;
#43463=DIRECTION ( 'NONE',  ( 0.000000000000000000, 0.000000000000000000, -1.000000000000000000 ) ) ;
#43465=CARTESIAN_POINT ( 'NONE',  ( -1.723188456408593527, 1.574803149606302854, 1.311251662046200694 ) ) ;
#43470=CARTESIAN_POINT ( 'NONE',  ( -1.882988517681398966, 1.574803149606302854, 1.069164917025789530 ) ) ;
#43473=B_SPLINE_CURVE_WITH_KNOTS ( 'NONE', 3,
 ( #44354, #40497, #4615, #20359 ),
 .UNSPECIFIED., .F., .F.,
 ( 4, 4 ),
 ( 0.001065024714398824521, 0.003565326717754890851 ),
 .UNSPECIFIED. ) ;
#43475=LINE ( 'NONE', #5017, #21865 ) ;
#43477=EDGE_CURVE ( 'NONE', #7931, #21785, #4717, .T. ) ;
#43479=EDGE_CURVE ( 'NONE', #1977, #30098, #34479, .T. ) ;
#43480=ORIENTED_EDGE ( 'NONE', *, *, #37594, .F. ) ;
#43486=DIRECTION ( 'NONE',  ( -0.5877852522924802425, 0.000000000000000000, 0.8090169943749422332 ) ) ;
#43488=DIRECTION ( 'NONE',  ( -6.104789737168038204E-17, 1.000000000000000000, -1.134460028949771622E-16 ) ) ;
#43489=ORIENTED_EDGE ( 'NONE', *, *, #25927, .F. ) ;
#43500=VERTEX_POINT ( 'NONE', #35484 ) ;
#43503=ADVANCED_FACE ( 'NONE', ( #42714 ), #3210, .T. ) ;
#43504=CARTESIAN_POINT ( 'NONE',  ( 2.138597145901430352, 2.755905511811027164, 0.3393547186367261159 ) ) ;
#43505=EDGE_CURVE ( 'NONE', #18547, #37057, #22507, .T. ) ;
#43507=VERTEX_POINT ( 'NONE', #3733 ) ;
#43509=EDGE_CURVE ( 'NONE', #9779, #23437, #31107, .T. ) ;
#43511=VERTEX_POINT ( 'NONE', #11483 ) ;
#43516=CARTESIAN_POINT ( 'NONE',  ( 0.2841802383804452603, 0.03247133209088205741, 1.841575167587790718 ) ) ;
#43519=CARTESIAN_POINT ( 'NONE',  ( -0.5272349255865266260, 5.905511811023623991, 2.905303903342410621 ) ) ;
#43520=CARTESIAN_POINT ( 'NONE',  ( 0.04921259842519669359, 1.643073385594818525, 2.245762300990225224 ) ) ;
#43521=ORIENTED_EDGE ( 'NONE', *, *, #18967, .T. ) ;
#43522=CARTESIAN_POINT ( 'NONE',  ( 1.295918523765950958, 1.485688605496056969, -2.653230334577374450 ) ) ;
#43523=LINE ( 'NONE', #23919, #41682 ) ;
#43532=DIRECTION ( 'NONE',  ( 0.000000000000000000, -0.000000000000000000, -1.000000000000000000 ) ) ;
#43534=CARTESIAN_POINT ( 'NONE',  ( 2.141071258218635531, 0.000000000000000000, -0.04689341889560144638 ) ) ;
#43537=DIRECTION ( 'NONE',  ( -0.01601477604151182663, 0.9998717552508123996, -0.000000000000000000 ) ) ;
#43538=VECTOR ( 'NONE', #39891, 39.37007874015748143 ) ;
#43547=EDGE_CURVE ( 'NONE', #17742, #3538, #29381, .T. ) ;
#43548=DIRECTION ( 'NONE',  ( 0.000000000000000000, 0.000000000000000000, 1.000000000000000000 ) ) ;
#43552=DIRECTION ( 'NONE',  ( -0.9998717552508121775, -0.01601477604151182663, 0.000000000000000000 ) ) ;
#43553=ORIENTED_EDGE ( 'NONE', *, *, #44602, .F. ) ;
#43557=CARTESIAN_POINT ( 'NONE',  ( 1.621795816027391979, 0.000000000000000000, -0.6396693727619211511 ) ) ;
#43558=DIRECTION ( 'NONE',  ( 0.000000000000000000, 0.000000000000000000, 1.000000000000000000 ) ) ;
#43566=VERTEX_POINT ( 'NONE', #4497 ) ;
#43568=LINE ( 'NONE', #8472, #38593 ) ;
#43585=PLANE ( 'NONE',  #11154 ) ;
#43587=CYLINDRICAL_SURFACE ( 'NONE', #31762, 2.165354330708661568 ) ;
#43592=ORIENTED_EDGE ( 'NONE', *, *, #25775, .T. ) ;
#43595=CARTESIAN_POINT ( 'NONE',  ( 0.2239970000120027616, 0.000000000000000000, -1.939803615689571048 ) ) ;
#43597=ORIENTED_EDGE ( 'NONE', *, *, #3198, .F. ) ;
#43599=CARTESIAN_POINT ( 'NONE',  ( -1.751183565233300543, 0.5249316475426857309, -0.6949723508179344034 ) ) ;
#43600=EDGE_CURVE ( 'NONE', #46032, #14806, #10231, .T. ) ;
#43606=PLANE ( 'NONE',  #15330 ) ;
#43609=ADVANCED_FACE ( 'NONE', ( #21012 ), #1385, .T. ) ;
#43611=DIRECTION ( 'NONE',  ( 0.7227948638273978821, 0.000000000000000000, -0.6910626489868580968 ) ) ;
#43614=DIRECTION ( 'NONE',  ( -0.5877852522924684742, 9.392878985996986848E-17, -0.8090169943749506709 ) ) ;
#43616=DIRECTION ( 'NONE',  ( -0.000000000000000000, -0.000000000000000000, 1.000000000000000000 ) ) ;
#43618=EDGE_LOOP ( 'NONE', ( #45897, #9745, #26801, #3809 ) ) ;
#43622=ORIENTED_EDGE ( 'NONE', *, *, #28169, .F. ) ;
#43623=CARTESIAN_POINT ( 'NONE',  ( -2.592410190554199634, 1.580416535242628928, 1.413664012880529119 ) ) ;
#43628=ORIENTED_EDGE ( 'NONE', *, *, #23112, .F. ) ;
#43631=AXIS2_PLACEMENT_3D ( 'NONE', #20384, #36141, #12645 ) ;
#43633=CARTESIAN_POINT ( 'NONE',  ( 0.2052282226254518727, 0.000000000000000000, -1.731265419273307682 ) ) ;
#43637=CARTESIAN_POINT ( 'NONE',  ( -1.790827367621149024, 1.613601776126088128, -1.241082175747989735 ) ) ;
#43638=CARTESIAN_POINT ( 'NONE',  ( -1.088998432874330735, 6.692913385826772199, 1.918626195649137500 ) ) ;
#43644=FACE_OUTER_BOUND ( 'NONE', #10305, .T. ) ;
#43645=B_SPLINE_CURVE_WITH_KNOTS ( 'NONE', 3,
 ( #22043, #24895, #41161, #5270 ),
 .UNSPECIFIED., .F., .F.,
 ( 4, 4 ),
 ( 0.0001113516447889145337, 0.002611425118082581591 ),
 .UNSPECIFIED. ) ;
#43659=CARTESIAN_POINT ( 'NONE',  ( 2.755905511811024056, 4.960629921259846142, -1.023622047244094224 ) ) ;
#43661=FACE_OUTER_BOUND ( 'NONE', #35211, .T. ) ;
#43663=EDGE_CURVE ( 'NONE', #38821, #20664, #28488, .T. ) ;
#43664=CARTESIAN_POINT ( 'NONE',  ( 2.280039352122881002, 0.9892193096974960520, 1.282827082053922485 ) ) ;
#43671=ORIENTED_EDGE ( 'NONE', *, *, #47232, .T. ) ;
#43681=DIRECTION ( 'NONE',  ( -0.000000000000000000, 1.000000000000000000, -0.000000000000000000 ) ) ;
#43683=EDGE_LOOP ( 'NONE', ( #22733, #44885, #47089, #20378 ) ) ;
#43685=CARTESIAN_POINT ( 'NONE',  ( 2.100190309385009169, 5.905511811023623991, 0.5298329251847516685 ) ) ;
#43699=DIRECTION ( 'NONE',  ( 1.142080616180678453E-16, -1.000000000000000000, 2.072570748943325363E-17 ) ) ;
#43700=EDGE_CURVE ( 'NONE', #25220, #21117, #24168, .T. ) ;
#43704=CARTESIAN_POINT ( 'NONE',  ( 0.002207914879453961535, -5.712274067634378313E-18, 0.04916304461325374242 ) ) ;
#43707=DIRECTION ( 'NONE',  ( 0.01601477604151182663, -0.9998717552508123996, 0.000000000000000000 ) ) ;
#43711=AXIS2_PLACEMENT_3D ( 'NONE', #23518, #4164, #49651 ) ;
#43712=ORIENTED_EDGE ( 'NONE', *, *, #27817, .T. ) ;
#43713=CARTESIAN_POINT ( 'NONE',  ( -1.546800823997126262, 1.683127104815683728, -1.546979550173933182 ) ) ;
#43717=ORIENTED_EDGE ( 'NONE', *, *, #11622, .T. ) ;
#43718=CARTESIAN_POINT ( 'NONE',  ( 1.645338673473796254, 0.05427277550655955352, -1.027111169014480296 ) ) ;
#43719=CARTESIAN_POINT ( 'NONE',  ( -1.350373579275921276, 0.006290961278228680842, 1.139832270491418553 ) ) ;
#43723=AXIS2_PLACEMENT_3D ( 'NONE', #22681, #6432, #49494 ) ;
#43727=ADVANCED_FACE ( 'NONE', ( #29522 ), #37787, .F. ) ;
#43729=CARTESIAN_POINT ( 'NONE',  ( -1.876322193478733524, 1.681962395836037016, 1.559262294237737434 ) ) ;
#43730=CARTESIAN_POINT ( 'NONE',  ( 0.000000000000000000, 0.000000000000000000, 0.000000000000000000 ) ) ;
#43732=ADVANCED_FACE ( 'NONE', ( #37023 ), #27964, .F. ) ;
#43741=DIRECTION ( 'NONE',  ( -0.1342332658176522420, -1.160734090543305153E-16, -0.9909497617679352555 ) ) ;
#43742=DIRECTION ( 'NONE',  ( -0.3090169943749582204, -1.160734090543304660E-16, 0.9510565162951500895 ) ) ;
#43744=ORIENTED_EDGE ( 'NONE', *, *, #46447, .F. ) ;
#43748=CARTESIAN_POINT ( 'NONE',  ( 2.043634885149959057, 6.692913385826772199, 0.7157624142946238388 ) ) ;
#43752=ORIENTED_EDGE ( 'NONE', *, *, #13774, .F. ) ;
#43754=CARTESIAN_POINT ( 'NONE',  ( -1.971834065208965203, 0.000000000000000000, 0.8963217522329899323 ) ) ;
#43756=VECTOR ( 'NONE', #6746, 39.37007874015748854 ) ;
#43757=ORIENTED_EDGE ( 'NONE', *, *, #41255, .T. ) ;
#43759=ORIENTED_EDGE ( 'NONE', *, *, #15867, .F. ) ;
#43760=CARTESIAN_POINT ( 'NONE',  ( 0.1155636338427008941, -0.5222242541845523167, 0.000000000000000000 ) ) ;
#43766=LINE ( 'NONE', #39402, #18502 ) ;
#43770=EDGE_CURVE ( 'NONE', #20204, #12025, #21388, .T. ) ;
#43772=CARTESIAN_POINT ( 'NONE',  ( -1.152568299495734250, 1.574803149606302854, 1.833124570921536467 ) ) ;
#43774=CARTESIAN_POINT ( 'NONE',  ( 0.002207914879453961535, -5.712274067634378313E-18, 0.04916304461325374242 ) ) ;
#43775=CARTESIAN_POINT ( 'NONE',  ( 1.695772546416037363, 1.745688802946234297, -2.417756147381349141 ) ) ;
#43778=LINE ( 'NONE', #938, #17443 ) ;
#43780=VERTEX_POINT ( 'NONE', #21775 ) ;
#43782=CARTESIAN_POINT ( 'NONE',  ( 1.973323729629757217, 0.000000000000000000, -0.7899196136953162695 ) ) ;
#43785=CYLINDRICAL_SURFACE ( 'NONE', #32330, 2.086614173228346303 ) ;
#43788=EDGE_LOOP ( 'NONE', ( #47174, #48678, #9463, #25387 ) ) ;
#43789=CARTESIAN_POINT ( 'NONE',  ( -0.2922638600240530793, 1.612444929547712125, -2.698310553500231634 ) ) ;
#43790=DIRECTION ( 'NONE',  ( 0.8805955318567321166, 0.000000000000000000, 0.4738686624730094055 ) ) ;
#43791=VECTOR ( 'NONE', #42950, 39.37007874015748854 ) ;
#43792=ADVANCED_FACE ( 'NONE', ( #14277 ), #34542, .T. ) ;
#43794=CARTESIAN_POINT ( 'NONE',  ( -1.979793062125317693, 1.688404340953838068, 2.191257344206539504 ) ) ;
#43798=VERTEX_POINT ( 'NONE', #14537 ) ;
#43799=VERTEX_POINT ( 'NONE', #18156 ) ;
#43805=DIRECTION ( 'NONE',  ( 0.04486483035051863633, -1.160734090543304660E-16, -0.9989930665413144784 ) ) ;
#43809=B_SPLINE_CURVE_WITH_KNOTS ( 'NONE', 3,
 ( #25648, #17147, #5264, #24891 ),
 .UNSPECIFIED., .F., .F.,
 ( 4, 4 ),
 ( 2.137550060313775870E-07, 0.002500695496946613028 ),
 .UNSPECIFIED. ) ;
#43814=ORIENTED_EDGE ( 'NONE', *, *, #19262, .T. ) ;
#43816=VERTEX_POINT ( 'NONE', #19153 ) ;
#43817=ORIENTED_EDGE ( 'NONE', *, *, #14540, .T. ) ;
#43819=CARTESIAN_POINT ( 'NONE',  ( -0.04921259842519707522, 1.574803149606302854, 2.164795024401847456 ) ) ;
#43823=CARTESIAN_POINT ( 'NONE',  ( 2.576863348864710801, 1.660943078747768364, 1.442554885838449819 ) ) ;
#43824=AXIS2_PLACEMENT_3D ( 'NONE', #35991, #16109, #28484 ) ;
#43825=CARTESIAN_POINT ( 'NONE',  ( 0.002207914879453961535, -5.712274067634378313E-18, 0.04916304461325374242 ) ) ;
#43827=EDGE_CURVE ( 'NONE', #34736, #30054, #46497, .T. ) ;
#43830=ORIENTED_EDGE ( 'NONE', *, *, #7438, .F. ) ;
#43835=EDGE_CURVE ( 'NONE', #17350, #41720, #30786, .T. ) ;
#43836=CARTESIAN_POINT ( 'NONE',  ( 1.692294915983738157, 1.738507761360482018, 1.862189238238326050 ) ) ;
#43838=CARTESIAN_POINT ( 'NONE',  ( 1.041962601392105725, 0.02949362477880272670, 1.648001814300100065 ) ) ;
#43841=CARTESIAN_POINT ( 'NONE',  ( 2.277873973731426194, 0.000000000000000000, 1.879489153247667854 ) ) ;
#43842=VERTEX_POINT ( 'NONE', #19398 ) ;
#43843=FACE_OUTER_BOUND ( 'NONE', #3940, .T. ) ;
#43846=EDGE_CURVE ( 'NONE', #34884, #47219, #46250, .T. ) ;
#43853=LINE ( 'NONE', #40001, #46364 ) ;
#43855=EDGE_CURVE ( 'NONE', #16487, #2592, #11468, .T. ) ;
#43856=ORIENTED_EDGE ( 'NONE', *, *, #14323, .T. ) ;
#43860=CARTESIAN_POINT ( 'NONE',  ( 1.588513588560381828, 0.05336261777518135074, -1.107536019441389019 ) ) ;
#43863=AXIS2_PLACEMENT_3D ( 'NONE', #49615, #7561, #33929 ) ;
#43864=LINE ( 'NONE', #48730, #22251 ) ;
#43867=CARTESIAN_POINT ( 'NONE',  ( -2.100227814008681637, 1.686526752338742385, -2.076109931251943763 ) ) ;
#43871=VECTOR ( 'NONE', #19653, 39.37007874015748143 ) ;
#43873=DIRECTION ( 'NONE',  ( 0.9959742939952384022, 0.000000000000000000, 0.08963930890344089242 ) ) ;
#43876=VERTEX_POINT ( 'NONE', #50104 ) ;
#43885=ORIENTED_EDGE ( 'NONE', *, *, #437, .T. ) ;
#43900=FACE_OUTER_BOUND ( 'NONE', #49350, .T. ) ;
#43906=ORIENTED_EDGE ( 'NONE', *, *, #34094, .T. ) ;
#43907=VECTOR ( 'NONE', #36748, 39.37007874015748854 ) ;
#43911=EDGE_CURVE ( 'NONE', #35300, #49387, #28686, .T. ) ;
#43913=ORIENTED_EDGE ( 'NONE', *, *, #34296, .T. ) ;
#43915=EDGE_CURVE ( 'NONE', #37948, #44472, #20850, .T. ) ;
#43916=ORIENTED_EDGE ( 'NONE', *, *, #14637, .F. ) ;
#43919=B_SPLINE_CURVE_WITH_KNOTS ( 'NONE', 3,
 ( #48832, #9643, #41146, #17640 ),
 .UNSPECIFIED., .F., .F.,
 ( 4, 4 ),
 ( 2.008334167098713497E-07, 0.002500501959281965520 ),
 .UNSPECIFIED. ) ;
#43921=ORIENTED_EDGE ( 'NONE', *, *, #1766, .F. ) ;
#43922=CARTESIAN_POINT ( 'NONE',  ( 0.6502734851936936566, 1.718317270777941941, -2.171228911417812046 ) ) ;
#43923=CARTESIAN_POINT ( 'NONE',  ( 0.5762653268100312864, 0.000000000000000000, -1.903066372058335620 ) ) ;
#43927=ORIENTED_EDGE ( 'NONE', *, *, #978, .T. ) ;
#43934=ADVANCED_FACE ( 'NONE', ( #3416 ), #50592, .T. ) ;
#43935=VERTEX_POINT ( 'NONE', #31297 ) ;
#43940=CARTESIAN_POINT ( 'NONE',  ( 0.5662636741187413447, 0.000000000000000000, 1.648861433446464186 ) ) ;
#43947=CARTESIAN_POINT ( 'NONE',  ( -2.099568260077699033, 6.692913385826772199, -0.5296909464896106812 ) ) ;
#43952=CARTESIAN_POINT ( 'NONE',  ( -1.642191404871911731, 0.000000000000000000, 0.5853255206279681655 ) ) ;
#43956=EDGE_CURVE ( 'NONE', #24752, #28976, #35674, .T. ) ;
#43957=ORIENTED_EDGE ( 'NONE', *, *, #38179, .F. ) ;
#43958=CARTESIAN_POINT ( 'NONE',  ( 2.308557526972506047, 5.905511811023623991, 1.841013194464793390 ) ) ;
#43967=CARTESIAN_POINT ( 'NONE',  ( 3.937007874015748143, 5.118110236220475784, 1.181102362204724310 ) ) ;
#43971=CARTESIAN_POINT ( 'NONE',  ( 2.662626360126375769, 1.757290156728792185, -0.6582052835281975156 ) ) ;
#43972=EDGE_CURVE ( 'NONE', #21553, #10178, #32116, .T. ) ;
#43974=ORIENTED_EDGE ( 'NONE', *, *, #1597, .T. ) ;
#43976=CARTESIAN_POINT ( 'NONE',  ( -0.3129956986278690789, 1.049866565067837820, 2.000361441164483445 ) ) ;
#43978=AXIS2_PLACEMENT_3D ( 'NONE', #44699, #18119, #48800 ) ;
#43979=EDGE_CURVE ( 'NONE', #30012, #41869, #12691, .T. ) ;
#43981=AXIS2_PLACEMENT_3D ( 'NONE', #28105, #27596, #4120 ) ;
#43985=CARTESIAN_POINT ( 'NONE',  ( 4.821444091131312140E-17, 0.07874015748031502893, 0.3937007874015748254 ) ) ;
#43986=ADVANCED_BREP_SHAPE_REPRESENTATION ( '', ( #23876, #26741 ), #4483 ) ;
#43988=B_SPLINE_CURVE_WITH_KNOTS ( 'NONE', 3,
 ( #7669, #7921, #23926, #39672 ),
 .UNSPECIFIED., .F., .F.,
 ( 4, 4 ),
 ( 2.051202603109093890E-07, 0.002500241469102131974 ),
 .UNSPECIFIED. ) ;
#43991=CARTESIAN_POINT ( 'NONE',  ( 0.2431224069212730987, 5.905511811023623991, 2.152304290637673478 ) ) ;
#43993=ORIENTED_EDGE ( 'NONE', *, *, #5690, .F. ) ;
#44001=CARTESIAN_POINT ( 'NONE',  ( 2.139229417893225627, 0.000000000000000000, -0.3394403656973398742 ) ) ;
#44008=CARTESIAN_POINT ( 'NONE',  ( -0.6233543567505162031, 1.574803149606302854, -2.073689640095379705 ) ) ;
#44013=CARTESIAN_POINT ( 'NONE',  ( 0.2156685157584260770, 1.510622172706404864, -2.945280361644574185 ) ) ;
#44014=ORIENTED_EDGE ( 'NONE', *, *, #45459, .T. ) ;
#44016=DIRECTION ( 'NONE',  ( 0.5508969814520945363, 0.000000000000000000, 0.8345732537213079727 ) ) ;
#44017=EDGE_CURVE ( 'NONE', #39335, #26738, #3464, .T. ) ;
#44022=AXIS2_PLACEMENT_3D ( 'NONE', #8920, #16676, #5045 ) ;
#44024=AXIS2_PLACEMENT_3D ( 'NONE', #5844, #29847, #33986 ) ;
#44026=CARTESIAN_POINT ( 'NONE',  ( -2.277873973731453727, 1.585326468414270495, 1.879489153247635214 ) ) ;
#44027=CARTESIAN_POINT ( 'NONE',  ( 0.5284761224300889015, 5.905511811023623991, -2.099874368989729234 ) ) ;
#44029=ADVANCED_FACE ( 'NONE', ( #35930 ), #12428, .T. ) ;
#44036=ORIENTED_EDGE ( 'NONE', *, *, #35242, .T. ) ;
#44037=CARTESIAN_POINT ( 'NONE',  ( 1.583112249919723213, 0.000000000000000000, -0.7301740747847023094 ) ) ;
#44040=ORIENTED_EDGE ( 'NONE', *, *, #4406, .F. ) ;
#44042=CARTESIAN_POINT ( 'NONE',  ( -1.152895553066196177, 0.000000000000000000, -1.833672301139088745 ) ) ;
#44044=DIRECTION ( 'NONE',  ( 5.063291518728965670E-17, 1.000000000000000000, 1.184615939703122503E-16 ) ) ;
#44048=CARTESIAN_POINT ( 'NONE',  ( 0.08139965876239094178, 1.610780518492231694, 0.000000000000000000 ) ) ;
#44050=DIRECTION ( 'NONE',  ( -0.9998717552508122886, -0.01601477604151181275, 0.000000000000000000 ) ) ;
#44053=CARTESIAN_POINT ( 'NONE',  ( 2.322368699764507216, 1.646673738916892837, -0.1535599007534338978 ) ) ;
#44054=EDGE_CURVE ( 'NONE', #37003, #14034, #40323, .T. ) ;
#44055=PLANE ( 'NONE',  #25524 ) ;
#44060=AXIS2_PLACEMENT_3D ( 'NONE', #25213, #24452, #32202 ) ;
#44062=ORIENTED_EDGE ( 'NONE', *, *, #13364, .F. ) ;
#44067=EDGE_CURVE ( 'NONE', #42204, #24086, #4904, .T. ) ;
#44068=B_SPLINE_CURVE_WITH_KNOTS ( 'NONE', 3,
 ( #49404, #36817, #1187, #13828 ),
 .UNSPECIFIED., .F., .F.,
 ( 4, 4 ),
 ( 6.437188407750467112E-07, 0.003699879688711244820 ),
 .UNSPECIFIED. ) ;
#44074=ORIENTED_EDGE ( 'NONE', *, *, #11278, .T. ) ;
#44078=ORIENTED_EDGE ( 'NONE', *, *, #17879, .T. ) ;
#44083=LINE ( 'NONE', #24225, #5645 ) ;
#44085=LINE ( 'NONE', #982, #36782 ) ;
#44089=ADVANCED_FACE ( 'NONE', ( #19982 ), #26350, .T. ) ;
#44091=ORIENTED_EDGE ( 'NONE', *, *, #20243, .F. ) ;
#44101=CARTESIAN_POINT ( 'NONE',  ( 2.157073429634569717, 0.5219348593605198650, 0.7526208317096673150 ) ) ;
#44104=B_SPLINE_CURVE_WITH_KNOTS ( 'NONE', 3,
 ( #27868, #31501, #12648, #23750 ),
 .UNSPECIFIED., .F., .F.,
 ( 4, 4 ),
 ( 0.001530659381711838756, 0.04616820643450836315 ),
 .UNSPECIFIED. ) ;
#44106=CIRCLE ( 'NONE', #22673, 2.244934639244525076 ) ;
#44107=ORIENTED_EDGE ( 'NONE', *, *, #21542, .T. ) ;
#44114=ORIENTED_EDGE ( 'NONE', *, *, #33098, .F. ) ;
#44115=CARTESIAN_POINT ( 'NONE',  ( -0.9914495361339012991, 1.703811331058339373, 2.781765111341808705 ) ) ;
#44118=CARTESIAN_POINT ( 'NONE',  ( 0.000000000000000000, 5.905511811023623991, 0.000000000000000000 ) ) ;
#44119=ORIENTED_EDGE ( 'NONE', *, *, #40583, .F. ) ;
#44120=DIRECTION ( 'NONE',  ( 0.000000000000000000, 0.000000000000000000, 1.000000000000000000 ) ) ;
#44121=CARTESIAN_POINT ( 'NONE',  ( 2.813306935136158149, 1.763089614240364256, 0.8968503919106445288 ) ) ;
#44123=ADVANCED_FACE ( 'NONE', ( #27735 ), #8125, .T. ) ;
#44125=CARTESIAN_POINT ( 'NONE',  ( 0.08139965876239094178, 1.610780518492231694, 0.000000000000000000 ) ) ;
#44128=EDGE_LOOP ( 'NONE', ( #44319, #48662, #23250, #22758, #16298, #4914, #22239, #41230, #12564, #26105, #39090 ) ) ;
#44131=CARTESIAN_POINT ( 'NONE',  ( -2.952069331832154919, 5.118110236220475784, -1.181102362204724310 ) ) ;
#44141=ORIENTED_EDGE ( 'NONE', *, *, #40583, .T. ) ;
#44144=ORIENTED_EDGE ( 'NONE', *, *, #30788, .T. ) ;
#44145=CARTESIAN_POINT ( 'NONE',  ( 2.576863348864710801, 1.660943078747768364, 1.442554885838449819 ) ) ;
#44149=CARTESIAN_POINT ( 'NONE',  ( 2.919426793319799707, 1.666276233232717896, 0.4451252810446822417 ) ) ;
#44151=EDGE_LOOP ( 'NONE', ( #46082, #24370, #40208, #13370, #3009, #7073, #25994, #43300, #30456, #42041, #19693, #50105, #17679 ) ) ;
#44153=CARTESIAN_POINT ( 'NONE',  ( -1.080768593899272823, 0.000000000000000000, -1.459517500771556620 ) ) ;
#44155=EDGE_CURVE ( 'NONE', #6809, #5773, #13885, .T. ) ;
#44157=ADVANCED_FACE ( 'NONE', ( #30672 ), #46116, .T. ) ;
#44162=CARTESIAN_POINT ( 'NONE',  ( 0.000000000000000000, 6.692913385826772199, 0.000000000000000000 ) ) ;
#44164=( GEOMETRIC_REPRESENTATION_CONTEXT ( 3 ) GLOBAL_UNCERTAINTY_ASSIGNED_CONTEXT ( ( #29306 ) ) GLOBAL_UNIT_ASSIGNED_CONTEXT ( ( #10660, #3408, #30277 ) ) REPRESENTATION_CONTEXT ( 'NONE', 'WORKASPACE' ) );
#44167=CONICAL_SURFACE ( 'NONE', #40868, 1.850107469027523210, 0.6386652850508578450 ) ;
#44175=ORIENTED_EDGE ( 'NONE', *, *, #33812, .F. ) ;
#44177=ORIENTED_EDGE ( 'NONE', *, *, #47659, .T. ) ;
#44181=EDGE_LOOP ( 'NONE', ( #11848, #15314, #19348, #47652 ) ) ;
#44185=EDGE_LOOP ( 'NONE', ( #36323, #27166, #30473, #33065, #36867, #23417, #38161 ) ) ;
#44189=DIRECTION ( 'NONE',  ( -0.9998717552508122886, -0.01601477604151185785, 0.000000000000000000 ) ) ;
#44195=CARTESIAN_POINT ( 'NONE',  ( 2.518955203866161785, 1.653166854136447483, 0.2915536147086987273 ) ) ;
#44196=EDGE_CURVE ( 'NONE', #35414, #23952, #37291, .T. ) ;
#44201=AXIS2_PLACEMENT_3D ( 'NONE', #34653, #46238, #45732 ) ;
#44202=ORIENTED_EDGE ( 'NONE', *, *, #27515, .T. ) ;
#44208=CARTESIAN_POINT ( 'NONE',  ( -2.889674983507169337, 1.575792602931942232, -0.6090712660038034576 ) ) ;
#44211=CARTESIAN_POINT ( 'NONE',  ( -0.9838852166859196613, 5.905511811023623991, 1.929635236160304190 ) ) ;
#44214=CARTESIAN_POINT ( 'NONE',  ( 0.08139965876239094178, 1.610780518492231694, 0.000000000000000000 ) ) ;
#44217=DIRECTION ( 'NONE',  ( 5.779879058770898378E-18, 1.000000000000000000, 1.286990067732318227E-16 ) ) ;
#44223=ADVANCED_FACE ( 'NONE', ( #32658 ), #17913, .T. ) ;
#44227=DIRECTION ( 'NONE',  ( -0.2660368455666687892, 0.000000000000000000, -0.9639628606958549062 ) ) ;
#44230=CARTESIAN_POINT ( 'NONE',  ( 2.249085127468613443, 1.747331752236621183, 1.154398728974792565 ) ) ;
#44231=ORIENTED_EDGE ( 'NONE', *, *, #23210, .F. ) ;
#44232=CARTESIAN_POINT ( 'NONE',  ( 0.1155636338427008941, -0.5222242541845523167, 0.000000000000000000 ) ) ;
#44233=CARTESIAN_POINT ( 'NONE',  ( 2.623503965249849301, 1.205361022782829114E-17, 1.355882097269873965 ) ) ;
#44237=DIRECTION ( 'NONE',  ( -2.582876339026174526E-17, -1.000000000000000000, -1.131632063491654496E-16 ) ) ;
#44242=CARTESIAN_POINT ( 'NONE',  ( 1.836342932631641167, 0.000000000000000000, 1.044063857347276469 ) ) ;
#44246=CARTESIAN_POINT ( 'NONE',  ( -1.929629134066536134, 6.692913385826772199, 0.9824921284572121216 ) ) ;
#44257=DIRECTION ( 'NONE',  ( 0.000000000000000000, -1.000000000000000000, -0.000000000000000000 ) ) ;
#44259=VERTEX_POINT ( 'NONE', #48599 ) ;
#44260=LINE ( 'NONE', #24654, #8581 ) ;
#44261=CARTESIAN_POINT ( 'NONE',  ( 2.823445274216730638, 1.205361022782829114E-17, 0.8656477926280680135 ) ) ;
#44266=ORIENTED_EDGE ( 'NONE', *, *, #4382, .T. ) ;
#44268=CARTESIAN_POINT ( 'NONE',  ( 1.412396057062172305, -1.971265646866911096E-16, 1.691415513056038877 ) ) ;
#44273=LINE ( 'NONE', #8912, #9210 ) ;
#44275=ORIENTED_EDGE ( 'NONE', *, *, #31083, .F. ) ;
#44285=ORIENTED_EDGE ( 'NONE', *, *, #23268, .F. ) ;
#44289=CARTESIAN_POINT ( 'NONE',  ( -2.077187562400836907, 1.584429483328545274, 1.719447080701160591 ) ) ;
#44290=PLANE ( 'NONE',  #42364 ) ;
#44296=DIRECTION ( 'NONE',  ( -0.9998717552508122886, -0.01601477604151181275, 0.000000000000000000 ) ) ;
#44297=VECTOR ( 'NONE', #48191, 39.37007874015748143 ) ;
#44299=CARTESIAN_POINT ( 'NONE',  ( 1.806430656273612767, 0.5249316475426862860, 0.5351997119015522442 ) ) ;
#44302=CARTESIAN_POINT ( 'NONE',  ( -0.4788131938641533303, 1.525670379232220375, 2.914091152102185944 ) ) ;
#44307=ORIENTED_EDGE ( 'NONE', *, *, #9469, .F. ) ;
#44313=CARTESIAN_POINT ( 'NONE',  ( 0.002207914879453961969, 5.905511811023623991, 0.04916304461325442243 ) ) ;
#44319=ORIENTED_EDGE ( 'NONE', *, *, #36697, .T. ) ;
#44321=FACE_OUTER_BOUND ( 'NONE', #46399, .T. ) ;
#44322=VERTEX_POINT ( 'NONE', #1651 ) ;
#44325=ORIENTED_EDGE ( 'NONE', *, *, #41150, .T. ) ;
#44328=CARTESIAN_POINT ( 'NONE',  ( 1.466506618346834934, 1.205361022782829114E-17, -1.470210429041567401 ) ) ;
#44334=EDGE_LOOP ( 'NONE', ( #48751, #2550, #27304, #15632 ) ) ;
#44336=DIRECTION ( 'NONE',  ( -0.9195277725514544587, 0.000000000000000000, 0.3930250316539147803 ) ) ;
#44337=ORIENTED_EDGE ( 'NONE', *, *, #18777, .T. ) ;
#44339=ORIENTED_EDGE ( 'NONE', *, *, #2397, .T. ) ;
#44340=DIRECTION ( 'NONE',  ( 0.000000000000000000, 1.000000000000000000, 0.000000000000000000 ) ) ;
#44342=CONICAL_SURFACE ( 'NONE', #27020, 3.483074324928249421, 1.244861948955335196 ) ;
#44344=ADVANCED_FACE ( 'NONE', ( #10675 ), #10923, .T. ) ;
#44348=CARTESIAN_POINT ( 'NONE',  ( 2.516879689376027684, 1.751575581218955513, 0.2912724671682164201 ) ) ;
#44350=DIRECTION ( 'NONE',  ( -0.5128992774059071280, 0.000000000000000000, 0.8584487936018655452 ) ) ;
#44351=VECTOR ( 'NONE', #40356, 39.37007874015748143 ) ;
#44354=CARTESIAN_POINT ( 'NONE',  ( 0.4521076751547876138, 1.616718085813380945, 2.215705648545971407 ) ) ;
#44356=ADVANCED_FACE ( 'NONE', ( #26168 ), #31049, .F. ) ;
#44357=LINE ( 'NONE', #43841, #25177 ) ;
#44359=CARTESIAN_POINT ( 'NONE',  ( 0.8004649005966348874, 0.000000000000000000, -1.548759025234849762 ) ) ;
#44362=AXIS2_PLACEMENT_3D ( 'NONE', #11829, #23442, #38950 ) ;
#44365=EDGE_CURVE ( 'NONE', #42296, #10925, #3176, .T. ) ;
#44369=EDGE_CURVE ( 'NONE', #11744, #39972, #31737, .T. ) ;
#44371=CARTESIAN_POINT ( 'NONE',  ( -0.3780516546848963766, 0.01461794527752662519, 1.807623340459256989 ) ) ;
#44372=CARTESIAN_POINT ( 'NONE',  ( 2.947574761915768171, 1.205361022782829114E-17, -0.1816379373804913322 ) ) ;
#44375=CARTESIAN_POINT ( 'NONE',  ( 1.236813753895252166, 1.640077341046696890, -2.681693691597563767 ) ) ;
#44376=LINE ( 'NONE', #21406, #5604 ) ;
#44382=DIRECTION ( 'NONE',  ( -1.156061316345074457E-16, -1.000000000000000000, 1.040474016969491568E-17 ) ) ;
#44383=CIRCLE ( 'NONE', #14694, 2.165354330708661568 ) ;
#44385=CARTESIAN_POINT ( 'NONE',  ( -2.150793259809249847, 1.575027863729615341, -0.2506944975021367372 ) ) ;
#44386=EDGE_LOOP ( 'NONE', ( #23644, #7956, #39667, #40722 ) ) ;
#44388=CARTESIAN_POINT ( 'NONE',  ( 1.152568299495707382, 6.692913385826772199, 1.833124570921553342 ) ) ;
#44391=VECTOR ( 'NONE', #35971, 39.37007874015748143 ) ;
#44396=B_SPLINE_CURVE_WITH_KNOTS ( 'NONE', 3,
 ( #44742, #48337, #1900, #13017 ),
 .UNSPECIFIED., .F., .F.,
 ( 4, 4 ),
 ( 2.395904123760600257E-07, 0.002500455472051103887 ),
 .UNSPECIFIED. ) ;
#44397=CIRCLE ( 'NONE', #22959, 1.743387098533651480 ) ;
#44403=CARTESIAN_POINT ( 'NONE',  ( 0.07982360342473591996, 1.709180471932028711, 0.000000000000000000 ) ) ;
#44412=B_SPLINE_CURVE_WITH_KNOTS ( 'NONE', 3,
 ( #26413, #6297, #2671, #49106 ),
 .UNSPECIFIED., .F., .F.,
 ( 4, 4 ),
 ( 0.1211873102087489551, 0.1625992483279400380 ),
 .UNSPECIFIED. ) ;
#44414=CARTESIAN_POINT ( 'NONE',  ( -2.715141060683412100, 0.000000000000000000, -1.160506983230102040 ) ) ;
#44417=DIRECTION ( 'NONE',  ( 1.000000000000000000, 0.000000000000000000, 0.000000000000000000 ) ) ;
#44418=VECTOR ( 'NONE', #44257, 39.37007874015748143 ) ;
#44423=DIRECTION ( 'NONE',  ( -0.000000000000000000, 1.000000000000000000, -0.000000000000000000 ) ) ;
#44428=CIRCLE ( 'NONE', #13969, 2.244934639244525076 ) ;
#44429=PLANE ( 'NONE',  #38918 ) ;
#44439=CARTESIAN_POINT ( 'NONE',  ( 0.5111248625547512026, 1.013073221274083169, 2.540917155971571528 ) ) ;
#44453=B_SPLINE_CURVE_WITH_KNOTS ( 'NONE', 3,
 ( #28232, #27724, #8373, #43465 ),
 .UNSPECIFIED., .F., .F.,
 ( 4, 4 ),
 ( 0.1211873102087489551, 0.1625992483279400380 ),
 .UNSPECIFIED. ) ;
#44462=CARTESIAN_POINT ( 'NONE',  ( -2.122513613727505799, 1.575480814016643638, -0.4339716895473832436 ) ) ;
#44467=CARTESIAN_POINT ( 'NONE',  ( -1.067222945812429824, 0.5249316497054297148, -1.552631840991228973 ) ) ;
#44472=VERTEX_POINT ( 'NONE', #43923 ) ;
#44473=CARTESIAN_POINT ( 'NONE',  ( 2.393386496973425981, 1.651176226490313592, 0.8294036017652782755 ) ) ;
#44475=ORIENTED_EDGE ( 'NONE', *, *, #15970, .F. ) ;
#44479=EDGE_CURVE ( 'NONE', #45444, #32706, #8316, .T. ) ;
#44488=CARTESIAN_POINT ( 'NONE',  ( -1.330356682269850044, 1.588168657012911877, -1.747353411991260819 ) ) ;
#44489=DIRECTION ( 'NONE',  ( -0.000000000000000000, 1.000000000000000000, -0.000000000000000000 ) ) ;
#44491=VECTOR ( 'NONE', #43611, 39.37007874015748143 ) ;
#44493=LINE ( 'NONE', #4240, #43125 ) ;
#44505=CARTESIAN_POINT ( 'NONE',  ( -2.014664160120487768, 1.577208220393157223, -0.8075893616760145832 ) ) ;
#44510=ADVANCED_FACE ( 'NONE', ( #43412 ), #18138, .T. ) ;
#44515=CARTESIAN_POINT ( 'NONE',  ( -1.735196932040237394, 1.680109596358665636, 1.320828101803479315 ) ) ;
#44516=CARTESIAN_POINT ( 'NONE',  ( 2.889674983507178219, 5.905511811023623991, -0.6090712660037602699 ) ) ;
#44521=CARTESIAN_POINT ( 'NONE',  ( 0.000000000000000000, 6.692913385826772199, 0.000000000000000000 ) ) ;
#44522=VERTEX_POINT ( 'NONE', #28179 ) ;
#44525=ORIENTED_EDGE ( 'NONE', *, *, #47753, .T. ) ;
#44526=CYLINDRICAL_SURFACE ( 'NONE', #50427, 2.165354330708661568 ) ;
#44527=ORIENTED_EDGE ( 'NONE', *, *, #50951, .F. ) ;
#44528=EDGE_LOOP ( 'NONE', ( #21695, #7081, #703, #47361 ) ) ;
#44529=CARTESIAN_POINT ( 'NONE',  ( -2.356851836761542529, 1.575923956308009632, -0.5884142439354561605 ) ) ;
#44531=CARTESIAN_POINT ( 'NONE',  ( 2.168245791271197209, 1.753049777144058297, -2.004968704497248844 ) ) ;
#44532=ORIENTED_EDGE ( 'NONE', *, *, #39249, .T. ) ;
#44533=FACE_OUTER_BOUND ( 'NONE', #11544, .T. ) ;
#44534=CARTESIAN_POINT ( 'NONE',  ( 0.000000000000000000, 0.000000000000000000, 0.000000000000000000 ) ) ;
#44535=CARTESIAN_POINT ( 'NONE',  ( 1.807908292590730825, 0.5224481969157015460, 1.378813476911973535 ) ) ;
#44536=AXIS2_PLACEMENT_3D ( 'NONE', #27775, #24169, #43258 ) ;
#44539=EDGE_CURVE ( 'NONE', #2307, #12681, #17567, .T. ) ;
#44540=CARTESIAN_POINT ( 'NONE',  ( 0.2841802383804452603, 0.03247133209088205741, 1.841575167587790718 ) ) ;
#44542=ORIENTED_EDGE ( 'NONE', *, *, #26840, .T. ) ;
#44545=AXIS2_PLACEMENT_3D ( 'NONE', #23741, #23232, #4381 ) ;
#44550=CARTESIAN_POINT ( 'NONE',  ( 1.232620761116212771, 5.905511811023623991, -1.780282403660734980 ) ) ;
#44554=CARTESIAN_POINT ( 'NONE',  ( -2.044241703397525978, 1.205361022782829114E-17, -0.7159595814952911530 ) ) ;
#44556=DIRECTION ( 'NONE',  ( 0.04486483035050446017, 0.000000000000000000, 0.9989930665413151445 ) ) ;
#44561=ADVANCED_FACE ( 'NONE', ( #16318 ), #15556, .T. ) ;
#44570=VECTOR ( 'NONE', #16495, 39.37007874015748854 ) ;
#44575=CARTESIAN_POINT ( 'NONE',  ( 0.1250607540065018508, 1.205361022782829114E-17, -1.938545675207280272 ) ) ;
#44576=ORIENTED_EDGE ( 'NONE', *, *, #13629, .T. ) ;
#44579=CONICAL_SURFACE ( 'NONE', #17398, 2.246510896728926010, 0.01601546068027819014 ) ;
#44587=CARTESIAN_POINT ( 'NONE',  ( 0.1735763337869204448, 1.714436956846898896, -2.477597915911436299 ) ) ;
#44590=DIRECTION ( 'NONE',  ( -0.9998717552508122886, -0.01601477604151182316, 0.000000000000000000 ) ) ;
#44591=VERTEX_POINT ( 'NONE', #42904 ) ;
#44594=CARTESIAN_POINT ( 'NONE',  ( 2.278027606577265107, 1.645963535160160696, -0.4694667435916627385 ) ) ;
#44602=EDGE_CURVE ( 'NONE', #1849, #39003, #47767, .T. ) ;
#44605=EDGE_CURVE ( 'NONE', #4372, #46764, #2748, .T. ) ;
#44609=CONICAL_SURFACE ( 'NONE', #28957, 3.483074324928249421, 1.244861948955335196 ) ;
#44613=VECTOR ( 'NONE', #46869, 39.37007874015748143 ) ;
#44619=CARTESIAN_POINT ( 'NONE',  ( -1.083598637574820334, 1.702374950942735499, 2.747180975113330259 ) ) ;
#44621=ORIENTED_EDGE ( 'NONE', *, *, #15834, .T. ) ;
#44626=B_SPLINE_CURVE_WITH_KNOTS ( 'NONE', 3,
 ( #14660, #2532, #46125, #10780 ),
 .UNSPECIFIED., .F., .F.,
 ( 4, 4 ),
 ( 1.995997118274627782E-07, 0.001216554165443645879 ),
 .UNSPECIFIED. ) ;
#44627=EDGE_CURVE ( 'NONE', #26908, #49287, #36042, .T. ) ;
#44629=CARTESIAN_POINT ( 'NONE',  ( -2.494510946366233384, 1.676303183382823025, -1.012685720897419150 ) ) ;
#44633=CARTESIAN_POINT ( 'NONE',  ( -2.100227814008681637, 1.588094595312779855, -2.076109931251943763 ) ) ;
#44648=AXIS2_PLACEMENT_3D ( 'NONE', #8461, #31706, #11569 ) ;
#44654=CARTESIAN_POINT ( 'NONE',  ( 0.1067246931122726866, 0.02962905676920215767, 0.000000000000000000 ) ) ;
#44655=DIRECTION ( 'NONE',  ( 0.01601477604151182663, -0.9998717552508123996, 0.000000000000000000 ) ) ;
#44667=DIRECTION ( 'NONE',  ( -3.986037398843765983E-20, -1.000000000000000000, -1.160734090543304660E-16 ) ) ;
#44669=LINE ( 'NONE', #45426, #9412 ) ;
#44676=EDGE_LOOP ( 'NONE', ( #24689, #35110, #4341, #25087 ) ) ;
#44680=CONICAL_SURFACE ( 'NONE', #45527, 3.483074324928249421, 1.244861948955335196 ) ;
#44681=VERTEX_POINT ( 'NONE', #5205 ) ;
#44687=VERTEX_POINT ( 'NONE', #9336 ) ;
#44699=CARTESIAN_POINT ( 'NONE',  ( 0.1155636338427008941, -0.5222242541845523167, 0.000000000000000000 ) ) ;
#44700=LINE ( 'NONE', #9612, #22074 ) ;
#44702=ORIENTED_EDGE ( 'NONE', *, *, #4071, .T. ) ;
#44703=DIRECTION ( 'NONE',  ( 0.000000000000000000, 1.000000000000000000, -0.000000000000000000 ) ) ;
#44705=LINE ( 'NONE', #9358, #38978 ) ;
#44706=ORIENTED_EDGE ( 'NONE', *, *, #3587, .F. ) ;
#44710=AXIS2_PLACEMENT_3D ( 'NONE', #40539, #5164, #24533 ) ;
#44711=LINE ( 'NONE', #25115, #16249 ) ;
#44712=CARTESIAN_POINT ( 'NONE',  ( -0.7328193673159020260, 1.696164507524817511, 2.092647490920610309 ) ) ;
#44718=ORIENTED_EDGE ( 'NONE', *, *, #29460, .T. ) ;
#44720=LINE ( 'NONE', #25627, #46501 ) ;
#44721=AXIS2_PLACEMENT_3D ( 'NONE', #14013, #9886, #25121 ) ;
#44723=B_SPLINE_CURVE_WITH_KNOTS ( 'NONE', 3,
 ( #37752, #33121, #13992, #2375 ),
 .UNSPECIFIED., .F., .F.,
 ( 4, 4 ),
 ( 0.1211775127643062860, 0.1625894504277921315 ),
 .UNSPECIFIED. ) ;
#44727=CARTESIAN_POINT ( 'NONE',  ( -1.560823827823494936, 0.000000000000000000, 0.8212364767474445992 ) ) ;
#44728=LINE ( 'NONE', #49083, #6298 ) ;
#44730=EDGE_LOOP ( 'NONE', ( #1684, #6004, #35062, #21040 ) ) ;
#44733=B_SPLINE_CURVE_WITH_KNOTS ( 'NONE', 3,
 ( #29741, #49820, #22002, #49566 ),
 .UNSPECIFIED., .F., .F.,
 ( 4, 4 ),
 ( 2.271247881248620160E-07, 0.002500295357758199402 ),
 .UNSPECIFIED. ) ;
#44740=DIRECTION ( 'NONE',  ( -0.000000000000000000, -1.000000000000000000, 0.000000000000000000 ) ) ;
#44741=B_SPLINE_CURVE_WITH_KNOTS ( 'NONE', 3,
 ( #42484, #26980, #50677, #3502 ),
 .UNSPECIFIED., .F., .F.,
 ( 4, 4 ),
 ( 0.1211873102087489551, 0.1625992483279400380 ),
 .UNSPECIFIED. ) ;
#44742=CARTESIAN_POINT ( 'NONE',  ( 2.491402175429653809, 1.458524810485662959, -1.585592796919505609 ) ) ;
#44748=CARTESIAN_POINT ( 'NONE',  ( 0.6770709118595397147, 1.627661423436544519, -2.638295496325671063 ) ) ;
#44760=CARTESIAN_POINT ( 'NONE',  ( -1.556712866041156662, 1.548291375251236834, 2.509548638715847435 ) ) ;
#44762=DIRECTION ( 'NONE',  ( -0.6579387259397136978, 0.000000000000000000, 0.7530714660036097463 ) ) ;
#44767=LINE ( 'NONE', #1671, #10610 ) ;
#44772=EDGE_CURVE ( 'NONE', #36107, #1640, #26386, .T. ) ;
#44775=ORIENTED_EDGE ( 'NONE', *, *, #2303, .T. ) ;
#44778=VERTEX_POINT ( 'NONE', #50053 ) ;
#44791=AXIS2_PLACEMENT_3D ( 'NONE', #4907, #43106, #35132 ) ;
#44793=CARTESIAN_POINT ( 'NONE',  ( -2.145573069125249699, 1.587379441712122086, -2.028682512702774332 ) ) ;
#44794=ORIENTED_EDGE ( 'NONE', *, *, #33754, .T. ) ;
#44797=EDGE_CURVE ( 'NONE', #35652, #18042, #4034, .T. ) ;
#44799=CONICAL_SURFACE ( 'NONE', #10214, 1.850107469027523210, 0.6386652850508578450 ) ;
#44802=CARTESIAN_POINT ( 'NONE',  ( 1.958513403246152640, 1.640845930445798073, -1.233835998176425308 ) ) ;
#44803=B_SPLINE_CURVE_WITH_KNOTS ( 'NONE', 3,
 ( #30709, #39206, #46667, #30460 ),
 .UNSPECIFIED., .F., .F.,
 ( 4, 4 ),
 ( 0.01092706744755390577, 0.03073589647694806304 ),
 .UNSPECIFIED. ) ;
#44804=CARTESIAN_POINT ( 'NONE',  ( -2.100227814008681637, 0.000000000000000000, -2.076109931251943763 ) ) ;
#44812=ORIENTED_EDGE ( 'NONE', *, *, #29200, .F. ) ;
#44817=ORIENTED_EDGE ( 'NONE', *, *, #6210, .T. ) ;
#44818=VERTEX_POINT ( 'NONE', #14226 ) ;
#44822=ORIENTED_EDGE ( 'NONE', *, *, #14715, .F. ) ;
#44825=CARTESIAN_POINT ( 'NONE',  ( -2.923830769312651068, 1.673677222459564851, 0.4126138247051237551 ) ) ;
#44832=VECTOR ( 'NONE', #6665, 39.37007874015748143 ) ;
#44836=AXIS2_PLACEMENT_3D ( 'NONE', #31745, #49602, #33916 ) ;
#44844=ORIENTED_EDGE ( 'NONE', *, *, #47370, .F. ) ;
#44845=CARTESIAN_POINT ( 'NONE',  ( 2.151809081513405442, 2.755905511811027164, 0.2418202932658665705 ) ) ;
#44848=VERTEX_POINT ( 'NONE', #42099 ) ;
#44849=CARTESIAN_POINT ( 'NONE',  ( -2.695799277629577162, 1.571269479597534824, -1.205759334241492731 ) ) ;
#44850=CARTESIAN_POINT ( 'NONE',  ( -1.221295136473707243, 0.000000000000000000, 1.323086612934683215 ) ) ;
#44855=DIRECTION ( 'NONE',  ( -0.7818314824680309139, -7.233942271706491519E-17, 0.6234898018587318180 ) ) ;
#44857=DIRECTION ( 'NONE',  ( 0.9998717552508121775, 0.01601477604151182663, 0.000000000000000000 ) ) ;
#44858=ORIENTED_EDGE ( 'NONE', *, *, #37655, .T. ) ;
#44859=CARTESIAN_POINT ( 'NONE',  ( -0.7728391137233561192, 0.5249316497054296038, -1.718240423813754747 ) ) ;
#44860=CARTESIAN_POINT ( 'NONE',  ( -1.236813753895213086, 1.699986652445209634, -2.681693691597581974 ) ) ;
#44865=AXIS2_PLACEMENT_3D ( 'NONE', #16451, #36842, #5590 ) ;
#44866=VERTEX_POINT ( 'NONE', #7245 ) ;
#44880=VERTEX_POINT ( 'NONE', #45692 ) ;
#44885=ORIENTED_EDGE ( 'NONE', *, *, #30997, .T. ) ;
#44894=CARTESIAN_POINT ( 'NONE',  ( -1.325491792074585229, 5.905511811023623991, -2.638988599164752369 ) ) ;
#44896=EDGE_CURVE ( 'NONE', #31511, #36611, #45313, .T. ) ;
#44901=ORIENTED_EDGE ( 'NONE', *, *, #34521, .F. ) ;
#44902=CONICAL_SURFACE ( 'NONE', #23456, 2.246510896728926010, 0.01601546068027819014 ) ;
#44905=ORIENTED_EDGE ( 'NONE', *, *, #8495, .F. ) ;
#44906=DIRECTION ( 'NONE',  ( 0.01601477604151182663, -0.9998717552508123996, 0.000000000000000000 ) ) ;
#44912=ORIENTED_EDGE ( 'NONE', *, *, #30155, .T. ) ;
#44913=AXIS2_PLACEMENT_3D ( 'NONE', #19628, #38515, #46472 ) ;
#44916=DIRECTION ( 'NONE',  ( 0.8090169943749506709, 0.000000000000000000, -0.5877852522924684742 ) ) ;
#44918=CARTESIAN_POINT ( 'NONE',  ( -1.720314620805551087, 0.000000000000000000, 0.2826945007888154726 ) ) ;
#44919=CARTESIAN_POINT ( 'NONE',  ( -1.453832412804729302, 0.000000000000000000, -1.018633753700964428 ) ) ;
#44921=EDGE_CURVE ( 'NONE', #12966, #36796, #260, .T. ) ;
#44925=DIRECTION ( 'NONE',  ( -0.6579387259397136978, 0.000000000000000000, 0.7530714660036097463 ) ) ;
#44926=ORIENTED_EDGE ( 'NONE', *, *, #28330, .F. ) ;
#44931=ORIENTED_EDGE ( 'NONE', *, *, #29700, .F. ) ;
#44941=CARTESIAN_POINT ( 'NONE',  ( -0.1450934409768900590, 0.000000000000000000, 2.161127057262024032 ) ) ;
#44947=CARTESIAN_POINT ( 'NONE',  ( 0.9319704666822036243, 0.04284687812831378811, 1.655805649632502430 ) ) ;
#44951=FACE_OUTER_BOUND ( 'NONE', #30927, .T. ) ;
#44953=ADVANCED_FACE ( 'NONE', ( #35622 ), #38983, .T. ) ;
#44956=( BOUNDED_CURVE ( )  B_SPLINE_CURVE ( 3, ( #28672, #20153, #47744, #36689 ),
 .UNSPECIFIED., .F., .F. ) 
 B_SPLINE_CURVE_WITH_KNOTS ( ( 4, 4 ),
 ( 1.282939940669038714, 1.333860994033941205 ),
 .UNSPECIFIED. ) 
 CURVE ( )  GEOMETRIC_REPRESENTATION_ITEM ( )  RATIONAL_B_SPLINE_CURVE ( ( 1.000000000000000000, 0.9997839321993498007, 0.9997839321993498007, 1.000000000000000000 ) ) 
 REPRESENTATION_ITEM ( '' )  );
#44958=CARTESIAN_POINT ( 'NONE',  ( 1.232620761116212771, 6.692913385826772199, -1.780282403660734758 ) ) ;
#44959=ADVANCED_FACE ( 'NONE', ( #35878 ), #18178, .F. ) ;
#44962=DIRECTION ( 'NONE',  ( 0.000000000000000000, 0.000000000000000000, 1.000000000000000000 ) ) ;
#44967=CARTESIAN_POINT ( 'NONE',  ( 0.7381027496705269142, 1.205361022782829114E-17, -2.859439394060913298 ) ) ;
#44968=CARTESIAN_POINT ( 'NONE',  ( 1.836615784862988932, 1.645866884192403123, 2.027377764185913200 ) ) ;
#44969=PLANE ( 'NONE',  #31247 ) ;
#44979=VECTOR ( 'NONE', #43616, 39.37007874015748143 ) ;
#44986=CARTESIAN_POINT ( 'NONE',  ( 1.443077687459978886, 1.639689301329355198, 2.319355385847401418 ) ) ;
#44989=ADVANCED_FACE ( 'NONE', ( #34865 ), #29712, .F. ) ;
#44991=CARTESIAN_POINT ( 'NONE',  ( -1.478704527843389682, 1.589829732135338070, -1.951536704579532433 ) ) ;
#44993=CARTESIAN_POINT ( 'NONE',  ( 0.08139965876239094178, 1.610780518492231694, 0.000000000000000000 ) ) ;
#44995=ORIENTED_EDGE ( 'NONE', *, *, #5595, .T. ) ;
#44997=DIRECTION ( 'NONE',  ( 0.000000000000000000, 0.000000000000000000, 1.000000000000000000 ) ) ;
#44998=CARTESIAN_POINT ( 'NONE',  ( 2.013079221890065273, 0.03945196200391452857, -0.1396696942857607870 ) ) ;
#45001=DIRECTION ( 'NONE',  ( -0.3090169943749582204, 0.000000000000000000, 0.9510565162951500895 ) ) ;
#45003=EDGE_LOOP ( 'NONE', ( #15261, #30379, #933, #2421 ) ) ;
#45005=DIRECTION ( 'NONE',  ( 0.000000000000000000, 0.000000000000000000, 1.000000000000000000 ) ) ;
#45006=DIRECTION ( 'NONE',  ( 0.000000000000000000, 0.000000000000000000, 1.000000000000000000 ) ) ;
#45007=CARTESIAN_POINT ( 'NONE',  ( 0.000000000000000000, 6.692913385826772199, 0.000000000000000000 ) ) ;
#45010=ORIENTED_EDGE ( 'NONE', *, *, #21936, .F. ) ;
#45011=ORIENTED_EDGE ( 'NONE', *, *, #39319, .T. ) ;
#45015=VECTOR ( 'NONE', #19513, 39.37007874015748143 ) ;
#45021=EDGE_CURVE ( 'NONE', #13400, #51046, #16517, .T. ) ;
#45022=ORIENTED_EDGE ( 'NONE', *, *, #40092, .F. ) ;
#45026=CARTESIAN_POINT ( 'NONE',  ( -1.843472447131334624, 1.579950168977349412, -1.157898127912315944 ) ) ;
#45027=EDGE_CURVE ( 'NONE', #39907, #47540, #5115, .T. ) ;
#45034=ORIENTED_EDGE ( 'NONE', *, *, #5283, .F. ) ;
#45035=ORIENTED_EDGE ( 'NONE', *, *, #13214, .F. ) ;
#45046=CARTESIAN_POINT ( 'NONE',  ( -0.3136974817027967100, 1.522126940893053337, -2.936457595020224520 ) ) ;
#45057=CARTESIAN_POINT ( 'NONE',  ( -2.160407304981126764, 1.574803149606302854, -0.1462862061266896330 ) ) ;
#45060=CARTESIAN_POINT ( 'NONE',  ( -0.5968551078519344077, 0.01230706739460726146, 1.730372017133659845 ) ) ;
#45063=ORIENTED_EDGE ( 'NONE', *, *, #82, .T. ) ;
#45070=ORIENTED_EDGE ( 'NONE', *, *, #39906, .F. ) ;
#45074=EDGE_CURVE ( 'NONE', #17294, #31774, #1532, .T. ) ;
#45076=VERTEX_POINT ( 'NONE', #16520 ) ;
#45083=CARTESIAN_POINT ( 'NONE',  ( -2.154691421597259904, 1.673393017852502718, -0.2175766031914168064 ) ) ;
#45085=EDGE_LOOP ( 'NONE', ( #27248, #18956, #18536, #7395 ) ) ;
#45087=CARTESIAN_POINT ( 'NONE',  ( -1.743145509346914590, -1.899488058094683170E-15, 0.000000000000000000 ) ) ;
#45089=ORIENTED_EDGE ( 'NONE', *, *, #20569, .T. ) ;
#45094=ORIENTED_EDGE ( 'NONE', *, *, #31264, .F. ) ;
#45099=LINE ( 'NONE', #9759, #18721 ) ;
#45113=ADVANCED_FACE ( 'NONE', ( #47964 ), #28637, .F. ) ;
#45117=EDGE_CURVE ( 'NONE', #44259, #50692, #24872, .T. ) ;
#45121=CARTESIAN_POINT ( 'NONE',  ( -0.3857230305054721864, 0.000000000000000000, 1.849896105471422025 ) ) ;
#45122=LINE ( 'NONE', #1774, #356 ) ;
#45123=LINE ( 'NONE', #1775, #36793 ) ;
#45126=ORIENTED_EDGE ( 'NONE', *, *, #29515, .F. ) ;
#45128=ORIENTED_EDGE ( 'NONE', *, *, #33301, .T. ) ;
#45129=DIRECTION ( 'NONE',  ( -0.9998717552508122886, -0.01601477604151185785, 0.000000000000000000 ) ) ;
#45135=CARTESIAN_POINT ( 'NONE',  ( 1.472219874544873131, 0.000000000000000000, 2.560030851058970214 ) ) ;
#45138=VERTEX_POINT ( 'NONE', #21162 ) ;
#45140=DIRECTION ( 'NONE',  ( -0.9998717552508121775, -0.01601477604151182663, 0.000000000000000000 ) ) ;
#45145=VECTOR ( 'NONE', #756, 39.37007874015748143 ) ;
#45146=ORIENTED_EDGE ( 'NONE', *, *, #38571, .F. ) ;
#45147=ORIENTED_EDGE ( 'NONE', *, *, #11979, .T. ) ;
#45159=ORIENTED_EDGE ( 'NONE', *, *, #7530, .F. ) ;
#45160=VERTEX_POINT ( 'NONE', #17037 ) ;
#45164=CIRCLE ( 'NONE', #20454, 2.164630168518208109 ) ;
#45166=CARTESIAN_POINT ( 'NONE',  ( -2.339241080213612545, 0.000000000000000000, 1.802537235681884065 ) ) ;
#45170=ORIENTED_EDGE ( 'NONE', *, *, #32815, .F. ) ;
#45173=EDGE_CURVE ( 'NONE', #30240, #20976, #29820, .T. ) ;
#45176=ORIENTED_EDGE ( 'NONE', *, *, #20888, .F. ) ;
#45178=DIRECTION ( 'NONE',  ( 0.5128992774058948045, 0.000000000000000000, 0.8584487936018727616 ) ) ;
#45182=ORIENTED_EDGE ( 'NONE', *, *, #7096, .T. ) ;
#45192=EDGE_LOOP ( 'NONE', ( #23487, #36169, #6415, #25897 ) ) ;
#45210=EDGE_LOOP ( 'NONE', ( #21462, #46741, #15841, #15208 ) ) ;
#45212=ADVANCED_FACE ( 'NONE', ( #2047 ), #30173, .F. ) ;
#45216=LINE ( 'NONE', #5998, #4090 ) ;
#45232=VECTOR ( 'NONE', #44237, 39.37007874015748143 ) ;
#45235=ORIENTED_EDGE ( 'NONE', *, *, #5257, .F. ) ;
#45237=CARTESIAN_POINT ( 'NONE',  ( 0.1067246931122726866, 0.02962905676920215767, 0.000000000000000000 ) ) ;
#45248=CARTESIAN_POINT ( 'NONE',  ( -0.7380211471543357549, 0.01609890615456165824, -1.645940171248041928 ) ) ;
#45252=( BOUNDED_CURVE ( )  B_SPLINE_CURVE ( 3, ( #26887, #42382, #10398, #6533 ),
 .UNSPECIFIED., .F., .F. ) 
 B_SPLINE_CURVE_WITH_KNOTS ( ( 4, 4 ),
 ( 6.208269093772826430, 6.259010602608490181 ),
 .UNSPECIFIED. ) 
 CURVE ( )  GEOMETRIC_REPRESENTATION_ITEM ( )  RATIONAL_B_SPLINE_CURVE ( ( 1.000000000000000000, 0.9997854531153357316, 0.9997854531153357316, 1.000000000000000000 ) ) 
 REPRESENTATION_ITEM ( '' )  );
#45256=ORIENTED_EDGE ( 'NONE', *, *, #2064, .T. ) ;
#45270=ORIENTED_EDGE ( 'NONE', *, *, #29275, .F. ) ;
#45272=LINE ( 'NONE', #6817, #19902 ) ;
#45279=CARTESIAN_POINT ( 'NONE',  ( 0.2508718039770792552, 1.711920121901901348, -2.238407143905190910 ) ) ;
#45280=CARTESIAN_POINT ( 'NONE',  ( -1.247273217833388514, 0.007942302252338809612, -1.260601835943744087 ) ) ;
#45281=EDGE_CURVE ( 'NONE', #39129, #9746, #50000, .T. ) ;
#45284=DIRECTION ( 'NONE',  ( -1.267583980596140612E-16, 1.000000000000000000, 2.300325776299552367E-17 ) ) ;
#45287=EDGE_CURVE ( 'NONE', #23634, #17198, #33811, .T. ) ;
#45289=CARTESIAN_POINT ( 'NONE',  ( 0.08139965876239094178, 1.610780518492231694, 0.000000000000000000 ) ) ;
#45290=EDGE_CURVE ( 'NONE', #1678, #11612, #50287, .T. ) ;
#45293=CARTESIAN_POINT ( 'NONE',  ( 2.059921668671832240, 6.692913385826772199, 0.7210543110491620666 ) ) ;
#45295=ORIENTED_EDGE ( 'NONE', *, *, #10414, .F. ) ;
#45300=AXIS2_PLACEMENT_3D ( 'NONE', #33639, #1619, #2128 ) ;
#45301=ORIENTED_EDGE ( 'NONE', *, *, #6261, .F. ) ;
#45307=CARTESIAN_POINT ( 'NONE',  ( -2.225563356869989295, 1.047115081372295142, 1.253512298962777605 ) ) ;
#45309=CARTESIAN_POINT ( 'NONE',  ( 1.959936762177996838, 0.000000000000000000, -0.8199101346145926117 ) ) ;
#45310=ADVANCED_FACE ( 'NONE', ( #22179 ), #17791, .T. ) ;
#45313=CIRCLE ( 'NONE', #23078, 2.244934639244525076 ) ;
#45316=CARTESIAN_POINT ( 'NONE',  ( 0.08119777152254364916, 1.623385212329073957, 0.000000000000000000 ) ) ;
#45319=EDGE_LOOP ( 'NONE', ( #32020, #22514, #14087, #18582 ) ) ;
#45320=ORIENTED_EDGE ( 'NONE', *, *, #5121, .T. ) ;
#45322=ORIENTED_EDGE ( 'NONE', *, *, #11123, .T. ) ;
#45323=CARTESIAN_POINT ( 'NONE',  ( 0.000000000000000000, 6.692913385826772199, 0.000000000000000000 ) ) ;
#45327=VERTEX_POINT ( 'NONE', #37426 ) ;
#45330=CARTESIAN_POINT ( 'NONE',  ( 2.473328170516846836, 1.757793565757150178, -1.612973743985320008 ) ) ;
#45332=CARTESIAN_POINT ( 'NONE',  ( -0.4788131938641533303, 1.711801685632677428, 2.914091152102185944 ) ) ;
#45337=AXIS2_PLACEMENT_3D ( 'NONE', #2701, #49392, #41944 ) ;
#45341=ORIENTED_EDGE ( 'NONE', *, *, #23160, .T. ) ;
#45344=ORIENTED_EDGE ( 'NONE', *, *, #19760, .F. ) ;
#45345=VECTOR ( 'NONE', #44382, 39.37007874015748143 ) ;
#45349=EDGE_CURVE ( 'NONE', #41090, #15209, #27298, .T. ) ;
#45350=EDGE_LOOP ( 'NONE', ( #15581, #7626, #5826, #46012 ) ) ;
#45351=CARTESIAN_POINT ( 'NONE',  ( 0.002207914879453961969, 6.692913385826772199, 0.04916304461325451958 ) ) ;
#45352=CARTESIAN_POINT ( 'NONE',  ( -0.2052282226254269204, 0.000000000000000000, -1.731265419273310346 ) ) ;
#45359=CARTESIAN_POINT ( 'NONE',  ( 0.7090793742677682365, 0.03927686936677046714, 1.749277966691849429 ) ) ;
#45361=ORIENTED_EDGE ( 'NONE', *, *, #27385, .F. ) ;
#45365=ORIENTED_EDGE ( 'NONE', *, *, #49938, .F. ) ;
#45370=CARTESIAN_POINT ( 'NONE',  ( 0.1580252402616749152, 0.000000000000000000, -1.939804032141613899 ) ) ;
#45375=CARTESIAN_POINT ( 'NONE',  ( 1.068402561569975484, 0.000000000000000000, -1.884154513482173554 ) ) ;
#45377=ORIENTED_EDGE ( 'NONE', *, *, #11167, .F. ) ;
#45378=CARTESIAN_POINT ( 'NONE',  ( -1.942732458483407143, 5.905511811023623991, 2.223636218514597029 ) ) ;
#45383=CARTESIAN_POINT ( 'NONE',  ( -1.364345965745727973, 1.205361022782829114E-17, 1.150974876880269893 ) ) ;
#45384=CONICAL_SURFACE ( 'NONE', #13276, 2.246510896728926010, 0.01601546068027819014 ) ;
#45389=CARTESIAN_POINT ( 'NONE',  ( -1.741986320419516954, 0.0003450591842249390597, 0.08333880254314324221 ) ) ;
#45395=FACE_OUTER_BOUND ( 'NONE', #21849, .T. ) ;
#45398=ORIENTED_EDGE ( 'NONE', *, *, #3587, .T. ) ;
#45410=VECTOR ( 'NONE', #2244, 39.37007874015748143 ) ;
#45412=CARTESIAN_POINT ( 'NONE',  ( -0.5756566573089010319, 5.905511811023623103, 2.896516654582635297 ) ) ;
#45415=DIRECTION ( 'NONE',  ( 0.9998717552508121775, 0.01601477604151182663, 0.000000000000000000 ) ) ;
#45417=CONICAL_SURFACE ( 'NONE', #13315, 3.033577403570480779, 1.554780866114618743 ) ;
#45421=VECTOR ( 'NONE', #32192, 39.37007874015748143 ) ;
#45423=CYLINDRICAL_SURFACE ( 'NONE', #26775, 2.164630168518208109 ) ;
#45425=VERTEX_POINT ( 'NONE', #15187 ) ;
#45426=CARTESIAN_POINT ( 'NONE',  ( -0.6233543567505155369, 6.692913385826772199, -2.073689640095379705 ) ) ;
#45427=CARTESIAN_POINT ( 'NONE',  ( 0.07982360342473591996, 1.709180471932028711, 0.000000000000000000 ) ) ;
#45428=EDGE_CURVE ( 'NONE', #30012, #43842, #30937, .T. ) ;
#45429=ORIENTED_EDGE ( 'NONE', *, *, #45612, .F. ) ;
#45431=CARTESIAN_POINT ( 'NONE',  ( 2.793030215715258446, 1.762782749918499814, 0.9592557174602684977 ) ) ;
#45432=ORIENTED_EDGE ( 'NONE', *, *, #8366, .F. ) ;
#45433=VERTEX_POINT ( 'NONE', #22934 ) ;
#45444=VERTEX_POINT ( 'NONE', #23688 ) ;
#45446=CARTESIAN_POINT ( 'NONE',  ( -0.8244711865321519006, 0.01471425056033665718, -1.598608591632243892 ) ) ;
#45450=B_SPLINE_CURVE_WITH_KNOTS ( 'NONE', 3,
 ( #26144, #13766, #30017, #1886 ),
 .UNSPECIFIED., .F., .F.,
 ( 4, 4 ),
 ( 2.331048520511536045E-07, 0.002500624525913899138 ),
 .UNSPECIFIED. ) ;
#45451=AXIS2_PLACEMENT_3D ( 'NONE', #19719, #35480, #12239 ) ;
#45456=ORIENTED_EDGE ( 'NONE', *, *, #46972, .T. ) ;
#45459=EDGE_CURVE ( 'NONE', #29978, #15353, #38687, .T. ) ;
#45461=CARTESIAN_POINT ( 'NONE',  ( 2.093903048064389427, 0.000000000000000000, -0.4274415146361335571 ) ) ;
#45465=EDGE_CURVE ( 'NONE', #31969, #1849, #20578, .T. ) ;
#45473=ORIENTED_EDGE ( 'NONE', *, *, #10997, .F. ) ;
#45482=ORIENTED_EDGE ( 'NONE', *, *, #23160, .F. ) ;
#45483=LINE ( 'NONE', #9640, #50507 ) ;
#45490=DIRECTION ( 'NONE',  ( -0.9998717552508121775, -0.01601477604151185438, 0.000000000000000000 ) ) ;
#45497=CARTESIAN_POINT ( 'NONE',  ( 1.080407128400152184, 1.049866565067838264, 1.712347114214678001 ) ) ;
#45499=CARTESIAN_POINT ( 'NONE',  ( -0.8221900955658372201, 5.905511811023623991, 2.050660405798877317 ) ) ;
#45502=CARTESIAN_POINT ( 'NONE',  ( 0.000000000000000000, 6.692913385826772199, 0.000000000000000000 ) ) ;
#45506=VERTEX_POINT ( 'NONE', #4584 ) ;
#45508=CARTESIAN_POINT ( 'NONE',  ( 1.441820561149283586, 0.5249316497054297148, 1.212758805029070741 ) ) ;
#45510=CARTESIAN_POINT ( 'NONE',  ( -1.325491792074585451, 1.600165750963108646, -2.638988599164751481 ) ) ;
#45526=ORIENTED_EDGE ( 'NONE', *, *, #14715, .T. ) ;
#45527=AXIS2_PLACEMENT_3D ( 'NONE', #31911, #35010, #399 ) ;
#45529=CARTESIAN_POINT ( 'NONE',  ( 1.630393911741433000, 1.635590496292660179, -1.626902725537468619 ) ) ;
#45530=EDGE_CURVE ( 'NONE', #47803, #8328, #35528, .T. ) ;
#45535=ADVANCED_FACE ( 'NONE', ( #24721 ), #45384, .T. ) ;
#45538=VERTEX_POINT ( 'NONE', #1223 ) ;
#45541=EDGE_CURVE ( 'NONE', #2720, #36292, #21102, .T. ) ;
#45542=CARTESIAN_POINT ( 'NONE',  ( -2.099568260077699478, 5.905511811023623991, -0.5296909464896105701 ) ) ;
#45548=B_SPLINE_CURVE_WITH_KNOTS ( 'NONE', 3,
 ( #35850, #1500, #13377, #44850 ),
 .UNSPECIFIED., .F., .F.,
 ( 4, 4 ),
 ( 0.0008755238761999696888, 0.001539766364033689182 ),
 .UNSPECIFIED. ) ;
#45550=VERTEX_POINT ( 'NONE', #20323 ) ;
#45553=ORIENTED_EDGE ( 'NONE', *, *, #49241, .F. ) ;
#45558=VECTOR ( 'NONE', #26429, 39.37007874015748143 ) ;
#45571=VECTOR ( 'NONE', #1699, 39.37007874015748143 ) ;
#45572=CARTESIAN_POINT ( 'NONE',  ( -2.823445274216743073, 1.573787237234608005, 0.8656477926280277124 ) ) ;
#45574=DIRECTION ( 'NONE',  ( -0.01601477604151182663, 0.9998717552508123996, -0.000000000000000000 ) ) ;
#45577=CARTESIAN_POINT ( 'NONE',  ( -0.5905738936209794510, 0.01846054376545745376, 1.713635781666723146 ) ) ;
#45578=ORIENTED_EDGE ( 'NONE', *, *, #36695, .F. ) ;
#45580=CARTESIAN_POINT ( 'NONE',  ( 2.576863348864710801, 1.759415398959654819, 1.442554885838449819 ) ) ;
#45581=ORIENTED_EDGE ( 'NONE', *, *, #26876, .T. ) ;
#45582=CARTESIAN_POINT ( 'NONE',  ( -0.3136974817027969320, 1.205361022782829114E-17, -2.936457595020224520 ) ) ;
#45584=ORIENTED_EDGE ( 'NONE', *, *, #50240, .T. ) ;
#45587=ORIENTED_EDGE ( 'NONE', *, *, #11000, .F. ) ;
#45588=DIRECTION ( 'NONE',  ( 0.3930250316539147803, 0.000000000000000000, 0.9195277725514544587 ) ) ;
#45590=B_SPLINE_CURVE_WITH_KNOTS ( 'NONE', 3,
 ( #25448, #22098, #29062, #25963 ),
 .UNSPECIFIED., .F., .F.,
 ( 4, 4 ),
 ( 0.0007385519321130311256, 0.003238853935468911406 ),
 .UNSPECIFIED. ) ;
#45591=CIRCLE ( 'NONE', #44791, 2.244934639244525076 ) ;
#45594=CARTESIAN_POINT ( 'NONE',  ( 1.388309139374679146, 1.631713065620022274, -1.827118126197171399 ) ) ;
#45600=DIRECTION ( 'NONE',  ( 5.500355109725658086E-17, -1.000000000000000000, 1.022137253806229789E-16 ) ) ;
#45601=AXIS2_PLACEMENT_3D ( 'NONE', #36249, #43707, #616 ) ;
#45603=CARTESIAN_POINT ( 'NONE',  ( 0.4932906694934566239, 1.621072181458971251, 2.442642652141415738 ) ) ;
#45604=CARTESIAN_POINT ( 'NONE',  ( 0.000000000000000000, 6.692913385826772199, 0.000000000000000000 ) ) ;
#45606=DIRECTION ( 'NONE',  ( 0.000000000000000000, -1.000000000000000000, 0.000000000000000000 ) ) ;
#45612=EDGE_CURVE ( 'NONE', #38164, #42095, #3383, .T. ) ;
#45616=FACE_OUTER_BOUND ( 'NONE', #42909, .T. ) ;
#45617=EDGE_CURVE ( 'NONE', #17233, #9022, #23038, .T. ) ;
#45619=CARTESIAN_POINT ( 'NONE',  ( -1.216396646496118228, 1.593988306679904321, 2.131854889095133654 ) ) ;
#45621=CARTESIAN_POINT ( 'NONE',  ( -2.919426793319806368, 1.673754417692067564, 0.4451252810446391095 ) ) ;
#45625=DIRECTION ( 'NONE',  ( 8.741157232058135226E-17, -1.000000000000000000, 7.636919086868543885E-17 ) ) ;
#45627=EDGE_LOOP ( 'NONE', ( #35630, #44532, #16979, #29713 ) ) ;
#45629=CARTESIAN_POINT ( 'NONE',  ( 0.000000000000000000, 6.692913385826772199, 0.000000000000000000 ) ) ;
#45630=EDGE_LOOP ( 'NONE', ( #4314, #3442, #15622, #48497, #30612, #26001, #23424, #27680 ) ) ;
#45632=LINE ( 'NONE', #37682, #15338 ) ;
#45645=ORIENTED_EDGE ( 'NONE', *, *, #40780, .T. ) ;
#45647=CARTESIAN_POINT ( 'NONE',  ( -1.774034721664383030, 0.5252446251211232431, -1.229997447203279082 ) ) ;
#45649=VERTEX_POINT ( 'NONE', #49185 ) ;
#45653=DIRECTION ( 'NONE',  ( -0.000000000000000000, 1.000000000000000000, -0.000000000000000000 ) ) ;
#45654=ORIENTED_EDGE ( 'NONE', *, *, #31133, .T. ) ;
#45659=CARTESIAN_POINT ( 'NONE',  ( -0.2177357222769329415, 0.008167984067341605911, -1.870235122269071182 ) ) ;
#45660=DIRECTION ( 'NONE',  ( -0.9998717552508122886, -0.01601477604151185785, 0.000000000000000000 ) ) ;
#45661=B_SPLINE_CURVE_WITH_KNOTS ( 'NONE', 3,
 ( #16136, #32408, #40410, #40151 ),
 .UNSPECIFIED., .F., .F.,
 ( 4, 4 ),
 ( 0.01387794258156342664, 0.03074578613037699110 ),
 .UNSPECIFIED. ) ;
#45663=EDGE_LOOP ( 'NONE', ( #29001, #36424, #25879, #16675 ) ) ;
#45672=CIRCLE ( 'NONE', #48971, 2.165354330708661568 ) ;
#45674=LINE ( 'NONE', #34597, #6124 ) ;
#45675=VECTOR ( 'NONE', #8497, 39.37007874015748143 ) ;
#45680=ORIENTED_EDGE ( 'NONE', *, *, #24751, .F. ) ;
#45681=CARTESIAN_POINT ( 'NONE',  ( 0.7148041136150539154, 6.692913385826772199, -2.044646019095610612 ) ) ;
#45684=EDGE_CURVE ( 'NONE', #50196, #35952, #14110, .T. ) ;
#45685=B_SPLINE_CURVE_WITH_KNOTS ( 'NONE', 3,
 ( #34148, #30266, #45982, #18649 ),
 .UNSPECIFIED., .F., .F.,
 ( 4, 4 ),
 ( 2.176057262996888679E-07, 0.01608855240560840352 ),
 .UNSPECIFIED. ) ;
#45686=EDGE_CURVE ( 'NONE', #49770, #45076, #22318, .T. ) ;
#45689=ORIENTED_EDGE ( 'NONE', *, *, #17019, .T. ) ;
#45691=FACE_OUTER_BOUND ( 'NONE', #20429, .T. ) ;
#45692=CARTESIAN_POINT ( 'NONE',  ( -1.152568299495734694, 6.692913385826772199, 1.833124570921535801 ) ) ;
#45693=ORIENTED_EDGE ( 'NONE', *, *, #5890, .T. ) ;
#45695=FACE_OUTER_BOUND ( 'NONE', #4103, .T. ) ;
#45696=VECTOR ( 'NONE', #44227, 39.37007874015748143 ) ;
#45701=CARTESIAN_POINT ( 'NONE',  ( -0.9149808212874269708, 1.594821661612501940, -2.013400720915880626 ) ) ;
#45702=CARTESIAN_POINT ( 'NONE',  ( -1.556712866041156440, 1.596563264426776207, 2.509548638715847435 ) ) ;
#45704=EDGE_CURVE ( 'NONE', #43511, #17939, #26483, .T. ) ;
#45708=ADVANCED_FACE ( 'NONE', ( #33998 ), #14084, .T. ) ;
#45711=CARTESIAN_POINT ( 'NONE',  ( -1.183645401082143778, 0.000000000000000000, 1.279993023352344439 ) ) ;
#45712=ORIENTED_EDGE ( 'NONE', *, *, #23612, .F. ) ;
#45713=EDGE_CURVE ( 'NONE', #41147, #23660, #18213, .T. ) ;
#45717=ADVANCED_FACE ( 'NONE', ( #21607 ), #44579, .T. ) ;
#45719=ORIENTED_EDGE ( 'NONE', *, *, #41814, .T. ) ;
#45720=ORIENTED_EDGE ( 'NONE', *, *, #43425, .F. ) ;
#45722=FACE_OUTER_BOUND ( 'NONE', #13946, .T. ) ;
#45726=ORIENTED_EDGE ( 'NONE', *, *, #4675, .T. ) ;
#45728=VERTEX_POINT ( 'NONE', #7131 ) ;
#45730=CARTESIAN_POINT ( 'NONE',  ( 0.4788131938641105312, 5.905511811023623103, 2.914091152102192162 ) ) ;
#45732=DIRECTION ( 'NONE',  ( 0.000000000000000000, 0.000000000000000000, 1.000000000000000000 ) ) ;
#45733=DIRECTION ( 'NONE',  ( 0.000000000000000000, 0.000000000000000000, -1.000000000000000000 ) ) ;
#45734=ORIENTED_EDGE ( 'NONE', *, *, #38497, .T. ) ;
#45740=CARTESIAN_POINT ( 'NONE',  ( -2.298335196414549308, 1.562647740231880134, 1.853831591542948853 ) ) ;
#45741=AXIS2_PLACEMENT_3D ( 'NONE', #42966, #15112, #50175 ) ;
#45742=VERTEX_POINT ( 'NONE', #19745 ) ;
#45744=CARTESIAN_POINT ( 'NONE',  ( 0.1155636338427008941, -0.5222242541845523167, 0.000000000000000000 ) ) ;
#45749=CIRCLE ( 'NONE', #17771, 1.850107469027523432 ) ;
#45750=ADVANCED_FACE ( 'NONE', ( #3504 ), #39655, .T. ) ;
#45754=EDGE_LOOP ( 'NONE', ( #40823, #33006, #43190, #48789 ) ) ;
#45756=EDGE_CURVE ( 'NONE', #48407, #6577, #18009, .T. ) ;
#45757=CARTESIAN_POINT ( 'NONE',  ( 1.892591856222374469, 0.05823298773025239322, -0.4824499329568616157 ) ) ;
#45760=ORIENTED_EDGE ( 'NONE', *, *, #5928, .F. ) ;
#45762=CARTESIAN_POINT ( 'NONE',  ( 0.6235241006192022706, 0.000000000000000000, 2.074304693190358151 ) ) ;
#45767=CARTESIAN_POINT ( 'NONE',  ( 0.1155636338427008941, -0.5222242541845523167, 0.000000000000000000 ) ) ;
#45769=VERTEX_POINT ( 'NONE', #34501 ) ;
#45770=EDGE_CURVE ( 'NONE', #48829, #39458, #46222, .T. ) ;
#45773=LINE ( 'NONE', #6315, #1639 ) ;
#45778=VERTEX_POINT ( 'NONE', #23120 ) ;
#45782=ORIENTED_EDGE ( 'NONE', *, *, #30853, .F. ) ;
#45786=CIRCLE ( 'NONE', #35083, 2.165354330708661568 ) ;
#45788=VECTOR ( 'NONE', #17353, 39.37007874015748143 ) ;
#45790=CARTESIAN_POINT ( 'NONE',  ( -1.936609506549060722, 1.676883605369557051, 0.9862484270667263297 ) ) ;
#45792=ORIENTED_EDGE ( 'NONE', *, *, #19024, .T. ) ;
#45794=ORIENTED_EDGE ( 'NONE', *, *, #46353, .F. ) ;
#45795=CARTESIAN_POINT ( 'NONE',  ( 0.1170985530868079300, 0.02979521312206013725, -1.850078377359382298 ) ) ;
#45796=DIRECTION ( 'NONE',  ( 0.9998717552508121775, 0.01601477604151182663, 0.000000000000000000 ) ) ;
#45805=DIRECTION ( 'NONE',  ( 0.000000000000000000, 0.000000000000000000, 1.000000000000000000 ) ) ;
#45808=CARTESIAN_POINT ( 'NONE',  ( -0.5905738936209794510, 0.01846054376545745376, 1.713635781666723146 ) ) ;
#45809=CARTESIAN_POINT ( 'NONE',  ( 0.8013393943173970912, 1.496885474212027223, -2.841987189051758733 ) ) ;
#45810=EDGE_CURVE ( 'NONE', #41705, #30522, #37133, .T. ) ;
#45811=AXIS2_PLACEMENT_3D ( 'NONE', #14531, #34908, #45993 ) ;
#45815=CARTESIAN_POINT ( 'NONE',  ( 0.08119777152254364916, 1.623385212329073957, 0.000000000000000000 ) ) ;
#45816=EDGE_LOOP ( 'NONE', ( #15010, #4607, #873, #13835 ) ) ;
#45819=ADVANCED_FACE ( 'NONE', ( #127 ), #50681, .T. ) ;
#45830=CARTESIAN_POINT ( 'NONE',  ( -0.1227720337126170513, 0.000000000000000000, -1.913115909999223652 ) ) ;
#45833=CARTESIAN_POINT ( 'NONE',  ( 0.07982360342473591996, 1.709180471932028711, 0.000000000000000000 ) ) ;
#45844=AXIS2_PLACEMENT_3D ( 'NONE', #34154, #49837, #50583 ) ;
#45845=EDGE_LOOP ( 'NONE', ( #33579, #3570, #46312, #40706 ) ) ;
#45846=ORIENTED_EDGE ( 'NONE', *, *, #28330, .T. ) ;
#45847=DIRECTION ( 'NONE',  ( -1.206139481778042838E-16, 1.000000000000000000, 4.526717189434675613E-17 ) ) ;
#45850=ORIENTED_EDGE ( 'NONE', *, *, #18099, .F. ) ;
#45858=CARTESIAN_POINT ( 'NONE',  ( 1.358062732265305605, 1.638351821497108451, 2.368963978111557456 ) ) ;
#45863=CARTESIAN_POINT ( 'NONE',  ( -0.7680117299321171931, 1.703413802931311283, -2.597843860071421762 ) ) ;
#45864=CARTESIAN_POINT ( 'NONE',  ( -0.4350747367504791963, 6.692913385826772199, -2.121846421795420934 ) ) ;
#45871=ORIENTED_EDGE ( 'NONE', *, *, #4916, .F. ) ;
#45872=ORIENTED_EDGE ( 'NONE', *, *, #11493, .T. ) ;
#45876=B_SPLINE_CURVE_WITH_KNOTS ( 'NONE', 3,
 ( #22856, #45809, #26221, #38108 ),
 .UNSPECIFIED., .F., .F.,
 ( 4, 4 ),
 ( 2.074235228680312165E-07, 0.002500790534950076988 ),
 .UNSPECIFIED. ) ;
#45878=PLANE ( 'NONE',  #25953 ) ;
#45880=VERTEX_POINT ( 'NONE', #36025 ) ;
#45882=ADVANCED_FACE ( 'NONE', ( #13040 ), #28772, .T. ) ;
#45883=CARTESIAN_POINT ( 'NONE',  ( -1.979793062125317471, 0.000000000000000000, 2.191257344206539504 ) ) ;
#45885=ORIENTED_EDGE ( 'NONE', *, *, #40130, .T. ) ;
#45889=CARTESIAN_POINT ( 'NONE',  ( 1.392809637228761943, 0.03309421904702441325, -1.399748900407971064 ) ) ;
#45897=ORIENTED_EDGE ( 'NONE', *, *, #49008, .T. ) ;
#45901=VERTEX_POINT ( 'NONE', #44516 ) ;
#45902=B_SPLINE_CURVE_WITH_KNOTS ( 'NONE', 3,
 ( #45280, #37062, #29040, #9686 ),
 .UNSPECIFIED., .F., .F.,
 ( 4, 4 ),
 ( 0.0008074699510994055082, 0.001416670944113270067 ),
 .UNSPECIFIED. ) ;
#45907=ORIENTED_EDGE ( 'NONE', *, *, #25427, .F. ) ;
#45917=EDGE_CURVE ( 'NONE', #48631, #29859, #6317, .T. ) ;
#45919=CARTESIAN_POINT ( 'NONE',  ( -1.183645401082143778, 0.000000000000000000, 1.279993023352344439 ) ) ;
#45923=CONICAL_SURFACE ( 'NONE', #49190, 3.483074324928249421, 1.244861948955335196 ) ;
#45925=CARTESIAN_POINT ( 'NONE',  ( 1.052867436300554349, 1.491216683892185646, 2.758714587863916989 ) ) ;
#45926=ADVANCED_FACE ( 'NONE', ( #20524 ), #45417, .F. ) ;
#45927=DIRECTION ( 'NONE',  ( 0.01601477604151182663, -0.9998717552508123996, 0.000000000000000000 ) ) ;
#45929=DIRECTION ( 'NONE',  ( 0.2225209339563041788, -1.131720761168132053E-16, 0.9749279121818259508 ) ) ;
#45939=FACE_OUTER_BOUND ( 'NONE', #14573, .T. ) ;
#45943=LINE ( 'NONE', #18860, #3159 ) ;
#45945=FACE_OUTER_BOUND ( 'NONE', #48245, .T. ) ;
#45950=ORIENTED_EDGE ( 'NONE', *, *, #34008, .T. ) ;
#45951=CARTESIAN_POINT ( 'NONE',  ( -1.645058990017820300, 1.685622884702261626, 1.808123370684439513 ) ) ;
#45955=CARTESIAN_POINT ( 'NONE',  ( -2.014664160120487768, 1.577208220393157223, -0.8075893616760145832 ) ) ;
#45956=CARTESIAN_POINT ( 'NONE',  ( 0.1155636338427008941, -0.5222242541845523167, 0.000000000000000000 ) ) ;
#45957=CARTESIAN_POINT ( 'NONE',  ( 0.7759887336347247588, 0.04034854520891290042, -1.724780676950718794 ) ) ;
#45966=PLANE ( 'NONE',  #49583 ) ;
#45968=VERTEX_POINT ( 'NONE', #40414 ) ;
#45972=B_SPLINE_CURVE_WITH_KNOTS ( 'NONE', 3,
 ( #50804, #11619, #43101, #7747 ),
 .UNSPECIFIED., .F., .F.,
 ( 4, 4 ),
 ( 3.392876324466583160E-07, 0.04779162299089171478 ),
 .UNSPECIFIED. ) ;
#45973=CARTESIAN_POINT ( 'NONE',  ( 0.002207914879453961969, 6.692913385826772199, -2.115467123904953617 ) ) ;
#45975=B_SPLINE_CURVE_WITH_KNOTS ( 'NONE', 3,
 ( #17372, #1870, #13755, #29499 ),
 .UNSPECIFIED., .F., .F.,
 ( 4, 4 ),
 ( 2.396528101364543949E-07, 0.002500331867144249369 ),
 .UNSPECIFIED. ) ;
#45979=VERTEX_POINT ( 'NONE', #17165 ) ;
#45980=ORIENTED_EDGE ( 'NONE', *, *, #42091, .F. ) ;
#45982=CARTESIAN_POINT ( 'NONE',  ( 2.307697345854446969, 1.649818209929699186, -1.039876607722350910 ) ) ;
#45993=DIRECTION ( 'NONE',  ( 0.000000000000000000, 0.000000000000000000, 1.000000000000000000 ) ) ;
#45994=AXIS2_PLACEMENT_3D ( 'NONE', #16864, #24857, #32356 ) ;
#45995=B_SPLINE_CURVE_WITH_KNOTS ( 'NONE', 3,
 ( #6408, #42025, #14147, #3037 ),
 .UNSPECIFIED., .F., .F.,
 ( 4, 4 ),
 ( 0.0004731792943978242651, 0.002973409787418910231 ),
 .UNSPECIFIED. ) ;
#45996=EDGE_CURVE ( 'NONE', #5201, #37057, #47846, .T. ) ;
#46002=CARTESIAN_POINT ( 'NONE',  ( -0.5443978225238782498, 1.600757226547528500, -2.157565353623420723 ) ) ;
#46004=EDGE_LOOP ( 'NONE', ( #41, #4779, #8128, #47831, #19287, #29492, #31460, #39066, #21900, #22030, #23145, #11227, #3475 ) ) ;
#46009=ADVANCED_FACE ( 'NONE', ( #46705 ), #44609, .T. ) ;
#46010=ORIENTED_EDGE ( 'NONE', *, *, #14022, .F. ) ;
#46012=ORIENTED_EDGE ( 'NONE', *, *, #792, .T. ) ;
#46016=DIRECTION ( 'NONE',  ( -0.5128992774058948045, 9.966352232896248990E-17, -0.8584487936018727616 ) ) ;
#46018=ORIENTED_EDGE ( 'NONE', *, *, #24335, .T. ) ;
#46020=PLANE ( 'NONE',  #29853 ) ;
#46023=CARTESIAN_POINT ( 'NONE',  ( -1.002259110181423551, 1.593423740086483020, -1.967789019142131002 ) ) ;
#46026=ORIENTED_EDGE ( 'NONE', *, *, #20356, .F. ) ;
#46029=CARTESIAN_POINT ( 'NONE',  ( -1.068075307999488244, 6.692913385826772199, 1.883606783264637041 ) ) ;
#46030=VECTOR ( 'NONE', #42479, 39.37007874015748143 ) ;
#46032=VERTEX_POINT ( 'NONE', #29985 ) ;
#46034=DIRECTION ( 'NONE',  ( 1.953992523340275196E-14, 0.000000000000000000, 1.000000000000000000 ) ) ;
#46035=ORIENTED_EDGE ( 'NONE', *, *, #50619, .T. ) ;
#46040=DIRECTION ( 'NONE',  ( -0.01601477604151182663, 0.9998717552508123996, -0.000000000000000000 ) ) ;
#46041=CARTESIAN_POINT ( 'NONE',  ( 2.042485253772177156, 1.205361022782829114E-17, 0.6118985000151695441 ) ) ;
#46047=B_SPLINE_CURVE_WITH_KNOTS ( 'NONE', 3,
 ( #36006, #17908, #18161, #5778 ),
 .UNSPECIFIED., .F., .F.,
 ( 4, 4 ),
 ( 7.003658972180221081E-07, 0.002501219077655048462 ),
 .UNSPECIFIED. ) ;
#46048=VERTEX_POINT ( 'NONE', #45702 ) ;
#46049=EDGE_CURVE ( 'NONE', #36016, #10759, #9701, .T. ) ;
#46052=ORIENTED_EDGE ( 'NONE', *, *, #48882, .T. ) ;
#46056=CARTESIAN_POINT ( 'NONE',  ( -1.331808205664968492, 0.000000000000000000, 1.125026879082024367 ) ) ;
#46057=FACE_OUTER_BOUND ( 'NONE', #45350, .T. ) ;
#46059=ORIENTED_EDGE ( 'NONE', *, *, #49327, .T. ) ;
#46062=CARTESIAN_POINT ( 'NONE',  ( 2.024272128602276233, 1.049866565877818347, -0.04164796393617213599 ) ) ;
#46066=CARTESIAN_POINT ( 'NONE',  ( 2.325893555657776002, 1.679538594897605819, -0.05519379784448211895 ) ) ;
#46067=ORIENTED_EDGE ( 'NONE', *, *, #15053, .T. ) ;
#46074=DIRECTION ( 'NONE',  ( -0.01601477604151182663, 0.9998717552508123996, -0.000000000000000000 ) ) ;
#46075=ORIENTED_EDGE ( 'NONE', *, *, #38036, .T. ) ;
#46081=AXIS2_PLACEMENT_3D ( 'NONE', #37862, #18224, #44556 ) ;
#46082=ORIENTED_EDGE ( 'NONE', *, *, #36957, .F. ) ;
#46087=AXIS2_PLACEMENT_3D ( 'NONE', #50659, #3991, #19721 ) ;
#46088=CARTESIAN_POINT ( 'NONE',  ( -2.919426793319806368, 5.905511811023623991, 0.4451252810446391095 ) ) ;
#46089=CARTESIAN_POINT ( 'NONE',  ( 0.08139965876239094178, 1.610780518492231694, 0.000000000000000000 ) ) ;
#46090=EDGE_LOOP ( 'NONE', ( #29778, #45011, #19495, #20070 ) ) ;
#46093=CARTESIAN_POINT ( 'NONE',  ( 0.07982360342473591996, 1.709180471932028711, 0.000000000000000000 ) ) ;
#46100=ORIENTED_EDGE ( 'NONE', *, *, #50646, .T. ) ;
#46103=ADVANCED_FACE ( 'NONE', ( #2873 ), #18367, .F. ) ;
#46106=ADVANCED_FACE ( 'NONE', ( #19111 ), #34758, .T. ) ;
#46107=VECTOR ( 'NONE', #26628, 39.37007874015748143 ) ;
#46111=DIRECTION ( 'NONE',  ( -0.4738686624729965269, -1.160734090543304660E-16, -0.8805955318567391110 ) ) ;
#46113=B_SPLINE_CURVE_WITH_KNOTS ( 'NONE', 3,
 ( #33841, #37718, #14462, #10592 ),
 .UNSPECIFIED., .F., .F.,
 ( 4, 4 ),
 ( 0.001127418191887998586, 0.003627694388309332489 ),
 .UNSPECIFIED. ) ;
#46116=CONICAL_SURFACE ( 'NONE', #1625, 3.483074324928249421, 1.244861948955335196 ) ;
#46117=FACE_OUTER_BOUND ( 'NONE', #14746, .T. ) ;
#46119=ORIENTED_EDGE ( 'NONE', *, *, #398, .F. ) ;
#46123=ORIENTED_EDGE ( 'NONE', *, *, #11295, .F. ) ;
#46125=CARTESIAN_POINT ( 'NONE',  ( -2.165354330708661568, 1.673228346456695492, -0.01597875172208130037 ) ) ;
#46127=B_SPLINE_CURVE_WITH_KNOTS ( 'NONE', 3,
 ( #5282, #36024, #25161, #24906 ),
 .UNSPECIFIED., .F., .F.,
 ( 4, 4 ),
 ( 0.001455260405619622196, 0.003955466538311651695 ),
 .UNSPECIFIED. ) ;
#46130=VERTEX_POINT ( 'NONE', #22997 ) ;
#46131=DIRECTION ( 'NONE',  ( -9.390536051998764103E-17, -1.000000000000000000, -6.822623802544789917E-17 ) ) ;
#46134=PLANE ( 'NONE',  #31696 ) ;
#46136=VECTOR ( 'NONE', #14306, 39.37007874015748143 ) ;
#46145=ADVANCED_FACE ( 'NONE', ( #30746 ), #11126, .T. ) ;
#46146=ORIENTED_EDGE ( 'NONE', *, *, #31264, .T. ) ;
#46150=CARTESIAN_POINT ( 'NONE',  ( 1.971247363764867977, 1.574803149606302854, -0.8960709840011636951 ) ) ;
#46152=ORIENTED_EDGE ( 'NONE', *, *, #15524, .T. ) ;
#46154=DIRECTION ( 'NONE',  ( 0.000000000000000000, 1.160734090543304660E-16, -1.000000000000000000 ) ) ;
#46156=ORIENTED_EDGE ( 'NONE', *, *, #15769, .F. ) ;
#46159=ORIENTED_EDGE ( 'NONE', *, *, #5101, .T. ) ;
#46160=ORIENTED_EDGE ( 'NONE', *, *, #39482, .T. ) ;
#46163=ORIENTED_EDGE ( 'NONE', *, *, #41851, .F. ) ;
#46165=CARTESIAN_POINT ( 'NONE',  ( -1.979793062125317471, 0.000000000000000000, 2.191257344206539504 ) ) ;
#46171=ORIENTED_EDGE ( 'NONE', *, *, #25927, .T. ) ;
#46172=EDGE_LOOP ( 'NONE', ( #20701, #33564, #17270, #31859 ) ) ;
#46180=CARTESIAN_POINT ( 'NONE',  ( 0.9035029780573708980, 0.01393497246690909679, -1.762719797743741657 ) ) ;
#46182=CARTESIAN_POINT ( 'NONE',  ( 0.5272349255864847706, 5.905511811023623991, 2.905303903342417726 ) ) ;
#46192=EDGE_LOOP ( 'NONE', ( #3251, #18677, #27303, #14197 ) ) ;
#46193=EDGE_CURVE ( 'NONE', #10470, #38339, #49961, .T. ) ;
#46196=EDGE_CURVE ( 'NONE', #19475, #21072, #27614, .T. ) ;
#46197=VERTEX_POINT ( 'NONE', #39503 ) ;
#46198=DIRECTION ( 'NONE',  ( 0.000000000000000000, 1.000000000000000000, 0.000000000000000000 ) ) ;
#46200=B_SPLINE_CURVE_WITH_KNOTS ( 'NONE', 3,
 ( #17393, #25646, #20753, #36513 ),
 .UNSPECIFIED., .F., .F.,
 ( 4, 4 ),
 ( 4.095189062770323219E-07, 0.04904918211385326382 ),
 .UNSPECIFIED. ) ;
#46202=CARTESIAN_POINT ( 'NONE',  ( 2.064489077472676737, 1.642543324816299277, 1.055063358597729595 ) ) ;
#46203=B_SPLINE_CURVE_WITH_KNOTS ( 'NONE', 3,
 ( #18203, #14328, #49400, #33203 ),
 .UNSPECIFIED., .F., .F.,
 ( 4, 4 ),
 ( 0.01096540280937795438, 0.03073589712859321754 ),
 .UNSPECIFIED. ) ;
#46207=CARTESIAN_POINT ( 'NONE',  ( -1.569555324610094393, 0.001878576622170695463, 0.7887281490750877033 ) ) ;
#46214=CIRCLE ( 'NONE', #6668, 2.164630168518208109 ) ;
#46215=CARTESIAN_POINT ( 'NONE',  ( 0.4349608091550764555, 1.574803149606302854, 2.121218629000301004 ) ) ;
#46222=CIRCLE ( 'NONE', #28926, 2.086614173228346303 ) ;
#46226=CARTESIAN_POINT ( 'NONE',  ( 0.1155636338427008941, -0.5222242541845523167, 0.000000000000000000 ) ) ;
#46229=DIRECTION ( 'NONE',  ( -0.3930250316539147803, 1.288287287306305283E-16, -0.9195277725514544587 ) ) ;
#46234=ORIENTED_EDGE ( 'NONE', *, *, #48817, .F. ) ;
#46237=CARTESIAN_POINT ( 'NONE',  ( 0.2899689346265602041, 0.02164905224627299354, 1.873473513055692763 ) ) ;
#46238=DIRECTION ( 'NONE',  ( -0.000000000000000000, -1.000000000000000000, -0.000000000000000000 ) ) ;
#46241=CARTESIAN_POINT ( 'NONE',  ( 2.323794147221719175, 1.745121766917047790, -0.05509951330290247667 ) ) ;
#46245=VECTOR ( 'NONE', #8173, 39.37007874015748143 ) ;
#46246=ORIENTED_EDGE ( 'NONE', *, *, #25775, .F. ) ;
#46250=LINE ( 'NONE', #11166, #27114 ) ;
#46253=CARTESIAN_POINT ( 'NONE',  ( 0.2510238314733705400, 1.613497360050089036, -2.240096307734528835 ) ) ;
#46255=ORIENTED_EDGE ( 'NONE', *, *, #10751, .F. ) ;
#46257=VECTOR ( 'NONE', #40276, 39.37007874015748143 ) ;
#46262=FACE_OUTER_BOUND ( 'NONE', #24887, .T. ) ;
#46263=CARTESIAN_POINT ( 'NONE',  ( 1.325491792074624087, 1.739919523179865202, -2.638988599164732385 ) ) ;
#46275=CARTESIAN_POINT ( 'NONE',  ( 2.188498384461881940, 0.5221067302336409588, 0.6593410420848859754 ) ) ;
#46286=ORIENTED_EDGE ( 'NONE', *, *, #49037, .F. ) ;
#46289=CARTESIAN_POINT ( 'NONE',  ( 0.9838852166858921278, 0.000000000000000000, 1.929635236160317735 ) ) ;
#46296=EDGE_CURVE ( 'NONE', #42335, #48626, #48711, .T. ) ;
#46299=AXIS2_PLACEMENT_3D ( 'NONE', #49370, #10167, #22048 ) ;
#46301=VECTOR ( 'NONE', #9744, 39.37007874015748854 ) ;
#46303=DIRECTION ( 'NONE',  ( 1.000000000000000000, -0.000000000000000000, -0.000000000000000000 ) ) ;
#46305=AXIS2_PLACEMENT_3D ( 'NONE', #47309, #39858, #27719 ) ;
#46309=VERTEX_POINT ( 'NONE', #36401 ) ;
#46310=CARTESIAN_POINT ( 'NONE',  ( -2.160407304981126320, 1.673304745347873324, -0.1462862061266896330 ) ) ;
#46312=ORIENTED_EDGE ( 'NONE', *, *, #18461, .T. ) ;
#46317=CARTESIAN_POINT ( 'NONE',  ( 0.4349608091550758449, 6.692913385826772199, 2.121218629000301004 ) ) ;
#46321=ORIENTED_EDGE ( 'NONE', *, *, #5890, .F. ) ;
#46323=VECTOR ( 'NONE', #5988, 39.37007874015748143 ) ;
#46324=CARTESIAN_POINT ( 'NONE',  ( -1.420868632364155282, 0.000000000000000000, 1.070159647439151707 ) ) ;
#46326=EDGE_CURVE ( 'NONE', #10170, #43507, #37176, .T. ) ;
#46329=ORIENTED_EDGE ( 'NONE', *, *, #35774, .T. ) ;
#46330=ORIENTED_EDGE ( 'NONE', *, *, #3173, .T. ) ;
#46332=CARTESIAN_POINT ( 'NONE',  ( -1.225600105435525000, 0.000000000000000000, -1.239880218767125175 ) ) ;
#46333=VECTOR ( 'NONE', #19502, 39.37007874015748143 ) ;
#46337=CARTESIAN_POINT ( 'NONE',  ( 0.000000000000000000, 1.585169487999011917, 0.000000000000000000 ) ) ;
#46339=ORIENTED_EDGE ( 'NONE', *, *, #46347, .F. ) ;
#46344=CARTESIAN_POINT ( 'NONE',  ( 1.214590356376888280, 1.727355838235203667, 1.936932008856820930 ) ) ;
#46345=ORIENTED_EDGE ( 'NONE', *, *, #9824, .F. ) ;
#46347=EDGE_CURVE ( 'NONE', #695, #24400, #21422, .T. ) ;
#46350=ORIENTED_EDGE ( 'NONE', *, *, #48322, .T. ) ;
#46353=EDGE_CURVE ( 'NONE', #33976, #8620, #9316, .T. ) ;
#46360=DIRECTION ( 'NONE',  ( 0.000000000000000000, 0.000000000000000000, 1.000000000000000000 ) ) ;
#46362=FACE_OUTER_BOUND ( 'NONE', #6311, .T. ) ;
#46363=CARTESIAN_POINT ( 'NONE',  ( 1.723687301221656476, 1.205361022782829114E-17, -1.311649477509800876 ) ) ;
#46364=VECTOR ( 'NONE', #4632, 39.37007874015748143 ) ;
#46365=CARTESIAN_POINT ( 'NONE',  ( -2.576863348864732117, 1.580667355030889620, 1.442554885838411849 ) ) ;
#46366=FACE_OUTER_BOUND ( 'NONE', #14469, .T. ) ;
#46372=ORIENTED_EDGE ( 'NONE', *, *, #33760, .T. ) ;
#46374=CARTESIAN_POINT ( 'NONE',  ( 1.292259323372447977, 1.002375609920205468, 2.258827622949058700 ) ) ;
#46375=CARTESIAN_POINT ( 'NONE',  ( 0.002207914879453961535, -5.712274067634378313E-18, 0.04916304461325374242 ) ) ;
#46377=PLANE ( 'NONE',  #14078 ) ;
#46379=DIRECTION ( 'NONE',  ( -0.01601477604151182663, 0.9998717552508123996, -0.000000000000000000 ) ) ;
#46385=VERTEX_POINT ( 'NONE', #44633 ) ;
#46397=CARTESIAN_POINT ( 'NONE',  ( -0.8013691390275965443, 1.531806867628318747, -2.841978980033345703 ) ) ;
#46399=EDGE_LOOP ( 'NONE', ( #15298, #15394, #37620, #45980 ) ) ;
#46402=ORIENTED_EDGE ( 'NONE', *, *, #29197, .T. ) ;
#46404=VECTOR ( 'NONE', #44350, 39.37007874015748143 ) ;
#46408=ORIENTED_EDGE ( 'NONE', *, *, #43378, .T. ) ;
#46409=FACE_OUTER_BOUND ( 'NONE', #45192, .T. ) ;
#46411=ADVANCED_FACE ( 'NONE', ( #20906 ), #40788, .T. ) ;
#46420=CARTESIAN_POINT ( 'NONE',  ( 0.5110784536613244278, 1.503363781114207764, 2.908235870722285288 ) ) ;
#46422=CARTESIAN_POINT ( 'NONE',  ( 0.08139965876239094178, 1.610780518492231694, 0.000000000000000000 ) ) ;
#46425=CARTESIAN_POINT ( 'NONE',  ( -2.165177485265404655, 1.574805878788816393, -0.03196544748097695371 ) ) ;
#46426=DIRECTION ( 'NONE',  ( 1.000000000000000000, 1.288287287306305283E-16, -0.000000000000000000 ) ) ;
#46431=CARTESIAN_POINT ( 'NONE',  ( 2.491402175429653809, 1.458524810485662959, -1.585592796919505609 ) ) ;
#46436=B_SPLINE_CURVE_WITH_KNOTS ( 'NONE', 3,
 ( #46041, #15584, #35206, #15079 ),
 .UNSPECIFIED., .F., .F.,
 ( 4, 4 ),
 ( 6.541964665659682645E-07, 0.004810142676841229654 ),
 .UNSPECIFIED. ) ;
#46437=CARTESIAN_POINT ( 'NONE',  ( 0.5469786881612729301, 0.03668053021573630668, -1.796948620166157307 ) ) ;
#46439=B_SPLINE_CURVE_WITH_KNOTS ( 'NONE', 3,
 ( #38911, #46374, #50719, #3799 ),
 .UNSPECIFIED., .F., .F.,
 ( 4, 4 ),
 ( 3.948084238142846119E-07, 0.04530798946647138226 ),
 .UNSPECIFIED. ) ;
#46440=DIRECTION ( 'NONE',  ( -0.3513748240813434620, 0.000000000000000000, 0.9362348706397368714 ) ) ;
#46442=VECTOR ( 'NONE', #24624, 39.37007874015748143 ) ;
#46443=EDGE_CURVE ( 'NONE', #619, #42699, #1284, .T. ) ;
#46444=VERTEX_POINT ( 'NONE', #41049 ) ;
#46447=EDGE_CURVE ( 'NONE', #13689, #25755, #24685, .T. ) ;
#46450=EDGE_CURVE ( 'NONE', #782, #33984, #26552, .T. ) ;
#46453=DIRECTION ( 'NONE',  ( -0.01601477604151182663, 0.9998717552508123996, -0.000000000000000000 ) ) ;
#46454=ORIENTED_EDGE ( 'NONE', *, *, #29873, .T. ) ;
#46457=DIRECTION ( 'NONE',  ( 0.8090169943749506709, 0.000000000000000000, -0.5877852522924684742 ) ) ;
#46461=ADVANCED_FACE ( 'NONE', ( #14940 ), #42298, .T. ) ;
#46466=CIRCLE ( 'NONE', #6115, 1.850107469027523432 ) ;
#46472=DIRECTION ( 'NONE',  ( -1.118904554427321068E-16, -1.000000000000000000, -3.087980359898530052E-17 ) ) ;
#46483=DIRECTION ( 'NONE',  ( -0.000000000000000000, -1.000000000000000000, -0.000000000000000000 ) ) ;
#46485=CARTESIAN_POINT ( 'NONE',  ( -2.875074555560396483, 1.574099885360915829, -0.6730399204671311253 ) ) ;
#46486=LINE ( 'NONE', #2900, #30812 ) ;
#46488=DIRECTION ( 'NONE',  ( -1.953992523340275196E-14, 0.000000000000000000, 1.000000000000000000 ) ) ;
#46490=CARTESIAN_POINT ( 'NONE',  ( 0.7145799201508782339, 6.692913385826772199, 2.044048657746659448 ) ) ;
#46494=ORIENTED_EDGE ( 'NONE', *, *, #7190, .F. ) ;
#46497=LINE ( 'NONE', #26651, #13945 ) ;
#46499=CARTESIAN_POINT ( 'NONE',  ( -2.473328087642055362, 1.582272202671235473, -1.612973869535263338 ) ) ;
#46500=B_SPLINE_CURVE_WITH_KNOTS ( 'NONE', 3,
 ( #44385, #9283, #24778, #40272 ),
 .UNSPECIFIED., .F., .F.,
 ( 4, 4 ),
 ( 5.909393220007465840E-06, 0.002506742884191285031 ),
 .UNSPECIFIED. ) ;
#46501=VECTOR ( 'NONE', #6006, 39.37007874015748143 ) ;
#46504=CARTESIAN_POINT ( 'NONE',  ( 0.000000000000000000, 5.905511811023623991, 0.000000000000000000 ) ) ;
#46511=CARTESIAN_POINT ( 'NONE',  ( 1.174087487603957980, 6.692913385826772199, 1.869141625116387928 ) ) ;
#46512=CARTESIAN_POINT ( 'NONE',  ( 2.164658444855302122, 5.905511811023623991, -0.04795272066889885720 ) ) ;
#46527=DIRECTION ( 'NONE',  ( -0.000000000000000000, 1.000000000000000000, -0.000000000000000000 ) ) ;
#46529=ORIENTED_EDGE ( 'NONE', *, *, #48842, .F. ) ;
#46533=CARTESIAN_POINT ( 'NONE',  ( -0.9494510123445516481, 1.031098797897046948, 2.389745905932011194 ) ) ;
#46539=EDGE_CURVE ( 'NONE', #24400, #13689, #16081, .T. ) ;
#46540=DIRECTION ( 'NONE',  ( 5.063291518728965670E-17, 1.000000000000000000, 1.184615939703122503E-16 ) ) ;
#46541=CARTESIAN_POINT ( 'NONE',  ( 0.07982360342473591996, 1.709180471932028711, 0.000000000000000000 ) ) ;
#46543=VECTOR ( 'NONE', #50332, 39.37007874015748143 ) ;
#46544=AXIS2_PLACEMENT_3D ( 'NONE', #35911, #27379, #42631 ) ;
#46545=ORIENTED_EDGE ( 'NONE', *, *, #1908, .F. ) ;
#46547=ADVANCED_FACE ( 'NONE', ( #7200 ), #10562, .F. ) ;
#46548=DIRECTION ( 'NONE',  ( -0.7818314824680309139, 0.000000000000000000, 0.6234898018587318180 ) ) ;
#46553=CARTESIAN_POINT ( 'NONE',  ( 2.100227814008711835, 1.653522055412836700, -2.076109931251913565 ) ) ;
#46559=ADVANCED_FACE ( 'NONE', ( #2305 ), #41548, .F. ) ;
#46563=CYLINDRICAL_SURFACE ( 'NONE', #9000, 2.165354330708661568 ) ;
#46566=FACE_OUTER_BOUND ( 'NONE', #27365, .T. ) ;
#46569=VERTEX_POINT ( 'NONE', #39187 ) ;
#46570=CARTESIAN_POINT ( 'NONE',  ( 2.793030215715258446, 5.905511811023623991, 0.9592557174602684977 ) ) ;
#46577=CARTESIAN_POINT ( 'NONE',  ( 2.152681973165668783, 1.676764294869834693, -0.8665810060396648140 ) ) ;
#46579=ADVANCED_FACE ( 'NONE', ( #31194 ), #24056, .T. ) ;
#46580=LINE ( 'NONE', #38369, #4040 ) ;
#46581=VECTOR ( 'NONE', #10370, 39.37007874015748143 ) ;
#46582=CARTESIAN_POINT ( 'NONE',  ( 2.298708793198899869, 5.118110236220475784, 1.181102362204724310 ) ) ;
#46583=CARTESIAN_POINT ( 'NONE',  ( 1.772156216928421291, 1.703477877919150618, 1.476192699911957451 ) ) ;
#46585=AXIS2_PLACEMENT_3D ( 'NONE', #48, #12437, #31557 ) ;
#46586=DIRECTION ( 'NONE',  ( 0.000000000000000000, 0.000000000000000000, 1.000000000000000000 ) ) ;
#46587=VERTEX_POINT ( 'NONE', #35325 ) ;
#46588=DIRECTION ( 'NONE',  ( -0.9998717552508121775, -0.01601477604151182663, 0.000000000000000000 ) ) ;
#46590=LINE ( 'NONE', #23371, #32281 ) ;
#46591=VECTOR ( 'NONE', #8638, 39.37007874015748143 ) ;
#46592=EDGE_LOOP ( 'NONE', ( #50481, #44525, #17500, #34632 ) ) ;
#46593=CARTESIAN_POINT ( 'NONE',  ( -2.043634885149970160, 1.574803149606302854, 0.7157624142945940848 ) ) ;
#46598=CARTESIAN_POINT ( 'NONE',  ( 0.5546681269544795345, 1.683977579361253696, -2.194778965963542383 ) ) ;
#46599=B_SPLINE_CURVE_WITH_KNOTS ( 'NONE', 3,
 ( #37362, #33748, #36590, #9732 ),
 .UNSPECIFIED., .F., .F.,
 ( 4, 4 ),
 ( 0.0004380968183548472812, 0.002938328190805584474 ),
 .UNSPECIFIED. ) ;
#46602=CARTESIAN_POINT ( 'NONE',  ( -1.567214440306964107, 0.002817858044914879883, 0.7874684655159520652 ) ) ;
#46604=B_SPLINE_CURVE_WITH_KNOTS ( 'NONE', 3,
 ( #25878, #41627, #6258, #22012 ),
 .UNSPECIFIED., .F., .F.,
 ( 4, 4 ),
 ( 0.0006403145629956773222, 0.003140563976786123635 ),
 .UNSPECIFIED. ) ;
#46606=CARTESIAN_POINT ( 'NONE',  ( -2.137971680030238186, 1.583472898301503173, 1.642030245039320713 ) ) ;
#46609=DIRECTION ( 'NONE',  ( 0.000000000000000000, 0.000000000000000000, -1.000000000000000000 ) ) ;
#46610=CONICAL_SURFACE ( 'NONE', #13669, 3.483074324928249421, 1.244861948955335196 ) ;
#46614=AXIS2_PLACEMENT_3D ( 'NONE', #33981, #7363, #49664 ) ;
#46617=CARTESIAN_POINT ( 'NONE',  ( 1.647640870277422342, 0.000000000000000000, 1.293031892269974170 ) ) ;
#46623=AXIS2_PLACEMENT_3D ( 'NONE', #32612, #847, #44962 ) ;
#46628=ORIENTED_EDGE ( 'NONE', *, *, #5257, .T. ) ;
#46631=DIRECTION ( 'NONE',  ( -0.01601477604151182663, 0.9998717552508123996, -0.000000000000000000 ) ) ;
#46633=CARTESIAN_POINT ( 'NONE',  ( 2.734482843737263025, 1.761870738172414796, -1.115254632218672493 ) ) ;
#46634=DIRECTION ( 'NONE',  ( -0.000000000000000000, 1.000000000000000000, -0.000000000000000000 ) ) ;
#46638=ORIENTED_EDGE ( 'NONE', *, *, #48701, .F. ) ;
#46640=ADVANCED_FACE ( 'NONE', ( #4590 ), #35602, .T. ) ;
#46642=DIRECTION ( 'NONE',  ( -0.000000000000000000, -1.000000000000000000, -0.000000000000000000 ) ) ;
#46644=ORIENTED_EDGE ( 'NONE', *, *, #40909, .F. ) ;
#46646=DIRECTION ( 'NONE',  ( 1.042246309068005903E-16, 1.000000000000000000, -7.572362681945165783E-17 ) ) ;
#46648=CIRCLE ( 'NONE', #31880, 2.165354330708661568 ) ;
#46651=AXIS2_PLACEMENT_3D ( 'NONE', #32494, #20078, #20859 ) ;
#46652=DIRECTION ( 'NONE',  ( -0.01601477604151182663, 0.9998717552508123996, -0.000000000000000000 ) ) ;
#46658=EDGE_LOOP ( 'NONE', ( #44702, #35089, #40116, #45235 ) ) ;
#46660=AXIS2_PLACEMENT_3D ( 'NONE', #125, #3756, #31126 ) ;
#46661=DIRECTION ( 'NONE',  ( 0.9998717552508121775, 0.01601477604151182663, 0.000000000000000000 ) ) ;
#46662=ORIENTED_EDGE ( 'NONE', *, *, #29830, .F. ) ;
#46664=ORIENTED_EDGE ( 'NONE', *, *, #49482, .T. ) ;
#46666=CARTESIAN_POINT ( 'NONE',  ( -1.410501566226150194, 5.905511811023623991, 1.689247093817288325 ) ) ;
#46667=CARTESIAN_POINT ( 'NONE',  ( -2.394586187573013003, 1.579445130333736458, 1.232696188189307929 ) ) ;
#46670=ADVANCED_FACE ( 'NONE', ( #4331 ), #14152, .T. ) ;
#46672=CARTESIAN_POINT ( 'NONE',  ( 2.274988110810610031, 1.744340048923221920, -0.4687729985174870495 ) ) ;
#46674=CARTESIAN_POINT ( 'NONE',  ( 1.599172890215260212, 5.905511811023623991, 1.460879300779193368 ) ) ;
#46685=ORIENTED_EDGE ( 'NONE', *, *, #43505, .T. ) ;
#46686=VERTEX_POINT ( 'NONE', #43302 ) ;
#46689=EDGE_CURVE ( 'NONE', #29725, #9082, #15694, .T. ) ;
#46691=ORIENTED_EDGE ( 'NONE', *, *, #42157, .F. ) ;
#46696=DIRECTION ( 'NONE',  ( 0.000000000000000000, 0.000000000000000000, 1.000000000000000000 ) ) ;
#46699=CARTESIAN_POINT ( 'NONE',  ( -1.109524193798323788, 0.000000000000000000, 1.344750771968458380 ) ) ;
#46700=ORIENTED_EDGE ( 'NONE', *, *, #21156, .T. ) ;
#46702=ORIENTED_EDGE ( 'NONE', *, *, #38464, .T. ) ;
#46703=ORIENTED_EDGE ( 'NONE', *, *, #50115, .T. ) ;
#46705=FACE_OUTER_BOUND ( 'NONE', #14280, .T. ) ;
#46706=CARTESIAN_POINT ( 'NONE',  ( -1.530693736245496872, 1.574803149606302854, -1.531579597454065800 ) ) ;
#46709=DIRECTION ( 'NONE',  ( 0.000000000000000000, 1.160734090543304660E-16, -1.000000000000000000 ) ) ;
#46710=CONICAL_SURFACE ( 'NONE', #20362, 3.483074324928249421, 1.244861948955335196 ) ;
#46716=B_SPLINE_CURVE_WITH_KNOTS ( 'NONE', 3,
 ( #49904, #49654, #2712, #17955 ),
 .UNSPECIFIED., .F., .F.,
 ( 4, 4 ),
 ( 2.656981594551095277E-07, 0.002500557877147534767 ),
 .UNSPECIFIED. ) ;
#46718=EDGE_LOOP ( 'NONE', ( #44144, #36143, #25672, #5863 ) ) ;
#46720=CARTESIAN_POINT ( 'NONE',  ( -1.408960544533061299, 0.005352583808700523381, 1.060663264281380025 ) ) ;
#46722=DIRECTION ( 'NONE',  ( 5.063291518728965670E-17, 1.000000000000000000, 1.184615939703122503E-16 ) ) ;
#46723=ORIENTED_EDGE ( 'NONE', *, *, #13070, .F. ) ;
#46724=ORIENTED_EDGE ( 'NONE', *, *, #19647, .T. ) ;
#46728=CARTESIAN_POINT ( 'NONE',  ( 0.08139965876239094178, 1.610780518492231694, 0.000000000000000000 ) ) ;
#46730=ORIENTED_EDGE ( 'NONE', *, *, #27044, .F. ) ;
#46732=LINE ( 'NONE', #22774, #39161 ) ;
#46733=EDGE_CURVE ( 'NONE', #39685, #23170, #20847, .T. ) ;
#46740=DIRECTION ( 'NONE',  ( 0.7818314824680309139, 7.233942271706491519E-17, -0.6234898018587318180 ) ) ;
#46741=ORIENTED_EDGE ( 'NONE', *, *, #40733, .T. ) ;
#46742=CARTESIAN_POINT ( 'NONE',  ( -2.043634885149970160, 1.574803149606302854, 0.7157624142945940848 ) ) ;
#46744=EDGE_CURVE ( 'NONE', #21187, #20924, #20375, .T. ) ;
#46748=VECTOR ( 'NONE', #27597, 39.37007874015748143 ) ;
#46750=ORIENTED_EDGE ( 'NONE', *, *, #39545, .F. ) ;
#46755=CARTESIAN_POINT ( 'NONE',  ( 1.951645782807981178, 0.03882318759419040033, -0.4959286063371406983 ) ) ;
#46762=DIRECTION ( 'NONE',  ( -1.118904554427325505E-16, -1.000000000000000000, 3.087980359898369198E-17 ) ) ;
#46764=VERTEX_POINT ( 'NONE', #36859 ) ;
#46765=ORIENTED_EDGE ( 'NONE', *, *, #29490, .T. ) ;
#46766=DIRECTION ( 'NONE',  ( 0.9909497617679331460, 0.000000000000000000, 0.1342332658176667026 ) ) ;
#46770=EDGE_CURVE ( 'NONE', #27061, #7202, #48749, .T. ) ;
#46774=CARTESIAN_POINT ( 'NONE',  ( -2.074049943651441019, 1.574803149606302854, 0.6221544894623937116 ) ) ;
#46777=DIRECTION ( 'NONE',  ( 0.000000000000000000, 0.000000000000000000, -1.000000000000000000 ) ) ;
#46778=LINE ( 'NONE', #27690, #3798 ) ;
#46781=ORIENTED_EDGE ( 'NONE', *, *, #32040, .F. ) ;
#46785=CARTESIAN_POINT ( 'NONE',  ( -1.088998432874330735, 5.905511811023623991, 1.918626195649137500 ) ) ;
#46788=DIRECTION ( 'NONE',  ( -0.9998717552508122886, -0.01601477604151181275, 0.000000000000000000 ) ) ;
#46792=CONICAL_SURFACE ( 'NONE', #21260, 1.850107469027523210, 0.6386652850508578450 ) ;
#46796=EDGE_CURVE ( 'NONE', #23287, #2346, #25316, .T. ) ;
#46797=AXIS2_PLACEMENT_3D ( 'NONE', #14798, #10917, #19158 ) ;
#46800=CIRCLE ( 'NONE', #27034, 2.165354330708661568 ) ;
#46811=CARTESIAN_POINT ( 'NONE',  ( 2.919426793319799707, 0.000000000000000000, 0.4451252810446820196 ) ) ;
#46812=CARTESIAN_POINT ( 'NONE',  ( -1.915856643696823625, 1.586962021640019538, -1.899833043120999099 ) ) ;
#46816=DIRECTION ( 'NONE',  ( 2.866708903754509961E-17, 1.000000000000000000, -1.255987235303920130E-16 ) ) ;
#46818=CARTESIAN_POINT ( 'NONE',  ( 2.949782676795221992, 0.000000000000000000, -0.1324748927672375898 ) ) ;
#46824=ORIENTED_EDGE ( 'NONE', *, *, #9620, .F. ) ;
#46828=VECTOR ( 'NONE', #31847, 39.37007874015748143 ) ;
#46835=CARTESIAN_POINT ( 'NONE',  ( -0.7381027496704858359, 1.609316782724114825, -2.859439394060923512 ) ) ;
#46836=CARTESIAN_POINT ( 'NONE',  ( 0.1071992566810385378, 0.000000000000000000, -1.740088185897661788 ) ) ;
#46837=ADVANCED_FACE ( 'NONE', ( #32998 ), #48677, .F. ) ;
#46840=VERTEX_POINT ( 'NONE', #28585 ) ;
#46849=ORIENTED_EDGE ( 'NONE', *, *, #14401, .F. ) ;
#46856=EDGE_CURVE ( 'NONE', #32877, #19533, #30380, .T. ) ;
#46862=ORIENTED_EDGE ( 'NONE', *, *, #45173, .T. ) ;
#46864=CARTESIAN_POINT ( 'NONE',  ( -1.936750629140493007, 1.578456148182591168, 0.9863243683714766341 ) ) ;
#46868=ORIENTED_EDGE ( 'NONE', *, *, #12108, .F. ) ;
#46869=DIRECTION ( 'NONE',  ( 0.000000000000000000, 1.000000000000000000, -0.000000000000000000 ) ) ;
#46873=DIRECTION ( 'NONE',  ( 8.741157232058247392E-17, -1.000000000000000000, -7.636919086868415696E-17 ) ) ;
#46876=CARTESIAN_POINT ( 'NONE',  ( 1.228106025299609216, 1.734763879243638396, -2.436764970734814906 ) ) ;
#46880=ADVANCED_FACE ( 'NONE', ( #2508 ), #37624, .T. ) ;
#46881=ORIENTED_EDGE ( 'NONE', *, *, #10895, .T. ) ;
#46884=ORIENTED_EDGE ( 'NONE', *, *, #390, .F. ) ;
#46886=CARTESIAN_POINT ( 'NONE',  ( -2.411201994581868568, 1.049302529728235234, 0.8351922078364127922 ) ) ;
#46892=ORIENTED_EDGE ( 'NONE', *, *, #20236, .F. ) ;
#46894=EDGE_CURVE ( 'NONE', #23660, #49387, #27131, .T. ) ;
#46895=EDGE_LOOP ( 'NONE', ( #30908, #40075, #3153, #45147 ) ) ;
#46898=ORIENTED_EDGE ( 'NONE', *, *, #38319, .T. ) ;
#46900=LINE ( 'NONE', #11573, #50850 ) ;
#46911=ORIENTED_EDGE ( 'NONE', *, *, #11858, .T. ) ;
#46916=EDGE_CURVE ( 'NONE', #33610, #45880, #17740, .T. ) ;
#46922=CARTESIAN_POINT ( 'NONE',  ( -1.738757879605812073, 7.027592017269983715E-05, -0.1273499085982673085 ) ) ;
#46925=CARTESIAN_POINT ( 'NONE',  ( -0.2810210260108632063, 1.714875720633193934, -2.939398529262501558 ) ) ;
#46926=AXIS2_PLACEMENT_3D ( 'NONE', #29475, #13983, #8258 ) ;
#46929=ORIENTED_EDGE ( 'NONE', *, *, #17766, .T. ) ;
#46934=VECTOR ( 'NONE', #36422, 39.37007874015748854 ) ;
#46937=DIRECTION ( 'NONE',  ( 0.000000000000000000, 0.000000000000000000, -1.000000000000000000 ) ) ;
#46938=EDGE_LOOP ( 'NONE', ( #5745, #37713, #30482, #45035, #30381, #12463, #39890, #29500, #14648, #25979, #10039 ) ) ;
#46940=AXIS2_PLACEMENT_3D ( 'NONE', #2670, #23049, #18419 ) ;
#46942=CARTESIAN_POINT ( 'NONE',  ( 0.08139965876239094178, 1.610780518492231694, 0.000000000000000000 ) ) ;
#46944=ADVANCED_FACE ( 'NONE', ( #30124 ), #6781, .T. ) ;
#46947=FACE_OUTER_BOUND ( 'NONE', #39011, .T. ) ;
#46950=CARTESIAN_POINT ( 'NONE',  ( -2.122900408388392002, 1.686164691611804489, -2.052396256679426489 ) ) ;
#46955=CARTESIAN_POINT ( 'NONE',  ( -1.556712866041156440, 1.694999912340861004, 2.509548638715847435 ) ) ;
#46956=ORIENTED_EDGE ( 'NONE', *, *, #1036, .T. ) ;
#46960=EDGE_CURVE ( 'NONE', #16522, #32449, #33391, .T. ) ;
#46963=DIRECTION ( 'NONE',  ( 0.000000000000000000, 0.000000000000000000, 1.000000000000000000 ) ) ;
#46965=EDGE_CURVE ( 'NONE', #41036, #26643, #13872, .T. ) ;
#46972=EDGE_CURVE ( 'NONE', #50795, #48962, #23373, .T. ) ;
#46976=EDGE_CURVE ( 'NONE', #2834, #46309, #9868, .T. ) ;
#46977=DIRECTION ( 'NONE',  ( -0.000000000000000000, 1.000000000000000000, -0.000000000000000000 ) ) ;
#46982=ORIENTED_EDGE ( 'NONE', *, *, #24846, .F. ) ;
#46983=LINE ( 'NONE', #19895, #21757 ) ;
#46984=DIRECTION ( 'NONE',  ( -0.01601477604151182663, 0.9998717552508123996, -0.000000000000000000 ) ) ;
#46987=CARTESIAN_POINT ( 'NONE',  ( 2.043634885149959501, 1.574803149606302854, 0.7157624142946232837 ) ) ;
#46992=PLANE ( 'NONE',  #30373 ) ;
#47001=ORIENTED_EDGE ( 'NONE', *, *, #21983, .F. ) ;
#47004=VERTEX_POINT ( 'NONE', #28018 ) ;
#47007=EDGE_CURVE ( 'NONE', #47418, #15669, #27758, .T. ) ;
#47013=DIRECTION ( 'NONE',  ( 0.000000000000000000, 0.000000000000000000, 1.000000000000000000 ) ) ;
#47015=EDGE_LOOP ( 'NONE', ( #36036, #8576, #4238, #45885 ) ) ;
#47016=ORIENTED_EDGE ( 'NONE', *, *, #44605, .F. ) ;
#47017=LINE ( 'NONE', #18940, #30444 ) ;
#47018=DIRECTION ( 'NONE',  ( 0.000000000000000000, 0.000000000000000000, 1.000000000000000000 ) ) ;
#47019=DIRECTION ( 'NONE',  ( 0.000000000000000000, 0.000000000000000000, 1.000000000000000000 ) ) ;
#47020=EDGE_CURVE ( 'NONE', #18896, #14924, #2468, .T. ) ;
#47025=B_SPLINE_CURVE_WITH_KNOTS ( 'NONE', 3,
 ( #44531, #37066, #17946, #1685 ),
 .UNSPECIFIED., .F., .F.,
 ( 4, 4 ),
 ( 2.767205287773147393E-07, 0.002500421603420419601 ),
 .UNSPECIFIED. ) ;
#47032=EDGE_CURVE ( 'NONE', #34103, #36731, #42504, .T. ) ;
#47036=ORIENTED_EDGE ( 'NONE', *, *, #18043, .T. ) ;
#47041=CIRCLE ( 'NONE', #49512, 2.246510896728926010 ) ;
#47044=CARTESIAN_POINT ( 'NONE',  ( 2.061875708210571201, 1.740926663775191674, 1.053657044629532802 ) ) ;
#47061=VERTEX_POINT ( 'NONE', #15131 ) ;
#47063=B_SPLINE_CURVE_WITH_KNOTS ( 'NONE', 3,
 ( #11294, #15917, #27277, #19784 ),
 .UNSPECIFIED., .F., .F.,
 ( 4, 4 ),
 ( 0.0004412629834327503188, 0.04923299811573771112 ),
 .UNSPECIFIED. ) ;
#47064=DIRECTION ( 'NONE',  ( 0.9998717552508121775, 0.01601477604151182663, 0.000000000000000000 ) ) ;
#47065=LINE ( 'NONE', #34490, #18590 ) ;
#47067=ORIENTED_EDGE ( 'NONE', *, *, #29643, .F. ) ;
#47069=CARTESIAN_POINT ( 'NONE',  ( 0.3136974817028393425, 1.625700591256411531, -2.936457595020219635 ) ) ;
#47071=ORIENTED_EDGE ( 'NONE', *, *, #17303, .F. ) ;
#47075=B_SPLINE_CURVE_WITH_KNOTS ( 'NONE', 3,
 ( #9762, #14136, #2773, #41010 ),
 .UNSPECIFIED., .F., .F.,
 ( 4, 4 ),
 ( 0.0004868636330354340533, 0.002987072310269779825 ),
 .UNSPECIFIED. ) ;
#47081=ADVANCED_FACE ( 'NONE', ( #38880 ), #44680, .T. ) ;
#47083=DIRECTION ( 'NONE',  ( 3.586865599282426309E-17, -1.000000000000000000, -1.103923720497134591E-16 ) ) ;
#47084=EDGE_CURVE ( 'NONE', #27696, #3507, #49232, .T. ) ;
#47087=ORIENTED_EDGE ( 'NONE', *, *, #39086, .F. ) ;
#47089=ORIENTED_EDGE ( 'NONE', *, *, #46196, .T. ) ;
#47092=DIRECTION ( 'NONE',  ( -0.01601477604151182663, 0.9998717552508123996, -0.000000000000000000 ) ) ;
#47093=CONICAL_SURFACE ( 'NONE', #28996, 2.165354330708661568, 0.2617993877991570129 ) ;
#47097=CARTESIAN_POINT ( 'NONE',  ( 2.165460538733997353, 5.905511811023623991, 0.04798874274655766381 ) ) ;
#47099=ADVANCED_FACE ( 'NONE', ( #50440 ), #30887, .T. ) ;
#47102=CARTESIAN_POINT ( 'NONE',  ( -0.2198976605848039223, 1.205361022782829114E-17, -1.894256224240784103 ) ) ;
#47103=EDGE_CURVE ( 'NONE', #14452, #695, #32649, .T. ) ;
#47107=VERTEX_POINT ( 'NONE', #17427 ) ;
#47110=EDGE_CURVE ( 'NONE', #3878, #18162, #27669, .T. ) ;
#47111=CARTESIAN_POINT ( 'NONE',  ( 0.04921259842519689481, 0.009569417371913045700, 1.905847912026497948 ) ) ;
#47113=CARTESIAN_POINT ( 'NONE',  ( -0.1450362469327511061, 1.574803149606302854, -2.160491579385214411 ) ) ;
#47117=CARTESIAN_POINT ( 'NONE',  ( -1.628069513120385503, 0.001843152681973240061, -0.6423508795876955446 ) ) ;
#47125=DIRECTION ( 'NONE',  ( -3.981026654148627524E-17, 1.000000000000000000, 1.225234019452863932E-16 ) ) ;
#47127=DIRECTION ( 'NONE',  ( -3.986037398843765983E-20, -1.000000000000000000, -1.160734090543304660E-16 ) ) ;
#47131=EDGE_LOOP ( 'NONE', ( #7062, #34818, #34572, #20517 ) ) ;
#47132=CARTESIAN_POINT ( 'NONE',  ( 1.871031489114177715, 0.000000000000000000, 0.9882585515110396956 ) ) ;
#47133=EDGE_LOOP ( 'NONE', ( #48291, #13158, #963, #22902, #31842, #35192, #14487, #23663, #13118, #12197, #14294 ) ) ;
#47147=AXIS2_PLACEMENT_3D ( 'NONE', #34880, #34387, #42616 ) ;
#47151=PLANE ( 'NONE',  #33099 ) ;
#47154=ORIENTED_EDGE ( 'NONE', *, *, #43477, .T. ) ;
#47156=DIRECTION ( 'NONE',  ( -0.000000000000000000, 1.000000000000000000, -0.000000000000000000 ) ) ;
#47158=LINE ( 'NONE', #27573, #22732 ) ;
#47163=DIRECTION ( 'NONE',  ( 0.8090169943749506709, 6.819399030548774257E-17, -0.5877852522924684742 ) ) ;
#47164=EDGE_LOOP ( 'NONE', ( #16730, #46750, #4064, #20642 ) ) ;
#47169=FACE_OUTER_BOUND ( 'NONE', #29755, .T. ) ;
#47170=ADVANCED_FACE ( 'NONE', ( #48873 ), #44526, .T. ) ;
#47174=ORIENTED_EDGE ( 'NONE', *, *, #9479, .T. ) ;
#47175=ADVANCED_FACE ( 'NONE', ( #911 ), #7591, .T. ) ;
#47176=B_SPLINE_CURVE_WITH_KNOTS ( 'NONE', 3,
 ( #30557, #31316, #49870, #42421 ),
 .UNSPECIFIED., .F., .F.,
 ( 4, 4 ),
 ( 0.0001501286205249034299, 0.002650226654156385194 ),
 .UNSPECIFIED. ) ;
#47183=FACE_OUTER_BOUND ( 'NONE', #19031, .T. ) ;
#47191=CIRCLE ( 'NONE', #41498, 2.165354330708661568 ) ;
#47193=AXIS2_PLACEMENT_3D ( 'NONE', #36111, #47683, #21132 ) ;
#47194=FACE_OUTER_BOUND ( 'NONE', #47945, .T. ) ;
#47195=CARTESIAN_POINT ( 'NONE',  ( 1.892591856222374469, 0.05823298773025239322, -0.4824499329568616157 ) ) ;
#47197=VERTEX_POINT ( 'NONE', #32687 ) ;
#47198=AXIS2_PLACEMENT_3D ( 'NONE', #678, #16433, #32187 ) ;
#47199=CARTESIAN_POINT ( 'NONE',  ( 2.260029193386923652, 0.5219248566477788787, 0.3558038071150583792 ) ) ;
#47203=CARTESIAN_POINT ( 'NONE',  ( 2.112319093887386146, 0.000000000000000000, 0.3357951146312926904 ) ) ;
#47208=ORIENTED_EDGE ( 'NONE', *, *, #36697, .F. ) ;
#47217=CARTESIAN_POINT ( 'NONE',  ( 0.9319704666822036243, 0.04284687812831378811, 1.655805649632502430 ) ) ;
#47218=ORIENTED_EDGE ( 'NONE', *, *, #34482, .T. ) ;
#47219=VERTEX_POINT ( 'NONE', #5296 ) ;
#47220=CIRCLE ( 'NONE', #34893, 1.743387098533651480 ) ;
#47221=DIRECTION ( 'NONE',  ( -0.2225209339563184452, 1.288287287306305283E-16, 0.9749279121818227312 ) ) ;
#47222=LINE ( 'NONE', #27895, #50641 ) ;
#47224=ORIENTED_EDGE ( 'NONE', *, *, #14933, .F. ) ;
#47227=FACE_BOUND ( 'NONE', #22700, .T. ) ;
#47230=EDGE_CURVE ( 'NONE', #14792, #48519, #28215, .T. ) ;
#47232=EDGE_CURVE ( 'NONE', #21120, #7866, #51033, .T. ) ;
#47233=FACE_OUTER_BOUND ( 'NONE', #4795, .T. ) ;
#47235=AXIS2_PLACEMENT_3D ( 'NONE', #19211, #34223, #26457 ) ;
#47242=PLANE ( 'NONE',  #6410 ) ;
#47243=DIRECTION ( 'NONE',  ( -0.000000000000000000, -1.000000000000000000, -0.000000000000000000 ) ) ;
#47246=CARTESIAN_POINT ( 'NONE',  ( 1.514466370292996800, 0.000000000000000000, 2.534789744887420149 ) ) ;
#47247=B_SPLINE_CURVE_WITH_KNOTS ( 'NONE', 3,
 ( #35159, #34155, #49838, #6776 ),
 .UNSPECIFIED., .F., .F.,
 ( 4, 4 ),
 ( 0.1211873102087489551, 0.1625992483279400380 ),
 .UNSPECIFIED. ) ;
#47254=DIRECTION ( 'NONE',  ( 1.160706738777435820E-16, 1.000000000000000000, 5.589669052740852391E-17 ) ) ;
#47263=EDGE_CURVE ( 'NONE', #22597, #44259, #34450, .T. ) ;
#47267=CARTESIAN_POINT ( 'NONE',  ( 1.775400203342704986, 1.648464234653929106, -2.359903268218703332 ) ) ;
#47269=DIRECTION ( 'NONE',  ( -0.9998717552508121775, -0.01601477604151182316, 0.000000000000000000 ) ) ;
#47275=DIRECTION ( 'NONE',  ( -0.9998717552508122886, -0.01601477604151182316, 0.000000000000000000 ) ) ;
#47279=DIRECTION ( 'NONE',  ( -6.394449067488487880E-17, -1.000000000000000000, -9.687176266499690201E-17 ) ) ;
#47289=CARTESIAN_POINT ( 'NONE',  ( -1.883797214242443951, 0.5252390421956055766, -0.03533922825790704325 ) ) ;
#47290=DIRECTION ( 'NONE',  ( -0.9998717552508122886, -0.01601477604151180928, 0.000000000000000000 ) ) ;
#47291=ORIENTED_EDGE ( 'NONE', *, *, #8343, .T. ) ;
#47293=ORIENTED_EDGE ( 'NONE', *, *, #49744, .T. ) ;
#47294=CARTESIAN_POINT ( 'NONE',  ( 2.947574761915768171, 1.765190094501404072, -0.1816379373804911379 ) ) ;
#47295=FACE_OUTER_BOUND ( 'NONE', #50511, .T. ) ;
#47303=VECTOR ( 'NONE', #2895, 39.37007874015748143 ) ;
#47304=DIRECTION ( 'NONE',  ( 0.000000000000000000, 0.000000000000000000, 1.000000000000000000 ) ) ;
#47309=CARTESIAN_POINT ( 'NONE',  ( 0.000000000000000000, 1.574803149606302854, 0.000000000000000000 ) ) ;
#47310=CARTESIAN_POINT ( 'NONE',  ( -1.312248418042854858, 1.574803149606302854, -1.722429524498108711 ) ) ;
#47316=VECTOR ( 'NONE', #24757, 39.37007874015748854 ) ;
#47321=CARTESIAN_POINT ( 'NONE',  ( 1.174087487603957980, 5.905511811023623991, 1.869141625116387706 ) ) ;
#47326=ORIENTED_EDGE ( 'NONE', *, *, #40971, .T. ) ;
#47332=DIRECTION ( 'NONE',  ( 0.8090169943749422332, 0.000000000000000000, 0.5877852522924802425 ) ) ;
#47339=LINE ( 'NONE', #12524, #23860 ) ;
#47343=CARTESIAN_POINT ( 'NONE',  ( -1.968719161901109960, 1.044049570087769885, 1.632946417767990654 ) ) ;
#47361=ORIENTED_EDGE ( 'NONE', *, *, #12810, .F. ) ;
#47363=DIRECTION ( 'NONE',  ( 0.000000000000000000, 1.160734090543304660E-16, -1.000000000000000000 ) ) ;
#47365=DIRECTION ( 'NONE',  ( -0.01601477604151182663, 0.9998717552508123996, -0.000000000000000000 ) ) ;
#47368=VERTEX_POINT ( 'NONE', #25677 ) ;
#47369=CARTESIAN_POINT ( 'NONE',  ( 1.163887619842433718, 0.04656145577143805392, -1.518228404148327160 ) ) ;
#47370=EDGE_CURVE ( 'NONE', #27692, #41895, #25758, .T. ) ;
#47371=CARTESIAN_POINT ( 'NONE',  ( -0.8151651997737653366, 0.000000000000000000, -1.654713224395694571 ) ) ;
#47375=CARTESIAN_POINT ( 'NONE',  ( 2.079244330788078798, 1.744638041679277496, -1.431464546258592430 ) ) ;
#47376=PLANE ( 'NONE',  #10351 ) ;
#47379=VECTOR ( 'NONE', #13643, 39.37007874015748143 ) ;
#47384=CARTESIAN_POINT ( 'NONE',  ( 0.1067246931122726866, 0.02962905676920215767, 0.000000000000000000 ) ) ;
#47386=EDGE_CURVE ( 'NONE', #48433, #37126, #25863, .T. ) ;
#47400=ADVANCED_FACE ( 'NONE', ( #39072 ), #29857, .T. ) ;
#47401=CARTESIAN_POINT ( 'NONE',  ( -1.152568299495734250, 1.574803149606302854, 1.833124570921536467 ) ) ;
#47404=ORIENTED_EDGE ( 'NONE', *, *, #48108, .T. ) ;
#47407=ADVANCED_FACE ( 'NONE', ( #3199 ), #43438, .T. ) ;
#47412=AXIS2_PLACEMENT_3D ( 'NONE', #27328, #39472, #19832 ) ;
#47415=VERTEX_POINT ( 'NONE', #4209 ) ;
#47416=CARTESIAN_POINT ( 'NONE',  ( 2.889674983507178219, 0.000000000000000000, -0.6090712660037610471 ) ) ;
#47418=VERTEX_POINT ( 'NONE', #19188 ) ;
#47420=PLANE ( 'NONE',  #36608 ) ;
#47425=AXIS2_PLACEMENT_3D ( 'NONE', #23294, #11932, #19164 ) ;
#47427=LINE ( 'NONE', #31219, #50950 ) ;
#47429=CARTESIAN_POINT ( 'NONE',  ( 2.889674983507178219, 1.665813060096536402, -0.6090712660037608250 ) ) ;
#47430=CARTESIAN_POINT ( 'NONE',  ( -0.7855418668307149188, 0.000000000000000000, -2.846347029613745416 ) ) ;
#47432=CARTESIAN_POINT ( 'NONE',  ( -0.9914495361339011881, 1.605369965488712136, 2.781765111341808705 ) ) ;
#47442=ORIENTED_EDGE ( 'NONE', *, *, #47103, .F. ) ;
#47456=VECTOR ( 'NONE', #38929, 39.37007874015748854 ) ;
#47463=EDGE_CURVE ( 'NONE', #50445, #12429, #15976, .T. ) ;
#47468=ORIENTED_EDGE ( 'NONE', *, *, #26603, .F. ) ;
#47471=ORIENTED_EDGE ( 'NONE', *, *, #1118, .T. ) ;
#47474=VERTEX_POINT ( 'NONE', #50383 ) ;
#47475=EDGE_CURVE ( 'NONE', #50554, #39301, #49861, .T. ) ;
#47477=CYLINDRICAL_SURFACE ( 'NONE', #13457, 2.165354330708661568 ) ;
#47480=CARTESIAN_POINT ( 'NONE',  ( 2.712427995346972320, 1.659614058134468495, 0.4170853886664333543 ) ) ;
#47482=EDGE_LOOP ( 'NONE', ( #27637, #12155, #44036, #33208, #37020, #21749, #11427 ) ) ;
#47483=AXIS2_PLACEMENT_3D ( 'NONE', #26252, #35271, #45847 ) ;
#47484=CARTESIAN_POINT ( 'NONE',  ( 0.7090793742677682365, 0.03927686936677046714, 1.749277966691849429 ) ) ;
#47489=CARTESIAN_POINT ( 'NONE',  ( 2.088343298084792021, -7.108564423737583947E-17, 0.6267986818430602014 ) ) ;
#47495=AXIS2_PLACEMENT_3D ( 'NONE', #35444, #63, #47269 ) ;
#47505=VERTEX_POINT ( 'NONE', #42929 ) ;
#47506=CARTESIAN_POINT ( 'NONE',  ( 0.5762653268100312864, 0.000000000000000000, -1.903066372058335620 ) ) ;
#47510=CARTESIAN_POINT ( 'NONE',  ( 1.642191404871903071, 0.000000000000000000, 0.5853255206279913692 ) ) ;
#47511=CARTESIAN_POINT ( 'NONE',  ( 1.905671854841463952, 1.472358791367697650, 2.256015092822682089 ) ) ;
#47513=AXIS2_PLACEMENT_3D ( 'NONE', #25385, #21516, #33911 ) ;
#47514=EDGE_CURVE ( 'NONE', #12624, #45538, #9287, .T. ) ;
#47516=VERTEX_POINT ( 'NONE', #23828 ) ;
#47525=CARTESIAN_POINT ( 'NONE',  ( 0.4350747367505088947, 1.205361022782829114E-17, -2.121846421795415161 ) ) ;
#47538=ORIENTED_EDGE ( 'NONE', *, *, #29273, .T. ) ;
#47540=VERTEX_POINT ( 'NONE', #9100 ) ;
#47546=CARTESIAN_POINT ( 'NONE',  ( 0.4600188520506054979, 0.02342673975412612117, -1.851825020600145644 ) ) ;
#47547=ORIENTED_EDGE ( 'NONE', *, *, #26200, .F. ) ;
#47548=ORIENTED_EDGE ( 'NONE', *, *, #32469, .T. ) ;
#47550=ORIENTED_EDGE ( 'NONE', *, *, #32233, .F. ) ;
#47552=CARTESIAN_POINT ( 'NONE',  ( 0.1155636338427008941, -0.5222242541845523167, 0.000000000000000000 ) ) ;
#47556=EDGE_CURVE ( 'NONE', #37702, #22113, #5153, .T. ) ;
#47558=LINE ( 'NONE', #8361, #9747 ) ;
#47561=FACE_OUTER_BOUND ( 'NONE', #1710, .T. ) ;
#47564=ORIENTED_EDGE ( 'NONE', *, *, #34828, .T. ) ;
#47565=CARTESIAN_POINT ( 'NONE',  ( -1.731276487347650050, 1.684260316500282517, -1.723356343879357100 ) ) ;
#47567=CARTESIAN_POINT ( 'NONE',  ( -0.5150676061901260372, 0.000000000000000000, -1.804318609754868019 ) ) ;
#47570=CARTESIAN_POINT ( 'NONE',  ( -1.453832412804729302, 0.000000000000000000, -1.018633753700964428 ) ) ;
#47571=CARTESIAN_POINT ( 'NONE',  ( -0.1730139111830206189, 1.610516408500926477, -2.471348888976017122 ) ) ;
#47573=CARTESIAN_POINT ( 'NONE',  ( 2.151809081513405442, 5.118110236220475784, 0.2418202932658665705 ) ) ;
#47581=ORIENTED_EDGE ( 'NONE', *, *, #17080, .T. ) ;
#47582=VERTEX_POINT ( 'NONE', #36225 ) ;
#47583=LINE ( 'NONE', #12260, #29822 ) ;
#47584=CARTESIAN_POINT ( 'NONE',  ( 1.686111637834603938, 0.05492582915004715072, 0.9632209503012270080 ) ) ;
#47586=CARTESIAN_POINT ( 'NONE',  ( -0.2198976605848039223, 1.205361022782829114E-17, -1.894256224240784103 ) ) ;
#47587=CARTESIAN_POINT ( 'NONE',  ( 2.926032761125787029, 0.000000000000000000, 0.3963580683592521914 ) ) ;
#47592=EDGE_CURVE ( 'NONE', #37038, #3878, #6112, .T. ) ;
#47603=CARTESIAN_POINT ( 'NONE',  ( 0.2483335008317506531, 0.5236491086109019699, -2.210204286096038473 ) ) ;
#47607=FACE_OUTER_BOUND ( 'NONE', #4104, .T. ) ;
#47609=VECTOR ( 'NONE', #30865, 39.37007874015748143 ) ;
#47610=VERTEX_POINT ( 'NONE', #40093 ) ;
#47613=AXIS2_PLACEMENT_3D ( 'NONE', #25044, #25299, #33827 ) ;
#47618=LINE ( 'NONE', #671, #15362 ) ;
#47625=CARTESIAN_POINT ( 'NONE',  ( 1.266359212274407620, 1.486365060966521323, -2.667465348741127951 ) ) ;
#47626=EDGE_CURVE ( 'NONE', #15234, #10014, #44705, .T. ) ;
#47631=DIRECTION ( 'NONE',  ( -0.000000000000000000, -1.000000000000000000, -0.000000000000000000 ) ) ;
#47632=VERTEX_POINT ( 'NONE', #24084 ) ;
#47633=CARTESIAN_POINT ( 'NONE',  ( 2.928234411561841277, 1.447231713130496367, 0.3801048321602038538 ) ) ;
#47635=CARTESIAN_POINT ( 'NONE',  ( 1.810607833951273227, 0.05691986357332023266, -0.7203715021987137090 ) ) ;
#47638=CARTESIAN_POINT ( 'NONE',  ( -1.497193542162873259, 0.002659885201759431498, -0.9293214240255518455 ) ) ;
#47639=ORIENTED_EDGE ( 'NONE', *, *, #10751, .T. ) ;
#47644=CARTESIAN_POINT ( 'NONE',  ( 1.427293369312940152, 0.000000000000000000, -1.001115484471646111 ) ) ;
#47646=ORIENTED_EDGE ( 'NONE', *, *, #47659, .F. ) ;
#47650=VECTOR ( 'NONE', #31674, 39.37007874015748143 ) ;
#47651=DIRECTION ( 'NONE',  ( -0.000000000000000000, -1.000000000000000000, -0.000000000000000000 ) ) ;
#47652=ORIENTED_EDGE ( 'NONE', *, *, #41310, .T. ) ;
#47659=EDGE_CURVE ( 'NONE', #15209, #43842, #22219, .T. ) ;
#47661=VERTEX_POINT ( 'NONE', #28202 ) ;
#47672=EDGE_LOOP ( 'NONE', ( #6975, #32750, #3727, #28134, #50975, #34406 ) ) ;
#47673=CARTESIAN_POINT ( 'NONE',  ( 2.607957125084112704, 1.661418195339335213, 1.384772967396189491 ) ) ;
#47674=DIRECTION ( 'NONE',  ( 0.000000000000000000, 0.000000000000000000, -1.000000000000000000 ) ) ;
#47677=CARTESIAN_POINT ( 'NONE',  ( -2.734482843737247038, 1.205361022782829114E-17, -1.115254632218711794 ) ) ;
#47680=ORIENTED_EDGE ( 'NONE', *, *, #48007, .F. ) ;
#47681=CARTESIAN_POINT ( 'NONE',  ( -0.3929865681273516098, 1.607031701558540915, 2.441147462936593460 ) ) ;
#47682=DIRECTION ( 'NONE',  ( 0.000000000000000000, 0.000000000000000000, -1.000000000000000000 ) ) ;
#47683=DIRECTION ( 'NONE',  ( -0.01601477604151182663, 0.9998717552508123996, -0.000000000000000000 ) ) ;
#47686=DIRECTION ( 'NONE',  ( 0.9909497617679331460, 0.000000000000000000, 0.1342332658176667026 ) ) ;
#47691=VERTEX_POINT ( 'NONE', #49322 ) ;
#47695=DIRECTION ( 'NONE',  ( -0.9749279121818259508, 0.000000000000000000, 0.2225209339563041788 ) ) ;
#47696=CARTESIAN_POINT ( 'NONE',  ( 0.1155636338427008941, -0.5222242541845523167, 0.000000000000000000 ) ) ;
#47699=VERTEX_POINT ( 'NONE', #49567 ) ;
#47701=CARTESIAN_POINT ( 'NONE',  ( -2.932638728931780125, 0.000000000000000000, 0.3475908556737795085 ) ) ;
#47706=CARTESIAN_POINT ( 'NONE',  ( -2.074656761898998170, 0.000000000000000000, -0.6223516566630912239 ) ) ;
#47707=CARTESIAN_POINT ( 'NONE',  ( 2.542761396444682465, 0.9856902423583451256, -0.6308468877598402136 ) ) ;
#47708=VECTOR ( 'NONE', #41908, 39.37007874015748143 ) ;
#47709=FACE_OUTER_BOUND ( 'NONE', #11519, .T. ) ;
#47710=ORIENTED_EDGE ( 'NONE', *, *, #38571, .T. ) ;
#47717=ADVANCED_FACE ( 'NONE', ( #41118 ), #10122, .F. ) ;
#47723=LINE ( 'NONE', #16271, #39783 ) ;
#47726=PRODUCT_CONTEXT ( 'NONE', #5505, 'mechanical' ) ;
#47728=CARTESIAN_POINT ( 'NONE',  ( 0.000000000000000000, 0.000000000000000000, 0.000000000000000000 ) ) ;
#47737=DIRECTION ( 'NONE',  ( 2.866708903754509961E-17, 1.000000000000000000, -1.255987235303920130E-16 ) ) ;
#47738=FACE_OUTER_BOUND ( 'NONE', #43618, .T. ) ;
#47742=LINE ( 'NONE', #36950, #25601 ) ;
#47744=CARTESIAN_POINT ( 'NONE',  ( 0.6872259521622784417, 0.000000000000000000, 1.878032350763792158 ) ) ;
#47745=EDGE_CURVE ( 'NONE', #21072, #9746, #13749, .T. ) ;
#47747=DIRECTION ( 'NONE',  ( 0.000000000000000000, -1.000000000000000000, 0.000000000000000000 ) ) ;
#47748=ORIENTED_EDGE ( 'NONE', *, *, #50803, .T. ) ;
#47750=CARTESIAN_POINT ( 'NONE',  ( -1.263630850544466666, 0.000000000000000000, -1.276241334172347530 ) ) ;
#47753=EDGE_CURVE ( 'NONE', #31865, #8302, #50401, .T. ) ;
#47757=CARTESIAN_POINT ( 'NONE',  ( 2.019856298626497626, 1.049866565067837820, -0.1399740531529398979 ) ) ;
#47760=ORIENTED_EDGE ( 'NONE', *, *, #1822, .T. ) ;
#47761=CARTESIAN_POINT ( 'NONE',  ( 0.5469786881612729301, 0.03668053021573630668, -1.796948620166157307 ) ) ;
#47763=CARTESIAN_POINT ( 'NONE',  ( 2.695799277629594037, 1.453624836071520265, -1.205759334241453651 ) ) ;
#47764=EDGE_LOOP ( 'NONE', ( #8180, #42913, #44141, #48417 ) ) ;
#47766=CARTESIAN_POINT ( 'NONE',  ( -0.9149808212874269708, 1.594821661612501940, -2.013400720915880626 ) ) ;
#47767=LINE ( 'NONE', #7555, #29681 ) ;
#47769=AXIS2_PLACEMENT_3D ( 'NONE', #44521, #29552, #13808 ) ;
#47775=VERTEX_POINT ( 'NONE', #17283 ) ;
#47776=CARTESIAN_POINT ( 'NONE',  ( -2.491402175429631605, 1.567214198537667302, -1.585592796919542025 ) ) ;
#47777=FACE_OUTER_BOUND ( 'NONE', #31181, .T. ) ;
#47779=EDGE_CURVE ( 'NONE', #46840, #9567, #48820, .T. ) ;
#47780=CIRCLE ( 'NONE', #37934, 2.165354330708661568 ) ;
#47782=CIRCLE ( 'NONE', #1653, 2.164630168518208109 ) ;
#47783=B_SPLINE_CURVE_WITH_KNOTS ( 'NONE', 3,
 ( #36559, #13577, #29829, #21323 ),
 .UNSPECIFIED., .F., .F.,
 ( 4, 4 ),
 ( 2.103951477127680371E-07, 0.01599021799251365214 ),
 .UNSPECIFIED. ) ;
#47785=CARTESIAN_POINT ( 'NONE',  ( -0.7078551079828497850, 0.5249316497054297148, 1.746015920841205382 ) ) ;
#47789=CYLINDRICAL_SURFACE ( 'NONE', #6773, 2.165354330708661568 ) ;
#47791=EDGE_LOOP ( 'NONE', ( #16795, #13888, #39753, #37885 ) ) ;
#47793=VERTEX_POINT ( 'NONE', #5658 ) ;
#47797=DIRECTION ( 'NONE',  ( 1.241861098869884156E-16, 1.000000000000000000, 3.427318860986280993E-17 ) ) ;
#47799=CARTESIAN_POINT ( 'NONE',  ( -1.743268982565497449, 0.0004610889948519912205, -0.02902809809614041725 ) ) ;
#47803=VERTEX_POINT ( 'NONE', #20886 ) ;
#47806=B_SPLINE_CURVE_WITH_KNOTS ( 'NONE', 3,
 ( #41383, #24618, #24873, #20737 ),
 .UNSPECIFIED., .F., .F.,
 ( 4, 4 ),
 ( 0.01485121745614547892, 0.03075156861365398869 ),
 .UNSPECIFIED. ) ;
#47807=EDGE_CURVE ( 'NONE', #39165, #47661, #33835, .T. ) ;
#47808=CARTESIAN_POINT ( 'NONE',  ( -2.138597145901436125, 6.692913385826772199, 0.3393547186366932533 ) ) ;
#47809=CARTESIAN_POINT ( 'NONE',  ( 2.928234753086226938, 1.764879838232207732, 0.3801023109259407673 ) ) ;
#47810=DIRECTION ( 'NONE',  ( -0.7530714660036099684, 0.000000000000000000, -0.6579387259397138088 ) ) ;
#47814=EDGE_CURVE ( 'NONE', #39003, #13966, #39940, .T. ) ;
#47820=CARTESIAN_POINT ( 'NONE',  ( -1.503492009532958695, 1.205361022782829114E-17, -0.9334790059352082725 ) ) ;
#47821=CARTESIAN_POINT ( 'NONE',  ( 2.889674983507178219, 0.000000000000000000, -0.6090712660037610471 ) ) ;
#47826=DIRECTION ( 'NONE',  ( 0.9998717552508121775, 0.01601477604151182663, 0.000000000000000000 ) ) ;
#47831=ORIENTED_EDGE ( 'NONE', *, *, #17337, .F. ) ;
#47836=ADVANCED_FACE ( 'NONE', ( #32785 ), #12631, .T. ) ;
#47840=CARTESIAN_POINT ( 'NONE',  ( 0.000000000000000000, 6.692913385826772199, 0.000000000000000000 ) ) ;
#47843=CARTESIAN_POINT ( 'NONE',  ( -0.9146000759343694275, 1.693252956796532871, -2.012610095043610769 ) ) ;
#47846=LINE ( 'NONE', #29024, #15756 ) ;
#47850=DIRECTION ( 'NONE',  ( -0.9998717552508122886, -0.01601477604151182316, 0.000000000000000000 ) ) ;
#47853=B_SPLINE_CURVE_WITH_KNOTS ( 'NONE', 3,
 ( #20250, #32149, #35750, #40148 ),
 .UNSPECIFIED., .F., .F.,
 ( 4, 4 ),
 ( 2.103237516471686094E-07, 0.002500256604276755550 ),
 .UNSPECIFIED. ) ;
#47858=CARTESIAN_POINT ( 'NONE',  ( -2.122503961981847542, 1.608289367666104752, -0.4339694865994201955 ) ) ;
#47860=ORIENTED_EDGE ( 'NONE', *, *, #30120, .T. ) ;
#47864=ORIENTED_EDGE ( 'NONE', *, *, #1120, .F. ) ;
#47865=DIRECTION ( 'NONE',  ( 0.01601477604151182663, -0.9998717552508123996, 0.000000000000000000 ) ) ;
#47867=VECTOR ( 'NONE', #27807, 39.37007874015748143 ) ;
#47868=DIRECTION ( 'NONE',  ( -0.7227948638273978821, 0.000000000000000000, 0.6910626489868580968 ) ) ;
#47870=CARTESIAN_POINT ( 'NONE',  ( -1.999177773607318409, 1.049866565067837820, 0.3204690814597923043 ) ) ;
#47873=DIRECTION ( 'NONE',  ( -0.01601477604151182663, 0.9998717552508123996, -0.000000000000000000 ) ) ;
#47877=DIRECTION ( 'NONE',  ( 9.964307797194585150E-17, -1.000000000000000000, 5.953396763000637613E-17 ) ) ;
#47886=EDGE_CURVE ( 'NONE', #35873, #39853, #43853, .T. ) ;
#47887=CARTESIAN_POINT ( 'NONE',  ( -1.722315009966508548, 1.593974433676846880, -2.398471918813898984 ) ) ;
#47888=VERTEX_POINT ( 'NONE', #20376 ) ;
#47891=CARTESIAN_POINT ( 'NONE',  ( 0.07982360342473591996, 1.709180471932028711, 0.000000000000000000 ) ) ;
#47892=CARTESIAN_POINT ( 'NONE',  ( 1.367759369798452695, 0.5227967160397331003, -1.798833794882606085 ) ) ;
#47894=EDGE_CURVE ( 'NONE', #15197, #10377, #36132, .T. ) ;
#47901=LINE ( 'NONE', #8197, #50092 ) ;
#47905=DIRECTION ( 'NONE',  ( -0.01601477604151182663, 0.9998717552508123996, -0.000000000000000000 ) ) ;
#47911=DIRECTION ( 'NONE',  ( -0.7530714660036099684, 0.000000000000000000, -0.6579387259397138088 ) ) ;
#47918=EDGE_CURVE ( 'NONE', #29725, #20465, #37415, .T. ) ;
#47922=B_SPLINE_CURVE_WITH_KNOTS ( 'NONE', 3,
 ( #30038, #34921, #46755, #45757 ),
 .UNSPECIFIED., .F., .F.,
 ( 4, 4 ),
 ( 6.553284148700209415E-07, 0.004847467262264384957 ),
 .UNSPECIFIED. ) ;
#47933=ORIENTED_EDGE ( 'NONE', *, *, #4174, .F. ) ;
#47934=ORIENTED_EDGE ( 'NONE', *, *, #38236, .F. ) ;
#47935=VECTOR ( 'NONE', #33302, 39.37007874015748143 ) ;
#47936=CARTESIAN_POINT ( 'NONE',  ( -1.387661672111457634, 5.905511811023623991, -1.663104731517941470 ) ) ;
#47945=EDGE_LOOP ( 'NONE', ( #8206, #26119, #3872, #24279, #28159, #16573 ) ) ;
#47948=ORIENTED_EDGE ( 'NONE', *, *, #29109, .T. ) ;
#47950=ADVANCED_FACE ( 'NONE', ( #30164 ), #955, .T. ) ;
#47955=CARTESIAN_POINT ( 'NONE',  ( 2.755905511811024056, 4.960629921259846142, -1.023622047244094224 ) ) ;
#47956=CARTESIAN_POINT ( 'NONE',  ( 0.2483287796717625062, 1.509167455152593096, -2.942340884688746883 ) ) ;
#47957=VERTEX_POINT ( 'NONE', #33802 ) ;
#47961=LINE ( 'NONE', #1529, #6488 ) ;
#47964=FACE_OUTER_BOUND ( 'NONE', #37822, .T. ) ;
#47966=EDGE_CURVE ( 'NONE', #11883, #21408, #30423, .T. ) ;
#47967=AXIS2_PLACEMENT_3D ( 'NONE', #7636, #50191, #30624 ) ;
#47969=ORIENTED_EDGE ( 'NONE', *, *, #5253, .T. ) ;
#47976=VECTOR ( 'NONE', #6027, 39.37007874015748143 ) ;
#47978=CARTESIAN_POINT ( 'NONE',  ( 0.000000000000000000, 1.574803149606302854, 0.000000000000000000 ) ) ;
#47986=DIRECTION ( 'NONE',  ( -0.01601477604151182663, 0.9998717552508123996, -0.000000000000000000 ) ) ;
#47987=CARTESIAN_POINT ( 'NONE',  ( 0.2156353639037333347, 0.03137346048107473445, -1.846898229409209558 ) ) ;
#47992=DIRECTION ( 'NONE',  ( -0.5877852522924684742, 0.000000000000000000, -0.8090169943749506709 ) ) ;
#47993=CARTESIAN_POINT ( 'NONE',  ( 1.128560816269277955, 1.725977917706353670, 1.984842472008916170 ) ) ;
#47996=CARTESIAN_POINT ( 'NONE',  ( -2.160407304981126320, 1.673304745347873324, -0.1462862061266896330 ) ) ;
#47998=CARTESIAN_POINT ( 'NONE',  ( 1.859752236076028797, 0.5249316497054297148, 0.3015826091447992297 ) ) ;
#48001=ORIENTED_EDGE ( 'NONE', *, *, #49581, .T. ) ;
#48007=EDGE_CURVE ( 'NONE', #11192, #44848, #7544, .T. ) ;
#48008=VECTOR ( 'NONE', #40620, 39.37007874015748143 ) ;
#48014=EDGE_CURVE ( 'NONE', #50795, #7249, #16623, .T. ) ;
#48015=ORIENTED_EDGE ( 'NONE', *, *, #31555, .T. ) ;
#48022=ORIENTED_EDGE ( 'NONE', *, *, #1265, .F. ) ;
#48023=CARTESIAN_POINT ( 'NONE',  ( 0.9116672196811488327, 1.631344156046437899, 2.569185889370713127 ) ) ;
#48036=CARTESIAN_POINT ( 'NONE',  ( 2.109782028357643835, 1.650152804904060133, 1.745440299926597882 ) ) ;
#48037=ORIENTED_EDGE ( 'NONE', *, *, #47514, .T. ) ;
#48041=DIRECTION ( 'NONE',  ( -0.01601477604151182663, 0.9998717552508123996, -0.000000000000000000 ) ) ;
#48043=CARTESIAN_POINT ( 'NONE',  ( 0.9218113296639885990, 0.000000000000000000, -1.800737481590852118 ) ) ;
#48052=( LENGTH_UNIT ( ) NAMED_UNIT ( * ) SI_UNIT ( $, .METRE. ) );
#48054=AXIS2_PLACEMENT_3D ( 'NONE', #27126, #19129, #50821 ) ;
#48055=CIRCLE ( 'NONE', #11783, 2.246510896728926010 ) ;
#48057=CARTESIAN_POINT ( 'NONE',  ( 0.3543214468173200293, 1.713577057256821190, 2.228085083314873316 ) ) ;
#48061=AXIS2_PLACEMENT_3D ( 'NONE', #24108, #39854, #95 ) ;
#48063=CARTESIAN_POINT ( 'NONE',  ( 0.000000000000000000, 6.692913385826772199, 0.000000000000000000 ) ) ;
#48066=CARTESIAN_POINT ( 'NONE',  ( 1.905671854841464175, 0.000000000000000000, 2.256015092822681645 ) ) ;
#48067=CARTESIAN_POINT ( 'NONE',  ( 2.919426793319799707, 1.666276233232717896, 0.4451252810446822417 ) ) ;
#48072=CARTESIAN_POINT ( 'NONE',  ( -1.083598637574820112, 0.000000000000000000, 2.747180975113330259 ) ) ;
#48076=DIRECTION ( 'NONE',  ( 0.5128992774058948045, 0.000000000000000000, 0.8584487936018727616 ) ) ;
#48081=EDGE_CURVE ( 'NONE', #41856, #38999, #2360, .T. ) ;
#48082=CARTESIAN_POINT ( 'NONE',  ( -0.2156685157583831947, 1.617455082123532062, -2.945280361644576850 ) ) ;
#48086=CARTESIAN_POINT ( 'NONE',  ( -1.759095177137641075, 1.049866565067838264, 1.002495067533146988 ) ) ;
#48088=DIRECTION ( 'NONE',  ( 0.8805955318567391110, 0.000000000000000000, -0.4738686624729965269 ) ) ;
#48089=CIRCLE ( 'NONE', #3606, 2.246510896728926010 ) ;
#48093=CARTESIAN_POINT ( 'NONE',  ( -0.8783128861146038968, 0.01385187720497466773, 1.565997986929510644 ) ) ;
#48096=CARTESIAN_POINT ( 'NONE',  ( -1.695772546416002280, 0.000000000000000000, -2.417756147381373566 ) ) ;
#48097=VECTOR ( 'NONE', #30216, 39.37007874015748143 ) ;
#48102=DIRECTION ( 'NONE',  ( -1.156061316345074457E-16, -1.000000000000000000, 1.040474016969491568E-17 ) ) ;
#48108=EDGE_CURVE ( 'NONE', #41853, #22384, #16534, .T. ) ;
#48109=CARTESIAN_POINT ( 'NONE',  ( -0.7697430959579070198, 1.531135861556976119, -2.850707213328497858 ) ) ;
#48110=CARTESIAN_POINT ( 'NONE',  ( 0.000000000000000000, 5.118110236220475784, 0.000000000000000000 ) ) ;
#48113=DIRECTION ( 'NONE',  ( -0.01601477604151182663, 0.9998717552508123996, -0.000000000000000000 ) ) ;
#48116=DIRECTION ( 'NONE',  ( 0.000000000000000000, 0.000000000000000000, -1.000000000000000000 ) ) ;
#48119=EDGE_CURVE ( 'NONE', #46309, #40889, #41774, .T. ) ;
#48126=AXIS2_PLACEMENT_3D ( 'NONE', #41725, #10228, #14355 ) ;
#48127=CARTESIAN_POINT ( 'NONE',  ( -2.151809081513409438, 1.673437530708463017, 0.2418202932658340965 ) ) ;
#48128=CARTESIAN_POINT ( 'NONE',  ( 0.000000000000000000, 1.574803149606302854, 0.000000000000000000 ) ) ;
#48129=CARTESIAN_POINT ( 'NONE',  ( -0.8221900955658373311, 6.692913385826772199, 2.050660405798877317 ) ) ;
#48130=CONICAL_SURFACE ( 'NONE', #39097, 2.246510896728926010, 0.01601546068027819014 ) ;
#48132=VECTOR ( 'NONE', #13201, 39.37007874015748143 ) ;
#48135=CARTESIAN_POINT ( 'NONE',  ( 0.04921259842519667277, 1.675881784547888831, 2.245244178460735540 ) ) ;
#48138=CARTESIAN_POINT ( 'NONE',  ( 0.5756566573088583993, 1.502670515430445386, 2.896516654582643291 ) ) ;
#48143=CARTESIAN_POINT ( 'NONE',  ( -0.1071992566810134884, 0.000000000000000000, -1.740088185897663342 ) ) ;
#48145=EDGE_LOOP ( 'NONE', ( #50965, #46402, #47760, #18111 ) ) ;
#48146=CARTESIAN_POINT ( 'NONE',  ( 2.919426793319799707, 1.448220119383965443, 0.4451252810446820196 ) ) ;
#48147=CARTESIAN_POINT ( 'NONE',  ( 1.214590356376888280, 1.727355838235203667, 1.936932008856820930 ) ) ;
#48153=ORIENTED_EDGE ( 'NONE', *, *, #31083, .T. ) ;
#48156=CARTESIAN_POINT ( 'NONE',  ( -1.325491792074585451, 1.543512378121542961, -2.638988599164751925 ) ) ;
#48160=VERTEX_POINT ( 'NONE', #10992 ) ;
#48162=VERTEX_POINT ( 'NONE', #26731 ) ;
#48169=ORIENTED_EDGE ( 'NONE', *, *, #28603, .T. ) ;
#48170=CARTESIAN_POINT ( 'NONE',  ( 2.252332422952718183, 1.743977176619643910, -0.5645583697864726691 ) ) ;
#48171=CARTESIAN_POINT ( 'NONE',  ( 1.515849743713622910, 0.000000000000000000, -1.426682437664332559 ) ) ;
#48174=DIRECTION ( 'NONE',  ( -0.9839295885986321100, 0.000000000000000000, 0.1785568947986229116 ) ) ;
#48177=ADVANCED_FACE ( 'NONE', ( #38617 ), #3243, .T. ) ;
#48180=ORIENTED_EDGE ( 'NONE', *, *, #28828, .T. ) ;
#48186=CARTESIAN_POINT ( 'NONE',  ( -0.04921259842519707522, 1.574803149606302854, 2.164795024401847456 ) ) ;
#48187=DIRECTION ( 'NONE',  ( 0.000000000000000000, 1.160734090543304660E-16, -1.000000000000000000 ) ) ;
#48191=DIRECTION ( 'NONE',  ( -0.000000000000000000, -1.000000000000000000, -0.000000000000000000 ) ) ;
#48195=CIRCLE ( 'NONE', #31025, 2.244934639244525076 ) ;
#48197=EDGE_CURVE ( 'NONE', #14116, #23634, #47853, .T. ) ;
#48200=CARTESIAN_POINT ( 'NONE',  ( 1.081562861160096700, 0.04524287409729283588, -1.572369041216798768 ) ) ;
#48202=CARTESIAN_POINT ( 'NONE',  ( 0.07982360342473591996, 1.709180471932028711, 0.000000000000000000 ) ) ;
#48204=CARTESIAN_POINT ( 'NONE',  ( -0.8949303405208608453, 1.574803149606302854, -1.971765468592543202 ) ) ;
#48205=CARTESIAN_POINT ( 'NONE',  ( -1.325491792074585451, 1.698604322780517650, -2.638988599164751481 ) ) ;
#48213=FACE_OUTER_BOUND ( 'NONE', #47015, .T. ) ;
#48220=EDGE_LOOP ( 'NONE', ( #44817, #42155, #23335, #44858 ) ) ;
#48222=VERTEX_POINT ( 'NONE', #16906 ) ;
#48223=CARTESIAN_POINT ( 'NONE',  ( -1.472219874544909546, 1.205361022782829114E-17, 2.560030851058948898 ) ) ;
#48228=ORIENTED_EDGE ( 'NONE', *, *, #9469, .T. ) ;
#48230=CARTESIAN_POINT ( 'NONE',  ( 1.229551338984395059, 1.049866565877817237, -1.608606760006217717 ) ) ;
#48231=CARTESIAN_POINT ( 'NONE',  ( 0.2156685157584258827, 1.205361022782829114E-17, -2.945280361644574185 ) ) ;
#48239=EDGE_CURVE ( 'NONE', #7511, #48407, #16652, .T. ) ;
#48240=AXIS2_PLACEMENT_3D ( 'NONE', #45007, #5785, #29536 ) ;
#48243=ORIENTED_EDGE ( 'NONE', *, *, #14836, .T. ) ;
#48244=EDGE_CURVE ( 'NONE', #42191, #38194, #23203, .T. ) ;
#48245=EDGE_LOOP ( 'NONE', ( #20409, #6791, #19199, #28729 ) ) ;
#48246=CARTESIAN_POINT ( 'NONE',  ( -2.074656761898998170, 0.000000000000000000, -0.6223516566630912239 ) ) ;
#48248=CARTESIAN_POINT ( 'NONE',  ( 0.08139965876239094178, 1.610780518492231694, 0.000000000000000000 ) ) ;
#48255=FACE_OUTER_BOUND ( 'NONE', #32069, .T. ) ;
#48263=CARTESIAN_POINT ( 'NONE',  ( 1.549117706237081782, 1.699905508662957754, 1.698309735495537431 ) ) ;
#48267=B_SPLINE_CURVE_WITH_KNOTS ( 'NONE', 3,
 ( #25959, #17707, #14335, #21070 ),
 .UNSPECIFIED., .F., .F.,
 ( 4, 4 ),
 ( 2.174642743374414444E-07, 0.002500329454545664916 ),
 .UNSPECIFIED. ) ;
#48274=ORIENTED_EDGE ( 'NONE', *, *, #28169, .T. ) ;
#48278=ORIENTED_EDGE ( 'NONE', *, *, #18286, .T. ) ;
#48279=VERTEX_POINT ( 'NONE', #39625 ) ;
#48283=ORIENTED_EDGE ( 'NONE', *, *, #15436, .F. ) ;
#48285=CARTESIAN_POINT ( 'NONE',  ( -1.905671854841497481, 1.689559879305088996, 2.256015092822653223 ) ) ;
#48290=DIRECTION ( 'NONE',  ( 0.01601477604151182663, -0.9998717552508123996, 0.000000000000000000 ) ) ;
#48291=ORIENTED_EDGE ( 'NONE', *, *, #16036, .F. ) ;
#48297=DIRECTION ( 'NONE',  ( -0.01601477604151182663, 0.9998717552508123996, -0.000000000000000000 ) ) ;
#48307=DIRECTION ( 'NONE',  ( -0.9998717552508122886, -0.01601477604151180928, 0.000000000000000000 ) ) ;
#48313=EDGE_CURVE ( 'NONE', #9387, #45742, #47583, .T. ) ;
#48315=ORIENTED_EDGE ( 'NONE', *, *, #23612, .T. ) ;
#48316=ORIENTED_EDGE ( 'NONE', *, *, #10813, .T. ) ;
#48318=DIRECTION ( 'NONE',  ( -0.000000000000000000, 1.000000000000000000, -0.000000000000000000 ) ) ;
#48320=CARTESIAN_POINT ( 'NONE',  ( 2.919426793319799707, 0.000000000000000000, 0.4451252810446820196 ) ) ;
#48322=EDGE_CURVE ( 'NONE', #29978, #2834, #19738, .T. ) ;
#48324=DIRECTION ( 'NONE',  ( 0.000000000000000000, 0.000000000000000000, 1.000000000000000000 ) ) ;
#48325=PLANE ( 'NONE',  #8070 ) ;
#48327=CARTESIAN_POINT ( 'NONE',  ( 0.8227799331039051811, 6.692913385826772199, 2.052232022298800640 ) ) ;
#48333=CARTESIAN_POINT ( 'NONE',  ( 2.503359584574370800, 1.751360814071121430, 0.3887651481859802360 ) ) ;
#48337=CARTESIAN_POINT ( 'NONE',  ( 2.473322567160110452, 1.458187968338687357, -1.612982232707932173 ) ) ;
#48339=VERTEX_POINT ( 'NONE', #31627 ) ;
#48341=FACE_OUTER_BOUND ( 'NONE', #4232, .T. ) ;
#48342=VERTEX_POINT ( 'NONE', #1915 ) ;
#48344=EDGE_CURVE ( 'NONE', #8620, #10759, #13426, .T. ) ;
#48348=CARTESIAN_POINT ( 'NONE',  ( 0.04921259842519690175, 0.02870789531899127500, 1.849213118431110914 ) ) ;
#48349=ORIENTED_EDGE ( 'NONE', *, *, #49947, .F. ) ;
#48350=ORIENTED_EDGE ( 'NONE', *, *, #24971, .T. ) ;
#48358=EDGE_LOOP ( 'NONE', ( #42415, #47860, #2560, #43916 ) ) ;
#48361=LINE ( 'NONE', #16406, #22512 ) ;
#48364=FACE_OUTER_BOUND ( 'NONE', #8807, .T. ) ;
#48368=ORIENTED_EDGE ( 'NONE', *, *, #35057, .T. ) ;
#48369=VERTEX_POINT ( 'NONE', #17409 ) ;
#48371=B_SPLINE_CURVE_WITH_KNOTS ( 'NONE', 3,
 ( #44594, #40494, #12876, #39269 ),
 .UNSPECIFIED., .F., .F.,
 ( 4, 4 ),
 ( 0.01480784793388801278, 0.03075119829274991501 ),
 .UNSPECIFIED. ) ;
#48373=ADVANCED_FACE ( 'NONE', ( #14044 ), #11666, .T. ) ;
#48376=CARTESIAN_POINT ( 'NONE',  ( 0.2627480064045706332, 0.000000000000000000, 1.723473835155035605 ) ) ;
#48377=ADVANCED_FACE ( 'NONE', ( #5276 ), #33430, .F. ) ;
#48381=CARTESIAN_POINT ( 'NONE',  ( 0.000000000000000000, 0.07874015748031502893, 0.000000000000000000 ) ) ;
#48382=CARTESIAN_POINT ( 'NONE',  ( 1.472219874544873131, 0.000000000000000000, 2.560030851058970214 ) ) ;
#48383=DIRECTION ( 'NONE',  ( -0.9362348706397368714, 0.000000000000000000, -0.3513748240813434620 ) ) ;
#48387=CARTESIAN_POINT ( 'NONE',  ( 0.07982360342473591996, 1.709180471932028711, 0.000000000000000000 ) ) ;
#48390=DIRECTION ( 'NONE',  ( 0.000000000000000000, 0.000000000000000000, -1.000000000000000000 ) ) ;
#48391=CARTESIAN_POINT ( 'NONE',  ( 0.000000000000000000, 6.692913385826772199, 0.000000000000000000 ) ) ;
#48397=ORIENTED_EDGE ( 'NONE', *, *, #1822, .F. ) ;
#48398=DIRECTION ( 'NONE',  ( -0.01601477604151182663, 0.9998717552508123996, -0.000000000000000000 ) ) ;
#48403=CARTESIAN_POINT ( 'NONE',  ( -1.158605206299305079, 1.033703605627220856, -2.292445033001472510 ) ) ;
#48407=VERTEX_POINT ( 'NONE', #5535 ) ;
#48411=B_SPLINE_CURVE_WITH_KNOTS ( 'NONE', 3,
 ( #7158, #38396, #34272, #26507 ),
 .UNSPECIFIED., .F., .F.,
 ( 4, 4 ),
 ( 0.001167289351993227057, 0.003667579486304786175 ),
 .UNSPECIFIED. ) ;
#48412=EDGE_CURVE ( 'NONE', #50925, #24535, #21568, .T. ) ;
#48417=ORIENTED_EDGE ( 'NONE', *, *, #38582, .T. ) ;
#48428=ORIENTED_EDGE ( 'NONE', *, *, #24436, .F. ) ;
#48433=VERTEX_POINT ( 'NONE', #32664 ) ;
#48441=CARTESIAN_POINT ( 'NONE',  ( -1.891439052599157122, 1.677607092856729709, 1.073712343777111222 ) ) ;
#48442=CARTESIAN_POINT ( 'NONE',  ( 2.932638728931774352, 1.764957438482779528, 0.3475908556738225297 ) ) ;
#48445=AXIS2_PLACEMENT_3D ( 'NONE', #21558, #46040, #1938 ) ;
#48450=ORIENTED_EDGE ( 'NONE', *, *, #22247, .T. ) ;
#48454=AXIS2_PLACEMENT_3D ( 'NONE', #16424, #9183, #19766 ) ;
#48456=CARTESIAN_POINT ( 'NONE',  ( 1.500371432800224003, 1.481001073728986484, 2.543211078004788295 ) ) ;
#48459=CARTESIAN_POINT ( 'NONE',  ( -2.339241080213612101, 1.584370211609867685, 1.802537235681884065 ) ) ;
#48465=CARTESIAN_POINT ( 'NONE',  ( 3.937007874015748143, 4.960629921259846142, 1.023622047244094446 ) ) ;
#48468=DIRECTION ( 'NONE',  ( 0.7530714660036099684, 1.288287287306305530E-16, 0.6579387259397138088 ) ) ;
#48474=CARTESIAN_POINT ( 'NONE',  ( 2.491402175429654253, 1.659612532563349285, -1.585592796919505831 ) ) ;
#48485=ORIENTED_EDGE ( 'NONE', *, *, #7026, .F. ) ;
#48489=CARTESIAN_POINT ( 'NONE',  ( -0.6233543567505159810, 5.905511811023623991, -2.073689640095379705 ) ) ;
#48491=EDGE_CURVE ( 'NONE', #4498, #42300, #24095, .T. ) ;
#48492=ADVANCED_FACE ( 'NONE', ( #26917 ), #27168, .T. ) ;
#48495=EDGE_CURVE ( 'NONE', #2174, #21262, #10928, .T. ) ;
#48496=DIRECTION ( 'NONE',  ( 0.2225209339563184452, -1.160734090543304660E-16, -0.9749279121818227312 ) ) ;
#48497=ORIENTED_EDGE ( 'NONE', *, *, #29240, .T. ) ;
#48507=CARTESIAN_POINT ( 'NONE',  ( -1.105178190331685961, 1.205361022782829114E-17, -1.437421806808603542 ) ) ;
#48510=CARTESIAN_POINT ( 'NONE',  ( 0.3136974817028392315, 0.000000000000000000, -2.936457595020219635 ) ) ;
#48514=CARTESIAN_POINT ( 'NONE',  ( 2.623503965249849301, 1.205361022782829114E-17, 1.355882097269873965 ) ) ;
#48516=DIRECTION ( 'NONE',  ( 0.01601477604151182663, -0.9998717552508123996, 0.000000000000000000 ) ) ;
#48519=VERTEX_POINT ( 'NONE', #39049 ) ;
#48521=CONICAL_SURFACE ( 'NONE', #18095, 2.165354330708661568, 0.2617993877991570129 ) ;
#48524=EDGE_CURVE ( 'NONE', #50172, #28376, #30553, .T. ) ;
#48527=ADVANCED_FACE ( 'NONE', ( #15307 ), #46020, .T. ) ;
#48528=ORIENTED_EDGE ( 'NONE', *, *, #26974, .F. ) ;
#48530=ORIENTED_EDGE ( 'NONE', *, *, #13039, .F. ) ;
#48534=B_SPLINE_CURVE_WITH_KNOTS ( 'NONE', 3,
 ( #11256, #42982, #30880, #50434 ),
 .UNSPECIFIED., .F., .F.,
 ( 4, 4 ),
 ( 2.001965537720647568E-07, 0.002500201682199559936 ),
 .UNSPECIFIED. ) ;
#48535=CARTESIAN_POINT ( 'NONE',  ( 0.1198125009631641619, 0.5249316475426862860, -1.880232807967558761 ) ) ;
#48539=ORIENTED_EDGE ( 'NONE', *, *, #21799, .T. ) ;
#48542=ORIENTED_EDGE ( 'NONE', *, *, #19113, .T. ) ;
#48544=CARTESIAN_POINT ( 'NONE',  ( -2.076656781855024114, 1.674640491952791077, 0.6230015025396302697 ) ) ;
#48555=LINE ( 'NONE', #13238, #15827 ) ;
#48564=EDGE_CURVE ( 'NONE', #4986, #44778, #41385, .T. ) ;
#48565=VECTOR ( 'NONE', #7275, 39.37007874015748143 ) ;
#48568=DIRECTION ( 'NONE',  ( 0.9989930665413151445, 0.000000000000000000, -0.04486483035050446017 ) ) ;
#48569=ORIENTED_EDGE ( 'NONE', *, *, #4108, .T. ) ;
#48570=ORIENTED_EDGE ( 'NONE', *, *, #11859, .F. ) ;
#48571=DIRECTION ( 'NONE',  ( -0.9998717552508122886, -0.01601477604151185785, 0.000000000000000000 ) ) ;
#48573=VERTEX_POINT ( 'NONE', #26172 ) ;
#48574=LINE ( 'NONE', #48320, #211 ) ;
#48577=CARTESIAN_POINT ( 'NONE',  ( -0.5662636741187642153, 0.000000000000000000, 1.648861433446455971 ) ) ;
#48578=DIRECTION ( 'NONE',  ( 3.586865599282426309E-17, -1.000000000000000000, -1.103923720497134591E-16 ) ) ;
#48579=EDGE_LOOP ( 'NONE', ( #17213, #16870, #31448, #31279 ) ) ;
#48583=LINE ( 'NONE', #13267, #37275 ) ;
#48592=DIRECTION ( 'NONE',  ( 0.9959742939952397345, 1.036504026185339538E-17, -0.08963930890342654279 ) ) ;
#48593=CARTESIAN_POINT ( 'NONE',  ( -1.635196357419856472, 0.5249316475426862860, 0.9358222695712326011 ) ) ;
#48598=CARTESIAN_POINT ( 'NONE',  ( -2.277873973731453283, 1.205361022782829114E-17, 1.879489153247635214 ) ) ;
#48599=CARTESIAN_POINT ( 'NONE',  ( 2.437180031585944207, 1.658768335924418080, -1.667735833703099191 ) ) ;
#48601=EDGE_CURVE ( 'NONE', #41415, #40985, #30804, .T. ) ;
#48607=ORIENTED_EDGE ( 'NONE', *, *, #47807, .T. ) ;
#48608=DIRECTION ( 'NONE',  ( -5.207613805427244364E-18, -1.000000000000000000, -1.159565308550900415E-16 ) ) ;
#48613=ORIENTED_EDGE ( 'NONE', *, *, #13986, .F. ) ;
#48614=EDGE_LOOP ( 'NONE', ( #29543, #41111, #27339, #12112 ) ) ;
#48618=CYLINDRICAL_SURFACE ( 'NONE', #47769, 2.165354330708661568 ) ;
#48622=B_SPLINE_CURVE_WITH_KNOTS ( 'NONE', 3,
 ( #16666, #8652, #3064, #8401 ),
 .UNSPECIFIED., .F., .F.,
 ( 4, 4 ),
 ( 2.074994414937302994E-07, 0.002500489374955372577 ),
 .UNSPECIFIED. ) ;
#48626=VERTEX_POINT ( 'NONE', #312 ) ;
#48628=DIRECTION ( 'NONE',  ( 0.3930250316539147803, -1.160734090543304660E-16, 0.9195277725514544587 ) ) ;
#48631=VERTEX_POINT ( 'NONE', #20182 ) ;
#48632=ADVANCED_FACE ( 'NONE', ( #4444 ), #30699, .T. ) ;
#48633=CARTESIAN_POINT ( 'NONE',  ( 0.8454231601665999074, 1.623017753118757067, 2.112564685048140323 ) ) ;
#48634=CARTESIAN_POINT ( 'NONE',  ( -1.621795816027382875, 0.000000000000000000, -0.6396693727619442438 ) ) ;
#48643=ORIENTED_EDGE ( 'NONE', *, *, #28864, .T. ) ;
#48644=CARTESIAN_POINT ( 'NONE',  ( 0.8454231601665999074, 1.623017753118757067, 2.112564685048140323 ) ) ;
#48649=CARTESIAN_POINT ( 'NONE',  ( 2.111804831410495353, 1.708917971481227260, -0.9561481288353351760 ) ) ;
#48653=ORIENTED_EDGE ( 'NONE', *, *, #12507, .T. ) ;
#48655=ADVANCED_FACE ( 'NONE', ( #50861 ), #39812, .T. ) ;
#48661=EDGE_LOOP ( 'NONE', ( #36681, #21053, #33790, #42893 ) ) ;
#48662=ORIENTED_EDGE ( 'NONE', *, *, #13614, .F. ) ;
#48664=B_SPLINE_CURVE_WITH_KNOTS ( 'NONE', 3,
 ( #31149, #43256, #35277, #38891 ),
 .UNSPECIFIED., .F., .F.,
 ( 4, 4 ),
 ( 2.034093849253954962E-05, 0.002520358861215416576 ),
 .UNSPECIFIED. ) ;
#48668=AXIS2_PLACEMENT_3D ( 'NONE', #42322, #3596, #3093 ) ;
#48674=PLANE ( 'NONE',  #21515 ) ;
#48675=ORIENTED_EDGE ( 'NONE', *, *, #6815, .F. ) ;
#48676=EDGE_CURVE ( 'NONE', #47661, #38330, #12194, .T. ) ;
#48677=PLANE ( 'NONE',  #5935 ) ;
#48678=ORIENTED_EDGE ( 'NONE', *, *, #4123, .F. ) ;
#48684=CARTESIAN_POINT ( 'NONE',  ( 0.08119777152254364916, 1.623385212329073957, 0.000000000000000000 ) ) ;
#48685=B_SPLINE_CURVE_WITH_KNOTS ( 'NONE', 3,
 ( #26781, #34297, #37917, #6915 ),
 .UNSPECIFIED., .F., .F.,
 ( 4, 4 ),
 ( 0.001575154832295005101, 0.004075306633636652590 ),
 .UNSPECIFIED. ) ;
#48687=DIRECTION ( 'NONE',  ( 0.000000000000000000, -1.000000000000000000, 0.000000000000000000 ) ) ;
#48693=CARTESIAN_POINT ( 'NONE',  ( 0.8227799331039050701, 5.905511811023623991, 2.052232022298799752 ) ) ;
#48694=CARTESIAN_POINT ( 'NONE',  ( -2.164823134740035737, 1.574811347331577016, -0.04796011690018289753 ) ) ;
#48696=DIRECTION ( 'NONE',  ( -0.1785568947986370392, -1.142009442734629415E-16, 0.9839295885986295565 ) ) ;
#48698=ADVANCED_FACE ( 'NONE', ( #29150 ), #32794, .T. ) ;
#48701=EDGE_CURVE ( 'NONE', #28908, #6809, #39289, .T. ) ;
#48703=AXIS2_PLACEMENT_3D ( 'NONE', #50215, #18778, #19272 ) ;
#48706=VERTEX_POINT ( 'NONE', #17291 ) ;
#48709=ORIENTED_EDGE ( 'NONE', *, *, #17643, .F. ) ;
#48711=CIRCLE ( 'NONE', #42949, 2.246510896728926010 ) ;
#48717=DIRECTION ( 'NONE',  ( 1.160706738777443955E-16, 1.000000000000000000, -5.589669052740684758E-17 ) ) ;
#48720=ORIENTED_EDGE ( 'NONE', *, *, #32471, .T. ) ;
#48722=CARTESIAN_POINT ( 'NONE',  ( 1.139289024838126441, 1.634917426876648427, -2.479181505015526366 ) ) ;
#48725=CARTESIAN_POINT ( 'NONE',  ( -1.597750071202345135, 0.000000000000000000, -0.7364305798568749895 ) ) ;
#48727=CARTESIAN_POINT ( 'NONE',  ( 0.000000000000000000, 1.574803149606302854, 0.000000000000000000 ) ) ;
#48729=CARTESIAN_POINT ( 'NONE',  ( -1.675546303352015709, 1.681065010344670041, 1.399148864732502995 ) ) ;
#48730=CARTESIAN_POINT ( 'NONE',  ( -1.232995795418201812, 0.000000000000000000, 1.780798594093550680 ) ) ;
#48732=ORIENTED_EDGE ( 'NONE', *, *, #40000, .T. ) ;
#48733=CARTESIAN_POINT ( 'NONE',  ( -1.387241876633673598, 1.574803149606302854, 1.662624236931676824 ) ) ;
#48734=DIRECTION ( 'NONE',  ( 0.000000000000000000, -1.156482317317871478E-16, -1.000000000000000000 ) ) ;
#48737=B_SPLINE_CURVE_WITH_KNOTS ( 'NONE', 3,
 ( #36100, #44587, #12092, #20857 ),
 .UNSPECIFIED., .F., .F.,
 ( 4, 4 ),
 ( 0.01284703861903681646, 0.03074048250902328486 ),
 .UNSPECIFIED. ) ;
#48740=CARTESIAN_POINT ( 'NONE',  ( -1.662320194739477452, 1.205361022782829114E-17, -1.388601395075575784 ) ) ;
#48741=CARTESIAN_POINT ( 'NONE',  ( -1.695772546416001392, 1.551146592414875958, -2.417756147381374010 ) ) ;
#48743=ORIENTED_EDGE ( 'NONE', *, *, #31133, .F. ) ;
#48745=AXIS2_PLACEMENT_3D ( 'NONE', #12511, #23879, #8387 ) ;
#48749=CIRCLE ( 'NONE', #1807, 2.165354330708661568 ) ;
#48751=ORIENTED_EDGE ( 'NONE', *, *, #22784, .T. ) ;
#48753=CONICAL_SURFACE ( 'NONE', #26530, 2.165354330708661568, 0.2617993877991570129 ) ;
#48756=EDGE_CURVE ( 'NONE', #37287, #19191, #33991, .T. ) ;
#48758=DIRECTION ( 'NONE',  ( -0.01601477604151182663, 0.9998717552508123996, -0.000000000000000000 ) ) ;
#48759=VERTEX_POINT ( 'NONE', #46150 ) ;
#48762=DIRECTION ( 'NONE',  ( -0.000000000000000000, -1.000000000000000000, -0.000000000000000000 ) ) ;
#48763=B_SPLINE_CURVE_WITH_KNOTS ( 'NONE', 3,
 ( #34888, #49572, #18642, #38519 ),
 .UNSPECIFIED., .F., .F.,
 ( 4, 4 ),
 ( 2.655981481195813069E-07, 0.002500437463240591605 ),
 .UNSPECIFIED. ) ;
#48767=CARTESIAN_POINT ( 'NONE',  ( -0.8241443283111672402, 1.596276574288824301, 2.055867440327626916 ) ) ;
#48768=LINE ( 'NONE', #29448, #21004 ) ;
#48774=ORIENTED_EDGE ( 'NONE', *, *, #13908, .F. ) ;
#48777=AXIS2_PLACEMENT_3D ( 'NONE', #39067, #31074, #39321 ) ;
#48789=ORIENTED_EDGE ( 'NONE', *, *, #36691, .T. ) ;
#48794=ORIENTED_EDGE ( 'NONE', *, *, #24220, .T. ) ;
#48797=PLANE ( 'NONE',  #49080 ) ;
#48800=DIRECTION ( 'NONE',  ( 0.9998717552508121775, 0.01601477604151182663, 0.000000000000000000 ) ) ;
#48801=LINE ( 'NONE', #44958, #25338 ) ;
#48810=CIRCLE ( 'NONE', #26588, 2.246510896728926010 ) ;
#48817=EDGE_CURVE ( 'NONE', #19132, #39563, #10048, .T. ) ;
#48820=CIRCLE ( 'NONE', #21674, 1.850107469027523432 ) ;
#48824=VECTOR ( 'NONE', #29243, 39.37007874015748143 ) ;
#48826=DIRECTION ( 'NONE',  ( 0.01601477604151182663, -0.9998717552508123996, 0.000000000000000000 ) ) ;
#48827=CARTESIAN_POINT ( 'NONE',  ( 1.775400203342704986, 1.746929418358725172, -2.359903268218703332 ) ) ;
#48828=LINE ( 'NONE', #1377, #12202 ) ;
#48829=VERTEX_POINT ( 'NONE', #30174 ) ;
#48832=CARTESIAN_POINT ( 'NONE',  ( 0.3136974817028393425, 1.724153038295522800, -2.936457595020219635 ) ) ;
#48839=CARTESIAN_POINT ( 'NONE',  ( 0.000000000000000000, 6.692913385826772199, 0.000000000000000000 ) ) ;
#48842=EDGE_CURVE ( 'NONE', #50859, #19026, #10301, .T. ) ;
#48843=EDGE_LOOP ( 'NONE', ( #4079, #33456, #19922, #36894 ) ) ;
#48844=CARTESIAN_POINT ( 'NONE',  ( -2.150793259809249847, 1.575027863729615341, -0.2506944975021367372 ) ) ;
#48845=CARTESIAN_POINT ( 'NONE',  ( 0.04921259842519682542, 0.5249316475426857309, 1.883403453246504933 ) ) ;
#48848=DIRECTION ( 'NONE',  ( -0.000000000000000000, -1.000000000000000000, -0.000000000000000000 ) ) ;
#48850=CYLINDRICAL_SURFACE ( 'NONE', #48240, 2.165354330708661568 ) ;
#48853=ORIENTED_EDGE ( 'NONE', *, *, #40295, .F. ) ;
#48863=VERTEX_POINT ( 'NONE', #30435 ) ;
#48865=CARTESIAN_POINT ( 'NONE',  ( -1.743145509346916588, 0.000000000000000000, 0.000000000000000000 ) ) ;
#48866=CARTESIAN_POINT ( 'NONE',  ( -2.932023289724621673, 1.575122962489508449, 0.3475074887687388259 ) ) ;
#48867=CARTESIAN_POINT ( 'NONE',  ( -2.491402175429631605, 1.581999109372839385, -1.585592796919542025 ) ) ;
#48869=DIRECTION ( 'NONE',  ( 0.000000000000000000, 1.000000000000000000, 0.000000000000000000 ) ) ;
#48871=VECTOR ( 'NONE', #48892, 39.37007874015748143 ) ;
#48872=ORIENTED_EDGE ( 'NONE', *, *, #22057, .F. ) ;
#48873=FACE_OUTER_BOUND ( 'NONE', #23154, .T. ) ;
#48874=ORIENTED_EDGE ( 'NONE', *, *, #30685, .F. ) ;
#48876=CARTESIAN_POINT ( 'NONE',  ( -1.306307708855430905, 0.000000000000000000, -1.226175564698866349 ) ) ;
#48879=CARTESIAN_POINT ( 'NONE',  ( 0.7115265288965786361, 1.624529684782195282, -2.393174330701326902 ) ) ;
#48882=EDGE_CURVE ( 'NONE', #17742, #29343, #25535, .T. ) ;
#48885=EDGE_CURVE ( 'NONE', #1280, #43842, #16496, .T. ) ;
#48889=CARTESIAN_POINT ( 'NONE',  ( -1.679154924913551783, 0.000000000000000000, 0.4938453199301923724 ) ) ;
#48890=DIRECTION ( 'NONE',  ( 0.9998717552508121775, 0.01601477604151182663, 0.000000000000000000 ) ) ;
#48892=DIRECTION ( 'NONE',  ( 0.000000000000000000, 1.000000000000000000, -0.000000000000000000 ) ) ;
#48894=DIRECTION ( 'NONE',  ( -3.986037398843765983E-20, -1.000000000000000000, -1.160734090543304660E-16 ) ) ;
#48895=CIRCLE ( 'NONE', #30810, 2.165354330708661568 ) ;
#48897=ORIENTED_EDGE ( 'NONE', *, *, #40176, .F. ) ;
#48900=DIRECTION ( 'NONE',  ( -8.021399753802198224E-17, -1.000000000000000000, 8.389726389140549123E-17 ) ) ;
#48904=DIRECTION ( 'NONE',  ( -0.01601477604151182663, 0.9998717552508123996, -0.000000000000000000 ) ) ;
#48907=ORIENTED_EDGE ( 'NONE', *, *, #34767, .F. ) ;
#48912=DIRECTION ( 'NONE',  ( -0.9998717552508121775, -0.01601477604151182316, 0.000000000000000000 ) ) ;
#48922=CARTESIAN_POINT ( 'NONE',  ( -1.930190994932096782, 0.000000000000000000, -0.9827944786818723077 ) ) ;
#48926=ORIENTED_EDGE ( 'NONE', *, *, #39929, .F. ) ;
#48927=CARTESIAN_POINT ( 'NONE',  ( -0.04921259842519708216, 1.612473435230266317, 2.479391863569011090 ) ) ;
#48928=VECTOR ( 'NONE', #35868, 39.37007874015748854 ) ;
#48930=ORIENTED_EDGE ( 'NONE', *, *, #3839, .F. ) ;
#48936=EDGE_CURVE ( 'NONE', #22636, #18363, #27557, .T. ) ;
#48939=ORIENTED_EDGE ( 'NONE', *, *, #9702, .T. ) ;
#48945=EDGE_CURVE ( 'NONE', #32953, #41924, #36806, .T. ) ;
#48946=CARTESIAN_POINT ( 'NONE',  ( 0.1067246931122726866, 0.02962905676920215767, 0.000000000000000000 ) ) ;
#48949=DIRECTION ( 'NONE',  ( 0.9998717552508121775, 0.01601477604151182663, 0.000000000000000000 ) ) ;
#48954=LINE ( 'NONE', #21637, #40534 ) ;
#48956=ADVANCED_FACE ( 'NONE', ( #22682 ), #31497, .F. ) ;
#48960=B_SPLINE_CURVE_WITH_KNOTS ( 'NONE', 3,
 ( #2050, #45389, #10051, #25792 ),
 .UNSPECIFIED., .F., .F.,
 ( 4, 4 ),
 ( 0.0002761238990249075508, 0.003451782018764085365 ),
 .UNSPECIFIED. ) ;
#48961=B_SPLINE_CURVE_WITH_KNOTS ( 'NONE', 3,
 ( #31498, #20116, #19608, #35378 ),
 .UNSPECIFIED., .F., .F.,
 ( 4, 4 ),
 ( 6.288086478203287970E-07, 0.002380327432043047396 ),
 .UNSPECIFIED. ) ;
#48962=VERTEX_POINT ( 'NONE', #23690 ) ;
#48964=AXIS2_PLACEMENT_3D ( 'NONE', #47552, #7845, #347 ) ;
#48966=CONICAL_SURFACE ( 'NONE', #4489, 3.033577403570480779, 1.554780866114618743 ) ;
#48968=CARTESIAN_POINT ( 'NONE',  ( 0.1910111227923183275, 0.000000000000000000, -1.940223436340324570 ) ) ;
#48971=AXIS2_PLACEMENT_3D ( 'NONE', #25203, #8436, #39930 ) ;
#48973=B_SPLINE_CURVE_WITH_KNOTS ( 'NONE', 3,
 ( #30334, #11904, #15773, #46056 ),
 .UNSPECIFIED., .F., .F.,
 ( 4, 4 ),
 ( 0.1211775127643062860, 0.1625894504277921315 ),
 .UNSPECIFIED. ) ;
#48976=ORIENTED_EDGE ( 'NONE', *, *, #50626, .F. ) ;
#48983=CARTESIAN_POINT ( 'NONE',  ( -1.598711713507984022, 1.574803149606302854, -1.460438370699401522 ) ) ;
#48989=CARTESIAN_POINT ( 'NONE',  ( 1.083598637574781920, 1.736150426126270130, 2.747180975113346246 ) ) ;
#48999=DIRECTION ( 'NONE',  ( 0.7530714660036196273, 1.288287287306305530E-16, -0.6579387259397027066 ) ) ;
#49001=CARTESIAN_POINT ( 'NONE',  ( -2.153807523435207649, 5.905511811023623991, 0.2420910006175677753 ) ) ;
#49004=B_SPLINE_CURVE_WITH_KNOTS ( 'NONE', 3,
 ( #23587, #39336, #35468, #47294 ),
 .UNSPECIFIED., .F., .F.,
 ( 4, 4 ),
 ( 2.002016769723030562E-07, 0.002500200812166948009 ),
 .UNSPECIFIED. ) ;
#49005=AXIS2_PLACEMENT_3D ( 'NONE', #50668, #14866, #30609 ) ;
#49008=EDGE_CURVE ( 'NONE', #6577, #2835, #3310, .T. ) ;
#49009=CARTESIAN_POINT ( 'NONE',  ( -2.695799277629577162, 1.571269479597534824, -1.205759334241492731 ) ) ;
#49011=DIRECTION ( 'NONE',  ( -0.9998717552508121775, -0.01601477604151182663, 0.000000000000000000 ) ) ;
#49013=CARTESIAN_POINT ( 'NONE',  ( -1.709950266952966036, 0.000000000000000000, -0.3398067978735320183 ) ) ;
#49014=ORIENTED_EDGE ( 'NONE', *, *, #50626, .T. ) ;
#49016=AXIS2_PLACEMENT_3D ( 'NONE', #27373, #10882, #43115 ) ;
#49019=CARTESIAN_POINT ( 'NONE',  ( 2.152441353505198940, 6.692913385826772199, -0.2419059403264808283 ) ) ;
#49020=DIRECTION ( 'NONE',  ( 0.4338837391175656699, 1.045612331811453550E-16, -0.9009688679024154823 ) ) ;
#49024=DIRECTION ( 'NONE',  ( -0.9998717552508122886, -0.01601477604151185785, 0.000000000000000000 ) ) ;
#49025=FACE_OUTER_BOUND ( 'NONE', #14146, .T. ) ;
#49026=ORIENTED_EDGE ( 'NONE', *, *, #39906, .T. ) ;
#49028=LINE ( 'NONE', #29457, #28219 ) ;
#49037=EDGE_CURVE ( 'NONE', #19985, #1980, #20124, .T. ) ;
#49046=CARTESIAN_POINT ( 'NONE',  ( -1.405314191946755997, 1.685393272164901646, 1.683309666213049560 ) ) ;
#49047=ORIENTED_EDGE ( 'NONE', *, *, #26702, .T. ) ;
#49050=CARTESIAN_POINT ( 'NONE',  ( 2.110884035022549732, 1.741711621820001943, -0.9557545615714394538 ) ) ;
#49051=CARTESIAN_POINT ( 'NONE',  ( 1.901071203648723618, 1.705542687144442571, -1.313853494766966223 ) ) ;
#49055=DIRECTION ( 'NONE',  ( 0.000000000000000000, 0.000000000000000000, 1.000000000000000000 ) ) ;
#49057=CARTESIAN_POINT ( 'NONE',  ( 2.168245791271197209, 1.753049777144058297, -2.004968704497248844 ) ) ;
#49059=DIRECTION ( 'NONE',  ( 0.9195277725514489076, 0.000000000000000000, 0.3930250316539278810 ) ) ;
#49064=ADVANCED_FACE ( 'NONE', ( #36086 ), #38945, .T. ) ;
#49073=ADVANCED_FACE ( 'NONE', ( #35827 ), #9223, .F. ) ;
#49075=CARTESIAN_POINT ( 'NONE',  ( -1.812531910417308101, 1.588581096961242389, 1.999811551830815715 ) ) ;
#49079=VECTOR ( 'NONE', #38126, 39.37007874015748143 ) ;
#49080=AXIS2_PLACEMENT_3D ( 'NONE', #41356, #37493, #2111 ) ;
#49083=CARTESIAN_POINT ( 'NONE',  ( -0.8329809839909440017, 1.205361022782829114E-17, -2.833254665166566877 ) ) ;
#49084=DIRECTION ( 'NONE',  ( 0.01601477604151182663, -0.9998717552508123996, 0.000000000000000000 ) ) ;
#49087=CARTESIAN_POINT ( 'NONE',  ( 0.1067246931122726866, 0.02962905676920215767, 0.000000000000000000 ) ) ;
#49090=VERTEX_POINT ( 'NONE', #43557 ) ;
#49091=CARTESIAN_POINT ( 'NONE',  ( -1.627052366890036739, 1.591492494466993923, -2.155719988184307212 ) ) ;
#49102=CARTESIAN_POINT ( 'NONE',  ( -1.971247363764855320, 1.574803149606302854, -0.8960709840011922278 ) ) ;
#49103=EDGE_CURVE ( 'NONE', #19688, #3143, #37447, .T. ) ;
#49106=CARTESIAN_POINT ( 'NONE',  ( 1.833791099076603537, 1.574803149606302854, -1.151507526013694216 ) ) ;
#49109=CIRCLE ( 'NONE', #11231, 1.743387098533651480 ) ;
#49114=DIRECTION ( 'NONE',  ( -0.9998717552508121775, -0.01601477604151182663, 0.000000000000000000 ) ) ;
#49117=AXIS2_PLACEMENT_3D ( 'NONE', #33010, #34016, #33518 ) ;
#49119=CARTESIAN_POINT ( 'NONE',  ( 1.300279662861326013, 0.04874602395362847423, 1.413491677621213860 ) ) ;
#49123=ORIENTED_EDGE ( 'NONE', *, *, #20504, .T. ) ;
#49135=ORIENTED_EDGE ( 'NONE', *, *, #15936, .F. ) ;
#49142=LINE ( 'NONE', #21819, #22817 ) ;
#49149=CONICAL_SURFACE ( 'NONE', #26913, 2.165354330708661568, 0.2617993877991570129 ) ;
#49157=B_SPLINE_CURVE_WITH_KNOTS ( 'NONE', 3,
 ( #16349, #44467, #4981, #36997 ),
 .UNSPECIFIED., .F., .F.,
 ( 4, 4 ),
 ( 0.1211873102087489551, 0.1625992483279400380 ),
 .UNSPECIFIED. ) ;
#49158=DIRECTION ( 'NONE',  ( 0.9998717552508121775, 0.01601477604151182663, 0.000000000000000000 ) ) ;
#49160=DIRECTION ( 'NONE',  ( -0.000000000000000000, -1.000000000000000000, -0.000000000000000000 ) ) ;
#49161=DIRECTION ( 'NONE',  ( -3.986037398843765983E-20, -1.000000000000000000, -1.160734090543304660E-16 ) ) ;
#49162=ORIENTED_EDGE ( 'NONE', *, *, #17462, .T. ) ;
#49176=B_SPLINE_CURVE_WITH_KNOTS ( 'NONE', 3,
 ( #39589, #39332, #7344, #19198 ),
 .UNSPECIFIED., .F., .F.,
 ( 4, 4 ),
 ( 0.1211873102087489551, 0.1625992483279400103 ),
 .UNSPECIFIED. ) ;
#49177=ADVANCED_FACE ( 'NONE', ( #1986 ), #38150, .F. ) ;
#49178=ORIENTED_EDGE ( 'NONE', *, *, #23210, .T. ) ;
#49181=CARTESIAN_POINT ( 'NONE',  ( 0.9914495361338625523, 1.636256239573039117, 2.781765111341823360 ) ) ;
#49184=ORIENTED_EDGE ( 'NONE', *, *, #11264, .F. ) ;
#49185=CARTESIAN_POINT ( 'NONE',  ( 0.6507993007407579800, 1.619900495825837838, -2.173134161263437392 ) ) ;
#49189=CARTESIAN_POINT ( 'NONE',  ( 2.389170071857189992, 1.752995279934814965, 1.341552826535246545 ) ) ;
#49190=AXIS2_PLACEMENT_3D ( 'NONE', #3724, #50403, #7351 ) ;
#49193=EDGE_LOOP ( 'NONE', ( #15554, #25730, #11012, #49446 ) ) ;
#49198=ORIENTED_EDGE ( 'NONE', *, *, #48412, .F. ) ;
#49202=VECTOR ( 'NONE', #26009, 39.37007874015748854 ) ;
#49206=CARTESIAN_POINT ( 'NONE',  ( 2.011396482730577251, 0.9928247669144205645, 1.666980445438335234 ) ) ;
#49207=B_SPLINE_CURVE_WITH_KNOTS ( 'NONE', 3,
 ( #27991, #20244, #36009, #12504 ),
 .UNSPECIFIED., .F., .F.,
 ( 4, 4 ),
 ( 0.1211873102087489551, 0.1625992483279400380 ),
 .UNSPECIFIED. ) ;
#49214=CARTESIAN_POINT ( 'NONE',  ( -0.8329809839909436686, 1.706281419137876565, -2.833254665166566877 ) ) ;
#49215=CARTESIAN_POINT ( 'NONE',  ( 2.164658444855302122, 5.905511811023623991, -0.04795272066889885720 ) ) ;
#49216=CARTESIAN_POINT ( 'NONE',  ( 0.4788131938641113083, 0.000000000000000000, 2.914091152102192162 ) ) ;
#49217=CARTESIAN_POINT ( 'NONE',  ( -1.739713118882874276, 4.162957430336159157E-05, 0.1138408270437312325 ) ) ;
#49229=FACE_OUTER_BOUND ( 'NONE', #16015, .T. ) ;
#49231=ORIENTED_EDGE ( 'NONE', *, *, #41594, .T. ) ;
#49232=B_SPLINE_CURVE_WITH_KNOTS ( 'NONE', 3,
 ( #50691, #15886, #47343, #12021 ),
 .UNSPECIFIED., .F., .F.,
 ( 4, 4 ),
 ( 0.0002011623507270493549, 0.04991335192709614454 ),
 .UNSPECIFIED. ) ;
#49233=DIRECTION ( 'NONE',  ( -0.7530714660036099684, 7.639920857896035043E-17, -0.6579387259397138088 ) ) ;
#49235=EDGE_LOOP ( 'NONE', ( #28874, #37231, #33499, #41606 ) ) ;
#49237=CARTESIAN_POINT ( 'NONE',  ( -2.348444893129629563, 1.580171291669419276, 1.319637673352544338 ) ) ;
#49238=ORIENTED_EDGE ( 'NONE', *, *, #38399, .F. ) ;
#49241=EDGE_CURVE ( 'NONE', #45327, #35692, #2323, .T. ) ;
#49250=DIRECTION ( 'NONE',  ( 0.000000000000000000, 1.000000000000000000, -1.156482317317871478E-16 ) ) ;
#49256=EDGE_CURVE ( 'NONE', #22312, #9751, #1729, .T. ) ;
#49257=AXIS2_PLACEMENT_3D ( 'NONE', #18163, #14545, #38305 ) ;
#49258=CIRCLE ( 'NONE', #26231, 2.164630168518208109 ) ;
#49270=CONICAL_SURFACE ( 'NONE', #16444, 3.033577403570480779, 1.554780866114618743 ) ;
#49273=CIRCLE ( 'NONE', #44362, 2.246510896728926010 ) ;
#49279=EDGE_CURVE ( 'NONE', #36035, #27704, #18322, .T. ) ;
#49284=VERTEX_POINT ( 'NONE', #38876 ) ;
#49286=DIRECTION ( 'NONE',  ( 0.000000000000000000, 0.000000000000000000, -1.000000000000000000 ) ) ;
#49287=VERTEX_POINT ( 'NONE', #46836 ) ;
#49291=EDGE_CURVE ( 'NONE', #19894, #30240, #30881, .T. ) ;
#49295=EDGE_LOOP ( 'NONE', ( #1272, #28989, #3891, #44576 ) ) ;
#49298=AXIS2_PLACEMENT_3D ( 'NONE', #7798, #23537, #43150 ) ;
#49305=ORIENTED_EDGE ( 'NONE', *, *, #7985, .T. ) ;
#49306=DIRECTION ( 'NONE',  ( -0.000000000000000000, 1.000000000000000000, -0.000000000000000000 ) ) ;
#49307=ORIENTED_EDGE ( 'NONE', *, *, #40776, .T. ) ;
#49309=CARTESIAN_POINT ( 'NONE',  ( -0.8429824507881226170, 1.205361022782829114E-17, -1.637047627937372241 ) ) ;
#49310=DIRECTION ( 'NONE',  ( 0.000000000000000000, -1.000000000000000000, 0.000000000000000000 ) ) ;
#49312=CONICAL_SURFACE ( 'NONE', #36160, 3.033577403570480779, 1.554780866114618743 ) ;
#49316=EDGE_CURVE ( 'NONE', #14608, #39550, #31862, .T. ) ;
#49317=DIRECTION ( 'NONE',  ( -0.000000000000000000, 1.000000000000000000, -0.000000000000000000 ) ) ;
#49320=LINE ( 'NONE', #41364, #46323 ) ;
#49322=CARTESIAN_POINT ( 'NONE',  ( -0.4433489891367861091, 6.692913385826772199, 2.167441310503416485 ) ) ;
#49324=VERTEX_POINT ( 'NONE', #34752 ) ;
#49327=EDGE_CURVE ( 'NONE', #4522, #10796, #2690, .T. ) ;
#49329=CARTESIAN_POINT ( 'NONE',  ( 0.6233543567505469563, 6.692913385826772199, -2.073689640095370379 ) ) ;
#49330=ORIENTED_EDGE ( 'NONE', *, *, #13325, .F. ) ;
#49332=DIRECTION ( 'NONE',  ( -0.000000000000000000, -1.000000000000000000, -0.000000000000000000 ) ) ;
#49333=EDGE_LOOP ( 'NONE', ( #11443, #4217, #13297, #45553, #17553, #46644 ) ) ;
#49334=FACE_OUTER_BOUND ( 'NONE', #50424, .T. ) ;
#49339=AXIS2_PLACEMENT_3D ( 'NONE', #1567, #24295, #40812 ) ;
#49340=CARTESIAN_POINT ( 'NONE',  ( -1.087426130748108788, 0.01050254589070086231, -1.412988192946641020 ) ) ;
#49342=FACE_OUTER_BOUND ( 'NONE', #8347, .T. ) ;
#49347=VECTOR ( 'NONE', #3923, 39.37007874015748143 ) ;
#49350=EDGE_LOOP ( 'NONE', ( #32544, #16837, #46892, #2046 ) ) ;
#49353=CARTESIAN_POINT ( 'NONE',  ( 0.07982360342473591996, 1.709180471932028711, 0.000000000000000000 ) ) ;
#49355=CARTESIAN_POINT ( 'NONE',  ( -2.823445274216743073, 1.576824725690453954, 0.8656477926280276014 ) ) ;
#49358=DIRECTION ( 'NONE',  ( -0.000000000000000000, -1.000000000000000000, -0.000000000000000000 ) ) ;
#49366=EDGE_CURVE ( 'NONE', #36553, #49324, #13411, .T. ) ;
#49370=CARTESIAN_POINT ( 'NONE',  ( 2.464291103507799008, 0.000000000000000000, -1.626664315311302733 ) ) ;
#49377=EDGE_LOOP ( 'NONE', ( #39233, #30851, #29790, #28718 ) ) ;
#49387=VERTEX_POINT ( 'NONE', #42741 ) ;
#49389=VECTOR ( 'NONE', #12172, 39.37007874015748143 ) ;
#49391=CARTESIAN_POINT ( 'NONE',  ( 0.002207914879453961969, 5.905511811023623991, 0.04916304461325442243 ) ) ;
#49392=DIRECTION ( 'NONE',  ( -0.01601477604151182663, 0.9998717552508123996, -0.000000000000000000 ) ) ;
#49394=ORIENTED_EDGE ( 'NONE', *, *, #7399, .F. ) ;
#49396=DIRECTION ( 'NONE',  ( -1.105928667600717569E-16, 1.000000000000000000, -6.607616187506203079E-17 ) ) ;
#49399=ADVANCED_FACE ( 'NONE', ( #14627 ), #42251, .T. ) ;
#49400=CARTESIAN_POINT ( 'NONE',  ( -2.348388583459264822, 1.678599427619271722, 1.319607371826798659 ) ) ;
#49402=CIRCLE ( 'NONE', #15643, 2.246510896728926010 ) ;
#49404=CARTESIAN_POINT ( 'NONE',  ( 1.162932091021788183, 1.205361022782829114E-17, -1.684364178081092067 ) ) ;
#49406=FACE_OUTER_BOUND ( 'NONE', #46718, .T. ) ;
#49407=EDGE_LOOP ( 'NONE', ( #3846, #44014, #40885, #45720, #6061, #50272, #37099, #16224, #46075, #14424, #3925, #19940, #46881, #29530, #48720, #18073, #21431, #47208, #22578, #18181, #15754, #19917, #4768 ) ) ;
#49410=VECTOR ( 'NONE', #25560, 39.37007874015748143 ) ;
#49412=CYLINDRICAL_SURFACE ( 'NONE', #28106, 2.086614173228346303 ) ;
#49413=FACE_OUTER_BOUND ( 'NONE', #7006, .T. ) ;
#49414=ORIENTED_EDGE ( 'NONE', *, *, #49316, .T. ) ;
#49416=EDGE_CURVE ( 'NONE', #6398, #4293, #39635, .T. ) ;
#49422=ORIENTED_EDGE ( 'NONE', *, *, #47032, .F. ) ;
#49427=FACE_OUTER_BOUND ( 'NONE', #13360, .T. ) ;
#49429=EDGE_CURVE ( 'NONE', #42191, #45506, #48361, .T. ) ;
#49433=DIRECTION ( 'NONE',  ( 0.000000000000000000, 0.000000000000000000, 1.000000000000000000 ) ) ;
#49435=CARTESIAN_POINT ( 'NONE',  ( -0.8578470342358641698, 1.030463582533445166, 2.425782518084936612 ) ) ;
#49436=ORIENTED_EDGE ( 'NONE', *, *, #13070, .T. ) ;
#49437=DIRECTION ( 'NONE',  ( -0.01601477604151182663, 0.9998717552508123996, -0.000000000000000000 ) ) ;
#49440=DIRECTION ( 'NONE',  ( -3.986037398843765983E-20, -1.000000000000000000, -1.160734090543304660E-16 ) ) ;
#49443=AXIS2_PLACEMENT_3D ( 'NONE', #5626, #38394, #43003 ) ;
#49446=ORIENTED_EDGE ( 'NONE', *, *, #35548, .F. ) ;
#49453=CARTESIAN_POINT ( 'NONE',  ( 1.744867630759598498, 0.5220937483424626935, 1.454430778622096465 ) ) ;
#49455=CARTESIAN_POINT ( 'NONE',  ( 1.450992585860268136, 0.5222384346921369325, 1.735592794888963120 ) ) ;
#49457=ORIENTED_EDGE ( 'NONE', *, *, #33502, .F. ) ;
#49458=FACE_OUTER_BOUND ( 'NONE', #1728, .T. ) ;
#49459=DIRECTION ( 'NONE',  ( 0.000000000000000000, 0.000000000000000000, -1.000000000000000000 ) ) ;
#49460=CARTESIAN_POINT ( 'NONE',  ( -0.6380732109764247761, 1.697682040615038801, -2.127022210610377773 ) ) ;
#49464=CARTESIAN_POINT ( 'NONE',  ( 0.08139965876239094178, 1.610780518492231694, 0.000000000000000000 ) ) ;
#49472=VERTEX_POINT ( 'NONE', #19999 ) ;
#49473=DIRECTION ( 'NONE',  ( 0.9998717552508121775, 0.01601477604151182663, 0.000000000000000000 ) ) ;
#49475=VECTOR ( 'NONE', #6071, 39.37007874015748143 ) ;
#49481=ORIENTED_EDGE ( 'NONE', *, *, #19037, .T. ) ;
#49482=EDGE_CURVE ( 'NONE', #42262, #12924, #23312, .T. ) ;
#49487=EDGE_CURVE ( 'NONE', #39685, #26900, #33253, .T. ) ;
#49488=ORIENTED_EDGE ( 'NONE', *, *, #44797, .T. ) ;
#49494=DIRECTION ( 'NONE',  ( 0.000000000000000000, 0.000000000000000000, 1.000000000000000000 ) ) ;
#49497=ORIENTED_EDGE ( 'NONE', *, *, #44539, .T. ) ;
#49498=EDGE_LOOP ( 'NONE', ( #48874, #26542, #4046, #13587 ) ) ;
#49499=CARTESIAN_POINT ( 'NONE',  ( 2.926032761125787029, 0.000000000000000000, 0.3963580683592521914 ) ) ;
#49506=DIRECTION ( 'NONE',  ( 0.000000000000000000, 0.000000000000000000, 1.000000000000000000 ) ) ;
#49510=ORIENTED_EDGE ( 'NONE', *, *, #11410, .T. ) ;
#49512=AXIS2_PLACEMENT_3D ( 'NONE', #39215, #27586, #19082 ) ;
#49515=CARTESIAN_POINT ( 'NONE',  ( 2.118006771444148839, 0.000000000000000000, 0.3034726681826900307 ) ) ;
#49516=CARTESIAN_POINT ( 'NONE',  ( 0.1067246931122726866, 0.02962905676920215767, 0.000000000000000000 ) ) ;
#49517=EDGE_LOOP ( 'NONE', ( #20261, #12371, #34952, #30960 ) ) ;
#49525=LINE ( 'NONE', #2337, #32583 ) ;
#49527=CARTESIAN_POINT ( 'NONE',  ( -0.8952071785065479625, 5.905511811023623991, 1.972340328593135794 ) ) ;
#49531=ORIENTED_EDGE ( 'NONE', *, *, #11349, .T. ) ;
#49532=CARTESIAN_POINT ( 'NONE',  ( -0.5756566573089004768, 1.710292258889409833, 2.896516654582634853 ) ) ;
#49539=EDGE_CURVE ( 'NONE', #43566, #17400, #25791, .T. ) ;
#49541=ORIENTED_EDGE ( 'NONE', *, *, #13638, .F. ) ;
#49542=CARTESIAN_POINT ( 'NONE',  ( 1.312248418042880171, 6.692913385826772199, -1.722429524498088949 ) ) ;
#49544=CIRCLE ( 'NONE', #22400, 1.850107469027523432 ) ;
#49552=ORIENTED_EDGE ( 'NONE', *, *, #17468, .T. ) ;
#49558=LINE ( 'NONE', #36981, #45788 ) ;
#49559=CIRCLE ( 'NONE', #5092, 3.033577403570481668 ) ;
#49564=ORIENTED_EDGE ( 'NONE', *, *, #43846, .F. ) ;
#49565=DIRECTION ( 'NONE',  ( 3.169619151431853688E-17, 0.9659258262890662028, -0.2588190451025280114 ) ) ;
#49566=CARTESIAN_POINT ( 'NONE',  ( -2.576863348864732117, 1.679095609600309347, 1.442554885838411849 ) ) ;
#49567=CARTESIAN_POINT ( 'NONE',  ( 1.882988517681383200, 1.574803149606302854, 1.069164917025817507 ) ) ;
#49572=CARTESIAN_POINT ( 'NONE',  ( 1.955086072690433996, 1.651253202320272839, 2.212843190815307004 ) ) ;
#49577=DIRECTION ( 'NONE',  ( 0.000000000000000000, 0.000000000000000000, 1.000000000000000000 ) ) ;
#49581=EDGE_CURVE ( 'NONE', #25112, #31964, #33938, .T. ) ;
#49583=AXIS2_PLACEMENT_3D ( 'NONE', #37755, #49059, #25865 ) ;
#49588=VECTOR ( 'NONE', #36914, 39.37007874015748143 ) ;
#49602=DIRECTION ( 'NONE',  ( -0.5877852522924802425, 0.000000000000000000, 0.8090169943749422332 ) ) ;
#49613=ORIENTED_EDGE ( 'NONE', *, *, #24096, .T. ) ;
#49614=VERTEX_POINT ( 'NONE', #37561 ) ;
#49615=CARTESIAN_POINT ( 'NONE',  ( 0.000000000000000000, 1.574803149606302854, 0.000000000000000000 ) ) ;
#49622=EDGE_LOOP ( 'NONE', ( #45295, #43752, #22427, #28964, #14417, #3740, #34750, #12100, #37159, #45070, #28516, #25818, #27156 ) ) ;
#49636=ORIENTED_EDGE ( 'NONE', *, *, #146, .F. ) ;
#49638=CARTESIAN_POINT ( 'NONE',  ( -1.946505901478385203, 5.905511811023623991, 0.9915739042680188353 ) ) ;
#49639=VECTOR ( 'NONE', #30268, 39.37007874015748143 ) ;
#49644=DIRECTION ( 'NONE',  ( -0.9998717552508122886, -0.01601477604151182316, 0.000000000000000000 ) ) ;
#49650=EDGE_CURVE ( 'NONE', #38652, #16487, #33058, .T. ) ;
#49651=DIRECTION ( 'NONE',  ( 0.9998717552508121775, 0.01601477604151182663, 0.000000000000000000 ) ) ;
#49653=CARTESIAN_POINT ( 'NONE',  ( -2.055928985459924085, -8.304408758680925473E-17, 0.7197570096327614575 ) ) ;
#49654=CARTESIAN_POINT ( 'NONE',  ( -1.955094182356980070, 1.555721577805774691, 2.212836105613017246 ) ) ;
#49663=CARTESIAN_POINT ( 'NONE',  ( -0.6031363173298939229, 0.006153551727561678598, 1.747108239936284946 ) ) ;
#49664=DIRECTION ( 'NONE',  ( 0.000000000000000000, 0.000000000000000000, 1.000000000000000000 ) ) ;
#49669=CARTESIAN_POINT ( 'NONE',  ( -1.387661672111458078, 6.692913385826772199, -1.663104731517941692 ) ) ;
#49670=CARTESIAN_POINT ( 'NONE',  ( -2.160407304981126320, 1.574879494900809584, -0.1462862061266896330 ) ) ;
#49675=EDGE_CURVE ( 'NONE', #6064, #12848, #25628, .T. ) ;
#49678=AXIS2_PLACEMENT_3D ( 'NONE', #26764, #42514, #3276 ) ;
#49679=CARTESIAN_POINT ( 'NONE',  ( -2.058792518696834772, 0.5252116753648516934, 0.6171970515808470337 ) ) ;
#49680=DIRECTION ( 'NONE',  ( -3.986037398843765983E-20, -1.000000000000000000, -1.160734090543304660E-16 ) ) ;
#49684=CARTESIAN_POINT ( 'NONE',  ( -2.623503965249869729, 0.000000000000000000, 1.355882097269835107 ) ) ;
#49685=EDGE_CURVE ( 'NONE', #42744, #46569, #9422, .T. ) ;
#49688=ADVANCED_FACE ( 'NONE', ( #19179 ), #7071, .F. ) ;
#49689=DIRECTION ( 'NONE',  ( -4.943042645790397723E-17, 1.000000000000000000, -1.156482317317871478E-16 ) ) ;
#49693=VERTEX_POINT ( 'NONE', #50623 ) ;
#49695=EDGE_CURVE ( 'NONE', #17488, #18703, #38819, .T. ) ;
#49696=ORIENTED_EDGE ( 'NONE', *, *, #788, .F. ) ;
#49699=CONICAL_SURFACE ( 'NONE', #43978, 3.483074324928249421, 1.244861948955335196 ) ;
#49701=VECTOR ( 'NONE', #42594, 39.37007874015748143 ) ;
#49702=DIRECTION ( 'NONE',  ( -3.986037398843765983E-20, -1.000000000000000000, -1.160734090543304660E-16 ) ) ;
#49707=DIRECTION ( 'NONE',  ( -6.394449067488487880E-17, -1.000000000000000000, -9.687176266499690201E-17 ) ) ;
#49723=EDGE_LOOP ( 'NONE', ( #25613, #15677, #4188, #37190 ) ) ;
#49724=B_SPLINE_CURVE_WITH_KNOTS ( 'NONE', 3,
 ( #8035, #27644, #3915, #31536 ),
 .UNSPECIFIED., .F., .F.,
 ( 4, 4 ),
 ( 0.001238008921875009350, 0.04698876036832783792 ),
 .UNSPECIFIED. ) ;
#49725=EDGE_LOOP ( 'NONE', ( #39946, #29743, #46982, #26145, #26417, #30987, #41899, #30189, #42310, #22238, #9554 ) ) ;
#49726=CARTESIAN_POINT ( 'NONE',  ( -2.216785221661266014, 1.578142628253058843, -1.001018901021909269 ) ) ;
#49727=CARTESIAN_POINT ( 'NONE',  ( -0.4536155966250730032, 0.5249316497054298258, -1.828623345641975595 ) ) ;
#49731=VERTEX_POINT ( 'NONE', #46774 ) ;
#49736=CARTESIAN_POINT ( 'NONE',  ( -1.647545174055839556, 0.001531214329375737114, 0.5870650656849111249 ) ) ;
#49739=CONICAL_SURFACE ( 'NONE', #34133, 3.033577403570480779, 1.554780866114618743 ) ;
#49744=EDGE_CURVE ( 'NONE', #1426, #36108, #9318, .T. ) ;
#49746=EDGE_CURVE ( 'NONE', #47219, #50807, #39063, .T. ) ;
#49747=EDGE_CURVE ( 'NONE', #18734, #26436, #21343, .T. ) ;
#49749=VERTEX_POINT ( 'NONE', #26930 ) ;
#49753=VERTEX_POINT ( 'NONE', #2685 ) ;
#49755=CARTESIAN_POINT ( 'NONE',  ( 0.1067246931122726866, 0.02962905676920215767, 0.000000000000000000 ) ) ;
#49757=ORIENTED_EDGE ( 'NONE', *, *, #41376, .T. ) ;
#49758=CARTESIAN_POINT ( 'NONE',  ( 2.623503965249849301, 1.455362298632098428, 1.355882097269874187 ) ) ;
#49763=ORIENTED_EDGE ( 'NONE', *, *, #788, .T. ) ;
#49764=CARTESIAN_POINT ( 'NONE',  ( -2.101362156354032784, 1.641436391382051774, -0.5301003916084159329 ) ) ;
#49770=VERTEX_POINT ( 'NONE', #11693 ) ;
#49771=ORIENTED_EDGE ( 'NONE', *, *, #34363, .F. ) ;
#49779=PLANE ( 'NONE',  #5373 ) ;
#49781=LINE ( 'NONE', #29184, #47 ) ;
#49786=VERTEX_POINT ( 'NONE', #46029 ) ;
#49789=ORIENTED_EDGE ( 'NONE', *, *, #45686, .T. ) ;
#49790=ORIENTED_EDGE ( 'NONE', *, *, #49938, .T. ) ;
#49792=VERTEX_POINT ( 'NONE', #10691 ) ;
#49794=CARTESIAN_POINT ( 'NONE',  ( 1.387241876633648285, 6.692913385826772199, 1.662624236931697919 ) ) ;
#49795=VERTEX_POINT ( 'NONE', #3445 ) ;
#49796=CARTESIAN_POINT ( 'NONE',  ( 2.311075683235107814, 1.679301259607557384, 0.2633944203403243423 ) ) ;
#49799=EDGE_CURVE ( 'NONE', #23841, #13784, #24453, .T. ) ;
#49806=VECTOR ( 'NONE', #2390, 39.37007874015748143 ) ;
#49811=EDGE_CURVE ( 'NONE', #44866, #23296, #16078, .T. ) ;
#49812=CIRCLE ( 'NONE', #1221, 2.244934639244525076 ) ;
#49813=VECTOR ( 'NONE', #27469, 39.37007874015748143 ) ;
#49820=CARTESIAN_POINT ( 'NONE',  ( -2.607957063720690805, 1.678602264015800261, 1.384773081428535058 ) ) ;
#49821=CIRCLE ( 'NONE', #34221, 2.164630168518208109 ) ;
#49826=CARTESIAN_POINT ( 'NONE',  ( -2.047277537895663801, 1.675111054312220515, 0.7169459839182066307 ) ) ;
#49833=ORIENTED_EDGE ( 'NONE', *, *, #9787, .F. ) ;
#49837=DIRECTION ( 'NONE',  ( -0.01601477604151182663, 0.9998717552508123996, -0.000000000000000000 ) ) ;
#49838=CARTESIAN_POINT ( 'NONE',  ( -1.841876542352477886, 1.049866565877818347, -0.8407752412313899137 ) ) ;
#49842=CARTESIAN_POINT ( 'NONE',  ( 1.720314620805546646, 0.000000000000000000, 0.2826945007888405637 ) ) ;
#49861=B_SPLINE_CURVE_WITH_KNOTS ( 'NONE', 3,
 ( #38824, #14824, #19692, #30826 ),
 .UNSPECIFIED., .F., .F.,
 ( 4, 4 ),
 ( 2.002016001276121705E-07, 0.002500200811381732800 ),
 .UNSPECIFIED. ) ;
#49862=EDGE_CURVE ( 'NONE', #26872, #17017, #6381, .T. ) ;
#49865=DIRECTION ( 'NONE',  ( 1.558091277195102803E-17, -1.000000000000000000, 1.150229170499808965E-16 ) ) ;
#49870=CARTESIAN_POINT ( 'NONE',  ( 1.957708528393553582, 1.673641438755806732, -1.233304704937915330 ) ) ;
#49871=CARTESIAN_POINT ( 'NONE',  ( 2.151809081513405442, 6.692913385826772199, 0.2418202932658665705 ) ) ;
#49873=ORIENTED_EDGE ( 'NONE', *, *, #15233, .F. ) ;
#49876=CARTESIAN_POINT ( 'NONE',  ( -0.5433905323321888137, 1.526322510227913654, 2.902372092969472739 ) ) ;
#49884=CIRCLE ( 'NONE', #4597, 0.3937007874015748254 ) ;
#49888=FACE_OUTER_BOUND ( 'NONE', #38075, .T. ) ;
#49890=VECTOR ( 'NONE', #33924, 39.37007874015748854 ) ;
#49893=AXIS2_PLACEMENT_3D ( 'NONE', #33699, #42432, #46034 ) ;
#49900=CARTESIAN_POINT ( 'NONE',  ( -0.1876863054094430605, 0.000000000000000000, -1.901365838955026533 ) ) ;
#49903=LINE ( 'NONE', #27206, #21221 ) ;
#49904=CARTESIAN_POINT ( 'NONE',  ( -1.979793062125317471, 1.556934451446513545, 2.191257344206539504 ) ) ;
#49906=FACE_OUTER_BOUND ( 'NONE', #13010, .T. ) ;
#49911=CARTESIAN_POINT ( 'NONE',  ( 1.478089240774732582, 0.05159396975604255142, 1.241682111880268558 ) ) ;
#49920=CARTESIAN_POINT ( 'NONE',  ( 1.083598637574782364, 1.205361022782829114E-17, 2.747180975113346246 ) ) ;
#49928=VECTOR ( 'NONE', #20583, 39.37007874015748143 ) ;
#49929=ORIENTED_EDGE ( 'NONE', *, *, #50747, .F. ) ;
#49936=DIRECTION ( 'NONE',  ( -0.9998717552508122886, -0.01601477604151180928, 0.000000000000000000 ) ) ;
#49938=EDGE_CURVE ( 'NONE', #31986, #19249, #23150, .T. ) ;
#49940=DIRECTION ( 'NONE',  ( -0.01601477604151182663, 0.9998717552508123996, -0.000000000000000000 ) ) ;
#49942=DIRECTION ( 'NONE',  ( 0.08963930890342654279, -1.156097046908844086E-16, 0.9959742939952397345 ) ) ;
#49947=EDGE_CURVE ( 'NONE', #6064, #26089, #18863, .T. ) ;
#49948=CIRCLE ( 'NONE', #45844, 1.850107469027523432 ) ;
#49949=EDGE_LOOP ( 'NONE', ( #19310, #25510, #20779, #38061, #45128, #39327, #2194, #20135, #2667, #20056, #48349, #6130, #11999 ) ) ;
#49953=AXIS2_PLACEMENT_3D ( 'NONE', #48381, #1436, #33717 ) ;
#49954=ORIENTED_EDGE ( 'NONE', *, *, #49746, .T. ) ;
#49960=CARTESIAN_POINT ( 'NONE',  ( 2.319222573356612749, 1.745048544795088308, -0.1534186080535354380 ) ) ;
#49961=B_SPLINE_CURVE_WITH_KNOTS ( 'NONE', 3,
 ( #35382, #1176, #36145, #47203 ),
 .UNSPECIFIED., .F., .F.,
 ( 4, 4 ),
 ( 3.580237009053578663E-05, 0.004936055722876062785 ),
 .UNSPECIFIED. ) ;
#49964=LINE ( 'NONE', #41759, #7307 ) ;
#49967=CYLINDRICAL_SURFACE ( 'NONE', #38234, 2.165354330708661568 ) ;
#49969=EDGE_CURVE ( 'NONE', #41613, #38443, #20854, .T. ) ;
#49973=CARTESIAN_POINT ( 'NONE',  ( -1.740978969773838037, 0.000000000000000000, 0.09160132170885167124 ) ) ;
#49979=CARTESIAN_POINT ( 'NONE',  ( 0.5550072188453405442, 1.618366210323673338, -2.196007637835879045 ) ) ;
#49987=ORIENTED_EDGE ( 'NONE', *, *, #2313, .T. ) ;
#50000=LINE ( 'NONE', #26547, #22308 ) ;
#50001=CARTESIAN_POINT ( 'NONE',  ( -0.2431224069213027139, 5.905511811023623991, 2.152304290637670814 ) ) ;
#50002=EDGE_CURVE ( 'NONE', #23085, #11914, #44723, .T. ) ;
#50005=ADVANCED_FACE ( 'NONE', ( #10117 ), #49699, .T. ) ;
#50012=B_SPLINE_CURVE_WITH_KNOTS ( 'NONE', 3,
 ( #39450, #27565, #8719, #31708 ),
 .UNSPECIFIED., .F., .F.,
 ( 4, 4 ),
 ( 4.932109407666375322E-07, 0.04440089579718710378 ),
 .UNSPECIFIED. ) ;
#50013=FACE_OUTER_BOUND ( 'NONE', #39546, .T. ) ;
#50014=VERTEX_POINT ( 'NONE', #33880 ) ;
#50018=ORIENTED_EDGE ( 'NONE', *, *, #23407, .F. ) ;
#50019=ORIENTED_EDGE ( 'NONE', *, *, #12029, .T. ) ;
#50021=CARTESIAN_POINT ( 'NONE',  ( -1.806430656824982384, 0.5249316497054298258, 0.5351997120806747388 ) ) ;
#50023=ADVANCED_FACE ( 'NONE', ( #29224 ), #40687, .T. ) ;
#50031=LINE ( 'NONE', #14716, #43275 ) ;
#50035=CARTESIAN_POINT ( 'NONE',  ( 0.8668862056626265300, 0.04180443457634609727, -1.686684286392636789 ) ) ;
#50036=ADVANCED_FACE ( 'NONE', ( #28962 ), #10163, .T. ) ;
#50038=B_SPLINE_CURVE_WITH_KNOTS ( 'NONE', 3,
 ( #1559, #39771, #32296, #17312 ),
 .UNSPECIFIED., .F., .F.,
 ( 4, 4 ),
 ( 2.075011166194589347E-07, 0.002500489532013033724 ),
 .UNSPECIFIED. ) ;
#50040=PLANE ( 'NONE',  #8551 ) ;
#50041=CARTESIAN_POINT ( 'NONE',  ( 2.209387264600206180, 0.9904353868938117200, -1.399436384156840463 ) ) ;
#50046=DIRECTION ( 'NONE',  ( -0.4738686624730094610, -1.160734090543304907E-16, 0.8805955318567322276 ) ) ;
#50049=CARTESIAN_POINT ( 'NONE',  ( -0.8069532150559466377, 6.692913385826772199, -2.010061882867142824 ) ) ;
#50053=CARTESIAN_POINT ( 'NONE',  ( 2.164823134740037069, 1.574803149606302854, -0.04796011690015113127 ) ) ;
#50054=CIRCLE ( 'NONE', #1461, 1.850107469027523432 ) ;
#50065=LINE ( 'NONE', #42104, #43756 ) ;
#50073=CARTESIAN_POINT ( 'NONE',  ( -1.743434144314990553, 0.0004760342511857242553, -0.01934991164580179140 ) ) ;
#50085=EDGE_LOOP ( 'NONE', ( #12408, #29677, #14278, #42038 ) ) ;
#50086=DIRECTION ( 'NONE',  ( -0.01601477604151182663, 0.9998717552508123996, -0.000000000000000000 ) ) ;
#50087=CARTESIAN_POINT ( 'NONE',  ( 2.322368699764507216, 1.646673738916892837, -0.1535599007534338978 ) ) ;
#50088=ORIENTED_EDGE ( 'NONE', *, *, #26281, .T. ) ;
#50089=CARTESIAN_POINT ( 'NONE',  ( -1.399962034674500755, 1.689509322587608109, -2.010607907135041117 ) ) ;
#50091=ADVANCED_FACE ( 'NONE', ( #5984 ), #6246, .T. ) ;
#50092=VECTOR ( 'NONE', #7933, 39.37007874015748854 ) ;
#50093=CARTESIAN_POINT ( 'NONE',  ( -2.137893032918561254, 1.681902701049137638, 1.641967526060646554 ) ) ;
#50099=DIRECTION ( 'NONE',  ( -0.01601477604151182663, 0.9998717552508123996, -0.000000000000000000 ) ) ;
#50100=VERTEX_POINT ( 'NONE', #23004 ) ;
#50102=CARTESIAN_POINT ( 'NONE',  ( -0.1729294490429659770, 1.708950541169384163, -2.470410437739172682 ) ) ;
#50104=CARTESIAN_POINT ( 'NONE',  ( 1.785493683324574254, 0.000000000000000000, -1.119626681005672530 ) ) ;
#50105=ORIENTED_EDGE ( 'NONE', *, *, #31221, .F. ) ;
#50108=ORIENTED_EDGE ( 'NONE', *, *, #12850, .F. ) ;
#50114=FACE_OUTER_BOUND ( 'NONE', #24059, .T. ) ;
#50115=EDGE_CURVE ( 'NONE', #41705, #1977, #41002, .T. ) ;
#50117=FACE_OUTER_BOUND ( 'NONE', #45816, .T. ) ;
#50124=ADVANCED_FACE ( 'NONE', ( #14500 ), #28321, .T. ) ;
#50125=ORIENTED_EDGE ( 'NONE', *, *, #33792, .F. ) ;
#50126=CARTESIAN_POINT ( 'NONE',  ( -2.748374859398606596, 5.118110236220475784, -0.3226306186023585321 ) ) ;
#50130=VERTEX_POINT ( 'NONE', #38255 ) ;
#50138=ORIENTED_EDGE ( 'NONE', *, *, #24809, .F. ) ;
#50142=CARTESIAN_POINT ( 'NONE',  ( 0.2156685157584266599, 5.905511811023624880, -2.945280361644574629 ) ) ;
#50144=VECTOR ( 'NONE', #25153, 39.37007874015748143 ) ;
#50148=CARTESIAN_POINT ( 'NONE',  ( -1.472219874544909546, 1.205361022782829114E-17, 2.560030851058948898 ) ) ;
#50150=AXIS2_PLACEMENT_3D ( 'NONE', #40888, #6284, #25896 ) ;
#50151=ORIENTED_EDGE ( 'NONE', *, *, #398, .T. ) ;
#50154=B_SPLINE_CURVE_WITH_KNOTS ( 'NONE', 3,
 ( #44026, #44289, #31401, #8673 ),
 .UNSPECIFIED., .F., .F.,
 ( 4, 4 ),
 ( 2.558111634305129087E-07, 0.01955996689373667996 ),
 .UNSPECIFIED. ) ;
#50155=PLANE ( 'NONE',  #11593 ) ;
#50157=DIRECTION ( 'NONE',  ( 0.01601477604151182663, -0.9998717552508123996, 0.000000000000000000 ) ) ;
#50165=CARTESIAN_POINT ( 'NONE',  ( -0.3136974817027967100, 1.714375164834789356, -2.936457595020224520 ) ) ;
#50166=LINE ( 'NONE', #34726, #11304 ) ;
#50167=CARTESIAN_POINT ( 'NONE',  ( -1.152114531865843006, 1.205361022782829114E-17, 1.393499336327983729 ) ) ;
#50172=VERTEX_POINT ( 'NONE', #3632 ) ;
#50174=VECTOR ( 'NONE', #26695, 39.37007874015748143 ) ;
#50175=DIRECTION ( 'NONE',  ( 0.000000000000000000, 0.000000000000000000, 1.000000000000000000 ) ) ;
#50191=DIRECTION ( 'NONE',  ( -3.986037398843765983E-20, -1.000000000000000000, -1.160734090543304660E-16 ) ) ;
#50192=LINE ( 'NONE', #38134, #45410 ) ;
#50196=VERTEX_POINT ( 'NONE', #30751 ) ;
#50201=VERTEX_POINT ( 'NONE', #34382 ) ;
#50204=B_SPLINE_CURVE_WITH_KNOTS ( 'NONE', 3,
 ( #14969, #38472, #46425, #51028 ),
 .UNSPECIFIED., .F., .F.,
 ( 4, 4 ),
 ( 0.006151689351068225821, 0.007368043917412105820 ),
 .UNSPECIFIED. ) ;
#50207=CARTESIAN_POINT ( 'NONE',  ( 2.322368699764507216, 1.646673738916892837, -0.1535599007534338978 ) ) ;
#50210=EDGE_LOOP ( 'NONE', ( #15055, #28337, #35040, #45398 ) ) ;
#50215=CARTESIAN_POINT ( 'NONE',  ( 2.926032761125787029, 0.000000000000000000, 0.3963580683592521914 ) ) ;
#50217=ORIENTED_EDGE ( 'NONE', *, *, #32043, .F. ) ;
#50219=ADVANCED_FACE ( 'NONE', ( #26616 ), #42359, .F. ) ;
#50223=EDGE_CURVE ( 'NONE', #21800, #7708, #12664, .T. ) ;
#50225=CYLINDRICAL_SURFACE ( 'NONE', #9255, 2.164630168518208109 ) ;
#50227=DIRECTION ( 'NONE',  ( 0.000000000000000000, 0.000000000000000000, -1.000000000000000000 ) ) ;
#50230=CARTESIAN_POINT ( 'NONE',  ( 2.721588343797282317, 1.761660892206633910, -1.145422814530317579 ) ) ;
#50231=ADVANCED_FACE ( 'NONE', ( #31769 ), #16266, .T. ) ;
#50236=EDGE_LOOP ( 'NONE', ( #5752, #363, #30835, #7312 ) ) ;
#50237=ORIENTED_EDGE ( 'NONE', *, *, #13904, .T. ) ;
#50240=EDGE_CURVE ( 'NONE', #49090, #41090, #47220, .T. ) ;
#50241=CARTESIAN_POINT ( 'NONE',  ( -1.330356682269850044, 1.588168657012911877, -1.747353411991260819 ) ) ;
#50244=B_SPLINE_CURVE_WITH_KNOTS ( 'NONE', 3,
 ( #17352, #17603, #49051, #41354 ),
 .UNSPECIFIED., .F., .F.,
 ( 4, 4 ),
 ( 0.001655661513764574181, 0.004155744767597255133 ),
 .UNSPECIFIED. ) ;
#50245=AXIS2_PLACEMENT_3D ( 'NONE', #22958, #14708, #38711 ) ;
#50249=CARTESIAN_POINT ( 'NONE',  ( -0.9360721529196992519, 0.000000000000000000, 1.470771056236103158 ) ) ;
#50251=ORIENTED_EDGE ( 'NONE', *, *, #28903, .T. ) ;
#50252=ORIENTED_EDGE ( 'NONE', *, *, #1597, .F. ) ;
#50256=AXIS2_PLACEMENT_3D ( 'NONE', #8826, #40335, #22990 ) ;
#50267=EDGE_CURVE ( 'NONE', #45778, #24752, #8779, .T. ) ;
#50268=CARTESIAN_POINT ( 'NONE',  ( 1.700185224778670401, 1.636708331897141377, -1.557456981387029149 ) ) ;
#50272=ORIENTED_EDGE ( 'NONE', *, *, #25551, .F. ) ;
#50276=FACE_OUTER_BOUND ( 'NONE', #7790, .T. ) ;
#50277=CARTESIAN_POINT ( 'NONE',  ( -2.882374421599337655, 1.575897850148979318, -0.6410571176358736967 ) ) ;
#50280=VECTOR ( 'NONE', #46766, 39.37007874015748854 ) ;
#50282=EDGE_CURVE ( 'NONE', #6857, #26667, #45591, .T. ) ;
#50283=DIRECTION ( 'NONE',  ( -0.01601477604151182663, 0.9998717552508123996, -0.000000000000000000 ) ) ;
#50287=CIRCLE ( 'NONE', #43723, 1.743387098533651480 ) ;
#50288=VERTEX_POINT ( 'NONE', #11877 ) ;
#50291=DIRECTION ( 'NONE',  ( 5.500355109725808462E-17, -1.000000000000000000, -1.022137253806221654E-16 ) ) ;
#50292=ORIENTED_EDGE ( 'NONE', *, *, #28284, .T. ) ;
#50293=ORIENTED_EDGE ( 'NONE', *, *, #31089, .T. ) ;
#50297=CARTESIAN_POINT ( 'NONE',  ( 1.626841099230391219, 0.01754038748813176174, 1.234417208607474059 ) ) ;
#50298=ADVANCED_FACE ( 'NONE', ( #50809 ), #11628, .T. ) ;
#50300=B_SPLINE_CURVE_WITH_KNOTS ( 'NONE', 3,
 ( #17656, #45497, #33672, #14033 ),
 .UNSPECIFIED., .F., .F.,
 ( 4, 4 ),
 ( 0.1211775127643062722, 0.1625894504277921315 ),
 .UNSPECIFIED. ) ;
#50301=CARTESIAN_POINT ( 'NONE',  ( 2.589735824746187909, 0.9850668145931131825, 0.4004656049141078200 ) ) ;
#50304=FACE_OUTER_BOUND ( 'NONE', #34987, .T. ) ;
#50311=EDGE_CURVE ( 'NONE', #49770, #2009, #20027, .T. ) ;
#50312=DIRECTION ( 'NONE',  ( -0.000000000000000000, -1.000000000000000000, -0.000000000000000000 ) ) ;
#50318=ORIENTED_EDGE ( 'NONE', *, *, #16341, .T. ) ;
#50327=ORIENTED_EDGE ( 'NONE', *, *, #35026, .T. ) ;
#50332=DIRECTION ( 'NONE',  ( 1.042246309067994810E-16, 1.000000000000000000, 7.572362681945316160E-17 ) ) ;
#50345=DIRECTION ( 'NONE',  ( 0.9195277725514544587, 0.000000000000000000, -0.3930250316539147803 ) ) ;
#50346=B_SPLINE_CURVE_WITH_KNOTS ( 'NONE', 3,
 ( #36727, #16335, #13234, #9350 ),
 .UNSPECIFIED., .F., .F.,
 ( 4, 4 ),
 ( 7.000820791675995278E-07, 0.002501003665680686262 ),
 .UNSPECIFIED. ) ;
#50347=CARTESIAN_POINT ( 'NONE',  ( -0.7381027496704858359, 1.609316782724114825, -2.859439394060923512 ) ) ;
#50348=CARTESIAN_POINT ( 'NONE',  ( 1.500384305870146040, 1.742635665041250670, 2.543203386703559943 ) ) ;
#50355=ORIENTED_EDGE ( 'NONE', *, *, #33162, .F. ) ;
#50361=DIRECTION ( 'NONE',  ( -0.9195277725514544587, -4.558310254684937226E-17, 0.3930250316539147803 ) ) ;
#50362=ORIENTED_EDGE ( 'NONE', *, *, #40220, .F. ) ;
#50365=DIRECTION ( 'NONE',  ( -0.000000000000000000, 1.000000000000000000, -0.000000000000000000 ) ) ;
#50369=CARTESIAN_POINT ( 'NONE',  ( -0.6808484915247774438, 0.01701463086705359146, 1.674057048625058552 ) ) ;
#50377=EDGE_CURVE ( 'NONE', #22430, #8249, #24989, .T. ) ;
#50378=ORIENTED_EDGE ( 'NONE', *, *, #17558, .T. ) ;
#50379=CARTESIAN_POINT ( 'NONE',  ( 2.491402175429653809, 1.458524810485662959, -1.585592796919505609 ) ) ;
#50383=CARTESIAN_POINT ( 'NONE',  ( 3.937007874015748143, 4.960629921259846142, -1.023622047244094224 ) ) ;
#50384=ORIENTED_EDGE ( 'NONE', *, *, #13263, .T. ) ;
#50385=VERTEX_POINT ( 'NONE', #48741 ) ;
#50387=DIRECTION ( 'NONE',  ( -0.9839295885986321100, 0.000000000000000000, 0.1785568947986229116 ) ) ;
#50388=AXIS2_PLACEMENT_3D ( 'NONE', #35728, #12237, #9126 ) ;
#50392=ORIENTED_EDGE ( 'NONE', *, *, #4105, .T. ) ;
#50396=VERTEX_POINT ( 'NONE', #48489 ) ;
#50400=EDGE_CURVE ( 'NONE', #35952, #28312, #35409, .T. ) ;
#50401=B_SPLINE_CURVE_WITH_KNOTS ( 'NONE', 3,
 ( #21152, #28630, #25275, #36388 ),
 .UNSPECIFIED., .F., .F.,
 ( 4, 4 ),
 ( 2.472323665191410711E-07, 0.002500445596068602040 ),
 .UNSPECIFIED. ) ;
#50402=EDGE_CURVE ( 'NONE', #49284, #39633, #21426, .T. ) ;
#50403=DIRECTION ( 'NONE',  ( 0.01601477604151182663, -0.9998717552508123996, 0.000000000000000000 ) ) ;
#50404=CARTESIAN_POINT ( 'NONE',  ( 0.8446807076687119498, 1.721431058233622746, 2.110586427442081803 ) ) ;
#50408=LINE ( 'NONE', #30847, #43791 ) ;
#50414=DIRECTION ( 'NONE',  ( -0.01601477604151182663, 0.9998717552508123996, -0.000000000000000000 ) ) ;
#50424=EDGE_LOOP ( 'NONE', ( #25469, #39743, #8453, #43233 ) ) ;
#50425=CARTESIAN_POINT ( 'NONE',  ( -1.017106836739562814, 0.007823009827427474319, -1.483652934538973067 ) ) ;
#50426=DIRECTION ( 'NONE',  ( 0.5128992774058948045, 0.000000000000000000, 0.8584487936018727616 ) ) ;
#50427=AXIS2_PLACEMENT_3D ( 'NONE', #28268, #32423, #36291 ) ;
#50431=CARTESIAN_POINT ( 'NONE',  ( 0.07982360342473591996, 1.709180471932028711, 0.000000000000000000 ) ) ;
#50434=CARTESIAN_POINT ( 'NONE',  ( 2.947574761915768171, 1.447536563168191126, -0.1816379373804911657 ) ) ;
#50436=FACE_OUTER_BOUND ( 'NONE', #33664, .T. ) ;
#50438=EDGE_LOOP ( 'NONE', ( #32431, #3174, #29728, #20754 ) ) ;
#50440=FACE_OUTER_BOUND ( 'NONE', #459, .T. ) ;
#50444=VERTEX_POINT ( 'NONE', #44894 ) ;
#50445=VERTEX_POINT ( 'NONE', #20649 ) ;
#50446=LINE ( 'NONE', #7645, #29401 ) ;
#50447=B_SPLINE_CURVE_WITH_KNOTS ( 'NONE', 3,
 ( #38651, #38894, #15410, #23655 ),
 .UNSPECIFIED., .F., .F.,
 ( 4, 4 ),
 ( 3.432544043846355379E-07, 0.04340872033644440492 ),
 .UNSPECIFIED. ) ;
#50450=CIRCLE ( 'NONE', #13408, 2.164630168518208109 ) ;
#50452=CARTESIAN_POINT ( 'NONE',  ( 2.118566926156530084, 0.5221770508638550190, -0.8519995351685487606 ) ) ;
#50455=CARTESIAN_POINT ( 'NONE',  ( 1.516362329707282797, 1.735719643385797095, -2.003368222229618745 ) ) ;
#50457=CARTESIAN_POINT ( 'NONE',  ( 2.706338173250262269, 2.755905511811027164, -1.181102362204724088 ) ) ;
#50458=DIRECTION ( 'NONE',  ( -8.032339854997315857E-17, 1.000000000000000000, -1.007223559679407077E-16 ) ) ;
#50468=ORIENTED_EDGE ( 'NONE', *, *, #6348, .F. ) ;
#50470=CARTESIAN_POINT ( 'NONE',  ( 1.472697644137372697, 1.731489898814932316, 1.760436233057293354 ) ) ;
#50472=DIRECTION ( 'NONE',  ( 0.000000000000000000, 1.160734090543304660E-16, -1.000000000000000000 ) ) ;
#50473=ORIENTED_EDGE ( 'NONE', *, *, #6, .F. ) ;
#50475=DIRECTION ( 'NONE',  ( -0.01601477604151182663, 0.9998717552508123996, -0.000000000000000000 ) ) ;
#50480=ORIENTED_EDGE ( 'NONE', *, *, #50838, .F. ) ;
#50481=ORIENTED_EDGE ( 'NONE', *, *, #22724, .T. ) ;
#50488=( BOUNDED_CURVE ( )  B_SPLINE_CURVE ( 3, ( #12050, #30660, #35292, #11035 ),
 .UNSPECIFIED., .F., .F. ) 
 B_SPLINE_CURVE_WITH_KNOTS ( ( 4, 4 ),
 ( 3.094356967441856732, 3.141592653589793116 ),
 .UNSPECIFIED. ) 
 CURVE ( )  GEOMETRIC_REPRESENTATION_ITEM ( )  RATIONAL_B_SPLINE_CURVE ( ( 1.000000000000000000, 0.9998140744722292528, 0.9998140744722292528, 1.000000000000000000 ) ) 
 REPRESENTATION_ITEM ( '' )  );
#50490=B_SPLINE_CURVE_WITH_KNOTS ( 'NONE', 3,
 ( #43209, #27465, #46066, #22596 ),
 .UNSPECIFIED., .F., .F.,
 ( 4, 4 ),
 ( 4.753383040819987272E-07, 0.002500476700147301855 ),
 .UNSPECIFIED. ) ;
#50499=EDGE_CURVE ( 'NONE', #33697, #3514, #37455, .T. ) ;
#50507=VECTOR ( 'NONE', #17134, 39.37007874015748143 ) ;
#50508=CARTESIAN_POINT ( 'NONE',  ( 2.889674983507178219, 0.000000000000000000, -0.6090712660037610471 ) ) ;
#50510=DIRECTION ( 'NONE',  ( -1.000000000000000000, -1.908195823574487557E-16, 0.000000000000000000 ) ) ;
#50511=EDGE_LOOP ( 'NONE', ( #5917, #15447, #8762, #36573 ) ) ;
#50513=CARTESIAN_POINT ( 'NONE',  ( 0.07982360342473591996, 1.709180471932028711, 0.000000000000000000 ) ) ;
#50523=DIRECTION ( 'NONE',  ( -0.000000000000000000, -1.000000000000000000, -0.000000000000000000 ) ) ;
#50525=EDGE_CURVE ( 'NONE', #25220, #16985, #4050, .T. ) ;
#50526=CARTESIAN_POINT ( 'NONE',  ( 1.979793062125284608, 5.905511811023623991, 2.191257344206569257 ) ) ;
#50529=CARTESIAN_POINT ( 'NONE',  ( -1.882988517681399188, 6.692913385826772199, 1.069164917025788863 ) ) ;
#50530=CIRCLE ( 'NONE', #17654, 2.165354330708661568 ) ;
#50532=EDGE_CURVE ( 'NONE', #619, #50396, #28357, .T. ) ;
#50537=DIRECTION ( 'NONE',  ( 0.000000000000000000, 1.160734090543304660E-16, -1.000000000000000000 ) ) ;
#50538=EDGE_LOOP ( 'NONE', ( #40196, #40538, #8473, #41841, #6472, #21139, #28677, #21370, #41478, #36810, #31309 ) ) ;
#50540=CARTESIAN_POINT ( 'NONE',  ( 0.8446807076687119498, 1.721431058233622746, 2.110586427442081803 ) ) ;
#50550=CARTESIAN_POINT ( 'NONE',  ( 1.295932559091726111, 1.640989118791050583, -2.653223575520714750 ) ) ;
#50554=VERTEX_POINT ( 'NONE', #10567 ) ;
#50556=CARTESIAN_POINT ( 'NONE',  ( 1.930379001735549993, 1.749335058599799320, 2.234429108645952677 ) ) ;
#50560=DIRECTION ( 'NONE',  ( -0.000000000000000000, -1.000000000000000000, -0.000000000000000000 ) ) ;
#50565=ORIENTED_EDGE ( 'NONE', *, *, #20568, .T. ) ;
#50567=ORIENTED_EDGE ( 'NONE', *, *, #45756, .F. ) ;
#50576=LINE ( 'NONE', #23513, #15588 ) ;
#50580=CARTESIAN_POINT ( 'NONE',  ( 2.032117719318057958, 0.000000000000000000, 0.6430507823692680480 ) ) ;
#50583=DIRECTION ( 'NONE',  ( -0.9998717552508122886, -0.01601477604151182316, 0.000000000000000000 ) ) ;
#50587=FACE_OUTER_BOUND ( 'NONE', #49517, .T. ) ;
#50589=ORIENTED_EDGE ( 'NONE', *, *, #38435, .T. ) ;
#50591=CARTESIAN_POINT ( 'NONE',  ( 1.956098637639549720, 1.739232450405700847, -1.232242025355393844 ) ) ;
#50592=CYLINDRICAL_SURFACE ( 'NONE', #36239, 2.165354330708661568 ) ;
#50596=ADVANCED_FACE ( 'NONE', ( #50013 ), #27249, .T. ) ;
#50598=CIRCLE ( 'NONE', #11124, 2.164630168518208109 ) ;
#50600=VERTEX_POINT ( 'NONE', #37696 ) ;
#50601=DIRECTION ( 'NONE',  ( 0.01601477604151182663, -0.9998717552508123996, 0.000000000000000000 ) ) ;
#50608=EDGE_LOOP ( 'NONE', ( #35912, #1540, #16571, #4219 ) ) ;
#50611=CARTESIAN_POINT ( 'NONE',  ( 2.139229417893225627, 0.000000000000000000, -0.3394403656973398742 ) ) ;
#50613=CARTESIAN_POINT ( 'NONE',  ( 0.08119777152254364916, 1.623385212329073957, 0.000000000000000000 ) ) ;
#50618=CARTESIAN_POINT ( 'NONE',  ( -2.950847925457031007, 1.574821451496988933, -0.08326053095501942392 ) ) ;
#50619=EDGE_CURVE ( 'NONE', #20464, #33352, #7894, .T. ) ;
#50623=CARTESIAN_POINT ( 'NONE',  ( -2.100227814008681193, 5.905511811023623991, -2.076109931251944207 ) ) ;
#50626=EDGE_CURVE ( 'NONE', #33537, #48962, #12285, .T. ) ;
#50627=EDGE_LOOP ( 'NONE', ( #11371, #32601, #19675, #13527 ) ) ;
#50630=EDGE_CURVE ( 'NONE', #49614, #28289, #15172, .T. ) ;
#50631=CARTESIAN_POINT ( 'NONE',  ( -0.6808484915247774438, 0.01701463086705359146, 1.674057048625058552 ) ) ;
#50635=LINE ( 'NONE', #34701, #42363 ) ;
#50636=DIRECTION ( 'NONE',  ( -0.000000000000000000, -1.000000000000000000, -0.000000000000000000 ) ) ;
#50637=DIRECTION ( 'NONE',  ( -0.01601477604151182663, 0.9998717552508123996, -0.000000000000000000 ) ) ;
#50641=VECTOR ( 'NONE', #8284, 39.37007874015748143 ) ;
#50646=EDGE_CURVE ( 'NONE', #19878, #17854, #40724, .T. ) ;
#50651=VERTEX_POINT ( 'NONE', #43504 ) ;
#50656=CARTESIAN_POINT ( 'NONE',  ( -0.1515599155143076138, 1.705474441417569320, -2.232975473887063966 ) ) ;
#50657=ADVANCED_FACE ( 'NONE', ( #17181 ), #661, .T. ) ;
#50659=CARTESIAN_POINT ( 'NONE',  ( 0.1067246931122726866, 0.02962905676920215767, 0.000000000000000000 ) ) ;
#50662=DIRECTION ( 'NONE',  ( -0.9998717552508122886, -0.01601477604151180928, 0.000000000000000000 ) ) ;
#50664=ORIENTED_EDGE ( 'NONE', *, *, #30172, .T. ) ;
#50665=FACE_OUTER_BOUND ( 'NONE', #25047, .T. ) ;
#50666=VERTEX_POINT ( 'NONE', #39900 ) ;
#50668=CARTESIAN_POINT ( 'NONE',  ( 0.1067246931122726866, 0.02962905676920215767, 0.000000000000000000 ) ) ;
#50670=ORIENTED_EDGE ( 'NONE', *, *, #20099, .T. ) ;
#50677=CARTESIAN_POINT ( 'NONE',  ( 0.6651440564695696445, 1.049866565877818347, 1.912327270024466008 ) ) ;
#50678=EDGE_CURVE ( 'NONE', #2997, #47957, #31117, .T. ) ;
#50679=DIRECTION ( 'NONE',  ( -0.3090169943749447312, 0.000000000000000000, -0.9510565162951544194 ) ) ;
#50680=AXIS2_PLACEMENT_3D ( 'NONE', #38052, #18418, #22798 ) ;
#50681=PLANE ( 'NONE',  #21523 ) ;
#50684=CARTESIAN_POINT ( 'NONE',  ( -2.734482843737247038, 1.578211097029592169, -1.115254632218712016 ) ) ;
#50685=CIRCLE ( 'NONE', #26850, 2.164630168518208109 ) ;
#50690=ADVANCED_FACE ( 'NONE', ( #47607 ), #40168, .T. ) ;
#50691=CARTESIAN_POINT ( 'NONE',  ( -1.350373579275921276, 0.006290961278228680842, 1.139832270491418553 ) ) ;
#50692=VERTEX_POINT ( 'NONE', #20276 ) ;
#50704=CIRCLE ( 'NONE', #28506, 2.246510896728926010 ) ;
#50711=CARTESIAN_POINT ( 'NONE',  ( -1.030301126714985971, 0.000000000000000000, -1.501813316714599500 ) ) ;
#50714=ADVANCED_FACE ( 'NONE', ( #16418 ), #4277, .F. ) ;
#50719=CARTESIAN_POINT ( 'NONE',  ( 1.112246780768851195, 0.5224230866457337807, 1.957537375840811888 ) ) ;
#50722=ADVANCED_FACE ( 'NONE', ( #40427 ), #36294, .F. ) ;
#50724=DIRECTION ( 'NONE',  ( 0.000000000000000000, 1.160734090543304660E-16, -1.000000000000000000 ) ) ;
#50728=DIRECTION ( 'NONE',  ( 0.9510565162951500895, 0.000000000000000000, 0.3090169943749582204 ) ) ;
#50729=DIRECTION ( 'NONE',  ( -0.9362348706397368714, 4.082259235907190839E-17, -0.3513748240813434620 ) ) ;
#50735=CARTESIAN_POINT ( 'NONE',  ( -2.165354330708661568, 1.574803149606301966, -1.520079223026944511E-17 ) ) ;
#50736=EDGE_CURVE ( 'NONE', #5605, #24001, #45902, .T. ) ;
#50737=LINE ( 'NONE', #4581, #47456 ) ;
#50745=EDGE_LOOP ( 'NONE', ( #36710, #32872, #226, #34076 ) ) ;
#50747=EDGE_CURVE ( 'NONE', #45160, #24001, #20230, .T. ) ;
#50754=VERTEX_POINT ( 'NONE', #41941 ) ;
#50758=FACE_OUTER_BOUND ( 'NONE', #2688, .T. ) ;
#50760=DIRECTION ( 'NONE',  ( -0.9998717552508122886, -0.01601477604151182316, 0.000000000000000000 ) ) ;
#50761=ORIENTED_EDGE ( 'NONE', *, *, #9783, .F. ) ;
#50764=CARTESIAN_POINT ( 'NONE',  ( -1.368795925040221295, 1.049866565877818347, 1.491914849825318967 ) ) ;
#50767=B_SPLINE_CURVE_WITH_KNOTS ( 'NONE', 3,
 ( #33051, #28639, #5406, #20902 ),
 .UNSPECIFIED., .F., .F.,
 ( 4, 4 ),
 ( 0.0004892548405474798738, 0.0008567996338181287259 ),
 .UNSPECIFIED. ) ;
#50769=CARTESIAN_POINT ( 'NONE',  ( 0.000000000000000000, 6.692913385826772199, 0.000000000000000000 ) ) ;
#50773=CARTESIAN_POINT ( 'NONE',  ( -0.3136974817027967100, 1.714375164834789356, -2.936457595020224520 ) ) ;
#50775=CARTESIAN_POINT ( 'NONE',  ( 0.08139965876239094178, 1.610780518492231694, 0.000000000000000000 ) ) ;
#50777=ORIENTED_EDGE ( 'NONE', *, *, #6454, .F. ) ;
#50778=CONICAL_SURFACE ( 'NONE', #10464, 2.246510896728926010, 0.01601546068027819014 ) ;
#50780=ADVANCED_FACE ( 'NONE', ( #9432 ), #25055, .F. ) ;
#50784=ORIENTED_EDGE ( 'NONE', *, *, #27590, .T. ) ;
#50785=PLANE ( 'NONE',  #43981 ) ;
#50786=CARTESIAN_POINT ( 'NONE',  ( 1.436585068920266606, 1.636014119286001156, -2.061015189343648579 ) ) ;
#50792=DIRECTION ( 'NONE',  ( 0.9998717552508121775, 0.01601477604151182663, 0.000000000000000000 ) ) ;
#50794=CARTESIAN_POINT ( 'NONE',  ( 1.735113842587030497, 0.05571068913886997875, 0.8778189866238004235 ) ) ;
#50795=VERTEX_POINT ( 'NONE', #33949 ) ;
#50796=DIRECTION ( 'NONE',  ( -0.1785568947986229116, 1.142151789626729957E-16, -0.9839295885986321100 ) ) ;
#50803=EDGE_CURVE ( 'NONE', #35466, #20464, #17650, .T. ) ;
#50804=CARTESIAN_POINT ( 'NONE',  ( -0.5756566573089004768, 1.527738838675063882, 2.896516654582634853 ) ) ;
#50806=FACE_OUTER_BOUND ( 'NONE', #17526, .T. ) ;
#50807=VERTEX_POINT ( 'NONE', #49638 ) ;
#50809=FACE_OUTER_BOUND ( 'NONE', #22254, .T. ) ;
#50811=B_SPLINE_CURVE_WITH_KNOTS ( 'NONE', 3,
 ( #38501, #10865, #50550, #42354 ),
 .UNSPECIFIED., .F., .F.,
 ( 4, 4 ),
 ( 2.220042605370945366E-07, 0.002500468061448395899 ),
 .UNSPECIFIED. ) ;
#50813=DIRECTION ( 'NONE',  ( 0.000000000000000000, 0.000000000000000000, -1.000000000000000000 ) ) ;
#50815=ORIENTED_EDGE ( 'NONE', *, *, #11220, .F. ) ;
#50819=VERTEX_POINT ( 'NONE', #41192 ) ;
#50820=CARTESIAN_POINT ( 'NONE',  ( -2.793030215715272213, 1.577298709702483093, 0.9592557174602283077 ) ) ;
#50821=DIRECTION ( 'NONE',  ( 1.558091277195270436E-17, -1.000000000000000000, -1.150229170499806500E-16 ) ) ;
#50828=EDGE_LOOP ( 'NONE', ( #40274, #20145, #47639, #23158 ) ) ;
#50834=VERTEX_POINT ( 'NONE', #33454 ) ;
#50838=EDGE_CURVE ( 'NONE', #42285, #49284, #29176, .T. ) ;
#50844=CIRCLE ( 'NONE', #30283, 2.164630168518208109 ) ;
#50846=VECTOR ( 'NONE', #51043, 39.37007874015748143 ) ;
#50847=EDGE_CURVE ( 'NONE', #44818, #44681, #18952, .T. ) ;
#50850=VECTOR ( 'NONE', #27307, 39.37007874015748143 ) ;
#50854=CARTESIAN_POINT ( 'NONE',  ( 0.6506240732632109225, 1.652706090825650342, -2.172499238757989559 ) ) ;
#50859=VERTEX_POINT ( 'NONE', #50142 ) ;
#50861=FACE_OUTER_BOUND ( 'NONE', #28204, .T. ) ;
#50866=LINE ( 'NONE', #50126, #50280 ) ;
#50867=CARTESIAN_POINT ( 'NONE',  ( -2.059323380196183439, 1.679060685761519567, -1.300380081340403837 ) ) ;
#50868=DIRECTION ( 'NONE',  ( -0.000000000000000000, 1.000000000000000000, -0.000000000000000000 ) ) ;
#50872=CARTESIAN_POINT ( 'NONE',  ( 0.7728391134718428646, 0.5249316475426863970, -1.718240423291419461 ) ) ;
#50873=CARTESIAN_POINT ( 'NONE',  ( -0.5111094159775860790, 1.525631179887897204, 2.908230251890296714 ) ) ;
#50876=B_SPLINE_CURVE_WITH_KNOTS ( 'NONE', 3,
 ( #21629, #10516, #49455, #29376 ),
 .UNSPECIFIED., .F., .F.,
 ( 4, 4 ),
 ( 4.515586042724347206E-07, 0.04476270047297285087 ),
 .UNSPECIFIED. ) ;
#50877=ORIENTED_EDGE ( 'NONE', *, *, #21845, .T. ) ;
#50884=LINE ( 'NONE', #23571, #46828 ) ;
#50888=VECTOR ( 'NONE', #6551, 39.37007874015748143 ) ;
#50893=ORIENTED_EDGE ( 'NONE', *, *, #1118, .F. ) ;
#50894=EDGE_CURVE ( 'NONE', #9822, #14116, #50635, .T. ) ;
#50895=VECTOR ( 'NONE', #20466, 39.37007874015748143 ) ;
#50899=EDGE_CURVE ( 'NONE', #4750, #8816, #23319, .T. ) ;
#50900=CONICAL_SURFACE ( 'NONE', #32851, 3.033577403570480779, 1.554780866114618743 ) ;
#50910=CYLINDRICAL_SURFACE ( 'NONE', #45451, 2.165354330708661568 ) ;
#50921=DIRECTION ( 'NONE',  ( 0.04486483035050446017, 0.000000000000000000, 0.9989930665413151445 ) ) ;
#50925=VERTEX_POINT ( 'NONE', #15329 ) ;
#50928=FACE_OUTER_BOUND ( 'NONE', #2352, .T. ) ;
#50935=AXIS2_PLACEMENT_3D ( 'NONE', #35004, #7133, #46588 ) ;
#50937=VERTEX_POINT ( 'NONE', #27194 ) ;
#50940=ADVANCED_FACE ( 'NONE', ( #42933 ), #22571, .F. ) ;
#50945=ORIENTED_EDGE ( 'NONE', *, *, #41727, .T. ) ;
#50949=ADVANCED_FACE ( 'NONE', ( #3709 ), #38580, .F. ) ;
#50950=VECTOR ( 'NONE', #23972, 39.37007874015748143 ) ;
#50951=EDGE_CURVE ( 'NONE', #32762, #1805, #46436, .T. ) ;
#50955=PLANE ( 'NONE',  #35965 ) ;
#50956=ORIENTED_EDGE ( 'NONE', *, *, #3290, .T. ) ;
#50957=CARTESIAN_POINT ( 'NONE',  ( 2.889674983507178219, 1.448941827424379936, -0.6090712660037606030 ) ) ;
#50965=ORIENTED_EDGE ( 'NONE', *, *, #23636, .T. ) ;
#50966=FACE_OUTER_BOUND ( 'NONE', #28775, .T. ) ;
#50969=ADVANCED_FACE ( 'NONE', ( #23080 ), #11086, .T. ) ;
#50975=ORIENTED_EDGE ( 'NONE', *, *, #33212, .T. ) ;
#50976=CARTESIAN_POINT ( 'NONE',  ( -1.695772546416002280, 0.000000000000000000, -2.417756147381373566 ) ) ;
#50978=EDGE_CURVE ( 'NONE', #10170, #16563, #38333, .T. ) ;
#50979=VECTOR ( 'NONE', #33839, 39.37007874015748143 ) ;
#50981=ORIENTED_EDGE ( 'NONE', *, *, #48313, .F. ) ;
#50982=FACE_OUTER_BOUND ( 'NONE', #33095, .T. ) ;
#50984=DIRECTION ( 'NONE',  ( 0.000000000000000000, -1.156482317317871478E-16, 1.000000000000000000 ) ) ;
#50988=ORIENTED_EDGE ( 'NONE', *, *, #12845, .T. ) ;
#50992=B_SPLINE_CURVE_WITH_KNOTS ( 'NONE', 3,
 ( #9190, #43520, #48135, #13323 ),
 .UNSPECIFIED., .F., .F.,
 ( 4, 4 ),
 ( 0.002252064165998921876, 0.004752375895586415447 ),
 .UNSPECIFIED. ) ;
#50993=CARTESIAN_POINT ( 'NONE',  ( 0.08139965876239094178, 1.610780518492231694, 0.000000000000000000 ) ) ;
#50994=ORIENTED_EDGE ( 'NONE', *, *, #5746, .F. ) ;
#51004=AXIS2_PLACEMENT_3D ( 'NONE', #33326, #5695, #41564 ) ;
#51006=EDGE_CURVE ( 'NONE', #5331, #15130, #12744, .T. ) ;
#51009=ORIENTED_EDGE ( 'NONE', *, *, #14205, .T. ) ;
#51012=CARTESIAN_POINT ( 'NONE',  ( -0.04921259842519689481, 0.000000000000000000, 1.742692369722729895 ) ) ;
#51018=EDGE_CURVE ( 'NONE', #46764, #33537, #12987, .T. ) ;
#51022=ORIENTED_EDGE ( 'NONE', *, *, #16404, .T. ) ;
#51024=CARTESIAN_POINT ( 'NONE',  ( 2.010517631316622644, 0.000000000000000000, 0.8058170502102376398 ) ) ;
#51028=CARTESIAN_POINT ( 'NONE',  ( -2.164823134740035737, 1.574811347331577016, -0.04796011690018289753 ) ) ;
#51031=AXIS2_PLACEMENT_3D ( 'NONE', #24266, #28118, #21166 ) ;
#51033=B_SPLINE_CURVE_WITH_KNOTS ( 'NONE', 3,
 ( #1679, #13559, #24154, #39897 ),
 .UNSPECIFIED., .F., .F.,
 ( 4, 4 ),
 ( 2.559137362607186136E-07, 0.01646004363529606287 ),
 .UNSPECIFIED. ) ;
#51035=EDGE_CURVE ( 'NONE', #35836, #40833, #838, .T. ) ;
#51041=FACE_OUTER_BOUND ( 'NONE', #3241, .T. ) ;
#51042=CIRCLE ( 'NONE', #839, 1.850107469027523432 ) ;
#51043=DIRECTION ( 'NONE',  ( 0.9749279121818259508, 2.578990239907041302E-17, -0.2225209339563041788 ) ) ;
#51046=VERTEX_POINT ( 'NONE', #8853 ) ;
#51050=CARTESIAN_POINT ( 'NONE',  ( -1.735432873265435161, 1.581680620477750931, 1.321016258651915409 ) ) ;
#51052=ORIENTED_EDGE ( 'NONE', *, *, #42197, .T. ) ;
#51074=COLOUR_RGB('Sky Blue',0.24,0.69,0.87);
#51075=FILL_AREA_STYLE_COLOUR('',#51074);
#51076=FILL_AREA_STYLE('',(#51075));
#51077=SURFACE_STYLE_FILL_AREA(#51076);
#51078=SURFACE_SIDE_STYLE('',(#51077));
#51079=SURFACE_STYLE_USAGE(.BOTH.,#51078);
#51080=PRESENTATION_STYLE_ASSIGNMENT((#51079));
ENDSEC;
END-ISO-10303-21;
